ISO-10303-21;
HEADER;
FILE_DESCRIPTION (('STEP AP214'),
    '1' );
FILE_NAME ('Negative Post.step',
    '2026-10-05T22:38:29',
    ( '' ),
    ( '' ),
    'SwSTEP 2.0',
    'SolidWorks 2020',
    '' );
FILE_SCHEMA (( 'AUTOMOTIVE_DESIGN' ));
ENDSEC;

DATA;
#1=ORIENTED_EDGE ( 'NONE', *, *, #7882, .T. ) ;
#7=CARTESIAN_POINT ( 'NONE',  ( 10.13049857835000012, 3.092060693447000297, 8.629378633793999498 ) ) ;
#8=CARTESIAN_POINT ( 'NONE',  ( 10.70780830849999887, 5.157484706885999692, -6.267808298721999627 ) ) ;
#9=CARTESIAN_POINT ( 'NONE',  ( 8.298061260823001106, 5.118905885020002877, 6.382684838875003486 ) ) ;
#14=CARTESIAN_POINT ( 'NONE',  ( 8.817635841231000526, 3.894644548817000285, 6.044465307984999924 ) ) ;
#15=ORIENTED_EDGE ( 'NONE', *, *, #36574, .T. ) ;
#16=ADVANCED_FACE ( 'NONE', ( #60887 ), #64896, .T. ) ;
#18=CARTESIAN_POINT ( 'NONE',  ( 11.09999999999999787, 2.363924005032890907, -6.981107664647397293 ) ) ;
#19=CYLINDRICAL_SURFACE ( 'NONE', #27188, 3.500000000000000000 ) ;
#23=CARTESIAN_POINT ( 'NONE',  ( 10.96871661479000082, 6.473054195915000086, 5.205103511516999681 ) ) ;
#25=CARTESIAN_POINT ( 'NONE',  ( 11.12426277055000057, 7.494722804685999940, 6.525523669353000322 ) ) ;
#31=CARTESIAN_POINT ( 'NONE',  ( 8.842811534616762614, 2.713269201112010087, -7.026666560124946947 ) ) ;
#33=CARTESIAN_POINT ( 'NONE',  ( 8.330224159023998709, 2.898680183691999979, -6.607597200868999820 ) ) ;
#44=CARTESIAN_POINT ( 'NONE',  ( 7.733151861820001471, 2.920631402299000534, -6.523085346364998038 ) ) ;
#45=CARTESIAN_POINT ( 'NONE',  ( 10.26693915877000052, 5.500023470133998948, -6.419501519420999891 ) ) ;
#49=CARTESIAN_POINT ( 'NONE',  ( 8.041787892231001322, 5.114458628598999468, -6.690862273930999748 ) ) ;
#52=DIRECTION ( 'NONE',  ( 0.000000000000000000, -1.000000000000000000, 0.000000000000000000 ) ) ;
#53=DIRECTION ( 'NONE',  ( 1.000000000000000000, 0.000000000000000000, 0.000000000000000000 ) ) ;
#58=ORIENTED_EDGE ( 'NONE', *, *, #5676, .F. ) ;
#71=CARTESIAN_POINT ( 'NONE',  ( 11.09999763817999963, -1.407106875523000067, -11.46396985304999916 ) ) ;
#74=CARTESIAN_POINT ( 'NONE',  ( 4.500000000000000000, -13.10000000000000142, 0.000000000000000000 ) ) ;
#80=CARTESIAN_POINT ( 'NONE',  ( 9.351420280414000530, 4.953415418491999844, -8.946479654552000227 ) ) ;
#85=ORIENTED_EDGE ( 'NONE', *, *, #60976, .T. ) ;
#96=CARTESIAN_POINT ( 'NONE',  ( 0.1199860357128856997, -1.197242505009922908, -2.894009422536151011 ) ) ;
#111=CARTESIAN_POINT ( 'NONE',  ( 9.833904719592002408, 5.048004622677000341, -6.120508709481000231 ) ) ;
#115=VERTEX_POINT ( 'NONE', #31827 ) ;
#121=CARTESIAN_POINT ( 'NONE',  ( 0.1499942179680000265, 2.749953718116143087, -0.3599680999394002101 ) ) ;
#123=B_SPLINE_CURVE_WITH_KNOTS ( 'NONE', 3,
 ( #913, #28170, #54387, #23268, #22568, #44612 ),
 .UNSPECIFIED., .F., .F.,
 ( 4, 2, 4 ),
 ( 0.000000000000000000, 0.5000000000000000000, 1.000000000000000000 ),
 .UNSPECIFIED. ) ;
#129=VERTEX_POINT ( 'NONE', #36029 ) ;
#133=ADVANCED_FACE ( 'NONE', ( #9448 ), #52633, .T. ) ;
#141=CARTESIAN_POINT ( 'NONE',  ( 7.083500347624626770, 5.272504913147756156, -6.972355927689905641 ) ) ;
#151=CARTESIAN_POINT ( 'NONE',  ( 10.13586576648993542, 5.314625264832240070, -7.853278872970742341 ) ) ;
#153=CARTESIAN_POINT ( 'NONE',  ( 10.87751262143000019, 2.899999999999999911, 6.466455373849333554 ) ) ;
#158=CYLINDRICAL_SURFACE ( 'NONE', #24280, 3.500000000000000000 ) ;
#159=DIRECTION ( 'NONE',  ( 1.000000000000000000, -1.776356839337000228E-14, 0.000000000000000000 ) ) ;
#170=FACE_OUTER_BOUND ( 'NONE', #15935, .T. ) ;
#172=CARTESIAN_POINT ( 'NONE',  ( 7.414760841225000121, 5.517512745430000365, -8.643112676966000052 ) ) ;
#174=CARTESIAN_POINT ( 'NONE',  ( 9.490131263588281740, 4.919273367466419522, 8.488493135541203216 ) ) ;
#187=VECTOR ( 'NONE', #31580, 1000.000000000000000 ) ;
#190=CARTESIAN_POINT ( 'NONE',  ( 7.117714276092232062, 5.069132632172260067, -8.338946761425976462 ) ) ;
#192=ORIENTED_EDGE ( 'NONE', *, *, #17294, .T. ) ;
#194=ORIENTED_EDGE ( 'NONE', *, *, #47268, .T. ) ;
#195=CARTESIAN_POINT ( 'NONE',  ( 10.66951519566999806, 4.592673277375999952, 5.841403042559999648 ) ) ;
#203=ORIENTED_EDGE ( 'NONE', *, *, #51624, .T. ) ;
#205=B_SPLINE_CURVE_WITH_KNOTS ( 'NONE', 3,
 ( #23649, #19782, #46008, #23996, #18761 ),
 .UNSPECIFIED., .F., .F.,
 ( 4, 1, 4 ),
 ( 0.8746094594482839435, 0.9935764648741313154, 1.000000000000000000 ),
 .UNSPECIFIED. ) ;
#209=CARTESIAN_POINT ( 'NONE',  ( 10.28314886242000092, 2.387776420306999992, 7.684265965147999644 ) ) ;
#210=CARTESIAN_POINT ( 'NONE',  ( 11.09999999999999964, 4.000000000000000000, -7.500000000000000000 ) ) ;
#215=ADVANCED_FACE ( 'NONE', ( #63962 ), #25886, .F. ) ;
#219=B_SPLINE_CURVE_WITH_KNOTS ( 'NONE', 3,
 ( #58732, #10838, #32180, #5585, #347, #21664, #49972, #33901, #17109, #28659 ),
 .UNSPECIFIED., .F., .F.,
 ( 4, 2, 2, 2, 4 ),
 ( 0.2126015446065814829, 0.4094511584549361261, 0.6063007723032907137, 0.8031503861516453568, 1.000000000000000000 ),
 .UNSPECIFIED. ) ;
#225=CARTESIAN_POINT ( 'NONE',  ( 8.856851002545001350, 2.832432432432000269, -6.822293592207000934 ) ) ;
#227=VERTEX_POINT ( 'NONE', #53143 ) ;
#229=CARTESIAN_POINT ( 'NONE',  ( 0.9904415426042999515, 3.273731968234999901, -1.479853775367000246 ) ) ;
#231=AXIS2_PLACEMENT_3D ( 'NONE', #53437, #47852, #5532 ) ;
#232=CARTESIAN_POINT ( 'NONE',  ( 10.95519834123000003, 3.860336562672999960, -6.147350406894000585 ) ) ;
#233=EDGE_LOOP ( 'NONE', ( #37593, #40253, #39646, #55320, #24111 ) ) ;
#235=CARTESIAN_POINT ( 'NONE',  ( 9.928197172113101487, 5.125396288428318847, 6.749639981086157370 ) ) ;
#237=CARTESIAN_POINT ( 'NONE',  ( 2.300973465875999935, -3.500000000000000000, 0.000000000000000000 ) ) ;
#238=CARTESIAN_POINT ( 'NONE',  ( 7.667607780408999929, 5.638704226117999596, 8.266404648244000342 ) ) ;
#241=CARTESIAN_POINT ( 'NONE',  ( 7.847520280408001092, 3.511256298105000173, -6.013302684100999329 ) ) ;
#246=CARTESIAN_POINT ( 'NONE',  ( 2.959306799210166705, 3.058252359239905793, -1.762666431298143488 ) ) ;
#248=ORIENTED_EDGE ( 'NONE', *, *, #50052, .F. ) ;
#251=DIRECTION ( 'NONE',  ( 1.000000000000000000, 0.000000000000000000, 0.000000000000000000 ) ) ;
#259=CARTESIAN_POINT ( 'NONE',  ( 7.486426658771000220, 5.321913229613000063, 8.118244847118999630 ) ) ;
#260=ORIENTED_EDGE ( 'NONE', *, *, #5436, .F. ) ;
#265=ORIENTED_EDGE ( 'NONE', *, *, #31744, .F. ) ;
#267=EDGE_CURVE ( 'NONE', #32166, #65266, #66403, .T. ) ;
#268=CARTESIAN_POINT ( 'NONE',  ( 0.3804339246497162041, -3.380412643848677234, -0.4416305321314611398 ) ) ;
#270=CARTESIAN_POINT ( 'NONE',  ( 10.26685100253999927, 2.832432432432000269, 6.822293592207000934 ) ) ;
#278=ORIENTED_EDGE ( 'NONE', *, *, #15421, .F. ) ;
#281=CARTESIAN_POINT ( 'NONE',  ( 4.900006121741999898, 1.007237960741801164, 1.747572776708514297 ) ) ;
#286=CARTESIAN_POINT ( 'NONE',  ( 10.19255830160000009, 2.560287027313000063, 7.664549200117999561 ) ) ;
#287=ORIENTED_EDGE ( 'NONE', *, *, #54615, .F. ) ;
#289=CARTESIAN_POINT ( 'NONE',  ( 9.194604681486000075, 5.157771204918000230, 8.637848577075999401 ) ) ;
#290=CARTESIAN_POINT ( 'NONE',  ( 2.071806799209333416, 3.408904368339104263, 0.9161175952574878156 ) ) ;
#295=CARTESIAN_POINT ( 'NONE',  ( 8.241841482360854343, 3.974357482335666436, -8.874747363613822770 ) ) ;
#297=CARTESIAN_POINT ( 'NONE',  ( 9.814910518647794291, 2.650130971540564317, -7.499994893876710478 ) ) ;
#300=FACE_OUTER_BOUND ( 'NONE', #44362, .T. ) ;
#303=EDGE_CURVE ( 'NONE', #62021, #50139, #529, .T. ) ;
#311=CARTESIAN_POINT ( 'NONE',  ( 8.437857780412000963, 2.606995215518000286, 6.345762205468999717 ) ) ;
#313=CARTESIAN_POINT ( 'NONE',  ( 9.152520280414000453, 4.102804347295999854, -5.770625657082999460 ) ) ;
#315=DIRECTION ( 'NONE',  ( -1.000000000000000000, 0.000000000000000000, 0.000000000000000000 ) ) ;
#317=CARTESIAN_POINT ( 'NONE',  ( 9.444315208305999576, 2.927258006877999641, 8.897018628538001295 ) ) ;
#323=CARTESIAN_POINT ( 'NONE',  ( 8.829017219593000121, 5.290207928847999064, 8.768105151414001597 ) ) ;
#328=VECTOR ( 'NONE', #55122, 1000.000000000000114 ) ;
#336=CARTESIAN_POINT ( 'NONE',  ( 9.518314158773000244, 4.845406482350000488, -6.387189183984999907 ) ) ;
#339=CARTESIAN_POINT ( 'NONE',  ( 7.951287431685589269, 4.953067615740292418, -6.432288716792883498 ) ) ;
#342=CARTESIAN_POINT ( 'NONE',  ( 9.475279990687596410, 5.350441389720215213, 7.499985493516660107 ) ) ;
#347=CARTESIAN_POINT ( 'NONE',  ( 10.25036334590211773, 3.059888261081768590, -8.493457116339008905 ) ) ;
#348=CARTESIAN_POINT ( 'NONE',  ( 11.05220172819000091, 2.768652217526999859, -4.974789451568000231 ) ) ;
#349=CARTESIAN_POINT ( 'NONE',  ( 8.222961399606997901, 4.680050665548002087, 6.135920769709001021 ) ) ;
#356=CARTESIAN_POINT ( 'NONE',  ( 9.266948341230998309, 3.049618631524000367, 6.392542946894000266 ) ) ;
#367=CARTESIAN_POINT ( 'NONE',  ( 10.87889121877999976, 9.617170530054998778, 5.911408669357999912 ) ) ;
#373=DIRECTION ( 'NONE',  ( 1.000000000000000000, 4.884985026250000111E-14, 0.000000000000000000 ) ) ;
#385=CARTESIAN_POINT ( 'NONE',  ( 7.893560293058006216, 2.859109450078002546, -6.778905949012001386 ) ) ;
#388=CARTESIAN_POINT ( 'NONE',  ( 10.99999999997000089, 4.000000000000000000, 7.500000000000000000 ) ) ;
#389=CARTESIAN_POINT ( 'NONE',  ( 7.826132327310000747, 5.086383815897999483, 6.522343373212003748 ) ) ;
#391=FACE_OUTER_BOUND ( 'NONE', #34041, .T. ) ;
#392=ORIENTED_EDGE ( 'NONE', *, *, #24053, .T. ) ;
#398=CARTESIAN_POINT ( 'NONE',  ( 10.96083988456000036, 2.844674717313000034, 5.100114893396999527 ) ) ;
#404=VECTOR ( 'NONE', #30309, 1000.000000000000000 ) ;
#405=CARTESIAN_POINT ( 'NONE',  ( 11.09999999999999964, 4.000000000000000000, 7.500000000000000000 ) ) ;
#407=ADVANCED_FACE ( 'NONE', ( #22962 ), #48160, .F. ) ;
#411=B_SPLINE_CURVE_WITH_KNOTS ( 'NONE', 3,
 ( #32955, #65091, #6719, #11273 ),
 .UNSPECIFIED., .F., .F.,
 ( 4, 4 ),
 ( 0.000000000000000000, 1.000000000000000000 ),
 .UNSPECIFIED. ) ;
#412=B_SPLINE_CURVE_WITH_KNOTS ( 'NONE', 3,
 ( #28021, #10975, #54929, #1442, #55625, #33954, #64101, #28714 ),
 .UNSPECIFIED., .F., .F.,
 ( 4, 1, 1, 1, 1, 4 ),
 ( 0.000000000000000000, 0.2000000000000000111, 0.4000000000000000222, 0.5999999999999999778, 0.8000000000000000444, 1.000000000000000000 ),
 .UNSPECIFIED. ) ;
#419=ORIENTED_EDGE ( 'NONE', *, *, #22122, .T. ) ;
#420=CARTESIAN_POINT ( 'NONE',  ( 9.401145280412999128, 3.927090956378999742, -9.230892435423001530 ) ) ;
#422=CONICAL_SURFACE ( 'NONE', #39511, 13.04999999969999891, 0.7853981633972997312 ) ;
#439=CARTESIAN_POINT ( 'NONE',  ( 7.614999999996999946, 5.349999999999999645, -7.500000000000000000 ) ) ;
#441=CARTESIAN_POINT ( 'NONE',  ( 9.934212804449000345, 5.120437537252000126, -8.883398686237999442 ) ) ;
#443=LINE ( 'NONE', #11611, #41449 ) ;
#447=B_SPLINE_SURFACE_WITH_KNOTS ( 'NONE', 3, 3, ( 
 ( #68396, #63151, #9675, #42537, #51644, #8995, #69101, #31026, #41500, #35913, #63846, #15279, #3741, #52335, #46754, #36603, #4428, #15958, #9328 ),
 ( #51979, #4084, #31363, #47440, #68747, #16985, #54748, #5474, #65577, #11064, #16301, #38316, #32735, #38670, #42880, #54053, #58960, #32057, #53373 ),
 ( #32398, #6501, #53713, #576, #33085, #21887, #28183, #16646, #65227, #59644, #43222, #5808, #11742, #64527, #6847, #59293, #49499, #27150, #17340 ),
 ( #37972, #22926, #11397, #1609, #64874, #33431, #44277, #43574, #10710, #26810, #54399, #37289, #27846, #1265, #49153, #58608, #48123, #229, #43921 ) ),
 .UNSPECIFIED., .F., .F., .F.,
 ( 4, 4 ),
 ( 4, 1, 1, 1, 1, 1, 1, 1, 1, 1, 1, 1, 1, 1, 1, 1, 4 ),
 ( -0.1039370721279000015, 1.103937072127999963 ),
 ( 0.5600558712726999566, 0.5880915265348000132, 0.6161271817967999276, 0.6441628370587999530, 0.6721984923209000096, 0.7002341475828999240, 0.7282698028449000605, 0.7563054581070000060, 0.7843411133690000314, 0.8123767686310000569, 0.8404124238931000024, 0.8684480791551000278, 0.8964837344171000533, 0.9245193896790999677, 0.9525550449412000242, 0.9805907002032000497, 1.008626355465000124 ),
 .UNSPECIFIED. ) ;
#455=AXIS2_PLACEMENT_3D ( 'NONE', #28603, #17765, #7956 ) ;
#461=CARTESIAN_POINT ( 'NONE',  ( 8.821685841230998193, 2.633142096252999664, -7.791134854666999843 ) ) ;
#462=CARTESIAN_POINT ( 'NONE',  ( 7.883148997456999929, 5.167567567567999731, 6.822293592207000934 ) ) ;
#474=ORIENTED_EDGE ( 'NONE', *, *, #22248, .F. ) ;
#481=B_SPLINE_CURVE_WITH_KNOTS ( 'NONE', 3,
 ( #46917, #10879, #49, #58772, #15446 ),
 .UNSPECIFIED., .F., .F.,
 ( 4, 1, 4 ),
 ( 0.000000000000000000, 0.5000000000000000000, 1.000000000000000000 ),
 .UNSPECIFIED. ) ;
#487=B_SPLINE_CURVE_WITH_KNOTS ( 'NONE', 3,
 ( #56245, #40501, #34592, #24770, #50999, #23736, #61490, #8693, #13265, #40173, #7660, #28652, #18847, #3434, #19524, #62167 ),
 .UNSPECIFIED., .F., .F.,
 ( 4, 2, 2, 2, 2, 2, 2, 4 ),
 ( 0.000000000000000000, 0.2499999999999993339, 0.3749999999999994449, 0.4999999999999995559, 0.6249999999999996669, 0.7499999999999997780, 0.8749999999999998890, 1.000000000000000000 ),
 .UNSPECIFIED. ) ;
#496=PLANE ( 'NONE',  #6664 ) ;
#502=DIRECTION ( 'NONE',  ( 0.000000000000000000, -1.000000000000000000, 0.000000000000000000 ) ) ;
#511=DIRECTION ( 'NONE',  ( -0.7071052132515089905, -0.7071083491181088254, 2.836092545889034718E-08 ) ) ;
#515=CARTESIAN_POINT ( 'NONE',  ( 7.762835841224000610, 4.574593532473000046, -5.689090339675999530 ) ) ;
#517=CARTESIAN_POINT ( 'NONE',  ( 7.198460030931516762, 4.679653997254563436, -8.679420697515526584 ) ) ;
#523=VERTEX_POINT ( 'NONE', #44659 ) ;
#529=B_SPLINE_CURVE_WITH_KNOTS ( 'NONE', 3,
 ( #14964, #10403, #31745, #53061 ),
 .UNSPECIFIED., .F., .F.,
 ( 4, 4 ),
 ( 0.000000000000000000, 0.1253970409990855239 ),
 .UNSPECIFIED. ) ;
#533=FACE_OUTER_BOUND ( 'NONE', #790, .T. ) ;
#536=CARTESIAN_POINT ( 'NONE',  ( 7.243250223023721901, 3.136812440417415804, -8.580788443034522928 ) ) ;
#539=ORIENTED_EDGE ( 'NONE', *, *, #30229, .F. ) ;
#542=CARTESIAN_POINT ( 'NONE',  ( 9.945533384955998812, 2.906048475816000121, 8.880389653997999844 ) ) ;
#547=CARTESIAN_POINT ( 'NONE',  ( 11.09999999999999964, 4.000000000000000000, 7.500000000000000000 ) ) ;
#556=PLANE ( 'NONE',  #3403 ) ;
#561=CARTESIAN_POINT ( 'NONE',  ( 10.19255830160000009, 2.560287027313000063, 7.664549200117999561 ) ) ;
#573=CARTESIAN_POINT ( 'NONE',  ( 8.722714158775000115, 3.892978337449999771, -8.893414073324001023 ) ) ;
#576=CARTESIAN_POINT ( 'NONE',  ( 0.3377116734105999885, 1.258511261458999941, -3.306246502378999974 ) ) ;
#580=CARTESIAN_POINT ( 'NONE',  ( 1.932518698273000046, 1.300495226975000085, -3.293006394410000315 ) ) ;
#586=CARTESIAN_POINT ( 'NONE',  ( 8.026329719592000700, 5.601795057054999916, 7.176148573050999957 ) ) ;
#587=ORIENTED_EDGE ( 'NONE', *, *, #5822, .F. ) ;
#589=CARTESIAN_POINT ( 'NONE',  ( 8.105004719587000750, 2.627120679234999923, -8.556648795244999661 ) ) ;
#596=CARTESIAN_POINT ( 'NONE',  ( 11.10000000000000142, 2.402782103116360979, -8.046943094580276679 ) ) ;
#601=CARTESIAN_POINT ( 'NONE',  ( 9.079784991436001818, 7.881284392328999466, 5.316045437065000101 ) ) ;
#607=CARTESIAN_POINT ( 'NONE',  ( 7.256079719589999755, 2.531201476950000195, 8.216704145297999418 ) ) ;
#609=CARTESIAN_POINT ( 'NONE',  ( 10.11094409420000062, 5.100000000000000533, -6.571291218949999902 ) ) ;
#618=EDGE_CURVE ( 'NONE', #41936, #57550, #68288, .T. ) ;
#621=ADVANCED_FACE ( 'NONE', ( #24348 ), #36555, .F. ) ;
#625=ORIENTED_EDGE ( 'NONE', *, *, #32487, .T. ) ;
#627=ORIENTED_EDGE ( 'NONE', *, *, #37110, .F. ) ;
#631=B_SPLINE_CURVE_WITH_KNOTS ( 'NONE', 3,
 ( #60194, #12642, #28735, #50050, #49008, #43068, #64375, #6000, #44477, #65769, #33973, #59145, #27341, #22429, #767, #16838, #43428, #64722, #38160, #11587, #59837, #32931, #11942, #54241, #33282, #29083, #14027, #51081, #19609, #40929, #29778, #57008, #35013, #55983, #30117, #24162, #3184, #35692, #51758, #61911, #50393, #39910, #24512, #40585, #66117, #61569, #44814, #45833, #45154, #8432, #2493, #23475, #66812, #35352, #18237, #45498, #66461, #39558, #46181, #8775, #56675, #14373, #67488, #51420, #18583, #60882, #3515, #62251, #8089, #61229, #2836, #23817, #12998, #13345, #18923, #34322, #40248, #13684, #9108, #34670, #24853, #30446, #29432, #67145, #55642, #56328, #19258, #50738, #7741, #31476, #4202 ),
 .UNSPECIFIED., .F., .F.,
 ( 4, 1, 1, 1, 1, 1, 1, 1, 1, 1, 1, 1, 1, 1, 1, 1, 1, 1, 1, 1, 1, 1, 1, 1, 1, 1, 1, 1, 1, 1, 1, 1, 1, 1, 1, 1, 1, 1, 1, 1, 1, 1, 1, 1, 1, 1, 1, 1, 1, 1, 1, 1, 1, 1, 1, 1, 1, 1, 1, 1, 1, 1, 1, 1, 1, 1, 1, 1, 1, 1, 1, 1, 1, 1, 1, 1, 1, 1, 1, 1, 1, 1, 1, 1, 1, 1, 1, 1, 4 ),
 ( 0.000000000000000000, 0.004874450823355541522, 0.009661345194022003327, 0.01436103260279607101, 0.01897537103212419002, 0.02350775731914938119, 0.02796115294545339219, 0.03233656637161005237, 0.03663363768239984858, 0.04085119304253923694, 0.04498768735433079924, 0.04904154886712413369, 0.05301143935174792293, 0.05689644225696363633, 0.06069618962671503859, 0.06441093687713574101, 0.06804159303743011200, 0.07158970920874503652, 0.07498141635100204205, 0.08501006463908243604, 0.09841337508356413910, 0.1118176718332323377, 0.1187820131990808270, 0.1252437490255899066, 0.1404218166617251795, 0.1574035577456479040, 0.1761129495041070525, 0.1966414853897626713, 0.2019033837996370984, 0.2100638602301221347, 0.2234696548173721320, 0.2414626216399035907, 0.2502561337435587063, 0.2678629632046341524, 0.2752677410504689171, 0.2907998480710696776, 0.3002851497986598339, 0.3238876161481084592, 0.3442582269590512833, 0.3613588172231308460, 0.3751465592194264675, 0.3959010830434372408, 0.4196307664705191121, 0.4463514864640283908, 0.4514228443006744196, 0.4597736081350440318, 0.4670316664865736267, 0.4731994725281417624, 0.4907875272513019804, 0.4999891125105156986, 0.5206125037787298071, 0.5393828774126382397, 0.5563118703635043794, 0.5713334752878752587, 0.5782068158715422124, 0.5847575811334744245, 0.5906763917012011200, 0.5981799785644238421, 0.6175854672771887710, 0.6249630545279218907, 0.6409200020002955300, 0.6581577244971096308, 0.6766092828860079678, 0.6963689643179452604, 0.7014886240358610969, 0.7097912278688763843, 0.7168462699965328921, 0.7232171845259283138, 0.7405756818954355447, 0.7500085531557023621, 0.7700661893775517797, 0.7886464287371296455, 0.8057650030297832666, 0.8213545077432261587, 0.8410359930661466255, 0.8481241221261679453, 0.8668504199967879131, 0.8749138338875376286, 0.8911902668814143391, 0.9085325902296357281, 0.9268791062040830919, 0.9463236143299509351, 0.9513222611507794468, 0.9597458290560116900, 0.9666803444524524336, 0.9731718905766858496, 0.9852515542005497728, 0.9942041435450702513, 1.000000000000000000 ),
 .UNSPECIFIED. ) ;
#637=CARTESIAN_POINT ( 'NONE',  ( 10.44079719460000000, 5.435719122931000236, 7.303631812894000319 ) ) ;
#638=ORIENTED_EDGE ( 'NONE', *, *, #47754, .F. ) ;
#640=CARTESIAN_POINT ( 'NONE',  ( 10.93227693248999977, 2.539877577705000000, 6.453611809651000009 ) ) ;
#646=CARTESIAN_POINT ( 'NONE',  ( 7.100000000000154188, 5.265235852882342193, -6.934887023210864143 ) ) ;
#653=CARTESIAN_POINT ( 'NONE',  ( 10.66922466734516739, 4.845815779105637766, 4.789865691387857893 ) ) ;
#655=ORIENTED_EDGE ( 'NONE', *, *, #20266, .T. ) ;
#657=CARTESIAN_POINT ( 'NONE',  ( 9.099999886593998610, -3.819167204710999825E-14, 1.447156853930999928E-13 ) ) ;
#658=CARTESIAN_POINT ( 'NONE',  ( 7.577017219590000074, 5.480308727866000318, 8.192324747680999053 ) ) ;
#661=CARTESIAN_POINT ( 'NONE',  ( 9.608904719592000987, 4.946705552514000459, -6.253848946732999181 ) ) ;
#663=CARTESIAN_POINT ( 'NONE',  ( 3.148789388360131447, -0.09951366136684100527, -3.256401652200602737 ) ) ;
#665=CARTESIAN_POINT ( 'NONE',  ( 9.611387933856001098, 3.334846092635999959, 5.869117602953000556 ) ) ;
#678=ORIENTED_EDGE ( 'NONE', *, *, #66237, .T. ) ;
#684=B_SPLINE_CURVE_WITH_KNOTS ( 'NONE', 3,
 ( #26074, #9986, #26422, #58569 ),
 .UNSPECIFIED., .F., .F.,
 ( 4, 4 ),
 ( 0.000000000000000000, 1.000000000000000000 ),
 .UNSPECIFIED. ) ;
#685=CARTESIAN_POINT ( 'NONE',  ( 8.921614158776000281, 3.251172436837000301, -6.320036569851000152 ) ) ;
#688=PLANE ( 'NONE',  #67510 ) ;
#696=CARTESIAN_POINT ( 'NONE',  ( 10.00637913184999839, 5.119263020957999899, 8.420380450036001108 ) ) ;
#697=CARTESIAN_POINT ( 'NONE',  ( 10.01277517397999972, 3.440623091551000101, -9.267603345544999982 ) ) ;
#698=EDGE_CURVE ( 'NONE', #53063, #51133, #31661, .T. ) ;
#703=LINE ( 'NONE', #27621, #24063 ) ;
#707=CARTESIAN_POINT ( 'NONE',  ( 8.625073341231001223, 3.117378429069999957, 8.662179062556001341 ) ) ;
#710=CARTESIAN_POINT ( 'NONE',  ( 9.266851002542999538, 2.832432432432000269, 6.822293592207000934 ) ) ;
#712=B_SPLINE_CURVE_WITH_KNOTS ( 'NONE', 3,
 ( #8653, #51640, #4081, #36251 ),
 .UNSPECIFIED., .F., .F.,
 ( 4, 4 ),
 ( 0.000000000000000000, 1.000000000000000000 ),
 .UNSPECIFIED. ) ;
#715=CARTESIAN_POINT ( 'NONE',  ( 11.13250283087000092, 9.191281752207999034, 6.598833342203999308 ) ) ;
#718=VERTEX_POINT ( 'NONE', #41118 ) ;
#721=CARTESIAN_POINT ( 'NONE',  ( 9.959641781044998865, 5.406625910119999823, 7.700299649248999678 ) ) ;
#722=EDGE_CURVE ( 'NONE', #61638, #23923, #32242, .T. ) ;
#727=CARTESIAN_POINT ( 'NONE',  ( 8.560885841230001958, 4.228291488957999888, 8.941375734143997889 ) ) ;
#733=CARTESIAN_POINT ( 'NONE',  ( 10.48598278040999965, 5.506034726153999692, -7.274787238512000265 ) ) ;
#735=CARTESIAN_POINT ( 'NONE',  ( 7.948904172952001801, 4.897346594336003278, 6.290771953639007208 ) ) ;
#737=DIRECTION ( 'NONE',  ( 0.8660254037844289376, 0.000000000000000000, -0.5000000000000169864 ) ) ;
#740=CARTESIAN_POINT ( 'NONE',  ( 8.765417767663000959, 5.029951493281999753, -6.097931603992000404 ) ) ;
#741=EDGE_CURVE ( 'NONE', #62685, #5496, #3861, .T. ) ;
#746=CARTESIAN_POINT ( 'NONE',  ( 11.13709883525000066, 2.663413669911999904, 5.177930968215000540 ) ) ;
#755=CARTESIAN_POINT ( 'NONE',  ( 10.45746213570999927, 5.100000000000000533, -6.571291218949999902 ) ) ;
#757=CARTESIAN_POINT ( 'NONE',  ( 8.342859831669791504, 2.714084127472751629, -7.027014477893811950 ) ) ;
#758=B_SPLINE_CURVE_WITH_KNOTS ( 'NONE', 3,
 ( #19058, #30584, #36168, #20089, #57480, #2978, #30932, #52242, #34810, #40383 ),
 .UNSPECIFIED., .F., .F.,
 ( 4, 2, 2, 2, 4 ),
 ( 0.1253179912170450105, 0.3126267435314338261, 0.4999354958458225862, 0.6872442481602113462, 0.8745530004746001618 ),
 .UNSPECIFIED. ) ;
#767=CARTESIAN_POINT ( 'NONE',  ( 7.397780563817286215, 2.619533902629167965, 8.557926001834172069 ) ) ;
#770=AXIS2_PLACEMENT_3D ( 'NONE', #37977, #27155, #33437 ) ;
#773=ORIENTED_EDGE ( 'NONE', *, *, #61507, .T. ) ;
#777=FACE_OUTER_BOUND ( 'NONE', #56163, .T. ) ;
#783=CYLINDRICAL_SURFACE ( 'NONE', #42949, 1.350000000000000533 ) ;
#786=EDGE_CURVE ( 'NONE', #29932, #48584, #62192, .T. ) ;
#787=CARTESIAN_POINT ( 'NONE',  ( 8.830545280412000153, 3.207599814920999659, -6.150466394809999571 ) ) ;
#790=EDGE_LOOP ( 'NONE', ( #8197, #43500, #53236, #46954 ) ) ;
#798=VERTEX_POINT ( 'NONE', #25717 ) ;
#799=CARTESIAN_POINT ( 'NONE',  ( 6.886728317542999633, 3.037137096735000430, -6.379793420563999895 ) ) ;
#801=EDGE_CURVE ( 'NONE', #38352, #55375, #8952, .T. ) ;
#805=CARTESIAN_POINT ( 'NONE',  ( 9.155142860581458208, 2.899999999999999911, -6.163493177590811278 ) ) ;
#807=CARTESIAN_POINT ( 'NONE',  ( 10.53706676393788300, 5.286158710546891015, -7.027080267280216397 ) ) ;
#811=CARTESIAN_POINT ( 'NONE',  ( 11.13729092125999998, 5.336331659174000208, -5.186744570729000969 ) ) ;
#812=VECTOR ( 'NONE', #3122, 999.9999999999998863 ) ;
#813=LINE ( 'NONE', #29124, #66788 ) ;
#822=ORIENTED_EDGE ( 'NONE', *, *, #22160, .T. ) ;
#823=AXIS2_PLACEMENT_3D ( 'NONE', #45975, #56816, #14846 ) ;
#841=CARTESIAN_POINT ( 'NONE',  ( 8.331682176603999679, 5.101289360622999425, 6.607176324693000424 ) ) ;
#845=SHAPE_DEFINITION_REPRESENTATION ( #41120, #15732 ) ;
#848=B_SPLINE_CURVE_WITH_KNOTS ( 'NONE', 3,
 ( #68295, #61336, #45608, #41038 ),
 .UNSPECIFIED., .F., .F.,
 ( 4, 4 ),
 ( 0.000000000000000000, 1.000000000000000000 ),
 .UNSPECIFIED. ) ;
#853=CARTESIAN_POINT ( 'NONE',  ( 4.600001223043999943, 1.829647544581999737E-13, -13.09999975891967416 ) ) ;
#856=CARTESIAN_POINT ( 'NONE',  ( 8.087243290925727024, 5.285867343427418596, -7.027213786845273091 ) ) ;
#858=CARTESIAN_POINT ( 'NONE',  ( 9.608904719592000987, 4.946705552514000459, -6.253848946732999181 ) ) ;
#865=CARTESIAN_POINT ( 'NONE',  ( 7.136007566080033726, 5.350530049016002820, -7.853201045838831718 ) ) ;
#866=VERTEX_POINT ( 'NONE', #6104 ) ;
#869=B_SPLINE_CURVE_WITH_KNOTS ( 'NONE', 3,
 ( #26263, #31, #15769, #62955 ),
 .UNSPECIFIED., .F., .F.,
 ( 4, 4 ),
 ( 0.000000000000000000, 0.1844766778621776404 ),
 .UNSPECIFIED. ) ;
#875=CARTESIAN_POINT ( 'NONE',  ( 27.64127793187000037, 13.87069231928999891, -4.225386915259999654 ) ) ;
#876=FACE_OUTER_BOUND ( 'NONE', #24822, .T. ) ;
#877=ORIENTED_EDGE ( 'NONE', *, *, #25501, .F. ) ;
#881=CARTESIAN_POINT ( 'NONE',  ( 7.841306432805004611, 5.081857837045995474, -6.476218562526999456 ) ) ;
#884=DIRECTION ( 'NONE',  ( 0.000000000000000000, 0.000000000000000000, -1.000000000000000000 ) ) ;
#885=B_SPLINE_SURFACE_WITH_KNOTS ( 'NONE', 3, 3, ( 
 ( #48955, #21008, #38108, #37089 ),
 ( #43015, #43373, #16440, #48609 ),
 ( #15762, #5600, #58404, #64319 ),
 ( #23, #59434, #21344, #37769 ),
 ( #42673, #59094, #32876, #11196 ),
 ( #32534, #28676, #23422, #13292 ),
 ( #23068, #34263, #17487, #44066 ),
 ( #44757, #8033, #12937, #50338 ),
 ( #49641, #66061, #43715, #65008 ) ),
 .UNSPECIFIED., .F., .F., .F.,
 ( 4, 1, 1, 1, 1, 1, 4 ),
 ( 4, 4 ),
 ( -0.01864526228370000024, 0.000000000000000000, 0.2500000000000000000, 0.5000000000000000000, 0.7500000000000000000, 1.000000000000000000, 1.019255357118999950 ),
 ( -0.2206650646280000072, 1.220665064628000174 ),
 .UNSPECIFIED. ) ;
#888=CARTESIAN_POINT ( 'NONE',  ( 10.63461554336999981, 5.668731883089999535, 6.527253515312000154 ) ) ;
#889=CARTESIAN_POINT ( 'NONE',  ( 9.900934992105000276, 4.883852641422000040, -9.070888919673000927 ) ) ;
#893=CARTESIAN_POINT ( 'NONE',  ( 9.972537864286000087, 2.899999999999999911, -6.571291218949999902 ) ) ;
#894=EDGE_CURVE ( 'NONE', #28055, #27697, #3524, .T. ) ;
#898=B_SPLINE_CURVE_WITH_KNOTS ( 'NONE', 3,
 ( #49158, #53718, #235, #33090 ),
 .UNSPECIFIED., .F., .F.,
 ( 4, 4 ),
 ( 0.000000000000000000, 1.000000000000000000 ),
 .UNSPECIFIED. ) ;
#901=CARTESIAN_POINT ( 'NONE',  ( 10.80168826891999956, 3.998196217194999846, 9.431555066626000183 ) ) ;
#913=CARTESIAN_POINT ( 'NONE',  ( 8.757697342472001267, 2.899999999999999911, -6.397101765418000241 ) ) ;
#918=ORIENTED_EDGE ( 'NONE', *, *, #57966, .F. ) ;
#922=CARTESIAN_POINT ( 'NONE',  ( 10.99328643597520738, 6.237225121672477002, 5.127881282518703898 ) ) ;
#926=CARTESIAN_POINT ( 'NONE',  ( 2.600065990445999731, 2.304586066898000052, 2.969387198930000249 ) ) ;
#928=ADVANCED_FACE ( 'NONE', ( #43869 ), #27800, .F. ) ;
#930=CIRCLE ( 'NONE', #18804, 13.00000000000000178 ) ;
#934=CARTESIAN_POINT ( 'NONE',  ( 9.053329719590999858, 5.618384167307999277, 7.727742442702000503 ) ) ;
#935=ORIENTED_EDGE ( 'NONE', *, *, #21606, .T. ) ;
#937=CARTESIAN_POINT ( 'NONE',  ( 7.110504719587999567, 2.557426065706999818, -8.459317650138999056 ) ) ;
#940=ORIENTED_EDGE ( 'NONE', *, *, #36929, .F. ) ;
#943=ORIENTED_EDGE ( 'NONE', *, *, #1738, .T. ) ;
#944=CARTESIAN_POINT ( 'NONE',  ( 11.09999999999999964, 3.512324525112999751, -8.971282648301999174 ) ) ;
#954=CARTESIAN_POINT ( 'NONE',  ( 7.769579719591000355, 2.431401017850999935, 7.958393275880999873 ) ) ;
#958=VERTEX_POINT ( 'NONE', #12051 ) ;
#962=CARTESIAN_POINT ( 'NONE',  ( 11.07126769815000067, 6.557511878246000236, -5.495874711259999934 ) ) ;
#965=AXIS2_PLACEMENT_3D ( 'NONE', #37909, #1203, #48061 ) ;
#966=CARTESIAN_POINT ( 'NONE',  ( 0.1423795961331161819, -1.074693865285089478, -3.000024710404201045 ) ) ;
#967=CYLINDRICAL_SURFACE ( 'NONE', #19295, 1.350000000000000533 ) ;
#977=CARTESIAN_POINT ( 'NONE',  ( 9.436104719595000745, 5.619431609641999614, -8.115423117607999615 ) ) ;
#978=CARTESIAN_POINT ( 'NONE',  ( 10.99480479316000014, 3.850613903518000036, -9.347963496621000345 ) ) ;
#981=FACE_OUTER_BOUND ( 'NONE', #43868, .T. ) ;
#982=CARTESIAN_POINT ( 'NONE',  ( 7.681993940831000067, 3.468925063633002903, -6.455929610676999886 ) ) ;
#986=CARTESIAN_POINT ( 'NONE',  ( 1.977569202129666914, 2.124261041935755934, -2.802062795322278532 ) ) ;
#987=CARTESIAN_POINT ( 'NONE',  ( 10.12550053024000007, 5.788811067708000024, 7.335561454339999621 ) ) ;
#990=DIRECTION ( 'NONE',  ( 0.000000000000000000, 0.9835907196275001096, 0.1804142351995999538 ) ) ;
#992=CARTESIAN_POINT ( 'NONE',  ( 11.05286138047000222, 9.767097133436999812, -6.032307961834000309 ) ) ;
#993=CARTESIAN_POINT ( 'NONE',  ( 11.09999999999999964, 2.649999999999999911, 7.500000000000000000 ) ) ;
#1001=CARTESIAN_POINT ( 'NONE',  ( 10.59999999999999964, 4.599999999999999645, 4.756097560976000338 ) ) ;
#1003=EDGE_LOOP ( 'NONE', ( #60883, #57791, #7358 ) ) ;
#1005=CARTESIAN_POINT ( 'NONE',  ( 9.041948341230998665, 2.707986230053999854, 5.994446745591000436 ) ) ;
#1006=CARTESIAN_POINT ( 'NONE',  ( 8.912754719595000097, 2.481540185810000132, -7.878707153279001396 ) ) ;
#1008=CARTESIAN_POINT ( 'NONE',  ( 10.60689139207886988, 3.306467137587833172, 4.759459215648202957 ) ) ;
#1010=ADVANCED_FACE ( 'NONE', ( #32688 ), #15657, .T. ) ;
#1011=VERTEX_POINT ( 'NONE', #58142 ) ;
#1013=CARTESIAN_POINT ( 'NONE',  ( 9.332933391271998502, 5.100349772922000646, 8.693467186193998941 ) ) ;
#1019=VERTEX_POINT ( 'NONE', #26331 ) ;
#1020=DIRECTION ( 'NONE',  ( -1.000000000000000000, 0.000000000000000000, -3.472115270429000239E-14 ) ) ;
#1024=DIRECTION ( 'NONE',  ( 0.8843050081471363066, -0.1786785918943075702, -0.4313683036160176343 ) ) ;
#1025=CARTESIAN_POINT ( 'NONE',  ( 11.00284540370999942, 5.167376273215000815, 4.969475793453000279 ) ) ;
#1034=CARTESIAN_POINT ( 'NONE',  ( 9.418864158773999407, 3.210851187372000037, -6.346613542714999667 ) ) ;
#1037=EDGE_CURVE ( 'NONE', #55115, #37404, #15830, .T. ) ;
#1039=FACE_OUTER_BOUND ( 'NONE', #39336, .T. ) ;
#1041=EDGE_CURVE ( 'NONE', #38352, #51298, #47656, .T. ) ;
#1049=CARTESIAN_POINT ( 'NONE',  ( 11.13508722342999846, 2.662017522928000091, -5.085688471786000697 ) ) ;
#1050=CARTESIAN_POINT ( 'NONE',  ( 8.361434368299004660, 5.126350915548002263, 6.365320234831002288 ) ) ;
#1052=CARTESIAN_POINT ( 'NONE',  ( 11.09999233421999953, -1.199999999999999956, -11.47663049995799156 ) ) ;
#1056=CARTESIAN_POINT ( 'NONE',  ( 8.764829719592999169, 5.808262417891000062, 7.446016144116000213 ) ) ;
#1060=CARTESIAN_POINT ( 'NONE',  ( 7.108390820783056618, 3.867390187372035548, 8.850036383993245437 ) ) ;
#1061=CARTESIAN_POINT ( 'NONE',  ( 7.883148997456999929, 5.167567567567999731, 6.822293592207000934 ) ) ;
#1065=CARTESIAN_POINT ( 'NONE',  ( 10.99096914765000044, 9.108466108418001639, 6.431364469357999880 ) ) ;
#1071=CARTESIAN_POINT ( 'NONE',  ( 0.2500098862125000321, 0.000000000000000000, -3.249989426617000188 ) ) ;
#1075=CARTESIAN_POINT ( 'NONE',  ( 9.304732780410999382, 5.284130523641000110, 6.489275570566000795 ) ) ;
#1076=CARTESIAN_POINT ( 'NONE',  ( 9.285195242305000818, 5.269680202247999823, 8.747831873285999649 ) ) ;
#1078=ORIENTED_EDGE ( 'NONE', *, *, #21219, .T. ) ;
#1086=CARTESIAN_POINT ( 'NONE',  ( 8.350387243830999395, 3.399999999999999911, 6.632262360512000576 ) ) ;
#1088=CARTESIAN_POINT ( 'NONE',  ( 1.882430528421999982, -0.1982148001128000159, 3.252998300308999724 ) ) ;
#1092=EDGE_CURVE ( 'NONE', #65620, #63173, #16942, .T. ) ;
#1099=EDGE_CURVE ( 'NONE', #35088, #29684, #36309, .T. ) ;
#1103=CARTESIAN_POINT ( 'NONE',  ( 0.9374279487471000039, -2.315742118336999944, -2.746122198278999615 ) ) ;
#1105=B_SPLINE_CURVE_WITH_KNOTS ( 'NONE', 3,
 ( #52305, #25741, #42173, #52649, #53688, #11036 ),
 .UNSPECIFIED., .F., .F.,
 ( 4, 2, 4 ),
 ( 0.000000000000000000, 0.5000000000000000000, 1.000000000000000000 ),
 .UNSPECIFIED. ) ;
#1115=EDGE_LOOP ( 'NONE', ( #37361, #63353, #248, #26137, #18913 ) ) ;
#1116=CARTESIAN_POINT ( 'NONE',  ( 9.292835841232999883, 5.200883864107000321, -6.027780766890000308 ) ) ;
#1130=EDGE_LOOP ( 'NONE', ( #15241, #60982, #45864, #48062, #6883 ) ) ;
#1131=CARTESIAN_POINT ( 'NONE',  ( 8.559020380274414919, 4.705862675926775651, 8.704770267039732445 ) ) ;
#1135=DIRECTION ( 'NONE',  ( 0.000000000000000000, 0.9048270524660052549, -0.4257792915651026910 ) ) ;
#1139=ADVANCED_FACE ( 'NONE', ( #66480 ), #2857, .F. ) ;
#1145=ADVANCED_FACE ( 'NONE', ( #44144 ), #38890, .T. ) ;
#1149=CARTESIAN_POINT ( 'NONE',  ( 6.652728317542999648, 4.719833207100999850, -8.789699670502999496 ) ) ;
#1153=CARTESIAN_POINT ( 'NONE',  ( 10.02394528041000044, 5.481267232667000222, -8.005061172455999241 ) ) ;
#1157=CARTESIAN_POINT ( 'NONE',  ( 11.09999965054999826, -2.398081733189999864E-14, 0.000000000000000000 ) ) ;
#1160=DIRECTION ( 'NONE',  ( 0.000000000000000000, 0.000000000000000000, -1.000000000000000000 ) ) ;
#1165=CYLINDRICAL_SURFACE ( 'NONE', #35113, 3.500000000000000000 ) ;
#1186=DIRECTION ( 'NONE',  ( 0.000000000000000000, -1.000000000000000000, 0.000000000000000000 ) ) ;
#1192=ORIENTED_EDGE ( 'NONE', *, *, #19050, .T. ) ;
#1197=EDGE_CURVE ( 'NONE', #5681, #47380, #25405, .T. ) ;
#1199=CARTESIAN_POINT ( 'NONE',  ( 7.000000000000000888, 9.410344523941196471, 4.699947945108982061 ) ) ;
#1203=DIRECTION ( 'NONE',  ( -1.000000000000000000, 0.000000000000000000, 0.000000000000000000 ) ) ;
#1207=CARTESIAN_POINT ( 'NONE',  ( 9.070789158774999805, 5.349936549139000519, -7.138437102151999447 ) ) ;
#1209=CARTESIAN_POINT ( 'NONE',  ( 8.771640687503264644, 2.873222873813474632, 6.752018918873988085 ) ) ;
#1210=CARTESIAN_POINT ( 'NONE',  ( 6.826920280409000341, 5.346927244140000646, -8.589407719218000281 ) ) ;
#1214=CARTESIAN_POINT ( 'NONE',  ( 8.100000113405998903, 3.037570195374000164E-13, -12.39999890530004123 ) ) ;
#1216=EDGE_LOOP ( 'NONE', ( #57811, #11201, #40238 ) ) ;
#1226=CARTESIAN_POINT ( 'NONE',  ( 7.297051343136737422, 2.650314471270581063, -7.803711873237447527 ) ) ;
#1233=CARTESIAN_POINT ( 'NONE',  ( 9.991525552923999243, 4.805950298207000593, -8.932431532051998246 ) ) ;
#1241=ORIENTED_EDGE ( 'NONE', *, *, #9940, .T. ) ;
#1250=LINE ( 'NONE', #43208, #68567 ) ;
#1260=CARTESIAN_POINT ( 'NONE',  ( 9.003345280414000840, 2.319062457810000311, -7.919229449146000022 ) ) ;
#1265=CARTESIAN_POINT ( 'NONE',  ( 0.8396236793818999677, -2.525007632204000263, -2.706826389191999915 ) ) ;
#1267=CARTESIAN_POINT ( 'NONE',  ( 2.552384041004999826, 3.577765746644000266, 1.152375606624999937 ) ) ;
#1268=VERTEX_POINT ( 'NONE', #2512 ) ;
#1270=CARTESIAN_POINT ( 'NONE',  ( 6.899999691988000450, 12.20988339176000004, -3.111064831549000154 ) ) ;
#1274=CARTESIAN_POINT ( 'NONE',  ( 8.373670280412000011, 2.202812441249000219, 7.706988150133999405 ) ) ;
#1277=CARTESIAN_POINT ( 'NONE',  ( 8.145870280407001118, 3.552539078410000162, -8.999639305067001160 ) ) ;
#1280=CARTESIAN_POINT ( 'NONE',  ( 9.520797373037000355, 3.270552986600999912, 5.711478154812000163 ) ) ;
#1294=CARTESIAN_POINT ( 'NONE',  ( 10.20000030442999872, 12.49999969551000056, -3.568568717444000015E-10 ) ) ;
#1297=DIRECTION ( 'NONE',  ( -1.000000000000000000, 0.000000000000000000, 0.000000000000000000 ) ) ;
#1301=ORIENTED_EDGE ( 'NONE', *, *, #41104, .T. ) ;
#1303=FACE_OUTER_BOUND ( 'NONE', #8010, .T. ) ;
#1304=CARTESIAN_POINT ( 'NONE',  ( 8.404999999999999361, 5.190914425723000214, -8.768195054477999406 ) ) ;
#1305=DIRECTION ( 'NONE',  ( 0.000000000000000000, 1.000000000000000000, 0.000000000000000000 ) ) ;
#1314=CARTESIAN_POINT ( 'NONE',  ( 10.01622971959000097, 4.325866256860000369, -9.125812605905000652 ) ) ;
#1315=CARTESIAN_POINT ( 'NONE',  ( 3.418575286264000201, -1.583709913295999971, 2.797960796442000131 ) ) ;
#1317=LINE ( 'NONE', #11119, #24965 ) ;
#1318=CARTESIAN_POINT ( 'NONE',  ( 7.607791299150002295, 3.471796661068001999, -6.504286038290998384 ) ) ;
#1321=ORIENTED_EDGE ( 'NONE', *, *, #14631, .T. ) ;
#1323=CARTESIAN_POINT ( 'NONE',  ( 10.06344080699000010, 5.156228702401000952, 6.125219923432000613 ) ) ;
#1328=CARTESIAN_POINT ( 'NONE',  ( 10.12947109217999930, 5.100000000000000533, 6.152188490330000370 ) ) ;
#1344=CARTESIAN_POINT ( 'NONE',  ( 9.208107780409999776, 5.057081813675999626, 8.967637988488998957 ) ) ;
#1345=CARTESIAN_POINT ( 'NONE',  ( 9.807804719590000886, 3.988943694240999704, -8.966360307350999648 ) ) ;
#1347=CARTESIAN_POINT ( 'NONE',  ( 2.897287607496109807, 0.1609468932050526768, 3.253943878959492331 ) ) ;
#1349=CARTESIAN_POINT ( 'NONE',  ( 10.91307008594999850, 2.096286256021000050, 7.827189715349000210 ) ) ;
#1370=ORIENTED_EDGE ( 'NONE', *, *, #801, .T. ) ;
#1371=CARTESIAN_POINT ( 'NONE',  ( 9.161379719595000637, 5.511689883260999956, -7.095113581311000672 ) ) ;
#1375=ORIENTED_EDGE ( 'NONE', *, *, #64062, .T. ) ;
#1376=CARTESIAN_POINT ( 'NONE',  ( 8.158337970077000990E-06, 2.999989272562999965, 0.000000000000000000 ) ) ;
#1380=CARTESIAN_POINT ( 'NONE',  ( 9.517197013793715854, 5.205368702673863091, 8.206177812346076905 ) ) ;
#1387=CARTESIAN_POINT ( 'NONE',  ( 10.28774346735000123, 5.077605961126000267, -5.991341245382999503 ) ) ;
#1390=CARTESIAN_POINT ( 'NONE',  ( 7.982285464787000961, 4.608336336177999648, -6.267435635568999963 ) ) ;
#1394=CARTESIAN_POINT ( 'NONE',  ( 9.187739158772000536, 5.964723767581000757, 7.776480083716999836 ) ) ;
#1395=EDGE_LOOP ( 'NONE', ( #37179, #57187, #32619, #49048, #36873 ) ) ;
#1396=B_SPLINE_CURVE_WITH_KNOTS ( 'NONE', 3,
 ( #38125, #59801, #11903, #21699 ),
 .UNSPECIFIED., .F., .F.,
 ( 4, 4 ),
 ( 0.000000000000000000, 1.000000000000000000 ),
 .UNSPECIFIED. ) ;
#1398=CARTESIAN_POINT ( 'NONE',  ( 8.475341021510232054, 5.350570349241480450, 7.499981640446101494 ) ) ;
#1402=CARTESIAN_POINT ( 'NONE',  ( 9.475279990687596410, 5.350441389720215213, 7.499985493516660107 ) ) ;
#1404=CARTESIAN_POINT ( 'NONE',  ( 11.08492721656000057, 3.668390701878999849, 5.558148445539999649 ) ) ;
#1407=ORIENTED_EDGE ( 'NONE', *, *, #43007, .F. ) ;
#1410=DIRECTION ( 'NONE',  ( 0.7071090068939822615, 0.000000000000000000, -0.7071045554721071547 ) ) ;
#1412=AXIS2_PLACEMENT_3D ( 'NONE', #13011, #55655, #7755 ) ;
#1415=CARTESIAN_POINT ( 'NONE',  ( 7.983198341228001205, 5.321913229613000063, 8.118244847118999630 ) ) ;
#1418=CARTESIAN_POINT ( 'NONE',  ( 10.52638970730999901, 2.451081172664000274, 6.282749363171999946 ) ) ;
#1420=ORIENTED_EDGE ( 'NONE', *, *, #9940, .F. ) ;
#1421=CARTESIAN_POINT ( 'NONE',  ( 7.726448341228000061, 2.630487280353000390, 6.995957894972000268 ) ) ;
#1424=CARTESIAN_POINT ( 'NONE',  ( 9.574741131514889148, 3.579783539280448679, 8.799459768377362323 ) ) ;
#1431=EDGE_CURVE ( 'NONE', #59495, #14271, #42132, .T. ) ;
#1432=CARTESIAN_POINT ( 'NONE',  ( 1.014608762361999927, 1.892658550137999995, 3.053125390820000007 ) ) ;
#1438=CARTESIAN_POINT ( 'NONE',  ( 6.999999691988000095, 0.000000000000000000, 0.000000000000000000 ) ) ;
#1442=CARTESIAN_POINT ( 'NONE',  ( 8.370221971083998014, 8.037647819758998224, -4.982909524621000230 ) ) ;
#1443=DIRECTION ( 'NONE',  ( 0.000000000000000000, 0.000000000000000000, -1.000000000000000000 ) ) ;
#1446=CARTESIAN_POINT ( 'NONE',  ( 1.085247135132000107, 2.814509306356999918, 2.491368026013999870 ) ) ;
#1447=CARTESIAN_POINT ( 'NONE',  ( 10.66714959199030410, 5.079709024444567511, -8.329714913667638498 ) ) ;
#1448=B_SPLINE_CURVE_WITH_KNOTS ( 'NONE', 3,
 ( #31023, #3398, #41841, #19833, #40461, #62470, #46407, #52331, #35911, #61791 ),
 .UNSPECIFIED., .F., .F.,
 ( 4, 2, 2, 2, 4 ),
 ( 0.000000000000000000, 0.1250000000000001665, 0.2500000000000002776, 0.3750000000000004441, 0.5000000000000005551 ),
 .UNSPECIFIED. ) ;
#1455=DIRECTION ( 'NONE',  ( 0.000000000000000000, 0.000000000000000000, -1.000000000000000000 ) ) ;
#1457=CARTESIAN_POINT ( 'NONE',  ( 9.408231868349719917, 5.323181814481385388, 7.228671914213086858 ) ) ;
#1458=ORIENTED_EDGE ( 'NONE', *, *, #33084, .T. ) ;
#1459=CARTESIAN_POINT ( 'NONE',  ( 8.994485841233000656, 3.854507394315999758, -9.394302886912999639 ) ) ;
#1464=EDGE_LOOP ( 'NONE', ( #38827, #63076, #36669, #30707 ) ) ;
#1466=CARTESIAN_POINT ( 'NONE',  ( 27.64127793187000037, 2.399999999999999911, 6.571291218949999902 ) ) ;
#1467=CARTESIAN_POINT ( 'NONE',  ( 8.396419424012371735, 5.286796060078585491, 7.027454876807467166 ) ) ;
#1468=CARTESIAN_POINT ( 'NONE',  ( 10.83668832355999889, 4.288537082977999404, 9.448742031664000507 ) ) ;
#1470=CARTESIAN_POINT ( 'NONE',  ( 11.09999999969000051, 8.475027130630000016, -6.745942718869000210 ) ) ;
#1475=CYLINDRICAL_SURFACE ( 'NONE', #7670, 0.4999999999999998335 ) ;
#1491=EDGE_LOOP ( 'NONE', ( #34098, #13524, #34844, #26152 ) ) ;
#1492=CARTESIAN_POINT ( 'NONE',  ( 7.424590560819000373, 5.346164515353000191, -7.398308812559000636 ) ) ;
#1493=DIRECTION ( 'NONE',  ( 0.000000000000000000, -0.8648648648648720183, 0.5020047465136825426 ) ) ;
#1496=B_SPLINE_CURVE_WITH_KNOTS ( 'NONE', 3,
 ( #53555, #757, #32921, #64363 ),
 .UNSPECIFIED., .F., .F.,
 ( 4, 4 ),
 ( 0.000000000000000000, 0.1253988501910747455 ),
 .UNSPECIFIED. ) ;
#1497=CARTESIAN_POINT ( 'NONE',  ( 8.929995280412999392, 5.030502105212999453, -6.322203460290999999 ) ) ;
#1504=FACE_OUTER_BOUND ( 'NONE', #31225, .T. ) ;
#1505=FACE_OUTER_BOUND ( 'NONE', #35515, .T. ) ;
#1520=ORIENTED_EDGE ( 'NONE', *, *, #12013, .F. ) ;
#1530=CARTESIAN_POINT ( 'NONE',  ( 6.899999691988000450, 12.43893545635000031, -2.828937028792000152 ) ) ;
#1533=ORIENTED_EDGE ( 'NONE', *, *, #47663, .F. ) ;
#1537=CARTESIAN_POINT ( 'NONE',  ( 2.312398069789000310, -2.519008840803133698, -2.453290717214521077 ) ) ;
#1539=DIRECTION ( 'NONE',  ( 0.000000000000000000, 0.000000000000000000, 1.000000000000000000 ) ) ;
#1540=CARTESIAN_POINT ( 'NONE',  ( 10.26685100253999927, 2.832432432432000269, 6.822293592207000934 ) ) ;
#1542=CARTESIAN_POINT ( 'NONE',  ( 0.1274953728650994322, -0.5341933183653647665, -3.127475674304287967 ) ) ;
#1544=ORIENTED_EDGE ( 'NONE', *, *, #22077, .T. ) ;
#1545=FACE_OUTER_BOUND ( 'NONE', #6452, .T. ) ;
#1547=CARTESIAN_POINT ( 'NONE',  ( 8.424364158774000799, 3.292387953886000140, -6.294868737226000377 ) ) ;
#1553=CARTESIAN_POINT ( 'NONE',  ( 8.849204462305999996, 2.899999999999999911, -6.662590550603814776 ) ) ;
#1554=AXIS2_PLACEMENT_3D ( 'NONE', #1589, #22905, #65555 ) ;
#1556=CARTESIAN_POINT ( 'NONE',  ( 9.643864158774000828, 2.927176851028000293, -5.932007155957999878 ) ) ;
#1558=CARTESIAN_POINT ( 'NONE',  ( 10.64447074117000014, 5.073827170570999634, -8.340679549192000053 ) ) ;
#1574=CARTESIAN_POINT ( 'NONE',  ( 11.24323278040999874, 2.479734175328000223, -7.587230544849999703 ) ) ;
#1582=EDGE_LOOP ( 'NONE', ( #30528, #56779, #3834, #2096, #67818 ) ) ;
#1583=ORIENTED_EDGE ( 'NONE', *, *, #45645, .F. ) ;
#1584=CARTESIAN_POINT ( 'NONE',  ( 8.848264158775000610, 5.751585344281000545, -8.235867044345999588 ) ) ;
#1589=CARTESIAN_POINT ( 'NONE',  ( 0.000000000000000000, 2.899999999999999911, 7.500000000000000000 ) ) ;
#1592=DIRECTION ( 'NONE',  ( 0.000000000000000000, -0.8350135785640888653, -0.5502293372890927348 ) ) ;
#1602=VERTEX_POINT ( 'NONE', #47322 ) ;
#1604=CARTESIAN_POINT ( 'NONE',  ( 7.961495038489999843, 3.389986099490999827, -6.279439026173999849 ) ) ;
#1605=CARTESIAN_POINT ( 'NONE',  ( 8.704995280412999747, 5.140767546012999567, -6.196177269779999719 ) ) ;
#1609=CARTESIAN_POINT ( 'NONE',  ( 0.4283022342298000162, 1.316872153397000034, -3.459566938009000392 ) ) ;
#1612=CARTESIAN_POINT ( 'NONE',  ( 9.374036292344317900, 2.996224904950563150, 8.935525811917834460 ) ) ;
#1613=CARTESIAN_POINT ( 'NONE',  ( 2.399791516557000293, -2.527095471400999660, 2.312705381146000327 ) ) ;
#1614=ORIENTED_EDGE ( 'NONE', *, *, #62391, .F. ) ;
#1619=CARTESIAN_POINT ( 'NONE',  ( 7.705392219590000202, 3.245534453799999941, 8.949623695221001540 ) ) ;
#1622=CARTESIAN_POINT ( 'NONE',  ( 8.584535841227999953, 5.395910762051999932, -7.432402852051000153 ) ) ;
#1624=DIRECTION ( 'NONE',  ( 1.000000000000000000, 0.000000000000000000, 0.000000000000000000 ) ) ;
#1627=ORIENTED_EDGE ( 'NONE', *, *, #25480, .F. ) ;
#1642=CARTESIAN_POINT ( 'NONE',  ( 7.000002934099999408, 1.243449787579999883E-13, -12.49999584805017250 ) ) ;
#1644=AXIS2_PLACEMENT_3D ( 'NONE', #1722, #44391, #17814 ) ;
#1648=PLANE ( 'NONE',  #5957 ) ;
#1650=CARTESIAN_POINT ( 'NONE',  ( 8.087797165043788539, 2.143741258173240460, -7.557751568339210024 ) ) ;
#1651=CARTESIAN_POINT ( 'NONE',  ( 5.000030787343000327, 1.679270695423619619, 1.290525307673962674 ) ) ;
#1654=EDGE_CURVE ( 'NONE', #56837, #65371, #36476, .T. ) ;
#1662=CARTESIAN_POINT ( 'NONE',  ( 9.643864158774000828, 2.927176851028000293, -5.932007155957999878 ) ) ;
#1663=CARTESIAN_POINT ( 'NONE',  ( 3.341497993174000314, 3.378630897718999826, -0.07134658118214000366 ) ) ;
#1670=CARTESIAN_POINT ( 'NONE',  ( 1.954534975661666785, 1.236092914997090064, -3.291825510064176896 ) ) ;
#1672=CARTESIAN_POINT ( 'NONE',  ( 10.71256887705999894, 5.951815279772000089, 7.233043586354999555 ) ) ;
#1676=CARTESIAN_POINT ( 'NONE',  ( 9.180263857702785302, 2.858372283262407887, 8.226552109004314772 ) ) ;
#1678=CARTESIAN_POINT ( 'NONE',  ( 11.01895424672824397, 5.424779607850673813, 7.028465765783779240 ) ) ;
#1691=CARTESIAN_POINT ( 'NONE',  ( 7.282482780409000434, 3.448180532882000104, 9.222462917385000125 ) ) ;
#1692=CARTESIAN_POINT ( 'NONE',  ( 8.895035841232999729, 5.751585344281000545, -8.235867044345999588 ) ) ;
#1699=EDGE_CURVE ( 'NONE', #35262, #29277, #52901, .T. ) ;
#1701=CARTESIAN_POINT ( 'NONE',  ( 7.832795987768000678, 2.851255020980998811, 6.795938453665997692 ) ) ;
#1709=CARTESIAN_POINT ( 'NONE',  ( -15.86200481174999943, 5.599999999999999645, 6.571291218949999902 ) ) ;
#1711=ORIENTED_EDGE ( 'NONE', *, *, #29031, .F. ) ;
#1717=CARTESIAN_POINT ( 'NONE',  ( 9.889535841229999846, 5.798263352390999437, -8.113145944980999502 ) ) ;
#1721=( BOUNDED_SURFACE ( )  B_SPLINE_SURFACE ( 3, 3, ( 
 ( #15410, #32518, #53151, #43000, #4903, #48245, #43358, #63632, #22011 ),
 ( #1050, #47572, #9, #16081, #53834, #5931, #27273, #64659, #16763 ),
 ( #37413, #63280, #32862, #32182, #54175, #6273, #27614, #53497, #36736 ),
 ( #58734, #349, #68877, #20994, #42330, #15749, #60122, #45084, #23051 ) ),
 .UNSPECIFIED., .F., .F., .T. ) 
 B_SPLINE_SURFACE_WITH_KNOTS ( ( 4, 4 ),
 ( 4, 1, 1, 1, 1, 1, 4 ),
 ( 0.000000000000000000, 1.000000000000000000 ),
 ( -0.004644144098274999473, 0.000000000000000000, 0.03269534097185999855, 0.06255479614191999937, 0.08986301827557000022, 0.1148786485006000058, 0.1342276000085000087 ),
 .UNSPECIFIED. ) 
 GEOMETRIC_REPRESENTATION_ITEM ( )  RATIONAL_B_SPLINE_SURFACE ( (
 ( 1.157365337832999996, 1.157365337832999996, 1.157365337832999996, 1.157365337832999996, 1.157365337832999996, 1.157365337832999996, 1.157365337832999996, 1.157365337832999996, 1.157365337832999996),
 ( 0.9475448873890999213, 0.9475448873890999213, 0.9475448873890999213, 0.9475448873890999213, 0.9475448873890999213, 0.9475448873890999213, 0.9475448873890999213, 0.9475448873890999213, 0.9475448873890999213),
 ( 0.9475448873890999213, 0.9475448873890999213, 0.9475448873890999213, 0.9475448873890999213, 0.9475448873890999213, 0.9475448873890999213, 0.9475448873890999213, 0.9475448873890999213, 0.9475448873890999213),
 ( 1.157365337832999996, 1.157365337832999996, 1.157365337832999996, 1.157365337832999996, 1.157365337832999996, 1.157365337832999996, 1.157365337832999996, 1.157365337832999996, 1.157365337832999996) ) ) 
 REPRESENTATION_ITEM ( '' )  SURFACE ( )  );
#1722=CARTESIAN_POINT ( 'NONE',  ( 11.09999965054999826, -3.730349362740999292E-14, -9.259260025373999922E-14 ) ) ;
#1731=CARTESIAN_POINT ( 'NONE',  ( 10.95203274796000059, 2.845888289962000162, -5.182718820692000961 ) ) ;
#1733=DIRECTION ( 'NONE',  ( 1.000000000000000000, 0.000000000000000000, 0.000000000000000000 ) ) ;
#1738=EDGE_CURVE ( 'NONE', #38790, #21989, #49551, .T. ) ;
#1739=CARTESIAN_POINT ( 'NONE',  ( 7.930392219590000735, 3.164805384346000228, 9.104735843897000080 ) ) ;
#1743=CARTESIAN_POINT ( 'NONE',  ( 7.139655177822382015, 3.361094247794269574, 8.696675791344738116 ) ) ;
#1747=B_SPLINE_CURVE_WITH_KNOTS ( 'NONE', 3,
 ( #45743, #46770, #56573, #68073, #51662, #20190, #14948, #8677, #30024, #5490, #15296, #21224, #5140, #64548, #246, #52350, #42897, #63861 ),
 .UNSPECIFIED., .F., .F.,
 ( 4, 2, 2, 2, 2, 2, 2, 2, 4 ),
 ( 0.000000000000000000, 0.1250000000000000278, 0.2500000000000000555, 0.3749999999999999445, 0.4999999999999999445, 0.6249999999999998890, 0.7499999999999998890, 0.8750000000000000000, 1.000000000000000000 ),
 .UNSPECIFIED. ) ;
#1749=CARTESIAN_POINT ( 'NONE',  ( 9.409314688805999083, 2.634692233435000031, 8.920311306029999443 ) ) ;
#1751=CARTESIAN_POINT ( 'NONE',  ( 2.175038703101999982, 1.745712609554999961, -2.581970805235000110 ) ) ;
#1764=VECTOR ( 'NONE', #32559, 1000.000000000000000 ) ;
#1765=CARTESIAN_POINT ( 'NONE',  ( 8.047385841228999581, 4.468366666325000125, 8.882140983065999862 ) ) ;
#1766=CARTESIAN_POINT ( 'NONE',  ( 9.305881816721999655, 4.945299866898000829, 9.077891794505999812 ) ) ;
#1769=CARTESIAN_POINT ( 'NONE',  ( 9.345514158774999913, 5.775964236216999836, -8.174909295649001706 ) ) ;
#1771=DIRECTION ( 'NONE',  ( 0.000000000000000000, 0.000000000000000000, -1.000000000000000000 ) ) ;
#1772=CARTESIAN_POINT ( 'NONE',  ( 7.621422090919002912, 4.588776658069999570, 6.481258258681996232 ) ) ;
#1776=ORIENTED_EDGE ( 'NONE', *, *, #618, .T. ) ;
#1778=CARTESIAN_POINT ( 'NONE',  ( 1.925339139801000021, 1.756325177964999984, 2.941112093452000309 ) ) ;
#1785=CARTESIAN_POINT ( 'NONE',  ( 11.04471440339000132, 2.754763222384000176, 5.184237568466999235 ) ) ;
#1789=CARTESIAN_POINT ( 'NONE',  ( 7.614999999996999946, 5.349999999999999645, -7.500000000000000000 ) ) ;
#1792=CARTESIAN_POINT ( 'NONE',  ( 9.721802827886399712, 2.874603711570469677, 6.749639981088244589 ) ) ;
#1793=CARTESIAN_POINT ( 'NONE',  ( 1.609748578980999989, 1.927138280259999892, 3.227152792068999965 ) ) ;
#1795=CARTESIAN_POINT ( 'NONE',  ( 10.76087777166980075, 3.646736399438096132, -8.814656132371421648 ) ) ;
#1797=CARTESIAN_POINT ( 'NONE',  ( 10.62793268324000096, 3.100586971929999880, 8.599896650316999569 ) ) ;
#1799=EDGE_CURVE ( 'NONE', #57590, #42732, #8805, .T. ) ;
#1801=CARTESIAN_POINT ( 'NONE',  ( 7.115095033390245405, 5.350161709276040511, -7.499994210608702083 ) ) ;
#1807=CARTESIAN_POINT ( 'NONE',  ( 9.392285841233000809, 5.775964236216999836, -8.174909295649001706 ) ) ;
#1808=VERTEX_POINT ( 'NONE', #19640 ) ;
#1816=CARTESIAN_POINT ( 'NONE',  ( 10.77462860031000069, 5.575476001419000127, 8.682676628339999425 ) ) ;
#1822=EDGE_CURVE ( 'NONE', #61003, #58602, #36057, .T. ) ;
#1826=DIRECTION ( 'NONE',  ( 1.000000000000000000, 0.000000000000000000, 0.000000000000000000 ) ) ;
#1829=CARTESIAN_POINT ( 'NONE',  ( 10.79967784386921359, 3.012248194717311645, -4.853501387253247756 ) ) ;
#1835=ORIENTED_EDGE ( 'NONE', *, *, #52244, .T. ) ;
#1840=CARTESIAN_POINT ( 'NONE',  ( 7.430271682458000626, 3.037137096735000430, -6.379793420563999895 ) ) ;
#1846=CARTESIAN_POINT ( 'NONE',  ( 9.485829719593997567, 4.953415418491999844, -8.946479654552000227 ) ) ;
#1847=CARTESIAN_POINT ( 'NONE',  ( 4.099967492754000631, -2.049969825927307809, -8.734266014444028751E-09 ) ) ;
#1849=DIRECTION ( 'NONE',  ( 0.000000000000000000, -1.000000000000000000, 0.000000000000000000 ) ) ;
#1854=CARTESIAN_POINT ( 'NONE',  ( 1.105140132542249631, 0.9161175952574701631, 3.408904368339106927 ) ) ;
#1869=DIRECTION ( 'NONE',  ( 0.000000000000000000, 1.000000000000000000, 0.000000000000000000 ) ) ;
#1870=CARTESIAN_POINT ( 'NONE',  ( 5.477523075960999854, -12.82224764859999766, -2.276049205301000189 ) ) ;
#1875=CARTESIAN_POINT ( 'NONE',  ( 8.792630737453640322, 5.083486636429016770, -6.186355545360274100 ) ) ;
#1877=CARTESIAN_POINT ( 'NONE',  ( 7.000000000000000000, 10.29642145254486785, -4.279174610942646950 ) ) ;
#1885=CARTESIAN_POINT ( 'NONE',  ( 10.70271159698171992, 5.100000000000000533, 6.305985889763628727 ) ) ;
#1894=ORIENTED_EDGE ( 'NONE', *, *, #26066, .T. ) ;
#1897=ORIENTED_EDGE ( 'NONE', *, *, #20825, .T. ) ;
#1900=CARTESIAN_POINT ( 'NONE',  ( 8.216604719590000272, 5.331510020787000315, -8.114341808290998159 ) ) ;
#1912=CARTESIAN_POINT ( 'NONE',  ( 10.57793656291999973, 4.393379542724999531, -6.024362243994999311 ) ) ;
#1914=EDGE_CURVE ( 'NONE', #57987, #6055, #56083, .T. ) ;
#1924=ORIENTED_EDGE ( 'NONE', *, *, #13803, .F. ) ;
#1925=CARTESIAN_POINT ( 'NONE',  ( 10.52323372634000087, 3.325642821414999784, 5.689987891230000372 ) ) ;
#1926=CARTESIAN_POINT ( 'NONE',  ( 11.03905471959000018, 3.855072614532999875, -9.179480010827999692 ) ) ;
#1928=CIRCLE ( 'NONE', #20935, 2.750000000000000000 ) ;
#1935=ORIENTED_EDGE ( 'NONE', *, *, #53847, .F. ) ;
#1938=CARTESIAN_POINT ( 'NONE',  ( 9.088029719595001055, 2.881930053949999682, -8.823338183322999129 ) ) ;
#1939=CARTESIAN_POINT ( 'NONE',  ( 6.999999691988000095, -12.11716380430000051, -3.069905306952999791 ) ) ;
#1945=CARTESIAN_POINT ( 'NONE',  ( 8.725348536223823004, 2.649439212887079620, 7.500023728975156345 ) ) ;
#1953=ORIENTED_EDGE ( 'NONE', *, *, #35446, .T. ) ;
#1954=LINE ( 'NONE', #50195, #11797 ) ;
#1956=CARTESIAN_POINT ( 'NONE',  ( 8.506095280410999493, 2.305580295895999665, -7.860904109308999743 ) ) ;
#1958=CARTESIAN_POINT ( 'NONE',  ( 11.09999999999999964, 4.000000000000000000, -7.500000000000000000 ) ) ;
#1962=CARTESIAN_POINT ( 'NONE',  ( 2.304427617675000040, 1.234641978838000087, 3.195386953671000008 ) ) ;
#1970=CARTESIAN_POINT ( 'NONE',  ( 7.924357780410000274, 2.432118421226999949, 6.597517552098000060 ) ) ;
#1975=CARTESIAN_POINT ( 'NONE',  ( 7.440860841227999956, 3.609683333014999995, -6.158094852492999927 ) ) ;
#1977=CARTESIAN_POINT ( 'NONE',  ( 7.851683310611999644, 4.710036428759999616, 6.351753055261999847 ) ) ;
#1979=ORIENTED_EDGE ( 'NONE', *, *, #63681, .F. ) ;
#1980=CARTESIAN_POINT ( 'NONE',  ( 8.227533346876342080, 4.737976145808172390, 6.141445531819171855 ) ) ;
#1986=CARTESIAN_POINT ( 'NONE',  ( 10.97494570512294132, 8.502725158598858357, -6.546417107134506530 ) ) ;
#1987=CARTESIAN_POINT ( 'NONE',  ( 8.316694475082000437, 2.898380349184999982, 6.611503672649000407 ) ) ;
#1992=CARTESIAN_POINT ( 'NONE',  ( 8.513426658773999733, 5.040787533781999841, 8.522957620707000359 ) ) ;
#1998=CARTESIAN_POINT ( 'NONE',  ( -2.444943969992999916E-05, -2.899969545325999931, 0.000000000000000000 ) ) ;
#1999=CARTESIAN_POINT ( 'NONE',  ( 7.491097165042828188, 3.407826859982625578, -9.260216617036411080 ) ) ;
#2002=CARTESIAN_POINT ( 'NONE',  ( 8.205992358813000820, 3.399999999999999911, 6.138278517057000450 ) ) ;
#2005=VERTEX_POINT ( 'NONE', #26607 ) ;
#2009=CARTESIAN_POINT ( 'NONE',  ( 0.1499942179679999987, -2.750000000000000000, 0.000000000000000000 ) ) ;
#2011=CARTESIAN_POINT ( 'NONE',  ( 2.622152980194000005, -0.2193973046792999926, -3.207556849382000141 ) ) ;
#2013=ADVANCED_FACE ( 'NONE', ( #10856 ), #5603, .T. ) ;
#2015=CARTESIAN_POINT ( 'NONE',  ( 10.72422653164066730, 2.899999999999999911, -6.304440313833583609 ) ) ;
#2020=COLOUR_RGB ( '', 0.66274510, 0.83137255, 0.94901961) ;
#2021=CARTESIAN_POINT ( 'NONE',  ( 10.26537527815838580, 5.100000000000000533, 6.445686799303629755 ) ) ;
#2023=CARTESIAN_POINT ( 'NONE',  ( 9.786671076420999427, 2.381202181614999525, 7.612749448318000489 ) ) ;
#2026=CARTESIAN_POINT ( 'NONE',  ( 11.08333333333437842, 2.470076941866840237, 7.228155005602348915 ) ) ;
#2029=CARTESIAN_POINT ( 'NONE',  ( 10.52052890781999928, 2.899999999999999911, 6.152188490330000370 ) ) ;
#2033=CARTESIAN_POINT ( 'NONE',  ( 8.130886538030239308, 4.885509777356301875, -6.278165256758011736 ) ) ;
#2034=CARTESIAN_POINT ( 'NONE',  ( 11.35906500789999996, 2.719101288111000159, -7.157645240044000268 ) ) ;
#2035=ORIENTED_EDGE ( 'NONE', *, *, #57349, .F. ) ;
#2048=EDGE_CURVE ( 'NONE', #14563, #36985, #42657, .T. ) ;
#2049=CARTESIAN_POINT ( 'NONE',  ( 11.09647882763000126, 3.099775370665000196, 6.097099813297999660 ) ) ;
#2053=CARTESIAN_POINT ( 'NONE',  ( 8.016657426769000949, 2.906672751340000804, 6.403732826568004910 ) ) ;
#2055=CARTESIAN_POINT ( 'NONE',  ( 8.455992358796999397, 2.899999999999999911, -6.571291218954000257 ) ) ;
#2061=CARTESIAN_POINT ( 'NONE',  ( 11.07745841296999778, 5.274854172210999614, 5.088889326835999150 ) ) ;
#2069=CARTESIAN_POINT ( 'NONE',  ( 9.102795280413999990, 3.071719032003000116, -6.037263251225000182 ) ) ;
#2088=AXIS2_PLACEMENT_3D ( 'NONE', #24785, #24101, #40861 ) ;
#2095=CARTESIAN_POINT ( 'NONE',  ( 8.251329719592000345, 5.773189794777000117, 7.141495931231999883 ) ) ;
#2096=ORIENTED_EDGE ( 'NONE', *, *, #52477, .F. ) ;
#2098=AXIS2_PLACEMENT_3D ( 'NONE', #41474, #4399, #42170 ) ;
#2101=CARTESIAN_POINT ( 'NONE',  ( 8.204580816340586225, 2.648164948733333635, 7.853008025112000468 ) ) ;
#2102=CARTESIAN_POINT ( 'NONE',  ( 10.44806481732999792, 3.684980864017000091, -6.173120265414000052 ) ) ;
#2105=CARTESIAN_POINT ( 'NONE',  ( 9.753142190738998352, 4.104977339646000090, 9.293283246364000050 ) ) ;
#2106=ADVANCED_FACE ( 'NONE', ( #12247 ), #47478, .F. ) ;
#2108=DIRECTION ( 'NONE',  ( 1.000000000000000000, 0.000000000000000000, 0.000000000000000000 ) ) ;
#2112=CARTESIAN_POINT ( 'NONE',  ( 9.514114512910998300, 4.887632373702999189, 8.462748516415999234 ) ) ;
#2113=DIRECTION ( 'NONE',  ( 0.000000000000000000, 1.000000000000000000, 0.000000000000000000 ) ) ;
#2116=CARTESIAN_POINT ( 'NONE',  ( 8.625073341231001223, 3.117378429069999957, 8.662179062556001341 ) ) ;
#2117=CARTESIAN_POINT ( 'NONE',  ( 9.781673028307999118, 5.464749740720999505, 8.817329433105999925 ) ) ;
#2128=CARTESIAN_POINT ( 'NONE',  ( 1.310247135131999974, 2.440310627160000134, 2.160132089918000098 ) ) ;
#2132=CARTESIAN_POINT ( 'NONE',  ( 7.720433623367209286, 2.879779284299745168, 6.726083774559347361 ) ) ;
#2138=CARTESIAN_POINT ( 'NONE',  ( 7.500416666664126097, 4.176714586764424197, -6.150000000000000355 ) ) ;
#2144=CARTESIAN_POINT ( 'NONE',  ( 1.657430528421999893, -0.2286091751511999948, 3.751814989407999956 ) ) ;
#2146=DIRECTION ( 'NONE',  ( -1.000000000000000000, 0.000000000000000000, 0.000000000000000000 ) ) ;
#2155=CARTESIAN_POINT ( 'NONE',  ( 8.132072785282833394, 10.58563748539984850, 4.156721893235244103 ) ) ;
#2157=EDGE_CURVE ( 'NONE', #61768, #27955, #21192, .T. ) ;
#2159=CARTESIAN_POINT ( 'NONE',  ( 9.342560841233000346, 5.835196551504000517, -7.008466539623000813 ) ) ;
#2163=EDGE_LOOP ( 'NONE', ( #31496, #56603, #67810, #61087 ) ) ;
#2167=CARTESIAN_POINT ( 'NONE',  ( 5.000000000000000000, 0.6769230769231000533, -2.665384615385000266 ) ) ;
#2172=CARTESIAN_POINT ( 'NONE',  ( 0.7509734658760000015, -3.500000000000000000, 0.000000000000000000 ) ) ;
#2188=ORIENTED_EDGE ( 'NONE', *, *, #14440, .T. ) ;
#2189=CARTESIAN_POINT ( 'NONE',  ( 6.950909439180999350, 2.788803157567000035, -8.345558963038001821 ) ) ;
#2190=CARTESIAN_POINT ( 'NONE',  ( 10.60689139212527898, 4.693532862563775332, -4.759459215670841736 ) ) ;
#2195=B_SPLINE_SURFACE_WITH_KNOTS ( 'NONE', 3, 3, ( 
 ( #6315, #53193, #52850, #4947, #37117, #26634, #58431, #10536, #47952, #42704, #37453, #23448, #12969, #39181, #2128, #49669, #44444, #44785, #18553, #17155, #59810, #34291, #11913, #38842, #22745, #55613, #1088, #17514, #50020, #65394, #50365, #61199, #12613, #38488, #55953 ),
 ( #13319, #22402, #34643, #43743, #66086, #29054, #60506, #33944, #44095, #29401, #54916, #18206, #12271, #33598, #7019, #60167, #33253, #7359, #55266, #39882, #7714, #8060, #28354, #2465, #23789, #1778, #23095, #28704, #65742, #65039, #39529, #54571, #6668, #17866, #60852 ),
 ( #45124, #49317, #28008, #66431, #1432, #30088, #14679, #14340, #2806, #56978, #3823, #25507, #35323, #8403, #13655, #50709, #8743, #40553, #9081, #51050, #18897, #24133, #30757, #51729, #62221, #29748, #68142, #20259, #46495, #66782, #67800, #30418, #56299, #40223, #9761 ),
 ( #40901, #19580, #3151, #45467, #56640, #25162, #61881, #13997, #51393, #24483, #61539, #19920, #35663, #41586, #57312, #62896, #67117, #52066, #62557, #3487, #24824, #41245, #46150, #15015, #35997, #34983, #45805, #67455, #19227, #9413, #4171, #46836, #36341, #57656, #21289 ) ),
 .UNSPECIFIED., .F., .F., .F.,
 ( 4, 4 ),
 ( 4, 1, 1, 1, 1, 1, 1, 1, 1, 1, 1, 1, 1, 1, 1, 1, 1, 1, 1, 1, 1, 1, 1, 1, 1, 1, 1, 1, 1, 1, 1, 1, 4 ),
 ( -0.1039370721279000015, 1.103937072127999963 ),
 ( -0.01999999999996000116, 0.01250000000003000100, 0.04500000000002999517, 0.07750000000003000322, 0.1100000000000000006, 0.1424999999999999878, 0.1749999999999999889, 0.2074999999999999900, 0.2399999999999999911, 0.2725000000000000200, 0.3049999999999999933, 0.3375000000000000222, 0.3699999999999999956, 0.4025000000000000244, 0.4349999999999999978, 0.4675000000000000266, 0.5000000000000000000, 0.5324999999999999734, 0.5649999999999999467, 0.5975000000000000311, 0.6300000000000000044, 0.6624999999999999778, 0.6949999999999999512, 0.7275000000000000355, 0.7600000000000000089, 0.7924999999999999822, 0.8249999999999999556, 0.8575000000000000400, 0.8900000000000000133, 0.9224999999999999867, 0.9549999999999999600, 0.9875000000000000444, 1.020000000000000018 ),
 .UNSPECIFIED. ) ;
#2196=CARTESIAN_POINT ( 'NONE',  ( 9.079170280414000871, 4.815598936798999752, -8.835641302565999666 ) ) ;
#2209=DIRECTION ( 'NONE',  ( 0.000000000000000000, -1.000000000000000000, 0.000000000000000000 ) ) ;
#2217=CARTESIAN_POINT ( 'NONE',  ( 11.09999999999999964, 0.000000000000000000, 0.000000000000000000 ) ) ;
#2223=DIRECTION ( 'NONE',  ( 0.000000000000000000, 1.000000000000000000, 0.000000000000000000 ) ) ;
#2225=CARTESIAN_POINT ( 'NONE',  ( 7.000000000000000000, 7.526486366024999874, 3.526486366024999874 ) ) ;
#2228=DIRECTION ( 'NONE',  ( 0.000000000000000000, 0.9565994702956989171, -0.2914059941558995170 ) ) ;
#2236=VECTOR ( 'NONE', #24250, 999.9999999999998863 ) ;
#2237=CARTESIAN_POINT ( 'NONE',  ( 4.900006121741999010, 1.007237960741798055, -1.747572776708516296 ) ) ;
#2238=CARTESIAN_POINT ( 'NONE',  ( 7.000000000000000000, 10.24590114424279363, 4.325272293848827054 ) ) ;
#2243=VERTEX_POINT ( 'NONE', #15931 ) ;
#2244=ADVANCED_FACE ( 'NONE', ( #5446 ), #32707, .F. ) ;
#2245=CARTESIAN_POINT ( 'NONE',  ( 8.466090690305668076, 5.179931350395810874, 8.180989497825182255 ) ) ;
#2246=CARTESIAN_POINT ( 'NONE',  ( 2.759306799211165728, -3.058252359239909346, 1.762666431298136605 ) ) ;
#2247=CARTESIAN_POINT ( 'NONE',  ( 9.988985841228000595, 3.986577607995999806, -9.280166295424001177 ) ) ;
#2253=LINE ( 'NONE', #23567, #59966 ) ;
#2256=ORIENTED_EDGE ( 'NONE', *, *, #58583, .F. ) ;
#2257=CARTESIAN_POINT ( 'NONE',  ( 10.02799997617999850, 3.452028386838999818, -6.074524158096999749 ) ) ;
#2258=ORIENTED_EDGE ( 'NONE', *, *, #786, .F. ) ;
#2263=CARTESIAN_POINT ( 'NONE',  ( 11.06697824072435488, 2.733021759275644946, 6.467485083951054925 ) ) ;
#2268=CARTESIAN_POINT ( 'NONE',  ( 10.66042971959000063, 2.315663237570999566, -7.431702255173999738 ) ) ;
#2275=EDGE_CURVE ( 'NONE', #10113, #8792, #3596, .T. ) ;
#2279=CARTESIAN_POINT ( 'NONE',  ( 9.386379719595000282, 5.673443217382001080, -7.051790060464000476 ) ) ;
#2282=DIRECTION ( 'NONE',  ( 0.8660254037844288266, -2.732564487855089756E-14, 0.5000000000000169864 ) ) ;
#2291=CARTESIAN_POINT ( 'NONE',  ( 11.09999999999999787, 5.503163505825636292, 6.850128801896341102 ) ) ;
#2297=CARTESIAN_POINT ( 'NONE',  ( 9.450870280412999591, 2.928319778732999978, -8.861178115809998701 ) ) ;
#2303=CARTESIAN_POINT ( 'NONE',  ( 8.198728570659000070, 3.399995396149000371, 6.142472185125999573 ) ) ;
#2304=CARTESIAN_POINT ( 'NONE',  ( 3.453567742316999922, -1.715169620629000136, -3.156336854149000448 ) ) ;
#2310=ORIENTED_EDGE ( 'NONE', *, *, #13063, .T. ) ;
#2312=CARTESIAN_POINT ( 'NONE',  ( 8.667410841228999629, 4.727211190310000255, -8.622645617656999661 ) ) ;
#2314=CARTESIAN_POINT ( 'NONE',  ( 6.999998782146999332, -11.95749337870000062, 3.642574926947999892 ) ) ;
#2317=CARTESIAN_POINT ( 'NONE',  ( 8.228368194308000483, 4.806758213781000322, 6.177034601037000527 ) ) ;
#2320=CARTESIAN_POINT ( 'NONE',  ( 11.09999233421999953, 0.5000002011213999786, -9.776630298829998011 ) ) ;
#2325=CARTESIAN_POINT ( 'NONE',  ( 10.95501454684088749, 9.026663460494706470, -6.403348769895080395 ) ) ;
#2328=CARTESIAN_POINT ( 'NONE',  ( 7.739689158769000876, 3.600418141940000094, -8.839175402873999943 ) ) ;
#2331=VERTEX_POINT ( 'NONE', #64162 ) ;
#2339=DIRECTION ( 'NONE',  ( -1.000000000000000000, 0.000000000000000000, 0.000000000000000000 ) ) ;
#2348=ORIENTED_EDGE ( 'NONE', *, *, #9941, .T. ) ;
#2350=CARTESIAN_POINT ( 'NONE',  ( 9.476970280414001024, 5.511689883260999956, -7.095113581311000672 ) ) ;
#2351=CARTESIAN_POINT ( 'NONE',  ( 2.957488688014000111, -2.712413859928999749, 1.726084346459000107 ) ) ;
#2362=CARTESIAN_POINT ( 'NONE',  ( 10.97864812944000157, 5.273131703456000352, 7.958028903907000462 ) ) ;
#2365=CARTESIAN_POINT ( 'NONE',  ( 9.198965353459591654, 2.717767460002217916, 7.940252943362748894 ) ) ;
#2372=CARTESIAN_POINT ( 'NONE',  ( 0.7962103212659377149, -2.967632330001188201, -1.897762364885174913 ) ) ;
#2373=CARTESIAN_POINT ( 'NONE',  ( 10.91733584123000078, 3.256275267152000108, -6.361562334135999919 ) ) ;
#2374=ORIENTED_EDGE ( 'NONE', *, *, #4327, .T. ) ;
#2379=VERTEX_POINT ( 'NONE', #66236 ) ;
#2380=CARTESIAN_POINT ( 'NONE',  ( 8.283079719592000956, 2.376526778640999815, 7.686980884243000745 ) ) ;
#2381=CARTESIAN_POINT ( 'NONE',  ( 8.497235841230001085, 3.789127741898000057, -9.388182174781999123 ) ) ;
#2384=ORIENTED_EDGE ( 'NONE', *, *, #51224, .F. ) ;
#2385=CARTESIAN_POINT ( 'NONE',  ( 10.89227882974000039, 3.998355201738000630, 9.261308739708001170 ) ) ;
#2389=CARTESIAN_POINT ( 'NONE',  ( 7.939460911587998382, 2.865023798136999922, 6.766038833998996971 ) ) ;
#2390=ORIENTED_EDGE ( 'NONE', *, *, #8541, .T. ) ;
#2392=CARTESIAN_POINT ( 'NONE',  ( 1.480140132540750386, 3.408904368339106927, -0.9161175952574746040 ) ) ;
#2402=CARTESIAN_POINT ( 'NONE',  ( 6.999999691988000095, -11.00717859340000082, -1.432487142323000118 ) ) ;
#2405=CARTESIAN_POINT ( 'NONE',  ( 8.555820280412000045, 2.414630869937000046, -6.801495146585999407 ) ) ;
#2413=CYLINDRICAL_SURFACE ( 'NONE', #46311, 3.500000000000000000 ) ;
#2428=DIRECTION ( 'NONE',  ( -1.000000000000000000, 0.000000000000000000, 0.000000000000000000 ) ) ;
#2429=CARTESIAN_POINT ( 'NONE',  ( 7.775614158771000817, 4.636729845879000500, 9.378977473003999421 ) ) ;
#2437=CARTESIAN_POINT ( 'NONE',  ( 9.815201913989998417, 2.813632032385000148, 8.848857341496000117 ) ) ;
#2438=EDGE_CURVE ( 'NONE', #59495, #227, #18014, .T. ) ;
#2446=CARTESIAN_POINT ( 'NONE',  ( 10.51655086620999846, 4.930662802525000110, 8.573584269714999095 ) ) ;
#2451=CARTESIAN_POINT ( 'NONE',  ( 7.262114158771001193, 4.847807297114000491, 9.065373753110998578 ) ) ;
#2452=CARTESIAN_POINT ( 'NONE',  ( 10.96080777006000062, 2.054568739078000306, 7.810084630238000258 ) ) ;
#2454=ORIENTED_EDGE ( 'NONE', *, *, #55405, .T. ) ;
#2455=CARTESIAN_POINT ( 'NONE',  ( 9.684729719592999331, 2.370176859044999862, -6.912649125838000508 ) ) ;
#2464=AXIS2_PLACEMENT_3D ( 'NONE', #38344, #48498, #43251 ) ;
#2465=CARTESIAN_POINT ( 'NONE',  ( 1.829975240918999990, 3.378571531507999826, -0.5657499728117999505 ) ) ;
#2473=CARTESIAN_POINT ( 'NONE',  ( 10.06489140842196406, 5.349900232312646331, -7.500006335289779003 ) ) ;
#2475=CARTESIAN_POINT ( 'NONE',  ( 9.587885841227999251, 3.762712042852999872, 8.787816121229999666 ) ) ;
#2478=CONICAL_SURFACE ( 'NONE', #39314, 11.45000430352999921, 0.7853991313766258697 ) ;
#2480=CARTESIAN_POINT ( 'NONE',  ( 0.7467001509839000795, -0.1589293563100999951, 3.588678346333000313 ) ) ;
#2484=CARTESIAN_POINT ( 'NONE',  ( 10.07102359808000003, 4.042170458878000083, 8.920189456109998360 ) ) ;
#2485=EDGE_CURVE ( 'NONE', #16376, #32335, #50301, .T. ) ;
#2487=CARTESIAN_POINT ( 'NONE',  ( 7.100000000000000533, 5.326087788487999575, -7.247035225330000330 ) ) ;
#2493=CARTESIAN_POINT ( 'NONE',  ( 7.973714672046428475, 2.314332798270127167, 7.004429797696275273 ) ) ;
#2497=ORIENTED_EDGE ( 'NONE', *, *, #38767, .F. ) ;
#2500=CARTESIAN_POINT ( 'NONE',  ( 4.149992563291999836, 0.2617923565147994291, -1.999946284944287722 ) ) ;
#2501=DIRECTION ( 'NONE',  ( 0.000000000000000000, 0.7158784314710772145, 0.6982249432342778617 ) ) ;
#2502=CARTESIAN_POINT ( 'NONE',  ( 9.533434135307000901, 2.564753581125000181, 6.150586364588000343 ) ) ;
#2504=CARTESIAN_POINT ( 'NONE',  ( 10.68375192593000023, 4.547306763790999184, -8.749120576764999768 ) ) ;
#2506=CARTESIAN_POINT ( 'NONE',  ( 11.09999999999999964, 7.281355511280001025, -6.286510895624999762 ) ) ;
#2509=CARTESIAN_POINT ( 'NONE',  ( 10.98688827724838113, 5.367975154760830314, -6.994477628651915246 ) ) ;
#2512=CARTESIAN_POINT ( 'NONE',  ( 7.364999999998000035, 2.649999999999999911, -7.500000000000000000 ) ) ;
#2525=FACE_OUTER_BOUND ( 'NONE', #20210, .T. ) ;
#2530=CARTESIAN_POINT ( 'NONE',  ( 11.07076166751999935, 7.299647376920999520, -6.238566460401999691 ) ) ;
#2531=CARTESIAN_POINT ( 'NONE',  ( 0.3923104132283999901, -3.376221432737999795, -1.056438743269999980 ) ) ;
#2538=EDGE_CURVE ( 'NONE', #56515, #56175, #27023, .T. ) ;
#2544=EDGE_CURVE ( 'NONE', #23293, #2626, #5810, .T. ) ;
#2554=DIRECTION ( 'NONE',  ( 1.000000000000000000, 0.000000000000000000, 0.000000000000000000 ) ) ;
#2558=CARTESIAN_POINT ( 'NONE',  ( 10.44728840309080020, 2.899999999999999911, 6.305985889617041984 ) ) ;
#2561=CARTESIAN_POINT ( 'NONE',  ( 3.500000000000000000, 0.000000000000000000, 0.000000000000000000 ) ) ;
#2564=EDGE_CURVE ( 'NONE', #20189, #34088, #61198, .T. ) ;
#2568=CARTESIAN_POINT ( 'NONE',  ( 8.241912900173000267, 4.599999999999999645, 6.117539782833000928 ) ) ;
#2573=AXIS2_PLACEMENT_3D ( 'NONE', #66289, #18414, #39739 ) ;
#2574=ORIENTED_EDGE ( 'NONE', *, *, #7850, .F. ) ;
#2575=DIRECTION ( 'NONE',  ( 1.000000000000000000, 0.000000000000000000, 0.000000000000000000 ) ) ;
#2577=ORIENTED_EDGE ( 'NONE', *, *, #23518, .T. ) ;
#2578=CARTESIAN_POINT ( 'NONE',  ( 0.2500098862125000321, 0.000000000000000000, 0.000000000000000000 ) ) ;
#2580=CARTESIAN_POINT ( 'NONE',  ( 9.061929719594999710, 4.092867382745001059, -5.937785237406000505 ) ) ;
#2585=ORIENTED_EDGE ( 'NONE', *, *, #6064, .F. ) ;
#2588=CARTESIAN_POINT ( 'NONE',  ( 9.544414158773999901, 2.173570076733999823, -8.023168429484000441 ) ) ;
#2590=CARTESIAN_POINT ( 'NONE',  ( 10.72303311070000120, 3.890114357827999747, -8.859327677199999584 ) ) ;
#2595=CARTESIAN_POINT ( 'NONE',  ( 10.98960529797957797, 5.570865012723525744, -4.946148922830412964 ) ) ;
#2601=B_SPLINE_CURVE_WITH_KNOTS ( 'NONE', 3,
 ( #29683, #67054, #20883, #26826 ),
 .UNSPECIFIED., .F., .F.,
 ( 4, 4 ),
 ( 0.000000000000000000, 1.000000000000000000 ),
 .UNSPECIFIED. ) ;
#2605=CARTESIAN_POINT ( 'NONE',  ( 11.26847444708000090, 2.565620268983000329, -7.116623294300999270 ) ) ;
#2615=CARTESIAN_POINT ( 'NONE',  ( 9.983079719591000156, 5.002683760508999988, -8.912673867568997821 ) ) ;
#2616=CARTESIAN_POINT ( 'NONE',  ( 5.500000000000000000, 12.43893545635000031, 2.828937028792000152 ) ) ;
#2626=VERTEX_POINT ( 'NONE', #43639 ) ;
#2634=CARTESIAN_POINT ( 'NONE',  ( 4.149992563291999836, -1.999946284944288388, 0.2617923565147958764 ) ) ;
#2638=CARTESIAN_POINT ( 'NONE',  ( 9.401145280412999128, 3.927090956378999742, -9.230892435423001530 ) ) ;
#2639=CARTESIAN_POINT ( 'NONE',  ( 4.000000000000000000, -2.750000000000000000, 0.000000000000000000 ) ) ;
#2641=CARTESIAN_POINT ( 'NONE',  ( 10.31905590579000176, 2.899999999999999911, -6.571291218949999902 ) ) ;
#2643=CARTESIAN_POINT ( 'NONE',  ( 2.209063718793000231, 3.425644328890999901, 0.01271980431870000164 ) ) ;
#2646=CARTESIAN_POINT ( 'NONE',  ( 10.98768472639999949, 2.860900986606000007, -4.945212061661000469 ) ) ;
#2650=ORIENTED_EDGE ( 'NONE', *, *, #12277, .F. ) ;
#2652=CARTESIAN_POINT ( 'NONE',  ( 10.90000004630000063, 9.856474695503001371, 5.627825000517000298 ) ) ;
#2654=CARTESIAN_POINT ( 'NONE',  ( 10.56498513754044311, 5.349957030113837497, -7.500000808964303545 ) ) ;
#2655=CARTESIAN_POINT ( 'NONE',  ( 7.804619354695629063, 2.996383457933911032, 6.547394516041353363 ) ) ;
#2661=FACE_OUTER_BOUND ( 'NONE', #54085, .T. ) ;
#2667=CARTESIAN_POINT ( 'NONE',  ( 10.92122291580152371, 9.608538131000051052, -5.970078283598937219 ) ) ;
#2669=CARTESIAN_POINT ( 'NONE',  ( 10.90000000000000036, 5.283926297003000094, 7.082827057608000132 ) ) ;
#2673=CARTESIAN_POINT ( 'NONE',  ( 9.524624721938954153, 2.899999999999999911, -6.445686799096955966 ) ) ;
#2682=CARTESIAN_POINT ( 'NONE',  ( 11.09999999999999964, 4.000000000000000000, -7.500000000000000000 ) ) ;
#2683=CARTESIAN_POINT ( 'NONE',  ( 3.500000000000000444, 1.332139861897094546, 3.064909822328984568 ) ) ;
#2684=CARTESIAN_POINT ( 'NONE',  ( 10.11094409420000062, 5.100000000000000533, -6.571291218949999902 ) ) ;
#2686=AXIS2_PLACEMENT_3D ( 'NONE', #68665, #26379, #63067 ) ;
#2690=EDGE_CURVE ( 'NONE', #4735, #21492, #57171, .T. ) ;
#2695=CARTESIAN_POINT ( 'NONE',  ( 8.548770280408998445, 5.203550244299999683, -8.391678825488000371 ) ) ;
#2697=CARTESIAN_POINT ( 'NONE',  ( 2.922328358399999715, 1.841131904257000018, 2.833808463758999974 ) ) ;
#2703=CARTESIAN_POINT ( 'NONE',  ( 10.22108913916999917, 2.983268757921999637, 8.764704075288999974 ) ) ;
#2706=CARTESIAN_POINT ( 'NONE',  ( 9.566963020987998334, 5.215925787220999865, 6.177726425586999248 ) ) ;
#2707=CARTESIAN_POINT ( 'NONE',  ( 10.90000000000000036, 5.283926297003000094, 7.082827057608000132 ) ) ;
#2708=VECTOR ( 'NONE', #49482, 1000.000000000000000 ) ;
#2716=CARTESIAN_POINT ( 'NONE',  ( 10.84161084123000052, 2.641275823976000137, -7.444905437480000110 ) ) ;
#2724=CARTESIAN_POINT ( 'NONE',  ( 7.550614158771000284, 4.468366666325000125, 8.882140983065999862 ) ) ;
#2725=CARTESIAN_POINT ( 'NONE',  ( 9.442010841233001273, 5.045571591548999812, -9.086294919530001124 ) ) ;
#2726=CARTESIAN_POINT ( 'NONE',  ( 0.6825985948785217028, -0.3204594736343227002, 3.524357824565985897 ) ) ;
#2727=CARTESIAN_POINT ( 'NONE',  ( 10.30480165877000154, 5.828331171948000211, -7.226590957700000928 ) ) ;
#2729=CARTESIAN_POINT ( 'NONE',  ( 11.02445190299000011, 3.404087387974999768, 5.822483872269000216 ) ) ;
#2736=CARTESIAN_POINT ( 'NONE',  ( 1.428056799207624739, 2.150913519912206695, -2.798833948393627313 ) ) ;
#2741=ORIENTED_EDGE ( 'NONE', *, *, #67162, .T. ) ;
#2749=CARTESIAN_POINT ( 'NONE',  ( 11.09999999999999964, 3.512324525112999751, -8.971282648301999174 ) ) ;
#2750=CARTESIAN_POINT ( 'NONE',  ( 8.506095280410999493, 2.305580295895999665, -7.860904109308999743 ) ) ;
#2757=CARTESIAN_POINT ( 'NONE',  ( 0.000000000000000000, 0.000000000000000000, 0.000000000000000000 ) ) ;
#2763=B_SPLINE_SURFACE_WITH_KNOTS ( 'NONE', 3, 3, ( 
 ( #60568, #59870, #27726, #49376, #1840, #59526, #12676, #38904, #53931, #17576, #37856 ),
 ( #1492, #16872, #60226, #22458, #27372, #32962, #54276, #23158, #48699, #33314, #59181 ),
 ( #11975, #54630, #12329, #7421, #50082, #54979, #2189, #7077, #6377, #44506, #23503 ),
 ( #49040, #17222, #65800, #64754, #799, #11280, #66150, #6726, #1149, #32620, #22116 ) ),
 .UNSPECIFIED., .F., .F., .F.,
 ( 4, 4 ),
 ( 4, 1, 1, 1, 1, 1, 1, 1, 4 ),
 ( -0.1039370721279000015, 1.103937072127999963 ),
 ( 0.6999999999992999600, 0.7382352941170999827, 0.7764705882347999744, 0.8147058823525000770, 0.8529411764702999887, 0.8911764705879999804, 0.9294117647057000831, 0.9676470588234999948, 1.005882352940999924 ),
 .UNSPECIFIED. ) ;
#2767=CARTESIAN_POINT ( 'NONE',  ( 6.724999999999962341, 5.339057002848987210, -8.130112396048081891 ) ) ;
#2776=DIRECTION ( 'NONE',  ( 0.000000000000000000, 1.000000000000000000, 0.000000000000000000 ) ) ;
#2788=CARTESIAN_POINT ( 'NONE',  ( 11.12915085989000019, 3.083869275439000024, 8.585995236726001067 ) ) ;
#2792=EDGE_CURVE ( 'NONE', #49108, #68077, #61771, .T. ) ;
#2794=CARTESIAN_POINT ( 'NONE',  ( 9.214142219592000416, 5.421534627450999899, 6.381126373995999579 ) ) ;
#2795=CARTESIAN_POINT ( 'NONE',  ( 9.199602729599000384, 2.551394566582000145, 7.536605852160000119 ) ) ;
#2798=CARTESIAN_POINT ( 'NONE',  ( 9.395239158775000377, 5.045571591548999812, -9.086294919530001124 ) ) ;
#2806=CARTESIAN_POINT ( 'NONE',  ( 1.205336560124999901, -3.461062994654999780, -0.9617132324576000979 ) ) ;
#2813=CARTESIAN_POINT ( 'NONE',  ( 9.520528907821001141, 2.899999999999999911, 6.152188490330000370 ) ) ;
#2816=CARTESIAN_POINT ( 'NONE',  ( 8.213545280409999094, 3.608525622520999843, 5.913376237674000002 ) ) ;
#2817=CARTESIAN_POINT ( 'NONE',  ( 10.91620964606000044, 2.818413279081999789, -6.814156272943999504 ) ) ;
#2820=CARTESIAN_POINT ( 'NONE',  ( 1.700339139801000155, 1.841731729107999982, 3.084132442762999915 ) ) ;
#2824=CARTESIAN_POINT ( 'NONE',  ( 9.479214860607999782, 4.071727169861000029, 9.089299483126000112 ) ) ;
#2836=CARTESIAN_POINT ( 'NONE',  ( 8.294817490939964344, 4.669395409018583187, 9.123971829385043364 ) ) ;
#2845=CARTESIAN_POINT ( 'NONE',  ( 9.967852198058999136, 2.034774058634999605, 7.636878205663998997 ) ) ;
#2846=CARTESIAN_POINT ( 'NONE',  ( 9.819565861057999001, 2.688248842995000221, -7.873038103423000145 ) ) ;
#2847=CARTESIAN_POINT ( 'NONE',  ( 8.814947692958833514, 2.650138447187985413, -7.499997389691697158 ) ) ;
#2850=DIRECTION ( 'NONE',  ( 0.000000000000000000, -0.9835907196275001096, -0.1804142351995999538 ) ) ;
#2852=VECTOR ( 'NONE', #33316, 1000.000000000000000 ) ;
#2857=CYLINDRICAL_SURFACE ( 'NONE', #45952, 1.350000000000000533 ) ;
#2866=DIRECTION ( 'NONE',  ( -1.000000000000000000, 0.000000000000000000, 0.000000000000000000 ) ) ;
#2871=CIRCLE ( 'NONE', #17393, 1.699994593733000547 ) ;
#2877=FACE_OUTER_BOUND ( 'NONE', #61126, .T. ) ;
#2893=B_SPLINE_CURVE_WITH_KNOTS ( 'NONE', 3,
 ( #28176, #34120, #44272, #34472 ),
 .UNSPECIFIED., .F., .F.,
 ( 4, 4 ),
 ( 0.000000000000000000, 1.000000000000000000 ),
 .UNSPECIFIED. ) ;
#2898=CARTESIAN_POINT ( 'NONE',  ( 4.550000802215999229, 1.829647544581999737E-13, -13.04999934368000147 ) ) ;
#2902=CARTESIAN_POINT ( 'NONE',  ( 5.440293061358000060, 12.88483958404999896, 2.133988467672999878 ) ) ;
#2905=CARTESIAN_POINT ( 'NONE',  ( 8.150000662387999029, 3.037570195374000164E-13, -12.44999944941003989 ) ) ;
#2917=DIRECTION ( 'NONE',  ( -0.000000000000000000, 1.000000000000000000, 0.000000000000000000 ) ) ;
#2921=LINE ( 'NONE', #24600, #2236 ) ;
#2923=CARTESIAN_POINT ( 'NONE',  ( 8.465229719592999302, 2.567871051582000241, -6.869011921437000012 ) ) ;
#2924=CARTESIAN_POINT ( 'NONE',  ( 9.457462135716001583, 5.100000000000000533, -6.571291218949999902 ) ) ;
#2928=VERTEX_POINT ( 'NONE', #36235 ) ;
#2929=CARTESIAN_POINT ( 'NONE',  ( 7.821752845075590876, 2.830873829569032107, -8.205201578233504378 ) ) ;
#2934=CARTESIAN_POINT ( 'NONE',  ( 10.22440590001000160, 5.317411003666999925, -8.272452263128000638 ) ) ;
#2936=ORIENTED_EDGE ( 'NONE', *, *, #2544, .T. ) ;
#2939=CARTESIAN_POINT ( 'NONE',  ( 10.99328643597795896, 6.034724004534248287, -5.044002573406743295 ) ) ;
#2943=ORIENTED_EDGE ( 'NONE', *, *, #46367, .F. ) ;
#2945=CARTESIAN_POINT ( 'NONE',  ( 8.737804660583998739, 4.491756428607999396, -5.831236541471000123 ) ) ;
#2956=B_SPLINE_CURVE_WITH_KNOTS ( 'NONE', 3,
 ( #65821, #38217, #59546, #65120 ),
 .UNSPECIFIED., .F., .F.,
 ( 4, 4 ),
 ( 0.000000000000000000, 1.000000000000000000 ),
 .UNSPECIFIED. ) ;
#2957=CARTESIAN_POINT ( 'NONE',  ( 10.01622971959000097, 4.325866256860000369, -9.125812605905000652 ) ) ;
#2959=CARTESIAN_POINT ( 'NONE',  ( 9.144252007565954798, 5.327746249399065270, 6.363126469476570790 ) ) ;
#2960=CARTESIAN_POINT ( 'NONE',  ( 10.47253786429000044, 2.899999999999999911, -6.571291218949999902 ) ) ;
#2961=LINE ( 'NONE', #55424, #17164 ) ;
#2969=AXIS2_PLACEMENT_3D ( 'NONE', #1958, #39709, #33429 ) ;
#2974=DIRECTION ( 'NONE',  ( 1.000000000000000000, 0.000000000000000000, 0.000000000000000000 ) ) ;
#2978=CARTESIAN_POINT ( 'NONE',  ( 10.07963755961372776, 4.353097593134667598, 8.851823023821664194 ) ) ;
#2981=CARTESIAN_POINT ( 'NONE',  ( 0.3606221729291086975, -3.272802759155408747, 0.8804288485544362608 ) ) ;
#2982=CARTESIAN_POINT ( 'NONE',  ( 3.501249691757999827, 0.3639092243019000361, -3.573579329690000250 ) ) ;
#2993=CARTESIAN_POINT ( 'NONE',  ( 8.236460841226000085, 3.600418141940000094, -8.839175402873999943 ) ) ;
#2994=CARTESIAN_POINT ( 'NONE',  ( 7.866260132094000213, 4.690793098693000651, 6.339956846641999988 ) ) ;
#2995=CARTESIAN_POINT ( 'NONE',  ( 7.806090764269955962, 3.007686321021738607, 6.534914955162395955 ) ) ;
#2997=ORIENTED_EDGE ( 'NONE', *, *, #61726, .F. ) ;
#3005=VERTEX_POINT ( 'NONE', #21868 ) ;
#3009=CIRCLE ( 'NONE', #67719, 0.2999999999999999334 ) ;
#3010=LINE ( 'NONE', #3352, #52098 ) ;
#3019=DIRECTION ( 'NONE',  ( 0.000000000000000000, -1.000000000000000000, 0.000000000000000000 ) ) ;
#3023=CARTESIAN_POINT ( 'NONE',  ( 0.09997256829956271962, -2.799974420760032334, -1.315021563105355128E-09 ) ) ;
#3024=CARTESIAN_POINT ( 'NONE',  ( 7.043572165045040911, 2.453565085646790767, -8.528385632692831564 ) ) ;
#3032=CARTESIAN_POINT ( 'NONE',  ( 10.31457848836000046, 5.362142879234999882, 6.677781064327999339 ) ) ;
#3033=CARTESIAN_POINT ( 'NONE',  ( 0.1499942179679999987, 1.384928887584813584, 2.402872127494069421 ) ) ;
#3034=CARTESIAN_POINT ( 'NONE',  ( 10.11453584122999949, 5.322769172805999816, -7.951018786192998178 ) ) ;
#3035=CARTESIAN_POINT ( 'NONE',  ( 2.977758589606999795, 3.090212625808999913, -2.049442917693999888 ) ) ;
#3039=VERTEX_POINT ( 'NONE', #48107 ) ;
#3041=CARTESIAN_POINT ( 'NONE',  ( 11.02786554143000153, 5.596226216413000110, 7.209502215883999199 ) ) ;
#3043=CARTESIAN_POINT ( 'NONE',  ( 10.17500046684965120, 2.650307855385062972, 7.500001770945063484 ) ) ;
#3044=CARTESIAN_POINT ( 'NONE',  ( 9.848730799670999403, 2.769737997918999994, 6.441853401936000090 ) ) ;
#3045=CARTESIAN_POINT ( 'NONE',  ( 9.162715019320227583, 3.042330479684312472, 8.452182092981665562 ) ) ;
#3053=CARTESIAN_POINT ( 'NONE',  ( 0.9681103717476999826, 3.205765437135000173, -1.404659375816999844 ) ) ;
#3055=ORIENTED_EDGE ( 'NONE', *, *, #6336, .T. ) ;
#3058=CARTESIAN_POINT ( 'NONE',  ( 8.550900948453382000, 5.350547267263451090, -7.263495630725214092 ) ) ;
#3062=CARTESIAN_POINT ( 'NONE',  ( 8.539829719592999524, 5.633477595780999714, 7.451234169193000412 ) ) ;
#3063=CARTESIAN_POINT ( 'NONE',  ( 9.143660841233000269, 2.235961884443999459, -6.794506518623999902 ) ) ;
#3064=CARTESIAN_POINT ( 'NONE',  ( 0.6708157676188386542, 0.2100481489804951751, 3.532047167415213629 ) ) ;
#3065=CARTESIAN_POINT ( 'NONE',  ( 11.15264221959000146, 2.317063201199000222, -7.596564358366999947 ) ) ;
#3066=ORIENTED_EDGE ( 'NONE', *, *, #64730, .F. ) ;
#3071=DIRECTION ( 'NONE',  ( -0.1522489054329967118, -0.9525130356996803771, -0.2637028396066944946 ) ) ;
#3072=VERTEX_POINT ( 'NONE', #48451 ) ;
#3074=EDGE_CURVE ( 'NONE', #42736, #40281, #29519, .T. ) ;
#3085=LINE ( 'NONE', #28995, #10507 ) ;
#3088=CARTESIAN_POINT ( 'NONE',  ( 8.406645280410000254, 3.807713920470999991, -9.221758713517999695 ) ) ;
#3095=CARTESIAN_POINT ( 'NONE',  ( 8.335885841230000537, 4.310355144869000732, 9.459505265942000918 ) ) ;
#3116=ORIENTED_EDGE ( 'NONE', *, *, #69052, .F. ) ;
#3122=DIRECTION ( 'NONE',  ( -0.9999999999999987788, -4.835299792554983623E-08, 1.472960222966996186E-08 ) ) ;
#3124=CARTESIAN_POINT ( 'NONE',  ( 6.899999691988000450, 12.99045401563999924, -1.690592933733000125 ) ) ;
#3125=CARTESIAN_POINT ( 'NONE',  ( 10.53138775541999905, 5.607751175212000838, 7.280102404048999887 ) ) ;
#3132=CARTESIAN_POINT ( 'NONE',  ( 9.423523952092001110, 4.993991073313000406, 8.578107851305000864 ) ) ;
#3137=EDGE_CURVE ( 'NONE', #26116, #66034, #2961, .T. ) ;
#3138=EDGE_CURVE ( 'NONE', #57343, #27955, #66246, .T. ) ;
#3139=CARTESIAN_POINT ( 'NONE',  ( 8.572267219592999865, 2.606995215518000286, 6.345762205468999717 ) ) ;
#3140=CARTESIAN_POINT ( 'NONE',  ( 10.40726830891999910, 3.797905842462999892, 5.889914049998000500 ) ) ;
#3142=ORIENTED_EDGE ( 'NONE', *, *, #54835, .T. ) ;
#3143=CARTESIAN_POINT ( 'NONE',  ( 8.549914158773001205, 2.141799395716999843, -7.895788736628000848 ) ) ;
#3151=CARTESIAN_POINT ( 'NONE',  ( 1.009835424300000062, 3.696170276785000208, -0.6823948523853999859 ) ) ;
#3156=B_SPLINE_CURVE_WITH_KNOTS ( 'NONE', 3,
 ( #43988, #42944, #22301, #16707, #42602, #11462 ),
 .UNSPECIFIED., .F., .F.,
 ( 4, 1, 1, 4 ),
 ( 0.000000000000000000, 0.3333333333333000081, 0.6666666666667000474, 1.000000000000000000 ),
 .UNSPECIFIED. ) ;
#3159=FACE_OUTER_BOUND ( 'NONE', #12491, .T. ) ;
#3164=CARTESIAN_POINT ( 'NONE',  ( 9.523698341228998387, 4.852728889087999598, 8.683917172082999514 ) ) ;
#3168=CONICAL_SURFACE ( 'NONE', #51185, 12.44999944941000081, 0.7853981146832407223 ) ;
#3170=CARTESIAN_POINT ( 'NONE',  ( 1.361792155651999847, -1.181558911493999942, 3.215390670984000554 ) ) ;
#3172=CARTESIAN_POINT ( 'NONE',  ( 1.858550344655261810, 1.693358345689038202, 2.835668913445299477 ) ) ;
#3176=CARTESIAN_POINT ( 'NONE',  ( 9.757669403192000601, 4.489270656625000022, 5.986034819543999852 ) ) ;
#3184=CARTESIAN_POINT ( 'NONE',  ( 7.696932380987085764, 5.748606536197243599, 7.412610333444322741 ) ) ;
#3194=CARTESIAN_POINT ( 'NONE',  ( 10.71756692516999898, 3.040224182812999665, 8.808452309630000698 ) ) ;
#3195=CARTESIAN_POINT ( 'NONE',  ( 10.85290485628999946, 3.170386876061999537, -8.782184998573001167 ) ) ;
#3215=B_SPLINE_CURVE_WITH_KNOTS ( 'NONE', 3,
 ( #63658, #48274, #21696, #43032 ),
 .UNSPECIFIED., .F., .F.,
 ( 4, 4 ),
 ( 0.000000000000000000, 1.000000000000000000 ),
 .UNSPECIFIED. ) ;
#3221=CARTESIAN_POINT ( 'NONE',  ( 8.698544349573893442, 4.680090960897770103, -8.679957510353851546 ) ) ;
#3223=EDGE_CURVE ( 'NONE', #52567, #7034, #44259, .T. ) ;
#3224=CARTESIAN_POINT ( 'NONE',  ( 0.09605912983313999454, 2.413895893032000028, 2.806361486493000434 ) ) ;
#3230=CARTESIAN_POINT ( 'NONE',  ( 8.493376396436000064, 2.902501347630999984, -6.607668289109998483 ) ) ;
#3231=CARTESIAN_POINT ( 'NONE',  ( 10.79701415876999882, 5.792870175253000298, -7.049262931951000510 ) ) ;
#3236=ORIENTED_EDGE ( 'NONE', *, *, #33621, .T. ) ;
#3243=DIRECTION ( 'NONE',  ( 1.000000000000000000, 0.000000000000000000, 0.000000000000000000 ) ) ;
#3245=VERTEX_POINT ( 'NONE', #50865 ) ;
#3250=CARTESIAN_POINT ( 'NONE',  ( 2.709306799209334038, -3.058252359239909790, 1.762666431298136382 ) ) ;
#3254=CARTESIAN_POINT ( 'NONE',  ( 9.036851812263130057, 5.286388725631042895, -7.027200320027173319 ) ) ;
#3258=CARTESIAN_POINT ( 'NONE',  ( 10.73912476063878607, 2.651371201321757187, 7.263709536580951642 ) ) ;
#3264=CARTESIAN_POINT ( 'NONE',  ( 4.000000000000000888, -2.149963194831999935, 0.2827069376517963306 ) ) ;
#3266=ORIENTED_EDGE ( 'NONE', *, *, #45588, .F. ) ;
#3269=ADVANCED_FACE ( 'NONE', ( #38647 ), #39001, .T. ) ;
#3270=CARTESIAN_POINT ( 'NONE',  ( 8.233179719589999834, 5.203550244299999683, -8.391678825488000371 ) ) ;
#3271=CARTESIAN_POINT ( 'NONE',  ( 10.06805547886711594, 2.257110507042949799, -7.995645982437191712 ) ) ;
#3277=CARTESIAN_POINT ( 'NONE',  ( 7.882561745187770974, 2.667458184526113829, -7.203446184243078143 ) ) ;
#3279=CARTESIAN_POINT ( 'NONE',  ( 9.029445280412998542, 5.442817578555000146, -8.106149115450000053 ) ) ;
#3281=CARTESIAN_POINT ( 'NONE',  ( 9.753031682810998859, 4.922927894835999574, -8.639534507509999628 ) ) ;
#3283=ORIENTED_EDGE ( 'NONE', *, *, #22917, .F. ) ;
#3291=CARTESIAN_POINT ( 'NONE',  ( 5.500000000000000000, -11.00717859340000082, 1.432487142323000118 ) ) ;
#3296=DIRECTION ( 'NONE',  ( 1.000000000000000000, 0.000000000000000000, -6.069219200923000182E-14 ) ) ;
#3297=EDGE_CURVE ( 'NONE', #44223, #44911, #24975, .T. ) ;
#3300=CARTESIAN_POINT ( 'NONE',  ( 9.219485841232998524, 3.892978337449999771, -8.893414073324001023 ) ) ;
#3301=CARTESIAN_POINT ( 'NONE',  ( 10.60113158428548097, 5.349785647439726510, -7.263300972600675642 ) ) ;
#3309=CARTESIAN_POINT ( 'NONE',  ( 8.953746459558937332, 2.251940015626868519, 7.420647187261359079 ) ) ;
#3312=DIRECTION ( 'NONE',  ( -1.000000000000000000, 0.000000000000000000, 0.000000000000000000 ) ) ;
#3316=LINE ( 'NONE', #25674, #15394 ) ;
#3318=CARTESIAN_POINT ( 'NONE',  ( 9.243110841233001196, 4.112741311853999271, -5.603466076760000192 ) ) ;
#3320=B_SPLINE_CURVE_WITH_KNOTS ( 'NONE', 3,
 ( #36846, #3976, #67958, #58164 ),
 .UNSPECIFIED., .F., .F.,
 ( 4, 4 ),
 ( 0.000000000000000000, 1.000000000000000000 ),
 .UNSPECIFIED. ) ;
#3321=VECTOR ( 'NONE', #68066, 999.9999999999998863 ) ;
#3325=CARTESIAN_POINT ( 'NONE',  ( 0.2681673312783822150, 1.646699379977375699, 2.855331343420156376 ) ) ;
#3326=CARTESIAN_POINT ( 'NONE',  ( 2.490382077375999703, -2.404207915413000052, 2.200243182853999890 ) ) ;
#3327=EDGE_LOOP ( 'NONE', ( #15740, #25312, #25715, #3984 ) ) ;
#3329=DIRECTION ( 'NONE',  ( 1.000000000000000000, 0.000000000000000000, 0.000000000000000000 ) ) ;
#3331=CARTESIAN_POINT ( 'NONE',  ( 8.770176658772999900, 3.049618631524000367, 6.392542946894000266 ) ) ;
#3336=CARTESIAN_POINT ( 'NONE',  ( 0.6152921912379571978, 0.4809088339291435754, 3.497386196961711491 ) ) ;
#3337=CARTESIAN_POINT ( 'NONE',  ( 8.745593092018999926, 5.100000000000000533, 6.404090157675000228 ) ) ;
#3346=B_SPLINE_CURVE_WITH_KNOTS ( 'NONE', 3,
 ( #42390, #25618, #19689, #14449, #62332, #20369, #31220, #9183, #35429, #30523, #47636, #68250 ),
 .UNSPECIFIED., .F., .F.,
 ( 4, 1, 1, 1, 1, 1, 1, 1, 1, 4 ),
 ( 0.000000000000000000, 0.1111111114150000051, 0.2222222219940999943, 0.3333333325730999941, 0.4444444431521000216, 0.5555555537312000247, 0.6666666643101999412, 0.7777777748892999998, 0.8888888854682999163, 1.000000000000000000 ),
 .UNSPECIFIED. ) ;
#3348=CARTESIAN_POINT ( 'NONE',  ( 10.95238143012640109, 9.081849699400036613, -6.376793985733890224 ) ) ;
#3349=PLANE ( 'NONE',  #50592 ) ;
#3352=CARTESIAN_POINT ( 'NONE',  ( 7.550000000000000711, 4.000000000000000000, 8.849999999999999645 ) ) ;
#3358=CARTESIAN_POINT ( 'NONE',  ( 10.99548912979983939, 5.205161879957274529, 6.659293853268957619 ) ) ;
#3370=CARTESIAN_POINT ( 'NONE',  ( 9.625496329943999285, 3.134638325776999856, 8.626949804392001653 ) ) ;
#3372=DIRECTION ( 'NONE',  ( 1.000000000000000000, 0.000000000000000000, 0.000000000000000000 ) ) ;
#3373=CARTESIAN_POINT ( 'NONE',  ( 8.681370280410998674, 2.949305648881000330, -8.659807625323999503 ) ) ;
#3374=CARTESIAN_POINT ( 'NONE',  ( 3.355011260902999837, -1.961156070315999811, -3.146982238240999763 ) ) ;
#3379=ADVANCED_FACE ( 'NONE', ( #68995 ), #26706, .T. ) ;
#3381=CARTESIAN_POINT ( 'NONE',  ( 9.385781899350000401, 4.980865465981000106, 6.433345686594999613 ) ) ;
#3385=CARTESIAN_POINT ( 'NONE',  ( 10.58844943056000076, 3.754657019866000311, 5.545350295858999523 ) ) ;
#3394=ORIENTED_EDGE ( 'NONE', *, *, #26841, .F. ) ;
#3398=CARTESIAN_POINT ( 'NONE',  ( 5.000030787343001215, -2.099962892531005210, -0.2748844998327738542 ) ) ;
#3400=ORIENTED_EDGE ( 'NONE', *, *, #28809, .T. ) ;
#3403=AXIS2_PLACEMENT_3D ( 'NONE', #49133, #21867, #43204 ) ;
#3406=CARTESIAN_POINT ( 'NONE',  ( 11.00119221959000093, 4.640446572790000168, -9.059321223816999336 ) ) ;
#3408=CARTESIAN_POINT ( 'NONE',  ( 1.405140132540666942, -0.9161175952574773795, -3.408904368339105595 ) ) ;
#3411=LINE ( 'NONE', #67718, #6488 ) ;
#3412=CARTESIAN_POINT ( 'NONE',  ( 10.90000004630000063, 9.856474695503001371, 5.627825000517000298 ) ) ;
#3415=DIRECTION ( 'NONE',  ( -1.000000000000000000, 0.000000000000000000, 0.000000000000000000 ) ) ;
#3416=AXIS2_PLACEMENT_3D ( 'NONE', #21781, #49744, #64421 ) ;
#3422=FACE_OUTER_BOUND ( 'NONE', #52917, .T. ) ;
#3425=ORIENTED_EDGE ( 'NONE', *, *, #46204, .T. ) ;
#3429=CARTESIAN_POINT ( 'NONE',  ( 8.228673390747101024, 4.831902665061588387, 6.190044796983404041 ) ) ;
#3432=CARTESIAN_POINT ( 'NONE',  ( 8.464260841230998977, 2.029098103856999735, 7.726995416028000108 ) ) ;
#3434=CARTESIAN_POINT ( 'NONE',  ( 7.500005746562851350, 5.303016073863008550, 7.913359363012708592 ) ) ;
#3445=CARTESIAN_POINT ( 'NONE',  ( 9.356851002546999752, 2.832432432432000269, -6.822293592207000934 ) ) ;
#3447=AXIS2_PLACEMENT_3D ( 'NONE', #3901, #56025, #56722 ) ;
#3449=ORIENTED_EDGE ( 'NONE', *, *, #51146, .T. ) ;
#3455=CARTESIAN_POINT ( 'NONE',  ( 10.69578011722000177, 5.505003832924999507, -7.759263776825999770 ) ) ;
#3460=CARTESIAN_POINT ( 'NONE',  ( 10.84168637167000071, 2.681011538858999899, 6.554754637093000547 ) ) ;
#3466=EDGE_CURVE ( 'NONE', #56100, #38413, #51889, .T. ) ;
#3469=CARTESIAN_POINT ( 'NONE',  ( 10.64872393945999995, 2.614781729644000130, 6.717281948314999696 ) ) ;
#3471=CARTESIAN_POINT ( 'NONE',  ( 8.441604719589999917, 5.473983809665999622, -8.180077404516000072 ) ) ;
#3475=CARTESIAN_POINT ( 'NONE',  ( 8.636454719592999041, 3.869396554003000421, 5.695652484872999466 ) ) ;
#3476=CARTESIAN_POINT ( 'NONE',  ( 11.05639637898999972, 5.030226177531999632, 6.028288223959999748 ) ) ;
#3479=CARTESIAN_POINT ( 'NONE',  ( 9.915635841230999503, 3.210851187372000037, -6.346613542714999667 ) ) ;
#3487=CARTESIAN_POINT ( 'NONE',  ( 1.820428564792999859, -3.146289470026999879, -2.056511572473000093 ) ) ;
#3490=CARTESIAN_POINT ( 'NONE',  ( 8.324914158772999784, 2.633142096252999664, -7.791134854666999843 ) ) ;
#3495=DIRECTION ( 'NONE',  ( 0.000000000000000000, -0.9693731749023103417, 0.2455924424322025734 ) ) ;
#3499=CARTESIAN_POINT ( 'NONE',  ( 9.433107780409999421, 4.954905351382000944, 8.825777580285999235 ) ) ;
#3502=DIRECTION ( 'NONE',  ( 0.4384236320213994453, 0.6355252626312996034, 0.6355252626312994924 ) ) ;
#3503=CARTESIAN_POINT ( 'NONE',  ( 1.314110206211000165, 0.8376700968564000371, 3.321615185007000370 ) ) ;
#3505=CARTESIAN_POINT ( 'NONE',  ( 1.620140597451261044, -1.263880145926562948, -3.051407509797793516 ) ) ;
#3507=DIRECTION ( 'NONE',  ( -0.8660254037844288266, 0.000000000000000000, 0.5000000000000169864 ) ) ;
#3508=CARTESIAN_POINT ( 'NONE',  ( 10.92717848204000042, 5.023653513500000223, 8.718036113327999104 ) ) ;
#3514=LINE ( 'NONE', #20635, #47695 ) ;
#3515=CARTESIAN_POINT ( 'NONE',  ( 8.237473783029317431, 5.556797505346596999, 8.286080926133671198 ) ) ;
#3518=PLANE ( 'NONE',  #29431 ) ;
#3519=ORIENTED_EDGE ( 'NONE', *, *, #38934, .F. ) ;
#3520=DIRECTION ( 'NONE',  ( 0.000000000000000000, 0.000000000000000000, -1.000000000000000000 ) ) ;
#3524=CIRCLE ( 'NONE', #30339, 11.55000237494000537 ) ;
#3526=CARTESIAN_POINT ( 'NONE',  ( 10.15902941591999920, 4.166415211384999040, 9.114163806478000396 ) ) ;
#3527=EDGE_CURVE ( 'NONE', #51133, #46559, #29127, .T. ) ;
#3528=CARTESIAN_POINT ( 'NONE',  ( 10.40878363256000050, 3.093886843363999883, -6.480781753756000185 ) ) ;
#3534=CARTESIAN_POINT ( 'NONE',  ( 7.726448341228000061, 2.630487280353000390, 6.995957894972000268 ) ) ;
#3550=DIRECTION ( 'NONE',  ( 1.000000000000000000, 0.000000000000000000, 0.000000000000000000 ) ) ;
#3556=CARTESIAN_POINT ( 'NONE',  ( 0.3017198524092000178, -3.532786812989999969, -1.105428934477000080 ) ) ;
#3559=CARTESIAN_POINT ( 'NONE',  ( 8.571413182547999554, 4.599999999999999645, 5.927302706106000407 ) ) ;
#3567=EDGE_LOOP ( 'NONE', ( #50420, #59717, #47929, #9347, #26491 ) ) ;
#3568=ADVANCED_FACE ( 'NONE', ( #22476, #1505 ), #50433, .F. ) ;
#3570=VECTOR ( 'NONE', #55413, 1000.000000000000000 ) ;
#3571=CARTESIAN_POINT ( 'NONE',  ( 9.481330364773148389, 3.644056349852950127, -9.240156464735864716 ) ) ;
#3573=DIRECTION ( 'NONE',  ( 0.000000000000000000, 1.000000000000000000, 0.000000000000000000 ) ) ;
#3577=VERTEX_POINT ( 'NONE', #50096 ) ;
#3584=CARTESIAN_POINT ( 'NONE',  ( 8.186785374738994037, 2.888678623336002005, 6.695956381329003726 ) ) ;
#3591=CARTESIAN_POINT ( 'NONE',  ( 2.821806799211333594, -3.408904368339104263, -0.9161175952574813763 ) ) ;
#3592=CARTESIAN_POINT ( 'NONE',  ( 9.717214158771000143, 3.990126737362999609, -8.809457313313998839 ) ) ;
#3596=B_SPLINE_CURVE_WITH_KNOTS ( 'NONE', 3,
 ( #68718, #31678, #16274, #893 ),
 .UNSPECIFIED., .F., .F.,
 ( 4, 4 ),
 ( 0.000000000000000000, 1.000000000000000000 ),
 .UNSPECIFIED. ) ;
#3599=ORIENTED_EDGE ( 'NONE', *, *, #11468, .T. ) ;
#3604=CARTESIAN_POINT ( 'NONE',  ( 9.733247726267846289, 4.120954015165996687, -8.873126350618022684 ) ) ;
#3612=CARTESIAN_POINT ( 'NONE',  ( 7.744301850232000461, 3.130385018321999890, 6.467396599055999395 ) ) ;
#3613=CARTESIAN_POINT ( 'NONE',  ( 10.02394528041000044, 5.481267232667000222, -8.005061172455999241 ) ) ;
#3614=ORIENTED_EDGE ( 'NONE', *, *, #58389, .F. ) ;
#3616=CARTESIAN_POINT ( 'NONE',  ( 10.58996475420000039, 2.876740601533999797, -6.236530348556999392 ) ) ;
#3624=EDGE_LOOP ( 'NONE', ( #5415, #61793, #18763, #56843 ) ) ;
#3625=CARTESIAN_POINT ( 'NONE',  ( 11.09999999999999964, 2.649999999999999911, 7.500000000000000000 ) ) ;
#3626=CARTESIAN_POINT ( 'NONE',  ( 11.18237334122999904, 4.516636732814999888, -8.757876389238999693 ) ) ;
#3635=CARTESIAN_POINT ( 'NONE',  ( 9.576420280414000175, 4.861259245430999520, -8.806664389576001284 ) ) ;
#3636=CARTESIAN_POINT ( 'NONE',  ( 6.899999691988000450, 12.43893545635000031, 2.828937028792000152 ) ) ;
#3642=CARTESIAN_POINT ( 'NONE',  ( 8.886504504762845258, 2.780594424960459499, 8.755326434349345988 ) ) ;
#3644=ORIENTED_EDGE ( 'NONE', *, *, #64240, .T. ) ;
#3647=EDGE_CURVE ( 'NONE', #3577, #11746, #24416, .T. ) ;
#3650=LINE ( 'NONE', #24987, #6790 ) ;
#3653=CARTESIAN_POINT ( 'NONE',  ( 6.999999691988000095, -12.36734761319999798, 2.759114534468000368 ) ) ;
#3654=CARTESIAN_POINT ( 'NONE',  ( 7.966947972481352558, 2.969119817116051330, -6.520715660824929927 ) ) ;
#3658=CARTESIAN_POINT ( 'NONE',  ( 3.067338808729000110, -0.7022537682570999529, -3.352858224555000266 ) ) ;
#3663=CARTESIAN_POINT ( 'NONE',  ( 8.449239158774000558, 5.458692773671000253, 7.456452194274000078 ) ) ;
#3666=LINE ( 'NONE', #63773, #40012 ) ;
#3668=CARTESIAN_POINT ( 'NONE',  ( 10.99014425376339688, 7.742518842553854697, 6.423560035353997222 ) ) ;
#3670=CARTESIAN_POINT ( 'NONE',  ( 7.795984407058476506, 2.673910249782932347, -7.823565946277482475 ) ) ;
#3678=ADVANCED_FACE ( 'NONE', ( #18967 ), #62629, .F. ) ;
#3679=ORIENTED_EDGE ( 'NONE', *, *, #46178, .T. ) ;
#3683=CARTESIAN_POINT ( 'NONE',  ( 7.283304719589999365, 4.462983737834999687, -8.994919855354998717 ) ) ;
#3685=EDGE_CURVE ( 'NONE', #17499, #67326, #5208, .T. ) ;
#3691=CYLINDRICAL_SURFACE ( 'NONE', #37238, 1.350000000000000533 ) ;
#3694=CARTESIAN_POINT ( 'NONE',  ( -15.86200481174999943, 13.87069231928999891, 4.225386915259999654 ) ) ;
#3705=ORIENTED_EDGE ( 'NONE', *, *, #23301, .T. ) ;
#3706=CARTESIAN_POINT ( 'NONE',  ( 10.70441484796999987, 3.444517850837000239, 6.009055070331999815 ) ) ;
#3710=CARTESIAN_POINT ( 'NONE',  ( 8.590779719591999708, 2.836879604150999601, -8.783908972046001296 ) ) ;
#3711=CARTESIAN_POINT ( 'NONE',  ( 3.432088553994000257, 3.542926904065000215, -0.07481602154510001712 ) ) ;
#3718=CYLINDRICAL_SURFACE ( 'NONE', #40984, 1.350000000000000533 ) ;
#3720=B_SPLINE_CURVE_WITH_KNOTS ( 'NONE', 3,
 ( #27770, #59567, #37898, #32662, #65144, #11664, #43499, #16909, #17265, #60955, #56748, #13753, #40318, #34738, #13419, #29154, #8502, #29849 ),
 .UNSPECIFIED., .F., .F.,
 ( 4, 2, 2, 2, 2, 2, 2, 2, 4 ),
 ( 0.000000000000000000, 0.1250000000000000000, 0.2500000000000000000, 0.3750000000000000000, 0.5000000000000000000, 0.6250000000000000000, 0.7500000000000000000, 0.8750000000000000000, 1.000000000000000000 ),
 .UNSPECIFIED. ) ;
#3722=CARTESIAN_POINT ( 'NONE',  ( 9.662551629919999385, 4.094830335839000135, 9.119946295870999364 ) ) ;
#3726=EDGE_CURVE ( 'NONE', #34076, #27484, #30245, .T. ) ;
#3732=EDGE_CURVE ( 'NONE', #41793, #8371, #52143, .T. ) ;
#3741=CARTESIAN_POINT ( 'NONE',  ( 0.5267198524092000511, -3.063090672237000156, -0.9584583608479999572 ) ) ;
#3743=CARTESIAN_POINT ( 'NONE',  ( 10.39539221959000059, 5.667182949051000840, -7.250689098107000241 ) ) ;
#3752=CARTESIAN_POINT ( 'NONE',  ( 8.353629719588999691, 5.354408404900999230, -6.419792067946000103 ) ) ;
#3754=CIRCLE ( 'NONE', #50694, 0.2999999999999999334 ) ;
#3761=CONICAL_SURFACE ( 'NONE', #55134, 1.949999999913999860, 0.7853981633972997312 ) ;
#3770=CARTESIAN_POINT ( 'NONE',  ( 7.886573341228999112, 3.084076314893000159, 9.259847992573000397 ) ) ;
#3771=ADVANCED_FACE ( 'NONE', ( #35396 ), #8817, .F. ) ;
#3773=CARTESIAN_POINT ( 'NONE',  ( 11.09999999999999964, 2.649999999999999911, -7.500000000000000000 ) ) ;
#3781=CARTESIAN_POINT ( 'NONE',  ( 6.981311842138000934, 10.82753206518999534, -3.400792444267003667 ) ) ;
#3787=CARTESIAN_POINT ( 'NONE',  ( 11.09999999999999964, 4.000000000000000000, 7.500000000000000000 ) ) ;
#3788=ORIENTED_EDGE ( 'NONE', *, *, #28518, .T. ) ;
#3792=AXIS2_PLACEMENT_3D ( 'NONE', #63666, #64345, #21368 ) ;
#3795=CARTESIAN_POINT ( 'NONE',  ( 10.06728116094000036, 4.192860729918999496, -5.985054792427000336 ) ) ;
#3799=CARTESIAN_POINT ( 'NONE',  ( 9.013423559847998590, 4.933953210258000155, 8.417881984655998906 ) ) ;
#3802=CARTESIAN_POINT ( 'NONE',  ( 9.905792474809000936, 2.698958900805999761, 8.979236532123000103 ) ) ;
#3804=CARTESIAN_POINT ( 'NONE',  ( 9.534905769125000319, 3.030948166328000237, 8.761984216465000586 ) ) ;
#3810=CARTESIAN_POINT ( 'NONE',  ( 8.289114158772999730, 4.310355144869000732, 9.459505265942000918 ) ) ;
#3811=CARTESIAN_POINT ( 'NONE',  ( 10.22108913916999917, 2.983268757921999637, 8.764704075288999974 ) ) ;
#3816=CARTESIAN_POINT ( 'NONE',  ( 9.427245280414000561, 4.989193221215000307, -6.287302145481000082 ) ) ;
#3823=CARTESIAN_POINT ( 'NONE',  ( 1.300700459006000065, -0.3635854775007999473, -3.573745162754999871 ) ) ;
#3825=CARTESIAN_POINT ( 'NONE',  ( 8.275189158773001097, 3.061731693614000438, -8.535706278603999664 ) ) ;
#3826=FACE_OUTER_BOUND ( 'NONE', #14473, .T. ) ;
#3829=CARTESIAN_POINT ( 'NONE',  ( 9.514114512910998300, 4.887632373702999189, 8.462748516415999234 ) ) ;
#3834=ORIENTED_EDGE ( 'NONE', *, *, #49027, .F. ) ;
#3835=CARTESIAN_POINT ( 'NONE',  ( 7.673642219589999591, 4.696238830159999544, 5.830273622963999536 ) ) ;
#3841=CARTESIAN_POINT ( 'NONE',  ( 1.552519953415999909, -1.310877008326999826, -3.164872840607000359 ) ) ;
#3842=VERTEX_POINT ( 'NONE', #67879 ) ;
#3843=CARTESIAN_POINT ( 'NONE',  ( 2.001596192978043476, -3.143789697970717167, 1.012455472687556313 ) ) ;
#3846=CARTESIAN_POINT ( 'NONE',  ( 10.50244247011999832, 2.268911387573000038, 7.824865741583000300 ) ) ;
#3849=CARTESIAN_POINT ( 'NONE',  ( 9.629471092178999214, 5.100000000000000533, 6.152188490330000370 ) ) ;
#3850=CARTESIAN_POINT ( 'NONE',  ( 9.709999999999999076, 4.496968146123999865, -8.755198255949000696 ) ) ;
#3853=ADVANCED_FACE ( 'NONE', ( #66853 ), #49495, .F. ) ;
#3858=CARTESIAN_POINT ( 'NONE',  ( 8.737804660583998739, 4.491756428607999396, -5.831236541471000123 ) ) ;
#3859=ORIENTED_EDGE ( 'NONE', *, *, #40205, .T. ) ;
#3861=B_SPLINE_CURVE_WITH_KNOTS ( 'NONE', 3,
 ( #30628, #63103, #19791, #47051 ),
 .UNSPECIFIED., .F., .F.,
 ( 4, 4 ),
 ( 0.000000000000000000, 1.000000000000000000 ),
 .UNSPECIFIED. ) ;
#3865=VECTOR ( 'NONE', #26408, 1000.000000000000000 ) ;
#3867=CARTESIAN_POINT ( 'NONE',  ( 10.00138108374000012, 3.855364958793999985, 5.709478909302000638 ) ) ;
#3868=CARTESIAN_POINT ( 'NONE',  ( 10.88015784977000067, 2.793131772868000073, -6.864962922767000819 ) ) ;
#3874=CARTESIAN_POINT ( 'NONE',  ( 8.330260465798849268, 5.101896243649416185, -8.673380106616962237 ) ) ;
#3877=CIRCLE ( 'NONE', #40712, 11.84999999999999964 ) ;
#3879=CYLINDRICAL_SURFACE ( 'NONE', #33885, 1.350000000000000533 ) ;
#3882=CARTESIAN_POINT ( 'NONE',  ( 7.557540957726994968, 10.72894448916999544, 3.699722378877996931 ) ) ;
#3890=CARTESIAN_POINT ( 'NONE',  ( 10.88269270164825997, 5.042464834414079888, -4.893996439828388390 ) ) ;
#3897=CARTESIAN_POINT ( 'NONE',  ( 11.00301147230000076, 2.832304442428000169, 4.969741576018000373 ) ) ;
#3901=CARTESIAN_POINT ( 'NONE',  ( 11.09999999999999964, 4.000000000000000000, -7.500000000000000000 ) ) ;
#3904=DIRECTION ( 'NONE',  ( 1.000000000000000000, 0.000000000000000000, 0.000000000000000000 ) ) ;
#3905=FACE_OUTER_BOUND ( 'NONE', #1582, .T. ) ;
#3907=ORIENTED_EDGE ( 'NONE', *, *, #62563, .F. ) ;
#3917=ORIENTED_EDGE ( 'NONE', *, *, #27223, .T. ) ;
#3920=CARTESIAN_POINT ( 'NONE',  ( 8.856793857978997764, 5.100000000000000533, -6.339888365514000590 ) ) ;
#3928=CARTESIAN_POINT ( 'NONE',  ( 8.911640687508834091, 2.873222873817929734, -6.752018918866312447 ) ) ;
#3931=CARTESIAN_POINT ( 'NONE',  ( 9.073148997461000675, 5.167567567567999731, -6.822293592207000934 ) ) ;
#3932=EDGE_CURVE ( 'NONE', #20142, #47790, #68600, .T. ) ;
#3935=CARTESIAN_POINT ( 'NONE',  ( 2.998890132544666631, 2.798833948393634419, -2.150913519912196925 ) ) ;
#3936=CARTESIAN_POINT ( 'NONE',  ( 9.608904719592000987, 4.946705552514000459, -6.253848946732999181 ) ) ;
#3945=CARTESIAN_POINT ( 'NONE',  ( 8.944760841233000193, 4.990139824845000405, -9.121472988377998803 ) ) ;
#3953=CARTESIAN_POINT ( 'NONE',  ( 8.400739158770999637, 4.933589693325000525, -9.154576215408999573 ) ) ;
#3954=ORIENTED_EDGE ( 'NONE', *, *, #53660, .F. ) ;
#3955=CARTESIAN_POINT ( 'NONE',  ( 11.07336716268999943, 2.375546981533999791, -8.393546861057000541 ) ) ;
#3966=CARTESIAN_POINT ( 'NONE',  ( 10.27367334122999942, 3.065551304793999510, -8.487910413489000661 ) ) ;
#3968=FACE_OUTER_BOUND ( 'NONE', #68952, .T. ) ;
#3970=CARTESIAN_POINT ( 'NONE',  ( 10.31746213571000048, 5.100000000000000533, 6.571291218949999902 ) ) ;
#3974=CARTESIAN_POINT ( 'NONE',  ( 9.725595280412999699, 2.495531372253999791, -7.930944806125000746 ) ) ;
#3976=CARTESIAN_POINT ( 'NONE',  ( 1.433329478674677082, -2.750000000000000000, 3.881562544924731475E-10 ) ) ;
#3981=CARTESIAN_POINT ( 'NONE',  ( 8.836073038665773538, 3.765130766121813188, 9.264018223852634293 ) ) ;
#3982=DIRECTION ( 'NONE',  ( 0.000000000000000000, 0.000000000000000000, -1.000000000000000000 ) ) ;
#3984=ORIENTED_EDGE ( 'NONE', *, *, #36802, .T. ) ;
#3991=CARTESIAN_POINT ( 'NONE',  ( 7.949325904507976936, 5.068739420852621080, 6.584571070534249948 ) ) ;
#3994=CARTESIAN_POINT ( 'NONE',  ( 8.944760841233000193, 4.990139824845000405, -9.121472988377998803 ) ) ;
#3996=CARTESIAN_POINT ( 'NONE',  ( 7.921841810112000282, 2.875629839593000003, -6.725486766668000271 ) ) ;
#3999=VECTOR ( 'NONE', #69141, 1000.000000000000000 ) ;
#4002=EDGE_LOOP ( 'NONE', ( #25993, #15744, #58189, #1192, #7301, #38673, #11330, #41577, #68191, #58539 ) ) ;
#4010=EDGE_CURVE ( 'NONE', #23656, #36822, #11896, .T. ) ;
#4011=CARTESIAN_POINT ( 'NONE',  ( 10.90000000000000036, 2.778483479159999714, -6.925197956411000000 ) ) ;
#4013=CARTESIAN_POINT ( 'NONE',  ( 7.806713606405746297, 3.013404723643958061, 6.528857899631486106 ) ) ;
#4016=EDGE_CURVE ( 'NONE', #56617, #36930, #20191, .T. ) ;
#4023=CARTESIAN_POINT ( 'NONE',  ( 8.613580616166148118, 2.319743054166865992, -6.990328426993228206 ) ) ;
#4024=CARTESIAN_POINT ( 'NONE',  ( 8.199995020667000034, 2.894508905068999827, 6.645190348705000360 ) ) ;
#4025=CARTESIAN_POINT ( 'NONE',  ( 7.920870280406000496, 3.504660014889999786, -9.160103207264000957 ) ) ;
#4028=VERTEX_POINT ( 'NONE', #61363 ) ;
#4029=CARTESIAN_POINT ( 'NONE',  ( 2.136390132540208597, -0.4581489286485235790, 3.499999999999998224 ) ) ;
#4036=B_SPLINE_CURVE_WITH_KNOTS ( 'NONE', 3,
 ( #34101, #13470, #2959, #55768, #57127, #50515, #35811, #14150, #51207, #8554, #61689, #40368, #67607, #29902 ),
 .UNSPECIFIED., .F., .F.,
 ( 4, 2, 2, 2, 2, 2, 4 ),
 ( 0.000000000000000000, 0.1249999999999998057, 0.2499999999999996114, 0.4999999999999991673, 0.7499999999999993339, 0.8749999999999997780, 1.000000000000000000 ),
 .UNSPECIFIED. ) ;
#4038=CARTESIAN_POINT ( 'NONE',  ( 10.78969997251173929, 4.768152166674551218, 9.097113251175899862 ) ) ;
#4040=CONICAL_SURFACE ( 'NONE', #35309, 3.186893810805000005, 0.7853950157668545540 ) ;
#4048=ORIENTED_EDGE ( 'NONE', *, *, #54921, .F. ) ;
#4049=CARTESIAN_POINT ( 'NONE',  ( 9.423523952092001110, 4.993991073313000406, 8.578107851305000864 ) ) ;
#4050=B_SPLINE_CURVE_WITH_KNOTS ( 'NONE', 3,
 ( #57284, #986, #64932, #1670, #28241, #55152, #49558, #17405, #65289, #38730, #64593, #33146, #17759, #43982, #48186, #48879, #6211, #42940 ),
 .UNSPECIFIED., .F., .F.,
 ( 4, 2, 2, 2, 2, 2, 2, 2, 4 ),
 ( 0.000000000000000000, 0.1250000000000000000, 0.2500000000000000000, 0.3750000000000000000, 0.5000000000000000000, 0.6250000000000000000, 0.7500000000000000000, 0.8750000000000000000, 1.000000000000000000 ),
 .UNSPECIFIED. ) ;
#4052=AXIS2_PLACEMENT_3D ( 'NONE', #52385, #30389, #51699 ) ;
#4054=CARTESIAN_POINT ( 'NONE',  ( 2.426081430536000116, 3.527224658283000025, -0.3417833995711000439 ) ) ;
#4060=CARTESIAN_POINT ( 'NONE',  ( 3.061390132544625775, 3.499999999999999112, 0.4581489286485193602 ) ) ;
#4062=B_SPLINE_CURVE_WITH_KNOTS ( 'NONE', 3,
 ( #43964, #60033, #18082, #48511 ),
 .UNSPECIFIED., .F., .F.,
 ( 4, 4 ),
 ( 0.000000000000000000, 1.000000000000000000 ),
 .UNSPECIFIED. ) ;
#4065=CARTESIAN_POINT ( 'NONE',  ( 10.83668832355999889, 4.288537082977999404, 9.448742031664000507 ) ) ;
#4079=EDGE_CURVE ( 'NONE', #56837, #129, #30249, .T. ) ;
#4081=CARTESIAN_POINT ( 'NONE',  ( 8.666729817973333638, 2.899999999999999911, 6.535479089440332956 ) ) ;
#4084=CARTESIAN_POINT ( 'NONE',  ( 0.1785675383994000109, -1.568133397559999809, -2.874292603119999789 ) ) ;
#4087=CARTESIAN_POINT ( 'NONE',  ( 10.13035471959000056, 2.409325917207000511, -8.058043919563999680 ) ) ;
#4089=CARTESIAN_POINT ( 'NONE',  ( 1.311390132540666498, -3.500000000000000888, -0.4581489286485119217 ) ) ;
#4093=AXIS2_PLACEMENT_3D ( 'NONE', #7811, #34049, #2228 ) ;
#4101=ORIENTED_EDGE ( 'NONE', *, *, #32928, .T. ) ;
#4107=CARTESIAN_POINT ( 'NONE',  ( 0.1869138731963999878, 0.000000000000000000, 0.000000000000000000 ) ) ;
#4108=CARTESIAN_POINT ( 'NONE',  ( 9.269471092183000138, 5.100000000000000533, -6.152188490330000370 ) ) ;
#4113=CARTESIAN_POINT ( 'NONE',  ( 7.731795280408999993, 4.580608786027000612, 9.213365309690999538 ) ) ;
#4115=CARTESIAN_POINT ( 'NONE',  ( 10.82894633243952498, 2.649868422364484388, -7.263390030261542840 ) ) ;
#4118=EDGE_LOOP ( 'NONE', ( #34580, #19431, #37509 ) ) ;
#4121=EDGE_CURVE ( 'NONE', #54494, #17499, #32708, .T. ) ;
#4132=ORIENTED_EDGE ( 'NONE', *, *, #55235, .F. ) ;
#4134=VECTOR ( 'NONE', #15601, 1000.000000000000000 ) ;
#4137=CARTESIAN_POINT ( 'NONE',  ( 10.66852712374000056, 4.435471808682999395, -5.866466547508000673 ) ) ;
#4138=CARTESIAN_POINT ( 'NONE',  ( 8.678237328909947479, 5.064959164704544214, 6.230262016040554407 ) ) ;
#4142=CARTESIAN_POINT ( 'NONE',  ( 9.385781899350000401, 4.980865465981000106, 6.433345686594999613 ) ) ;
#4144=CIRCLE ( 'NONE', #37634, 12.50000000000000178 ) ;
#4145=CARTESIAN_POINT ( 'NONE',  ( 9.045397103852565124, 2.494519796715142235, -8.441659411582618233 ) ) ;
#4149=CARTESIAN_POINT ( 'NONE',  ( 10.13339736671999880, 5.653645990693000556, 6.501823474484000442 ) ) ;
#4152=CARTESIAN_POINT ( 'NONE',  ( 10.96261281413999988, 7.423575154918000685, -6.118088960612000804 ) ) ;
#4157=CARTESIAN_POINT ( 'NONE',  ( 11.02786554143000153, 5.596226216413000110, 7.209502215883999199 ) ) ;
#4161=CARTESIAN_POINT ( 'NONE',  ( 8.780820280412001466, 2.567871051582000241, -6.869011921437000012 ) ) ;
#4170=B_SPLINE_CURVE_WITH_KNOTS ( 'NONE', 3,
 ( #39781, #45374, #66334, #28608, #40132, #67024, #55164, #60414, #55860, #56542, #65647, #39089, #19133, #7966, #66681, #50268, #12519, #49920, #2033, #18114, #23351, #35230, #61445 ),
 .UNSPECIFIED., .F., .F.,
 ( 4, 2, 2, 2, 1, 2, 2, 2, 2, 2, 2, 4 ),
 ( 0.000000000000000000, 0.1250000000000140721, 0.1875000000000225653, 0.2187500000000262845, 0.2343750000000250355, 0.2421875000000237033, 0.2500000000000223710, 0.3750000000000177636, 0.4375000000000164313, 0.5000000000000150990, 0.7500000000000075495, 1.000000000000000000 ),
 .UNSPECIFIED. ) ;
#4171=CARTESIAN_POINT ( 'NONE',  ( 2.344930008642999830, -2.375092696518000146, -2.913277015014000160 ) ) ;
#4172=CARTESIAN_POINT ( 'NONE',  ( 7.373073341229000377, 3.394842219570000097, 9.388954446285000088 ) ) ;
#4173=CARTESIAN_POINT ( 'NONE',  ( 8.225464158772000545, 3.844886277615000125, -8.888911790991000927 ) ) ;
#4174=DIRECTION ( 'NONE',  ( -1.000000000000000000, 0.000000000000000000, 3.552713678903000467E-14 ) ) ;
#4183=CARTESIAN_POINT ( 'NONE',  ( 8.545864158774001851, 3.856772556595000179, 5.521246073317000125 ) ) ;
#4184=EDGE_CURVE ( 'NONE', #7152, #18020, #29174, .T. ) ;
#4190=CARTESIAN_POINT ( 'NONE',  ( 1.414247443154999839, -3.006852806188000216, -1.965371480138999871 ) ) ;
#4192=CARTESIAN_POINT ( 'NONE',  ( 2.049278142419042936, -3.167119488121065807, -0.9369383795961846451 ) ) ;
#4195=CARTESIAN_POINT ( 'NONE',  ( 10.69030645188999884, 5.903031974240000146, 7.830710565751001440 ) ) ;
#4202=CARTESIAN_POINT ( 'NONE',  ( 8.610875063856999745, 4.757997781751000410, 5.934102420827000124 ) ) ;
#4208=DIRECTION ( 'NONE',  ( 1.000000000000000000, 0.000000000000000000, 0.000000000000000000 ) ) ;
#4212=CARTESIAN_POINT ( 'NONE',  ( 9.290193290418001126, 2.377818438998999806, 7.540992072119000689 ) ) ;
#4213=CARTESIAN_POINT ( 'NONE',  ( 9.988718791410999387, 2.842026940133999702, -6.504333051298999635 ) ) ;
#4218=EDGE_CURVE ( 'NONE', #44139, #60354, #12645, .T. ) ;
#4219=CARTESIAN_POINT ( 'NONE',  ( 9.016029693782781962, 5.181541736818266131, 8.155019048524399849 ) ) ;
#4225=CARTESIAN_POINT ( 'NONE',  ( 5.399999746777999654, 0.000000000000000000, 0.000000000000000000 ) ) ;
#4230=ORIENTED_EDGE ( 'NONE', *, *, #43970, .T. ) ;
#4240=CARTESIAN_POINT ( 'NONE',  ( 0.4089629568059000020, 0.6171034757514999303, 3.149659041885999766 ) ) ;
#4242=AXIS2_PLACEMENT_3D ( 'NONE', #44518, #28428, #48710 ) ;
#4244=CARTESIAN_POINT ( 'NONE',  ( 11.09999999999999964, 2.700230688341999752, -5.136744347299999625 ) ) ;
#4247=EDGE_CURVE ( 'NONE', #10847, #13445, #3650, .T. ) ;
#4249=CARTESIAN_POINT ( 'NONE',  ( 10.92546721959000067, 5.641524285727999910, -7.883474821562000301 ) ) ;
#4257=CARTESIAN_POINT ( 'NONE',  ( 9.129428851719998406, 5.099284414202999827, 6.151604790022999758 ) ) ;
#4258=LINE ( 'NONE', #15104, #40753 ) ;
#4272=ADVANCED_FACE ( 'NONE', ( #63753 ), #34760, .F. ) ;
#4274=CARTESIAN_POINT ( 'NONE',  ( 2.678056799209334482, -2.150913519912214245, 2.798833948393621984 ) ) ;
#4284=CARTESIAN_POINT ( 'NONE',  ( 2.915556799211332706, -0.4581489286485083134, -3.500000000000000888 ) ) ;
#4285=CARTESIAN_POINT ( 'NONE',  ( 8.216604719590000272, 5.331510020787000315, -8.114341808290998159 ) ) ;
#4291=CARTESIAN_POINT ( 'NONE',  ( 8.674830025576062198, 2.649890579813255709, 7.499988935010339475 ) ) ;
#4293=CARTESIAN_POINT ( 'NONE',  ( 4.149992563291999836, -0.2617923565147979859, -1.999946284944288166 ) ) ;
#4302=CARTESIAN_POINT ( 'NONE',  ( 9.377520280414000098, 4.092867382745001059, -5.937785237406000505 ) ) ;
#4305=CARTESIAN_POINT ( 'NONE',  ( 9.766125411066999717, 4.735428155407000794, -8.791393655830999521 ) ) ;
#4321=ORIENTED_EDGE ( 'NONE', *, *, #19656, .T. ) ;
#4323=CARTESIAN_POINT ( 'NONE',  ( 8.548770280408998445, 5.203550244299999683, -8.391678825488000371 ) ) ;
#4324=CARTESIAN_POINT ( 'NONE',  ( 10.47253786429000044, 2.899999999999999911, -6.571291218949999902 ) ) ;
#4327=EDGE_CURVE ( 'NONE', #51766, #15157, #10279, .T. ) ;
#4339=CARTESIAN_POINT ( 'NONE',  ( 6.899999691988000450, -12.20988339176000004, -3.111064831550000243 ) ) ;
#4340=AXIS2_PLACEMENT_3D ( 'NONE', #5806, #6148, #16983 ) ;
#4343=CARTESIAN_POINT ( 'NONE',  ( 9.939260841229000221, 5.099602161831000124, -9.049221499261999924 ) ) ;
#4345=CARTESIAN_POINT ( 'NONE',  ( 7.961495038489999843, 3.389986099490999827, -6.279439026173999849 ) ) ;
#4347=EDGE_CURVE ( 'NONE', #20297, #67708, #9285, .T. ) ;
#4350=CARTESIAN_POINT ( 'NONE',  ( 3.444021066193000191, -0.7970639432754000886, 3.160059308709000092 ) ) ;
#4355=CARTESIAN_POINT ( 'NONE',  ( 3.499644761404835158, -1.843447052673009123, -2.761503345702634782 ) ) ;
#4356=CARTESIAN_POINT ( 'NONE',  ( 1.686390132541208509, -0.4581489286485234680, 3.499999999999998668 ) ) ;
#4370=ORIENTED_EDGE ( 'NONE', *, *, #11007, .T. ) ;
#4373=CARTESIAN_POINT ( 'NONE',  ( 6.612589158770999731, 5.292420046468999217, -7.844702366751000966 ) ) ;
#4396=CARTESIAN_POINT ( 'NONE',  ( 3.401913944286333980, -1.050734239995861019, -3.384364968950117625 ) ) ;
#4398=CARTESIAN_POINT ( 'NONE',  ( 11.12915085989000019, 3.083869275439000024, 8.585995236726001067 ) ) ;
#4399=DIRECTION ( 'NONE',  ( 0.8480635683784220058, 0.000000000000000000, -0.5298945026977139872 ) ) ;
#4401=CARTESIAN_POINT ( 'NONE',  ( 2.845251065309999827, 1.568303745132999749, -3.177790406895000253 ) ) ;
#4402=CYLINDRICAL_SURFACE ( 'NONE', #23168, 1.350000000000000533 ) ;
#4403=DIRECTION ( 'NONE',  ( 0.000000000000000000, 0.8648648648648717963, -0.5020047465136829867 ) ) ;
#4408=FACE_OUTER_BOUND ( 'NONE', #39180, .T. ) ;
#4413=CARTESIAN_POINT ( 'NONE',  ( 10.77962664842000073, 2.397507474987000009, 7.755423212350999407 ) ) ;
#4414=CARTESIAN_POINT ( 'NONE',  ( 11.09999999999999964, 5.299999999999999822, 6.469505845987999493 ) ) ;
#4422=CARTESIAN_POINT ( 'NONE',  ( 0.4021888528303215748, 2.957367267881657824, -1.739788196031706757 ) ) ;
#4428=CARTESIAN_POINT ( 'NONE',  ( 0.6912484304700000637, 2.302377811826000098, -2.236047032684999714 ) ) ;
#4431=CARTESIAN_POINT ( 'NONE',  ( 10.50897971959000010, 4.485029564998000318, -9.114435267298000909 ) ) ;
#4432=ORIENTED_EDGE ( 'NONE', *, *, #25440, .T. ) ;
#4433=CARTESIAN_POINT ( 'NONE',  ( 1.478056799207333460, 2.150913519912206695, -2.798833948393626869 ) ) ;
#4437=CARTESIAN_POINT ( 'NONE',  ( 9.170323341230000480, 5.558938731259999599, 6.272977177425000050 ) ) ;
#4439=CARTESIAN_POINT ( 'NONE',  ( 10.16000000000000014, 4.496968146123999865, -8.755198255949000696 ) ) ;
#4440=CARTESIAN_POINT ( 'NONE',  ( 8.362489158770998188, 5.592690705327999723, -8.535639167491000379 ) ) ;
#4456=CARTESIAN_POINT ( 'NONE',  ( 7.373073341229000377, 3.394842219570000097, 9.388954446285000088 ) ) ;
#4457=EDGE_LOOP ( 'NONE', ( #48790, #48754, #16300, #52974 ) ) ;
#4462=ORIENTED_EDGE ( 'NONE', *, *, #55425, .T. ) ;
#4464=CARTESIAN_POINT ( 'NONE',  ( 6.611566299282000791, 8.335736774492993106, -4.065895807218002034 ) ) ;
#4475=VERTEX_POINT ( 'NONE', #17604 ) ;
#4479=CARTESIAN_POINT ( 'NONE',  ( 9.701722306758000514, 4.253749110891999585, -8.839930742927998963 ) ) ;
#4483=CARTESIAN_POINT ( 'NONE',  ( 10.09696969267000100, 5.253376380222999131, 8.530663119653999260 ) ) ;
#4488=CARTESIAN_POINT ( 'NONE',  ( 9.285195242305000818, 5.269680202247999823, 8.747831873285999649 ) ) ;
#4490=CARTESIAN_POINT ( 'NONE',  ( 10.83658792121999959, 5.133186143592999962, 8.848368005200001107 ) ) ;
#4492=CARTESIAN_POINT ( 'NONE',  ( 8.722235841230000730, 3.844886277615000125, -8.888911790991000927 ) ) ;
#4493=CARTESIAN_POINT ( 'NONE',  ( 11.01762739314999884, 7.862581927908000701, -6.520239972965000241 ) ) ;
#4496=CARTESIAN_POINT ( 'NONE',  ( 10.87969287004431784, 5.549552169302327975, -8.346468143089040836 ) ) ;
#4498=CARTESIAN_POINT ( 'NONE',  ( 9.509901345851000443, 5.077442745148000647, 8.469003100811999474 ) ) ;
#4501=CARTESIAN_POINT ( 'NONE',  ( 8.929995280412999392, 5.030502105212999453, -6.322203460290999999 ) ) ;
#4503=CARTESIAN_POINT ( 'NONE',  ( 9.132625033077289345, 2.794592352500905541, 8.206332652464679356 ) ) ;
#4506=AXIS2_PLACEMENT_3D ( 'NONE', #67448, #62887, #9755 ) ;
#4508=ORIENTED_EDGE ( 'NONE', *, *, #44117, .T. ) ;
#4511=CARTESIAN_POINT ( 'NONE',  ( 7.886573341228999112, 3.084076314893000159, 9.259847992573000397 ) ) ;
#4514=CARTESIAN_POINT ( 'NONE',  ( 9.667489158770999680, 4.808846957865000604, -8.639578604182998944 ) ) ;
#4515=CARTESIAN_POINT ( 'NONE',  ( 10.90000053908999966, 0.000000000000000000, 0.000000000000000000 ) ) ;
#4517=VERTEX_POINT ( 'NONE', #57064 ) ;
#4518=CARTESIAN_POINT ( 'NONE',  ( 9.625496329943999285, 3.134638325776999856, 8.626949804392001653 ) ) ;
#4524=EDGE_LOOP ( 'NONE', ( #54508, #68012, #15369, #18504 ) ) ;
#4525=CARTESIAN_POINT ( 'NONE',  ( 8.058767219590999176, 2.432118421226999949, 6.597517552098000060 ) ) ;
#4535=CARTESIAN_POINT ( 'NONE',  ( 10.41103858098833790, 5.348820511807942601, 7.263526229479707830 ) ) ;
#4549=EDGE_LOOP ( 'NONE', ( #10593, #27962, #51852, #13002, #6695, #65973, #10325, #21314, #35450, #2497 ) ) ;
#4550=DIRECTION ( 'NONE',  ( 0.7071060865237062121, -0.7071074758487063683, -8.142070991701072997E-10 ) ) ;
#4552=CARTESIAN_POINT ( 'NONE',  ( 10.59344747867000081, 5.297752619853000944, 8.474195539311001113 ) ) ;
#4553=CARTESIAN_POINT ( 'NONE',  ( 11.19121071698999970, 3.005389011699000079, -6.023544385387999966 ) ) ;
#4559=AXIS2_PLACEMENT_3D ( 'NONE', #55432, #34800, #23267 ) ;
#4562=ADVANCED_FACE ( 'NONE', ( #25598 ), #46924, .F. ) ;
#4564=CARTESIAN_POINT ( 'NONE',  ( 7.555281674562000838, 4.314040636970999820, 8.819134391732999845 ) ) ;
#4567=CARTESIAN_POINT ( 'NONE',  ( 11.03667431141999877, 5.223173388369999337, -5.023616880107000249 ) ) ;
#4569=CARTESIAN_POINT ( 'NONE',  ( 8.008552228053002153, 8.952106511966999136, 5.726245348430995641 ) ) ;
#4574=ORIENTED_EDGE ( 'NONE', *, *, #59530, .F. ) ;
#4577=CARTESIAN_POINT ( 'NONE',  ( 5.500000000000000000, -12.78667792605000031, -2.345384795463000049 ) ) ;
#4583=CARTESIAN_POINT ( 'NONE',  ( 7.598073341229000022, 3.554857159507999853, 8.889479859586000288 ) ) ;
#4589=CARTESIAN_POINT ( 'NONE',  ( 7.802644552000999489, 3.157760251094000825, -6.317964942532003469 ) ) ;
#4591=CARTESIAN_POINT ( 'NONE',  ( 10.94033278040999946, 5.142729166069000435, -6.493505370358000128 ) ) ;
#4596=ORIENTED_EDGE ( 'NONE', *, *, #61266, .T. ) ;
#4600=ADVANCED_FACE ( 'NONE', ( #34614 ), #54197, .T. ) ;
#4603=AXIS2_PLACEMENT_3D ( 'NONE', #56350, #44834, #35035 ) ;
#4604=DIRECTION ( 'NONE',  ( 1.000000000000000000, 0.000000000000000000, 0.000000000000000000 ) ) ;
#4605=EDGE_CURVE ( 'NONE', #12182, #47849, #46821, .T. ) ;
#4609=ORIENTED_EDGE ( 'NONE', *, *, #62889, .F. ) ;
#4618=CARTESIAN_POINT ( 'NONE',  ( 7.656866975822993915, 3.528150633380001899, 6.493493947281997691 ) ) ;
#4623=CARTESIAN_POINT ( 'NONE',  ( 10.76685100253999927, 2.832432432432000269, 6.822293592207000934 ) ) ;
#4627=CARTESIAN_POINT ( 'NONE',  ( 9.102795280413999990, 3.071719032003000116, -6.037263251225000182 ) ) ;
#4629=ORIENTED_EDGE ( 'NONE', *, *, #2275, .T. ) ;
#4634=CARTESIAN_POINT ( 'NONE',  ( 9.342560841233000346, 5.835196551504000517, -7.008466539623000813 ) ) ;
#4635=CARTESIAN_POINT ( 'NONE',  ( 6.999998782146999332, 1.243449787579999883E-13, -12.50000000000276756 ) ) ;
#4639=DIRECTION ( 'NONE',  ( 1.000000000000000000, 0.000000000000000000, 0.000000000000000000 ) ) ;
#4640=VERTEX_POINT ( 'NONE', #53766 ) ;
#4643=CARTESIAN_POINT ( 'NONE',  ( 9.336654719594999818, 5.095038542659000136, -6.157541456184000062 ) ) ;
#4644=ORIENTED_EDGE ( 'NONE', *, *, #30786, .F. ) ;
#4645=CARTESIAN_POINT ( 'NONE',  ( 10.94349541711000029, 3.081616890687000065, -8.919380927961000793 ) ) ;
#4649=LINE ( 'NONE', #41383, #16191 ) ;
#4651=LINE ( 'NONE', #20745, #64778 ) ;
#4652=CARTESIAN_POINT ( 'NONE',  ( 8.552563423645223040, 3.075208796447511439, 6.073673062848093274 ) ) ;
#4653=VERTEX_POINT ( 'NONE', #5041 ) ;
#4658=DIRECTION ( 'NONE',  ( 0.000000000000000000, 1.000000000000000000, 0.000000000000000000 ) ) ;
#4659=CARTESIAN_POINT ( 'NONE',  ( 9.345514158774999913, 5.775964236216999836, -8.174909295649001706 ) ) ;
#4664=CARTESIAN_POINT ( 'NONE',  ( 8.631645280409999899, 3.826300099041999747, -9.055335252254000267 ) ) ;
#4675=LINE ( 'NONE', #51891, #31831 ) ;
#4679=EDGE_CURVE ( 'NONE', #47743, #6658, #10511, .T. ) ;
#4683=CARTESIAN_POINT ( 'NONE',  ( 5.500000000000000000, 11.95749337870000062, 3.642574926947999892 ) ) ;
#4689=CARTESIAN_POINT ( 'NONE',  ( 2.585745976258000400, -2.924233445111000140, -1.438799925142999925 ) ) ;
#4695=LINE ( 'NONE', #36878, #57212 ) ;
#4699=CARTESIAN_POINT ( 'NONE',  ( 10.97034794368816435, 8.644975688278298875, 6.526274310569194270 ) ) ;
#4703=VECTOR ( 'NONE', #64077, 1000.000000000000000 ) ;
#4713=CARTESIAN_POINT ( 'NONE',  ( 7.382754719588999315, 2.727583171400000062, -8.411095346025000197 ) ) ;
#4724=CARTESIAN_POINT ( 'NONE',  ( 9.022731225801246424, 2.899999999999999911, -6.450252854620909027 ) ) ;
#4727=CARTESIAN_POINT ( 'NONE',  ( 10.88582469064355784, 2.779316614152869569, 8.789661958747668535 ) ) ;
#4735=VERTEX_POINT ( 'NONE', #37208 ) ;
#4736=CARTESIAN_POINT ( 'NONE',  ( 11.09425120759000016, 2.431871068503000277, 7.769513029648000391 ) ) ;
#4737=CARTESIAN_POINT ( 'NONE',  ( 11.06205165877000063, 2.154392227069000132, -7.605898171884000192 ) ) ;
#4740=CARTESIAN_POINT ( 'NONE',  ( 9.318935841232999451, 2.644017913812000131, -7.838184857420000817 ) ) ;
#4747=B_SPLINE_CURVE_WITH_KNOTS ( 'NONE', 3,
 ( #57548, #57900, #31337, #9651 ),
 .UNSPECIFIED., .F., .F.,
 ( 4, 4 ),
 ( 0.000000000000000000, 1.000000000000000000 ),
 .UNSPECIFIED. ) ;
#4755=CARTESIAN_POINT ( 'NONE',  ( 11.06923869026000062, 5.425682056982999768, 8.012911262916999178 ) ) ;
#4756=LINE ( 'NONE', #57211, #54052 ) ;
#4757=CIRCLE ( 'NONE', #24839, 12.49999909015999577 ) ;
#4766=CARTESIAN_POINT ( 'NONE',  ( 9.807804719590000886, 3.988943694240999704, -8.966360307350999648 ) ) ;
#4768=CARTESIAN_POINT ( 'NONE',  ( 1.000973465875999890, 3.500000000000000000, 0.000000000000000000 ) ) ;
#4773=CARTESIAN_POINT ( 'NONE',  ( 11.12964528040999923, 3.869081149487999749, -9.017143166339000260 ) ) ;
#4784=CARTESIAN_POINT ( 'NONE',  ( 7.914964158766999880, 4.624432025063999419, -9.294334464733999823 ) ) ;
#4787=ORIENTED_EDGE ( 'NONE', *, *, #27139, .F. ) ;
#4791=ORIENTED_EDGE ( 'NONE', *, *, #3685, .F. ) ;
#4794=ORIENTED_EDGE ( 'NONE', *, *, #62529, .T. ) ;
#4795=CARTESIAN_POINT ( 'NONE',  ( 8.020125753392001400, 4.498951069075999953, -6.245588651729999441 ) ) ;
#4802=CARTESIAN_POINT ( 'NONE',  ( 8.539829719592999524, 5.633477595780999714, 7.451234169193000412 ) ) ;
#4803=EDGE_CURVE ( 'NONE', #31036, #56100, #53984, .T. ) ;
#4805=ORIENTED_EDGE ( 'NONE', *, *, #19446, .T. ) ;
#4806=CARTESIAN_POINT ( 'NONE',  ( 10.84289849785056603, 2.713620053740517957, -7.026897974086664611 ) ) ;
#4814=CARTESIAN_POINT ( 'NONE',  ( 11.88107297659999340, 9.756593325465996003, -5.710004264910002014 ) ) ;
#4821=VERTEX_POINT ( 'NONE', #54666 ) ;
#4826=CARTESIAN_POINT ( 'NONE',  ( 9.780284676292000157, 3.021596928575999819, -8.450035627617001666 ) ) ;
#4832=VERTEX_POINT ( 'NONE', #54314 ) ;
#4834=ORIENTED_EDGE ( 'NONE', *, *, #28863, .F. ) ;
#4838=CARTESIAN_POINT ( 'NONE',  ( 10.16829701902000060, 4.567214950372999738, 5.832525041908999341 ) ) ;
#4840=CARTESIAN_POINT ( 'NONE',  ( 7.024999999999923084, 5.339057002848925926, -8.130112396048053469 ) ) ;
#4841=AXIS2_PLACEMENT_3D ( 'NONE', #37703, #26879, #48195 ) ;
#4844=CARTESIAN_POINT ( 'NONE',  ( 11.04498420206273224, 2.508453239880112928, -8.445281263845473063 ) ) ;
#4849=CARTESIAN_POINT ( 'NONE',  ( 10.07367028041000090, 4.905765359186999852, -8.776126235875999271 ) ) ;
#4855=ORIENTED_EDGE ( 'NONE', *, *, #17354, .T. ) ;
#4860=CARTESIAN_POINT ( 'NONE',  ( 9.890475510420877470, 2.705325637622069124, 8.717411133782642096 ) ) ;
#4866=CARTESIAN_POINT ( 'NONE',  ( 10.53734212242000012, 2.992816679959000137, 8.731689474572998932 ) ) ;
#4872=CARTESIAN_POINT ( 'NONE',  ( 8.866801658774001282, 2.550580605805000012, 8.854682662413999594 ) ) ;
#4873=FACE_OUTER_BOUND ( 'NONE', #32951, .T. ) ;
#4878=VERTEX_POINT ( 'NONE', #59560 ) ;
#4881=PLANE ( 'NONE',  #42001 ) ;
#4894=ADVANCED_FACE ( 'NONE', ( #43138 ), #17616, .T. ) ;
#4899=CARTESIAN_POINT ( 'NONE',  ( 8.571413182547999554, 4.599999999999999645, 5.927302706106000407 ) ) ;
#4901=CARTESIAN_POINT ( 'NONE',  ( 10.31667774810000004, 3.819530253758000260, 6.062195927068000145 ) ) ;
#4902=CARTESIAN_POINT ( 'NONE',  ( 10.57793656291999973, 4.393379542724999531, -6.024362243994999311 ) ) ;
#4903=CARTESIAN_POINT ( 'NONE',  ( 8.200215090286000930, 5.110410283172001300, 6.692116316553004651 ) ) ;
#4906=CARTESIAN_POINT ( 'NONE',  ( 9.039804132582757390, 4.929468674194135147, 8.478882605368561087 ) ) ;
#4908=CARTESIAN_POINT ( 'NONE',  ( 8.919607780412000864, 5.165497731316000873, 8.645531386060000045 ) ) ;
#4913=CARTESIAN_POINT ( 'NONE',  ( 9.227928106276422682, 2.649889033192923016, 7.452433103127532377 ) ) ;
#4914=CARTESIAN_POINT ( 'NONE',  ( 8.598411888655869362, 2.943885513252815667, -6.252349181257627286 ) ) ;
#4918=CARTESIAN_POINT ( 'NONE',  ( 10.90664291662000451, 8.258660472640997341, 7.032076946551004681 ) ) ;
#4920=CARTESIAN_POINT ( 'NONE',  ( 11.12455253368000108, 7.320617754035000146, 6.383266958155999760 ) ) ;
#4922=VECTOR ( 'NONE', #51487, 1000.000000000000000 ) ;
#4927=CARTESIAN_POINT ( 'NONE',  ( 11.10000000009000054, 5.300000000088999741, -6.571291220400000022 ) ) ;
#4932=CARTESIAN_POINT ( 'NONE',  ( 0.5240331185627999933, -2.301202007355999779, -2.466905145517999998 ) ) ;
#4940=CARTESIAN_POINT ( 'NONE',  ( 10.88760471959000142, 5.634847467408999222, -7.088990678556999825 ) ) ;
#4947=CARTESIAN_POINT ( 'NONE',  ( 0.7857456912831999318, 2.980225901380999964, 1.319047437492999908 ) ) ;
#4948=LINE ( 'NONE', #26285, #17743 ) ;
#4949=CARTESIAN_POINT ( 'NONE',  ( 9.448736632827984039, 4.355932816508206962, -9.239297493378444415 ) ) ;
#4957=ORIENTED_EDGE ( 'NONE', *, *, #32219, .F. ) ;
#4966=CARTESIAN_POINT ( 'NONE',  ( 8.687922088694000067, 3.419384128876999718, -5.860036257779999147 ) ) ;
#4967=CIRCLE ( 'NONE', #47400, 1.550000000000000044 ) ;
#4969=CARTESIAN_POINT ( 'NONE',  ( 8.016657426769000949, 2.906672751340000804, 6.403732826568004910 ) ) ;
#4978=CARTESIAN_POINT ( 'NONE',  ( 8.266329719591000824, 4.769017407621999993, -8.862909124839001507 ) ) ;
#4980=ORIENTED_EDGE ( 'NONE', *, *, #19798, .T. ) ;
#4981=CARTESIAN_POINT ( 'NONE',  ( 7.961778384057998537, 4.370833349752165198, -6.185172849432923670 ) ) ;
#4992=CARTESIAN_POINT ( 'NONE',  ( 8.681370280410998674, 2.949305648881000330, -8.659807625323999503 ) ) ;
#4993=VERTEX_POINT ( 'NONE', #24231 ) ;
#5008=DIRECTION ( 'NONE',  ( 1.000000000000000000, 0.000000000000000000, 0.000000000000000000 ) ) ;
#5016=LINE ( 'NONE', #42769, #4703 ) ;
#5032=DIRECTION ( 'NONE',  ( 0.000000000000000000, 0.9565994702956989171, -0.2914059941558995170 ) ) ;
#5036=CARTESIAN_POINT ( 'NONE',  ( 7.995310464097279635, 3.151543199498028525, -6.329371383534729389 ) ) ;
#5038=CARTESIAN_POINT ( 'NONE',  ( 11.09999999999999964, 5.350000000000000533, -7.500000000000000000 ) ) ;
#5040=CARTESIAN_POINT ( 'NONE',  ( 8.330224159023998709, 2.898680183691999979, -6.607597200868999820 ) ) ;
#5041=CARTESIAN_POINT ( 'NONE',  ( 11.09999999999999964, 5.299316147296000423, -5.124965750789000296 ) ) ;
#5049=ORIENTED_EDGE ( 'NONE', *, *, #4605, .F. ) ;
#5056=CARTESIAN_POINT ( 'NONE',  ( 7.686568289202588389, 4.059993974225437618, -8.863793664233034164 ) ) ;
#5062=DIRECTION ( 'NONE',  ( 0.000000000000000000, -1.000000000000000000, 0.000000000000000000 ) ) ;
#5064=VECTOR ( 'NONE', #64420, 1000.000000000000114 ) ;
#5068=CARTESIAN_POINT ( 'NONE',  ( 7.134129719589999752, 5.287968704092000927, -6.611025344044000107 ) ) ;
#5070=CARTESIAN_POINT ( 'NONE',  ( 9.481858773912280824, 5.015405643915004319, 8.392875400259256935 ) ) ;
#5077=CARTESIAN_POINT ( 'NONE',  ( 8.199995020667000034, 2.894508905068999827, 6.645190348705000360 ) ) ;
#5091=CARTESIAN_POINT ( 'NONE',  ( 10.00122429346999908, 2.274087081648999753, 7.851326250696001097 ) ) ;
#5095=CARTESIAN_POINT ( 'NONE',  ( 9.468110841233000841, 4.082930418187999955, -6.104944817728999773 ) ) ;
#5097=CARTESIAN_POINT ( 'NONE',  ( 8.348432779685110106, 2.904641401162685099, 6.526586896465118137 ) ) ;
#5107=CARTESIAN_POINT ( 'NONE',  ( 10.25461802485000007, 2.860644035673999941, 6.604613005744999654 ) ) ;
#5116=ORIENTED_EDGE ( 'NONE', *, *, #10605, .F. ) ;
#5118=CARTESIAN_POINT ( 'NONE',  ( 9.518314158773000244, 4.845406482350000488, -6.387189183984999907 ) ) ;
#5119=ADVANCED_FACE ( 'NONE', ( #40651 ), #29510, .T. ) ;
#5122=CARTESIAN_POINT ( 'NONE',  ( 10.99107545325776059, 6.540855374579558124, 5.311061621516608433 ) ) ;
#5126=CARTESIAN_POINT ( 'NONE',  ( 10.31153584123000044, 2.716831823259000078, -7.950163994344000784 ) ) ;
#5127=VERTEX_POINT ( 'NONE', #41000 ) ;
#5135=CARTESIAN_POINT ( 'NONE',  ( 7.051920280410000075, 5.216734614776999734, -8.484106667489999865 ) ) ;
#5136=EDGE_CURVE ( 'NONE', #54335, #61003, #56046, .T. ) ;
#5139=EDGE_LOOP ( 'NONE', ( #25567, #14535, #4787, #24331, #23231, #13530 ) ) ;
#5140=CARTESIAN_POINT ( 'NONE',  ( 2.928056799210041028, 2.150913519912206695, -2.798833948393627313 ) ) ;
#5147=CARTESIAN_POINT ( 'NONE',  ( 10.15000066238999921, -1.190159082397999942E-13, -1.213918169242000045E-13 ) ) ;
#5156=ORIENTED_EDGE ( 'NONE', *, *, #7086, .F. ) ;
#5157=CARTESIAN_POINT ( 'NONE',  ( 7.293864158771000028, 3.416213390569000197, 6.162512717529000206 ) ) ;
#5158=ORIENTED_EDGE ( 'NONE', *, *, #23689, .T. ) ;
#5160=CARTESIAN_POINT ( 'NONE',  ( 9.433148997456999751, 5.167567567567999731, 6.822293592207000934 ) ) ;
#5163=CARTESIAN_POINT ( 'NONE',  ( 11.01812914314999858, 6.614778905590999791, -5.431520484943000326 ) ) ;
#5167=FACE_OUTER_BOUND ( 'NONE', #51693, .T. ) ;
#5178=CARTESIAN_POINT ( 'NONE',  ( 11.19121071698999970, 3.005389011699000079, -6.023544385387999966 ) ) ;
#5179=B_SPLINE_CURVE_WITH_KNOTS ( 'NONE', 3,
 ( #20510, #19483, #31018, #63145, #51973, #52327, #4422, #67360, #9321, #47090 ),
 .UNSPECIFIED., .F., .F.,
 ( 4, 2, 2, 2, 4 ),
 ( 0.2468845652704700078, 0.4351634239528525128, 0.6234422826352350455, 0.8117211413176175228, 1.000000000000000000 ),
 .UNSPECIFIED. ) ;
#5183=CARTESIAN_POINT ( 'NONE',  ( 8.436987556243993325, 2.901283824935000144, -6.624026488670998525 ) ) ;
#5189=CARTESIAN_POINT ( 'NONE',  ( 10.24477918374999952, 5.265206995764999398, 8.959504263949002123 ) ) ;
#5191=CARTESIAN_POINT ( 'NONE',  ( 9.070310841232000598, 5.361622798585000460, -7.185294144754000634 ) ) ;
#5195=CARTESIAN_POINT ( 'NONE',  ( 9.571961069101000419, 4.084683332033999470, 8.946609345378000455 ) ) ;
#5196=CARTESIAN_POINT ( 'NONE',  ( 4.074968078372999791, 0.000000000000000000, -2.074968475931999734 ) ) ;
#5198=CARTESIAN_POINT ( 'NONE',  ( 8.821685841230998193, 2.633142096252999664, -7.791134854666999843 ) ) ;
#5200=EDGE_CURVE ( 'NONE', #51368, #5489, #20688, .T. ) ;
#5203=CARTESIAN_POINT ( 'NONE',  ( 3.416991155292667504, 1.737579674229352333, -3.072309530587345794 ) ) ;
#5208=B_SPLINE_CURVE_WITH_KNOTS ( 'NONE', 3,
 ( #67190, #30490, #29478, #24557 ),
 .UNSPECIFIED., .F., .F.,
 ( 4, 4 ),
 ( 0.000000000000000000, 1.000000000000000000 ),
 .UNSPECIFIED. ) ;
#5212=CARTESIAN_POINT ( 'NONE',  ( 8.763579719593998618, 4.815598936798999752, -8.835641302565999666 ) ) ;
#5214=CARTESIAN_POINT ( 'NONE',  ( 3.106872424883109662, -1.723087394956521745, -2.764963742037524153 ) ) ;
#5215=B_SPLINE_CURVE_WITH_KNOTS ( 'NONE', 3,
 ( #65624, #60391, #12495, #39762, #34861, #29278, #3033, #23671, #18437, #56868, #18781, #34174, #50247, #55493, #56177, #67004, #7593, #2009 ),
 .UNSPECIFIED., .F., .F.,
 ( 4, 2, 2, 2, 2, 2, 2, 2, 4 ),
 ( 0.000000000000000000, 0.1249999999999998890, 0.2499999999999997780, 0.3749999999999997780, 0.4999999999999997780, 0.6249999999999998890, 0.7500000000000000000, 0.8750000000000000000, 1.000000000000000000 ),
 .UNSPECIFIED. ) ;
#5217=CARTESIAN_POINT ( 'NONE',  ( 10.64872393945999995, 2.614781729644000130, 6.717281948314999696 ) ) ;
#5223=CARTESIAN_POINT ( 'NONE',  ( 7.903989158771000056, 2.095715612964000218, 8.056490963156001328 ) ) ;
#5228=CARTESIAN_POINT ( 'NONE',  ( 1.118609070385999882, -2.100966486736999705, -2.491430570518000209 ) ) ;
#5233=CARTESIAN_POINT ( 'NONE',  ( 10.07770645819999977, 4.622041375574999833, 5.671348593713000596 ) ) ;
#5237=CARTESIAN_POINT ( 'NONE',  ( 8.713854719593998155, 5.442817578555000146, -8.106149115450000053 ) ) ;
#5241=CIRCLE ( 'NONE', #14187, 1.500000000000000000 ) ;
#5252=CARTESIAN_POINT ( 'NONE',  ( 10.66852712374000056, 4.435471808682999395, -5.866466547508000673 ) ) ;
#5258=CARTESIAN_POINT ( 'NONE',  ( 9.240545280410998430, 4.158911560497999815, 5.873540104660999184 ) ) ;
#5260=CARTESIAN_POINT ( 'NONE',  ( 7.399999999999995026, 4.000000000000000000, 9.109807621135329825 ) ) ;
#5267=CARTESIAN_POINT ( 'NONE',  ( 11.01356641589999974, 2.786433584103999994, 6.253463831328000211 ) ) ;
#5268=CARTESIAN_POINT ( 'NONE',  ( 7.000000000000000000, 0.8000000000000000444, -3.149999999999999911 ) ) ;
#5270=ORIENTED_EDGE ( 'NONE', *, *, #23663, .F. ) ;
#5277=CARTESIAN_POINT ( 'NONE',  ( 0.1621700897146000075, -0.4897778999537000244, -3.171902824723000336 ) ) ;
#5285=CARTESIAN_POINT ( 'NONE',  ( 10.31966721959000033, 4.764593388688000530, -5.997651217580999727 ) ) ;
#5300=CARTESIAN_POINT ( 'NONE',  ( 8.154280367422950704, 3.077394263664351648, 6.302239162262017302 ) ) ;
#5305=CARTESIAN_POINT ( 'NONE',  ( 10.97863725587999895, 5.126101790820000836, -4.940798661402999947 ) ) ;
#5306=EDGE_CURVE ( 'NONE', #15298, #52595, #1496, .T. ) ;
#5319=EDGE_LOOP ( 'NONE', ( #31789, #63161, #27500 ) ) ;
#5320=CARTESIAN_POINT ( 'NONE',  ( 8.664129719593997692, 5.524776413195999325, -7.147585171405999915 ) ) ;
#5323=CARTESIAN_POINT ( 'NONE',  ( 9.725191424783275806, 2.649754699899339538, 7.500009801425228773 ) ) ;
#5333=ORIENTED_EDGE ( 'NONE', *, *, #34423, .F. ) ;
#5335=CARTESIAN_POINT ( 'NONE',  ( 9.070310841232000598, 5.361622798585000460, -7.185294144754000634 ) ) ;
#5336=ORIENTED_EDGE ( 'NONE', *, *, #68958, .T. ) ;
#5343=CARTESIAN_POINT ( 'NONE',  ( 7.000000000000000000, 0.6769230769231000533, 2.665384615385000266 ) ) ;
#5349=EDGE_CURVE ( 'NONE', #36055, #61826, #46342, .T. ) ;
#5357=CARTESIAN_POINT ( 'NONE',  ( 9.842764158772000727, 5.798263352390999437, -8.113145944980999502 ) ) ;
#5361=ORIENTED_EDGE ( 'NONE', *, *, #33227, .T. ) ;
#5365=DIRECTION ( 'NONE',  ( 0.000000000000000000, 0.000000000000000000, -1.000000000000000000 ) ) ;
#5381=CARTESIAN_POINT ( 'NONE',  ( 10.90000037895999796, 0.2999996193951000034, 9.776630289319001577 ) ) ;
#5384=CARTESIAN_POINT ( 'NONE',  ( 7.510833333330749539, 4.353359643885027275, -6.185136886497772934 ) ) ;
#5387=EDGE_CURVE ( 'NONE', #16312, #66190, #6429, .T. ) ;
#5389=CARTESIAN_POINT ( 'NONE',  ( 0.1499942179680000542, -1.689975037551094017, -2.199046806507074958 ) ) ;
#5393=EDGE_CURVE ( 'NONE', #57153, #3039, #9782, .T. ) ;
#5396=CARTESIAN_POINT ( 'NONE',  ( 3.499617999551372094, -1.078410421222687265, -3.177282998230454680 ) ) ;
#5397=CARTESIAN_POINT ( 'NONE',  ( 10.31298165360522212, 2.920330592986121854, -8.329669302950199139 ) ) ;
#5398=ORIENTED_EDGE ( 'NONE', *, *, #48490, .F. ) ;
#5399=CARTESIAN_POINT ( 'NONE',  ( 10.85502524286000003, 2.899999999999999911, 6.518873296399666728 ) ) ;
#5405=AXIS2_PLACEMENT_3D ( 'NONE', #20116, #37229, #42137 ) ;
#5410=ORIENTED_EDGE ( 'NONE', *, *, #64730, .T. ) ;
#5411=CARTESIAN_POINT ( 'NONE',  ( 8.101203251003541439, 5.350537603185198776, -7.263478961105667153 ) ) ;
#5414=CIRCLE ( 'NONE', #8770, 11.84999999999999964 ) ;
#5415=ORIENTED_EDGE ( 'NONE', *, *, #57045, .T. ) ;
#5417=CARTESIAN_POINT ( 'NONE',  ( 7.324170280405000177, 5.383759907926999766, -8.542359279933998906 ) ) ;
#5419=CARTESIAN_POINT ( 'NONE',  ( 9.489492469587677448, 4.926922721015970730, 8.481275974749992841 ) ) ;
#5423=DIRECTION ( 'NONE',  ( 0.000000000000000000, 0.9916377111174247139, 0.1290528957048031888 ) ) ;
#5429=DIRECTION ( 'NONE',  ( 1.000000000000000000, 0.000000000000000000, 0.000000000000000000 ) ) ;
#5432=CARTESIAN_POINT ( 'NONE',  ( 8.186785167650000972, 5.111321349790002522, -6.695956001718002426 ) ) ;
#5436=EDGE_CURVE ( 'NONE', #28156, #22744, #39023, .T. ) ;
#5437=EDGE_CURVE ( 'NONE', #23656, #46704, #58889, .T. ) ;
#5441=ORIENTED_EDGE ( 'NONE', *, *, #38350, .F. ) ;
#5442=CARTESIAN_POINT ( 'NONE',  ( 10.78089701270000056, 5.735299658853000082, 7.801561896854000366 ) ) ;
#5443=CARTESIAN_POINT ( 'NONE',  ( 10.26693915877000052, 5.500023470133998948, -6.419501519420999891 ) ) ;
#5445=CARTESIAN_POINT ( 'NONE',  ( 9.368660841232999914, 2.702406276695999754, -6.981052078638000147 ) ) ;
#5446=FACE_OUTER_BOUND ( 'NONE', #63719, .T. ) ;
#5452=AXIS2_PLACEMENT_3D ( 'NONE', #5632, #58432, #52 ) ;
#5458=CARTESIAN_POINT ( 'NONE',  ( 10.22108913916999917, 2.983268757921999637, 8.764704075288999974 ) ) ;
#5467=VERTEX_POINT ( 'NONE', #25696 ) ;
#5471=CARTESIAN_POINT ( 'NONE',  ( 11.09999965054999826, -12.24999851416000141, 0.000000000000000000 ) ) ;
#5474=CARTESIAN_POINT ( 'NONE',  ( 0.4116496906523000043, 2.199938726422999924, 2.557617887446999916 ) ) ;
#5476=CARTESIAN_POINT ( 'NONE',  ( 11.37168584123000059, 2.803494217761000495, -6.967881733280000489 ) ) ;
#5477=ORIENTED_EDGE ( 'NONE', *, *, #38262, .F. ) ;
#5478=CARTESIAN_POINT ( 'NONE',  ( 8.960616452296999768, 2.899999999999999911, 6.279946362737000243 ) ) ;
#5483=CARTESIAN_POINT ( 'NONE',  ( 7.822385841228999048, 4.636729845879000500, 9.378977473003999421 ) ) ;
#5486=CARTESIAN_POINT ( 'NONE',  ( 7.955829719586001048, 5.418947913204000599, -8.493927145653000110 ) ) ;
#5489=VERTEX_POINT ( 'NONE', #31989 ) ;
#5490=CARTESIAN_POINT ( 'NONE',  ( 2.886390132543207976, 0.4581489286485156964, -3.499999999999998668 ) ) ;
#5496=VERTEX_POINT ( 'NONE', #26393 ) ;
#5502=ORIENTED_EDGE ( 'NONE', *, *, #19311, .T. ) ;
#5503=CARTESIAN_POINT ( 'NONE',  ( 8.218892219592001780, 3.011620138462000273, 8.801434747080000065 ) ) ;
#5507=CARTESIAN_POINT ( 'NONE',  ( 11.12440625316000009, 6.500244850899999705, -5.560228937576999542 ) ) ;
#5518=ORIENTED_EDGE ( 'NONE', *, *, #67769, .T. ) ;
#5524=CARTESIAN_POINT ( 'NONE',  ( 9.973493989215999278, 4.344963986309999804, -9.321593970653999861 ) ) ;
#5529=ORIENTED_EDGE ( 'NONE', *, *, #36574, .F. ) ;
#5531=CARTESIAN_POINT ( 'NONE',  ( 9.629022744239000176, 5.794335169544999609, 7.414871903737999759 ) ) ;
#5532=DIRECTION ( 'NONE',  ( 0.000000000000000000, -0.9048270524743471377, 0.4257792915473756490 ) ) ;
#5540=FACE_OUTER_BOUND ( 'NONE', #56381, .T. ) ;
#5541=FILL_AREA_STYLE_COLOUR ( '', #2020 ) ;
#5552=CARTESIAN_POINT ( 'NONE',  ( 8.126014158770999529, 5.189036231907000030, -8.048606212067999977 ) ) ;
#5554=CARTESIAN_POINT ( 'NONE',  ( 2.687702790109109952, 1.441822626232357685, -2.921506834555485099 ) ) ;
#5556=CARTESIAN_POINT ( 'NONE',  ( 10.14750576281000072, 2.602962605360999770, 6.738577830910999822 ) ) ;
#5562=CARTESIAN_POINT ( 'NONE',  ( 8.122954719591000128, 3.566637212418000136, 5.743604853744000316 ) ) ;
#5565=CIRCLE ( 'NONE', #43557, 11.35000000000000142 ) ;
#5568=CARTESIAN_POINT ( 'NONE',  ( 2.024566109761000376, -3.102129433205000009, 0.9990388109167002151 ) ) ;
#5573=VERTEX_POINT ( 'NONE', #58200 ) ;
#5574=CARTESIAN_POINT ( 'NONE',  ( 8.772439158776000667, 3.098073081301000009, -8.567513114264999174 ) ) ;
#5577=CARTESIAN_POINT ( 'NONE',  ( 7.946887679546887462, 4.820318833187246632, -6.338152156212514932 ) ) ;
#5585=CARTESIAN_POINT ( 'NONE',  ( 10.26328274790922812, 2.909659596545209670, -8.325272347294529141 ) ) ;
#5586=CARTESIAN_POINT ( 'NONE',  ( 10.74708949327000163, 5.603142351927999698, -6.963341971584000589 ) ) ;
#5592=EDGE_CURVE ( 'NONE', #54751, #23033, #37274, .T. ) ;
#5593=CARTESIAN_POINT ( 'NONE',  ( 9.331135841230999262, 4.141907758973999876, 6.047574021139999978 ) ) ;
#5597=DIRECTION ( 'NONE',  ( 0.000000000000000000, -1.000000000000000000, 0.000000000000000000 ) ) ;
#5600=CARTESIAN_POINT ( 'NONE',  ( 11.01817350255000072, 6.612266912192000134, 5.428976045567000419 ) ) ;
#5601=CARTESIAN_POINT ( 'NONE',  ( 11.12486389849000012, 7.229950150994000069, 6.290773257298000409 ) ) ;
#5603=CYLINDRICAL_SURFACE ( 'NONE', #34878, 0.4999999999999998335 ) ;
#5604=ORIENTED_EDGE ( 'NONE', *, *, #46115, .F. ) ;
#5616=CARTESIAN_POINT ( 'NONE',  ( 0.7791522574427000025, 2.971343835407000089, -0.7711576440234000351 ) ) ;
#5619=CARTESIAN_POINT ( 'NONE',  ( 9.793983440715679833, 2.684660541979530635, -7.853435705109036213 ) ) ;
#5622=CARTESIAN_POINT ( 'NONE',  ( 7.983198341228001205, 5.321913229613000063, 8.118244847118999630 ) ) ;
#5624=CARTESIAN_POINT ( 'NONE',  ( 8.227131012390005438, 3.380163391545999207, -6.126525137394006393 ) ) ;
#5625=CARTESIAN_POINT ( 'NONE',  ( 11.17788388625999829, 2.412139249855000056, -7.075601348558000048 ) ) ;
#5632=CARTESIAN_POINT ( 'NONE',  ( 11.09999999999999964, 0.000000000000000000, 0.000000000000000000 ) ) ;
#5645=CARTESIAN_POINT ( 'NONE',  ( 8.631025703289717299, 3.780324811990126488, -5.892885401209013274 ) ) ;
#5652=CARTESIAN_POINT ( 'NONE',  ( 5.500000000000000000, -12.43893545635000031, -2.828937028792000152 ) ) ;
#5654=CARTESIAN_POINT ( 'NONE',  ( 27.64127793187000037, 3.399999999999999911, 4.505338571134999803 ) ) ;
#5655=B_SPLINE_CURVE_WITH_KNOTS ( 'NONE', 3,
 ( #1328, #22303, #32806, #38039, #16709, #55161, #64940, #59365, #64601, #22646, #12171, #39086, #33501, #22994, #6218, #27911, #11812, #12514, #43991, #43644, #27558, #6914, #49916, #2029 ),
 .UNSPECIFIED., .F., .F.,
 ( 4, 2, 2, 1, 2, 2, 2, 2, 2, 2, 1, 2, 4 ),
 ( 0.000000000000000000, 0.1250000000000000000, 0.1875000000000000278, 0.2500000000000000555, 0.3125000000000001110, 0.3750000000000001110, 0.5000000000000001110, 0.6250000000000001110, 0.7500000000000001110, 0.8125000000000001110, 0.8750000000000001110, 0.9375000000000001110, 1.000000000000000000 ),
 .UNSPECIFIED. ) ;
#5656=AXIS2_PLACEMENT_3D ( 'NONE', #64708, #6680, #68666 ) ;
#5657=VERTEX_POINT ( 'NONE', #39641 ) ;
#5658=CARTESIAN_POINT ( 'NONE',  ( 9.003345280414000840, 2.319062457810000311, -7.919229449146000022 ) ) ;
#5660=VERTEX_POINT ( 'NONE', #60273 ) ;
#5663=EDGE_LOOP ( 'NONE', ( #57772, #37739, #6022, #16331 ) ) ;
#5675=CARTESIAN_POINT ( 'NONE',  ( 8.622785841227999626, 5.189036231907000030, -8.048606212067999977 ) ) ;
#5676=EDGE_CURVE ( 'NONE', #44476, #61826, #45710, .T. ) ;
#5678=CARTESIAN_POINT ( 'NONE',  ( 0.4268955145921133343, -1.033550240898596373, 3.083630227088956399 ) ) ;
#5680=EDGE_CURVE ( 'NONE', #5660, #64040, #3877, .T. ) ;
#5681=VERTEX_POINT ( 'NONE', #22857 ) ;
#5697=CARTESIAN_POINT ( 'NONE',  ( 10.55101852147976871, 5.350099180695919721, -7.263329207706104462 ) ) ;
#5701=CIRCLE ( 'NONE', #4559, 0.5000000000000000000 ) ;
#5702=CARTESIAN_POINT ( 'NONE',  ( 10.95213788436999991, 5.154141894912999788, -5.181730563652999777 ) ) ;
#5703=CARTESIAN_POINT ( 'NONE',  ( 7.910784822165987329, 5.348998117051813495, 7.262899563230552857 ) ) ;
#5707=CARTESIAN_POINT ( 'NONE',  ( 11.09999999999999964, 5.299999999999999822, -6.571291218949999902 ) ) ;
#5716=CARTESIAN_POINT ( 'NONE',  ( 11.09999999999999964, 5.771037996939999637, -5.145626010725000476 ) ) ;
#5727=ADVANCED_FACE ( 'NONE', ( #40325 ), #43617, .T. ) ;
#5733=VERTEX_POINT ( 'NONE', #16497 ) ;
#5744=EDGE_LOOP ( 'NONE', ( #37231, #47503, #60698, #46344, #65796, #13780, #14925, #14592, #30451, #42264, #12133, #27894 ) ) ;
#5751=CARTESIAN_POINT ( 'NONE',  ( 7.125270280406000190, 3.516145570366999706, -5.836512876186000121 ) ) ;
#5752=B_SPLINE_CURVE_WITH_KNOTS ( 'NONE', 3,
 ( #2568, #55025, #39637, #28111 ),
 .UNSPECIFIED., .F., .F.,
 ( 4, 4 ),
 ( 0.000000000000000000, 1.000000000000000000 ),
 .UNSPECIFIED. ) ;
#5755=ORIENTED_EDGE ( 'NONE', *, *, #26356, .F. ) ;
#5763=ORIENTED_EDGE ( 'NONE', *, *, #20514, .T. ) ;
#5767=VECTOR ( 'NONE', #41307, 1000.000000000000000 ) ;
#5771=CARTESIAN_POINT ( 'NONE',  ( 3.250973465878000290, -3.500000000000000000, 0.000000000000000000 ) ) ;
#5775=CARTESIAN_POINT ( 'NONE',  ( 10.35616100078999935, 2.777276096020000029, 8.995275123087999702 ) ) ;
#5776=FACE_OUTER_BOUND ( 'NONE', #38008, .T. ) ;
#5779=CARTESIAN_POINT ( 'NONE',  ( 9.179055905797000037, 2.899999999999999911, 6.571291218949999902 ) ) ;
#5791=CARTESIAN_POINT ( 'NONE',  ( 9.137543006348998631, 2.995704926864999784, 8.544754656710999541 ) ) ;
#5792=CARTESIAN_POINT ( 'NONE',  ( 10.09999999999999964, 0.000000000000000000, 0.000000000000000000 ) ) ;
#5795=CARTESIAN_POINT ( 'NONE',  ( 7.450407011341527053, 4.176709736710048304, -6.150651269157633827 ) ) ;
#5802=CARTESIAN_POINT ( 'NONE',  ( 9.700639158771000581, 4.262870449202000422, -8.811513791423999820 ) ) ;
#5806=CARTESIAN_POINT ( 'NONE',  ( 5.000000000000000000, 0.2999999999999999889, -11.34603454956999791 ) ) ;
#5808=CARTESIAN_POINT ( 'NONE',  ( 0.6667688295322999892, -3.457229061792999936, 0.7500022461462000356 ) ) ;
#5810=CIRCLE ( 'NONE', #231, 1.350000000000000311 ) ;
#5811=CARTESIAN_POINT ( 'NONE',  ( 10.23581084123000018, 3.621841509808999771, -8.806208131805998818 ) ) ;
#5812=ORIENTED_EDGE ( 'NONE', *, *, #50129, .T. ) ;
#5813=EDGE_CURVE ( 'NONE', #32611, #22269, #631, .T. ) ;
#5819=CARTESIAN_POINT ( 'NONE',  ( 7.886573341228999112, 3.084076314893000159, 9.259847992573000397 ) ) ;
#5822=EDGE_CURVE ( 'NONE', #42736, #2331, #38891, .T. ) ;
#5823=EDGE_CURVE ( 'NONE', #15298, #12624, #27250, .T. ) ;
#5824=CARTESIAN_POINT ( 'NONE',  ( 7.657479719584999955, 2.267583043933999676, -7.494013172964999470 ) ) ;
#5841=CARTESIAN_POINT ( 'NONE',  ( 8.951357780412001475, 2.821863697211000055, 6.127145479358000024 ) ) ;
#5844=LINE ( 'NONE', #21921, #55246 ) ;
#5847=ORIENTED_EDGE ( 'NONE', *, *, #13972, .F. ) ;
#5849=CARTESIAN_POINT ( 'NONE',  ( 0.4002456762477398788, -2.971400501378169245, -1.711618823381010790 ) ) ;
#5863=CARTESIAN_POINT ( 'NONE',  ( 10.38314899745999931, 5.167567567567999731, 6.822293592207000934 ) ) ;
#5866=FACE_OUTER_BOUND ( 'NONE', #10133, .T. ) ;
#5867=CARTESIAN_POINT ( 'NONE',  ( 2.800973465877999669, -3.500000000000000000, 0.000000000000000000 ) ) ;
#5871=CARTESIAN_POINT ( 'NONE',  ( 9.691082467489000152, 5.335647408863999352, 8.701220655673999715 ) ) ;
#5872=CARTESIAN_POINT ( 'NONE',  ( 2.290556799209333860, -3.500000000000002220, 0.4581489286484968781 ) ) ;
#5875=CARTESIAN_POINT ( 'NONE',  ( 10.91982473337999870, 9.073386231760999010, -6.344452675278001053 ) ) ;
#5887=ORIENTED_EDGE ( 'NONE', *, *, #37167, .F. ) ;
#5889=FACE_OUTER_BOUND ( 'NONE', #42644, .T. ) ;
#5890=CARTESIAN_POINT ( 'NONE',  ( 7.641204719590000138, 4.524487726177000013, 9.047753146378999745 ) ) ;
#5891=CARTESIAN_POINT ( 'NONE',  ( 8.365779719592000063, 2.949305648881000330, -8.659807625323999503 ) ) ;
#5893=CARTESIAN_POINT ( 'NONE',  ( 2.603868863154109370, -1.826195839757124739, -2.697973947297320763 ) ) ;
#5895=CARTESIAN_POINT ( 'NONE',  ( 9.555697025339000561, 2.440752375194999768, 6.680879724048000234 ) ) ;
#5903=EDGE_CURVE ( 'NONE', #57590, #69130, #63878, .T. ) ;
#5915=CARTESIAN_POINT ( 'NONE',  ( 9.617764158771999305, 5.322769172805999816, -7.951018786192998178 ) ) ;
#5921=CARTESIAN_POINT ( 'NONE',  ( 9.231494046297843425, 3.294621473794871580, -8.705007087319614811 ) ) ;
#5929=CARTESIAN_POINT ( 'NONE',  ( 10.25461802485000007, 2.860644035673999941, 6.604613005744999654 ) ) ;
#5930=CARTESIAN_POINT ( 'NONE',  ( 11.13731690826999809, 2.663709268392000062, -5.187964601092999395 ) ) ;
#5931=CARTESIAN_POINT ( 'NONE',  ( 7.935109315130008056, 5.090269470254001227, 6.488511505667004187 ) ) ;
#5937=CARTESIAN_POINT ( 'NONE',  ( 8.341920280410999311, 5.601795057054999916, 7.176148573050999957 ) ) ;
#5942=DIRECTION ( 'NONE',  ( 0.000000000000000000, -0.9048270524660053660, 0.4257792915651026910 ) ) ;
#5943=CARTESIAN_POINT ( 'NONE',  ( 11.07758455333000036, 5.275003855962000721, -5.089091206712999416 ) ) ;
#5946=B_SPLINE_CURVE_WITH_KNOTS ( 'NONE', 3,
 ( #42380, #21385, #53552, #5305, #15800 ),
 .UNSPECIFIED., .F., .F.,
 ( 4, 1, 4 ),
 ( 0.000000000000000000, 0.5000000000000000000, 1.000000000000000000 ),
 .UNSPECIFIED. ) ;
#5948=CARTESIAN_POINT ( 'NONE',  ( 11.04954357929999986, 9.924925438703999347, 5.808563670758999820 ) ) ;
#5949=ADVANCED_FACE ( 'NONE', ( #53485 ), #688, .T. ) ;
#5957=AXIS2_PLACEMENT_3D ( 'NONE', #23319, #24008, #34518 ) ;
#5961=B_SPLINE_CURVE_WITH_KNOTS ( 'NONE', 3,
 ( #16802, #44438, #49311, #1424, #38129, #32556, #38833, #60159, #11219, #54908 ),
 .UNSPECIFIED., .F., .F.,
 ( 4, 2, 2, 2, 4 ),
 ( 0.000000000000000000, 0.1954776249890681494, 0.3909552499781366319, 0.5864328749672050867, 0.7819104999562735969 ),
 .UNSPECIFIED. ) ;
#5962=CARTESIAN_POINT ( 'NONE',  ( 8.727045280411999784, 3.882020551409000042, 5.870058896428999695 ) ) ;
#5965=CARTESIAN_POINT ( 'NONE',  ( 7.555281674562000838, 4.314040636970999820, 8.819134391732999845 ) ) ;
#5968=CARTESIAN_POINT ( 'NONE',  ( 10.80374834123000127, 2.766954612461999918, -8.073381085840999560 ) ) ;
#5970=CARTESIAN_POINT ( 'NONE',  ( 7.613778970466999141, 4.858908887722000358, 6.437635593844006188 ) ) ;
#5972=CARTESIAN_POINT ( 'NONE',  ( 5.500000000000000000, 0.000000000000000000, 0.000000000000000000 ) ) ;
#5979=CARTESIAN_POINT ( 'NONE',  ( 10.85956136387000015, 2.936952989063999819, 5.179223561060999792 ) ) ;
#5981=VERTEX_POINT ( 'NONE', #16414 ) ;
#5982=EDGE_CURVE ( 'NONE', #66075, #14790, #60556, .T. ) ;
#5983=ADVANCED_FACE ( 'NONE', ( #1039 ), #43690, .T. ) ;
#5990=CARTESIAN_POINT ( 'NONE',  ( 8.680115641897847567, 4.300161509225400636, -5.864543311939105941 ) ) ;
#5997=CARTESIAN_POINT ( 'NONE',  ( 9.383148997457999130, 5.167567567567999731, 6.822293592207000934 ) ) ;
#6000=CARTESIAN_POINT ( 'NONE',  ( 7.360904521458606631, 3.242717731377448676, 9.067081841172152323 ) ) ;
#6016=VECTOR ( 'NONE', #159, 1000.000000000000000 ) ;
#6017=FACE_OUTER_BOUND ( 'NONE', #51748, .T. ) ;
#6019=CARTESIAN_POINT ( 'NONE',  ( 9.169760841232999837, 4.728328492779000136, -8.692725459657999920 ) ) ;
#6022=ORIENTED_EDGE ( 'NONE', *, *, #28601, .T. ) ;
#6033=ORIENTED_EDGE ( 'NONE', *, *, #21940, .T. ) ;
#6039=CARTESIAN_POINT ( 'NONE',  ( 9.395239158775000377, 5.045571591548999812, -9.086294919530001124 ) ) ;
#6047=CARTESIAN_POINT ( 'NONE',  ( 9.319055905798999007, 2.899999999999999911, -6.571291218949999902 ) ) ;
#6052=CARTESIAN_POINT ( 'NONE',  ( 8.384356144328393157, 5.054963279901980577, -6.361519316970982274 ) ) ;
#6054=CARTESIAN_POINT ( 'NONE',  ( 6.899999691988000450, 0.000000000000000000, 0.000000000000000000 ) ) ;
#6055=VERTEX_POINT ( 'NONE', #1376 ) ;
#6064=EDGE_CURVE ( 'NONE', #59855, #55474, #6118, .T. ) ;
#6068=EDGE_CURVE ( 'NONE', #48015, #15478, #487, .T. ) ;
#6078=VERTEX_POINT ( 'NONE', #29007 ) ;
#6083=CARTESIAN_POINT ( 'NONE',  ( 10.55880524123913666, 4.703942329535922617, 8.703471051125569957 ) ) ;
#6093=CARTESIAN_POINT ( 'NONE',  ( 9.807804719590000886, 3.988943694240999704, -8.966360307350999648 ) ) ;
#6095=DIRECTION ( 'NONE',  ( 0.000000000000000000, 0.000000000000000000, -1.000000000000000000 ) ) ;
#6096=CARTESIAN_POINT ( 'NONE',  ( 7.215860841226000133, 3.469376689055999829, -5.675721888027999817 ) ) ;
#6099=VERTEX_POINT ( 'NONE', #23396 ) ;
#6104=CARTESIAN_POINT ( 'NONE',  ( 10.33253786428999987, 2.899999999999999911, 6.571291218949999902 ) ) ;
#6113=CARTESIAN_POINT ( 'NONE',  ( 7.144614836148978299, 4.730263389345491731, -8.645049034184477676 ) ) ;
#6116=CARTESIAN_POINT ( 'NONE',  ( 11.00366064676999933, 2.264078662261999941, 7.798351372501000078 ) ) ;
#6118=CIRCLE ( 'NONE', #1644, 12.24999851416000141 ) ;
#6124=DIRECTION ( 'NONE',  ( 1.000000000000000000, 0.000000000000000000, 0.000000000000000000 ) ) ;
#6136=CARTESIAN_POINT ( 'NONE',  ( 9.702862956260233318, 2.713451880140764327, 7.026479373626208336 ) ) ;
#6145=CARTESIAN_POINT ( 'NONE',  ( 8.324914158772999784, 2.633142096252999664, -7.791134854666999843 ) ) ;
#6147=CYLINDRICAL_SURFACE ( 'NONE', #21517, 12.50000000000000000 ) ;
#6148=DIRECTION ( 'NONE',  ( -0.000000000000000000, 1.000000000000000000, 0.000000000000000000 ) ) ;
#6149=ADVANCED_FACE ( 'NONE', ( #29345 ), #2413, .T. ) ;
#6152=CARTESIAN_POINT ( 'NONE',  ( 10.76588584123000025, 3.166544027818999574, -8.574484964885998650 ) ) ;
#6158=CARTESIAN_POINT ( 'NONE',  ( 8.758795280412000395, 3.977267228909999730, 9.308925224542001331 ) ) ;
#6161=CARTESIAN_POINT ( 'NONE',  ( 8.493945280408999210, 5.563172860439999923, -7.424303164651000486 ) ) ;
#6164=ORIENTED_EDGE ( 'NONE', *, *, #36840, .F. ) ;
#6168=EDGE_CURVE ( 'NONE', #18734, #46559, #28878, .T. ) ;
#6180=CARTESIAN_POINT ( 'NONE',  ( 8.989142219592000771, 5.284130523641000110, 6.489275570566000795 ) ) ;
#6181=CYLINDRICAL_SURFACE ( 'NONE', #37353, 1.350000000000000533 ) ;
#6185=CARTESIAN_POINT ( 'NONE',  ( 10.96255546505999945, 5.431632148000000271, -4.905443575133999978 ) ) ;
#6186=ORIENTED_EDGE ( 'NONE', *, *, #12938, .T. ) ;
#6189=PLANE ( 'NONE',  #15377 ) ;
#6190=CARTESIAN_POINT ( 'NONE',  ( 8.187247165044786001, 3.359395650746410222, -5.756825428974689629 ) ) ;
#6200=CONICAL_SURFACE ( 'NONE', #26330, 0.4377388725247000623, 0.7853981633972997312 ) ;
#6201=CARTESIAN_POINT ( 'NONE',  ( 9.485829719593997567, 4.953415418491999844, -8.946479654552000227 ) ) ;
#6202=CARTESIAN_POINT ( 'NONE',  ( 11.15192953222999961, 2.359300361215999953, -6.636686939130999718 ) ) ;
#6204=VECTOR ( 'NONE', #17868, 1000.000000000000000 ) ;
#6205=DIRECTION ( 'NONE',  ( 0.000000000000000000, -1.000000000000000000, 0.000000000000000000 ) ) ;
#6206=CARTESIAN_POINT ( 'NONE',  ( 7.577053541547003945, 3.182130936862002102, -6.424376193309997873 ) ) ;
#6207=EDGE_CURVE ( 'NONE', #65266, #63941, #62292, .T. ) ;
#6211=CARTESIAN_POINT ( 'NONE',  ( 1.808651541364333371, -3.500000000000000000, -0.3376993977123543544 ) ) ;
#6212=EDGE_CURVE ( 'NONE', #48015, #16312, #30587, .T. ) ;
#6213=CARTESIAN_POINT ( 'NONE',  ( 9.662551629919999385, 4.094830335839000135, 9.119946295870999364 ) ) ;
#6217=CARTESIAN_POINT ( 'NONE',  ( 10.85408070804999880, 9.831992037111000116, -5.581278437649000779 ) ) ;
#6218=CARTESIAN_POINT ( 'NONE',  ( 10.39055228715993451, 2.705487803219565279, 8.717536521744987610 ) ) ;
#6224=ORIENTED_EDGE ( 'NONE', *, *, #1914, .T. ) ;
#6225=LINE ( 'NONE', #64262, #59903 ) ;
#6232=CARTESIAN_POINT ( 'NONE',  ( 9.106135841230999617, 4.192919163547999872, 5.525472271700999194 ) ) ;
#6234=CARTESIAN_POINT ( 'NONE',  ( 9.791229719590001324, 4.294368353031000396, -8.968663198664000191 ) ) ;
#6238=CARTESIAN_POINT ( 'NONE',  ( 10.51655086620999846, 4.930662802525000110, 8.573584269714999095 ) ) ;
#6249=AXIS2_PLACEMENT_3D ( 'NONE', #49323, #17872, #16475 ) ;
#6250=CARTESIAN_POINT ( 'NONE',  ( 11.09999999999999964, 5.299311513382999550, 5.124965750789000296 ) ) ;
#6252=CARTESIAN_POINT ( 'NONE',  ( 11.09999999999999964, 2.700000000000000178, 5.160242713806000303 ) ) ;
#6256=CARTESIAN_POINT ( 'NONE',  ( 9.525000000000000355, 4.417172942406000224, 8.783926296998000538 ) ) ;
#6259=CARTESIAN_POINT ( 'NONE',  ( 8.474089158773999486, 4.131080973160000447, -6.108642999115999395 ) ) ;
#6263=CARTESIAN_POINT ( 'NONE',  ( 7.963341518233496785, 5.029799759091138966, -6.519028237967030570 ) ) ;
#6271=CARTESIAN_POINT ( 'NONE',  ( 10.75109581085999899, 2.822145500011000063, 6.655897464539000552 ) ) ;
#6272=CARTESIAN_POINT ( 'NONE',  ( 11.12916633214000051, 2.728377425829000114, -4.814907997079999724 ) ) ;
#6273=CARTESIAN_POINT ( 'NONE',  ( 7.822787301102997581, 4.879242518472000967, 6.344068876191006012 ) ) ;
#6279=CARTESIAN_POINT ( 'NONE',  ( 9.074385841230999006, 3.981661882377999895, 8.959227447876999761 ) ) ;
#6280=ORIENTED_EDGE ( 'NONE', *, *, #55027, .F. ) ;
#6283=CARTESIAN_POINT ( 'NONE',  ( 7.272528695240493946, 2.858096677246901418, 6.733923262973229740 ) ) ;
#6285=VECTOR ( 'NONE', #38365, 1000.000000000000114 ) ;
#6288=CARTESIAN_POINT ( 'NONE',  ( 11.04766396148000140, 10.00030925724000141, 5.674005852106000169 ) ) ;
#6289=EDGE_CURVE ( 'NONE', #17232, #958, #57961, .T. ) ;
#6293=EDGE_CURVE ( 'NONE', #10305, #48780, #52248, .T. ) ;
#6297=CARTESIAN_POINT ( 'NONE',  ( 10.46085995768999943, 5.403395036974999677, 7.721808039505000387 ) ) ;
#6301=CARTESIAN_POINT ( 'NONE',  ( 9.047982780412000992, 2.806082850903000026, 8.615880516515998622 ) ) ;
#6302=CARTESIAN_POINT ( 'NONE',  ( 9.753142190738998352, 4.104977339646000090, 9.293283246364000050 ) ) ;
#6308=CARTESIAN_POINT ( 'NONE',  ( 10.42512334122999995, 3.371064118627999928, -6.294343971198999910 ) ) ;
#6311=CARTESIAN_POINT ( 'NONE',  ( 8.200215090286000930, 5.110410283172001300, 6.692116316553004651 ) ) ;
#6315=CARTESIAN_POINT ( 'NONE',  ( 0.6903817924015999141, 2.178673723483000035, -2.162625512369000358 ) ) ;
#6320=DIRECTION ( 'NONE',  ( 0.000000000000000000, 1.000000000000000000, 0.000000000000000000 ) ) ;
#6322=EDGE_LOOP ( 'NONE', ( #54620, #48317, #36401, #65758, #58729, #54153, #38076 ) ) ;
#6324=CARTESIAN_POINT ( 'NONE',  ( 3.000973465876999757, 3.500000000000000000, 0.000000000000000000 ) ) ;
#6327=CARTESIAN_POINT ( 'NONE',  ( 1.228292983454999820, -3.060375075103999976, 2.182311086106999642 ) ) ;
#6331=CARTESIAN_POINT ( 'NONE',  ( 11.01776904286000125, 4.914120883409999863, 8.587704221454000475 ) ) ;
#6336=EDGE_CURVE ( 'NONE', #36464, #43600, #21415, .T. ) ;
#6343=CARTESIAN_POINT ( 'NONE',  ( 8.497235841230001085, 3.789127741898000057, -9.388182174781999123 ) ) ;
#6346=CONICAL_SURFACE ( 'NONE', #18696, 12.44999944941000081, 0.7853981146832407223 ) ;
#6349=ORIENTED_EDGE ( 'NONE', *, *, #10001, .T. ) ;
#6354=CARTESIAN_POINT ( 'NONE',  ( 8.457129882803000598, 5.100036551512999949, -6.571411952062999440 ) ) ;
#6355=DIRECTION ( 'NONE',  ( 1.000000000000000000, 0.000000000000000000, 0.000000000000000000 ) ) ;
#6356=B_SPLINE_CURVE_WITH_KNOTS ( 'NONE', 3,
 ( #20419, #20079, #30571, #45964, #15175, #57820, #30919, #35144, #63049, #29908, #67274, #51886, #3981, #41408, #9929, #3642, #31267, #25321, #61695, #3309, #19046, #24644, #19389, #35484 ),
 .UNSPECIFIED., .F., .F.,
 ( 4, 2, 1, 2, 2, 2, 2, 2, 2, 1, 2, 2, 4 ),
 ( 0.000000000000000000, 0.06249999999999997224, 0.1249999999999999445, 0.1874999999999999167, 0.2499999999999998890, 0.3749999999999998335, 0.4999999999999997780, 0.6249999999999997780, 0.6874999999999997780, 0.7499999999999998890, 0.8125000000000000000, 0.8750000000000000000, 1.000000000000000000 ),
 .UNSPECIFIED. ) ;
#6361=ORIENTED_EDGE ( 'NONE', *, *, #34016, .F. ) ;
#6362=CARTESIAN_POINT ( 'NONE',  ( 8.725348536223823004, 2.649439212887079620, 7.500023728975156345 ) ) ;
#6364=CARTESIAN_POINT ( 'NONE',  ( 10.01277517397999972, 3.440623091551000101, -9.267603345544999982 ) ) ;
#6377=CARTESIAN_POINT ( 'NONE',  ( 6.833909439180999357, 4.719833207100999850, -8.789699670502999496 ) ) ;
#6381=VECTOR ( 'NONE', #59106, 1000.000000000000000 ) ;
#6382=CARTESIAN_POINT ( 'NONE',  ( 8.731095280410999138, 2.469361196073999842, -7.826019481986000059 ) ) ;
#6394=EDGE_CURVE ( 'NONE', #61732, #60041, #22613, .T. ) ;
#6397=CARTESIAN_POINT ( 'NONE',  ( 8.457129882803000598, 5.100036551512999949, -6.571411952062999440 ) ) ;
#6399=ORIENTED_EDGE ( 'NONE', *, *, #68326, .F. ) ;
#6401=EDGE_CURVE ( 'NONE', #27251, #32166, #43259, .T. ) ;
#6411=DIRECTION ( 'NONE',  ( 2.257582933432000069E-09, -1.000000000000000000, 1.101251388955000073E-09 ) ) ;
#6417=CARTESIAN_POINT ( 'NONE',  ( 11.09999999999999964, 4.000000000000000000, 7.500000000000000000 ) ) ;
#6424=CARTESIAN_POINT ( 'NONE',  ( 5.399998535875000449, -12.99045401563999924, -1.690592933733000125 ) ) ;
#6428=VECTOR ( 'NONE', #44718, 1000.000000000000000 ) ;
#6429=B_SPLINE_CURVE_WITH_KNOTS ( 'NONE', 3,
 ( #13509, #56835, #41438, #57500, #9609, #8589, #2655, #50899, #2995, #14531, #30602, #4013, #25011, #35847, #56485 ),
 .UNSPECIFIED., .F., .F.,
 ( 4, 2, 2, 2, 1, 2, 2, 4 ),
 ( 0.000000000000000000, 0.2500000000000239808, 0.3750000000000371370, 0.4375000000000440203, 0.4687500000000439648, 0.4843750000000439648, 0.5000000000000439648, 1.000000000000000000 ),
 .UNSPECIFIED. ) ;
#6435=AXIS2_PLACEMENT_3D ( 'NONE', #19039, #40707, #62033 ) ;
#6436=CARTESIAN_POINT ( 'NONE',  ( 9.360279719594000625, 3.031907308384000022, -8.729608011560001657 ) ) ;
#6440=CARTESIAN_POINT ( 'NONE',  ( 7.514210841224999271, 3.394203523730999539, -9.300711568980998933 ) ) ;
#6448=ORIENTED_EDGE ( 'NONE', *, *, #28203, .F. ) ;
#6450=CARTESIAN_POINT ( 'NONE',  ( 11.09999607187999970, 1.243449787579999883E-13, 0.000000000000000000 ) ) ;
#6451=CARTESIAN_POINT ( 'NONE',  ( 8.020125753392001400, 4.498951069075999953, -6.245588651729999441 ) ) ;
#6452=EDGE_LOOP ( 'NONE', ( #7048, #12548, #9766, #4508 ) ) ;
#6458=DIRECTION ( 'NONE',  ( 0.000000000000000000, 0.000000000000000000, -1.000000000000000000 ) ) ;
#6467=CARTESIAN_POINT ( 'NONE',  ( 10.56170778040999991, 5.057487376164999660, -8.595710652231000282 ) ) ;
#6475=ORIENTED_EDGE ( 'NONE', *, *, #17460, .F. ) ;
#6476=CARTESIAN_POINT ( 'NONE',  ( 11.00588826681000043, 3.012760565655999923, 5.961496895743000124 ) ) ;
#6479=FACE_OUTER_BOUND ( 'NONE', #21033, .T. ) ;
#6488=VECTOR ( 'NONE', #31372, 1000.000000000000000 ) ;
#6497=CARTESIAN_POINT ( 'NONE',  ( 9.881820280408998514, 4.325866256860000369, -9.125812605905000652 ) ) ;
#6501=CARTESIAN_POINT ( 'NONE',  ( 0.2691580992186000110, -1.644388561977000007, -3.014063655381999940 ) ) ;
#6503=CARTESIAN_POINT ( 'NONE',  ( 11.33382334123000135, 2.642405149457999869, -7.577896731332000257 ) ) ;
#6510=CARTESIAN_POINT ( 'NONE',  ( 7.320267219589999819, 2.466388272391000225, 6.935562100014999842 ) ) ;
#6513=CARTESIAN_POINT ( 'NONE',  ( 8.593395280410000225, 4.529523339102000890, -8.867457431226998921 ) ) ;
#6515=CARTESIAN_POINT ( 'NONE',  ( 9.242342830452999536, 5.206708472530999998, 8.808826521083998884 ) ) ;
#6522=DIRECTION ( 'NONE',  ( 1.000000000000000000, 0.000000000000000000, 0.000000000000000000 ) ) ;
#6525=EDGE_CURVE ( 'NONE', #21901, #8000, #33468, .T. ) ;
#6526=VERTEX_POINT ( 'NONE', #37664 ) ;
#6532=ORIENTED_EDGE ( 'NONE', *, *, #22160, .F. ) ;
#6536=CARTESIAN_POINT ( 'NONE',  ( 8.404999999999999361, 5.190914425723000214, -8.768195054477999406 ) ) ;
#6542=CARTESIAN_POINT ( 'NONE',  ( 10.20000099824999928, 0.000000000000000000, 0.000000000000000000 ) ) ;
#6551=EDGE_CURVE ( 'NONE', #24471, #16376, #14273, .T. ) ;
#6552=ORIENTED_EDGE ( 'NONE', *, *, #11840, .F. ) ;
#6554=CARTESIAN_POINT ( 'NONE',  ( 8.897989158775001073, 4.990139824845000405, -9.121472988377998803 ) ) ;
#6555=EDGE_CURVE ( 'NONE', #63357, #64129, #5844, .T. ) ;
#6556=CARTESIAN_POINT ( 'NONE',  ( 10.47212119989999835, 2.640756834784999896, -8.505248851866998194 ) ) ;
#6558=DIRECTION ( 'NONE',  ( 0.8480635683783692702, 0.3746919961710865610, 0.3746919961710865610 ) ) ;
#6563=CARTESIAN_POINT ( 'NONE',  ( 10.83668832355999889, 4.288537082977999404, 9.448742031664000507 ) ) ;
#6567=CIRCLE ( 'NONE', #32238, 13.00000000000000178 ) ;
#6569=B_SPLINE_CURVE_WITH_KNOTS ( 'NONE', 3,
 ( #49973, #2767, #40181, #30046 ),
 .UNSPECIFIED., .F., .F.,
 ( 4, 4 ),
 ( 0.000000000000000000, 1.000000000000000000 ),
 .UNSPECIFIED. ) ;
#6572=CARTESIAN_POINT ( 'NONE',  ( 11.05947712336470623, 5.538520942943965686, 7.349130516419430492 ) ) ;
#6575=PRESENTATION_STYLE_ASSIGNMENT (( #48196 ) ) ;
#6577=CARTESIAN_POINT ( 'NONE',  ( 9.842711596872401714, 5.100000000000000533, -6.305985889525932642 ) ) ;
#6580=CARTESIAN_POINT ( 'NONE',  ( 10.71434555353880924, 4.907414883814396944, 4.811875879775000975 ) ) ;
#6584=CARTESIAN_POINT ( 'NONE',  ( 9.015545280411000562, 4.175915362023999933, 5.699506188181000077 ) ) ;
#6585=CARTESIAN_POINT ( 'NONE',  ( 9.251970280414001380, 5.673443217382001080, -7.051790060464000476 ) ) ;
#6587=CARTESIAN_POINT ( 'NONE',  ( 10.88269269398620764, 2.957535174095307529, 4.893996436090802149 ) ) ;
#6588=ORIENTED_EDGE ( 'NONE', *, *, #3223, .T. ) ;
#6589=CARTESIAN_POINT ( 'NONE',  ( 11.05935155529000014, 2.480238120735000162, 6.610075178640000715 ) ) ;
#6594=CARTESIAN_POINT ( 'NONE',  ( 7.528515907654997896, 3.227039430994999236, 6.419564954296006931 ) ) ;
#6595=ORIENTED_EDGE ( 'NONE', *, *, #52955, .T. ) ;
#6601=CARTESIAN_POINT ( 'NONE',  ( 11.09999999999999964, 5.350000000000000533, 7.500000000000000000 ) ) ;
#6605=CARTESIAN_POINT ( 'NONE',  ( 7.762706781754004304, 3.200128145701000904, 6.302820412756005020 ) ) ;
#6608=EDGE_CURVE ( 'NONE', #59297, #4993, #36807, .T. ) ;
#6611=CARTESIAN_POINT ( 'NONE',  ( 9.758079719591000512, 4.905765359186999852, -8.776126235875999271 ) ) ;
#6612=CARTESIAN_POINT ( 'NONE',  ( 10.02052890782000105, 2.899999999999999911, 6.152188490330000370 ) ) ;
#6635=CARTESIAN_POINT ( 'NONE',  ( 8.995176658772999545, 2.707986230053999854, 5.994446745591000436 ) ) ;
#6637=DIRECTION ( 'NONE',  ( 0.000000000000000000, -0.4257792915651026910, -0.9048270524660053660 ) ) ;
#6638=CARTESIAN_POINT ( 'NONE',  ( 9.610944094206999466, 5.100000000000000533, -6.571291218949999902 ) ) ;
#6641=CARTESIAN_POINT ( 'NONE',  ( 10.86180282788866691, 2.874603711589708066, -6.749639981055100435 ) ) ;
#6649=CARTESIAN_POINT ( 'NONE',  ( 8.276217158405398067, 2.979004627675164940, -6.354038587687713679 ) ) ;
#6654=CARTESIAN_POINT ( 'NONE',  ( 9.475899447075999404, 4.122021000979000149, 9.013569734175000292 ) ) ;
#6656=EDGE_CURVE ( 'NONE', #2626, #53063, #68715, .T. ) ;
#6658=VERTEX_POINT ( 'NONE', #50574 ) ;
#6664=AXIS2_PLACEMENT_3D ( 'NONE', #59911, #38948, #53636 ) ;
#6668=CARTESIAN_POINT ( 'NONE',  ( 2.259112785886000285, 1.685541059001999908, -2.982097634516000184 ) ) ;
#6669=CARTESIAN_POINT ( 'NONE',  ( 10.98768472567999943, 6.720753181080999283, 5.471698459870999898 ) ) ;
#6674=FACE_OUTER_BOUND ( 'NONE', #43139, .T. ) ;
#6678=CARTESIAN_POINT ( 'NONE',  ( 10.99999648468999958, -1.199999999999999956, -9.776630298829998011 ) ) ;
#6680=DIRECTION ( 'NONE',  ( -1.000000000000000000, 0.000000000000000000, 0.000000000000000000 ) ) ;
#6681=CARTESIAN_POINT ( 'NONE',  ( 1.037565185690999980, 3.729267013836000011, 0.4700476753697999666 ) ) ;
#6692=EDGE_CURVE ( 'NONE', #2379, #61768, #18488, .T. ) ;
#6694=CARTESIAN_POINT ( 'NONE',  ( 9.398026887492090253, 5.281042804537088742, 7.060559036506083075 ) ) ;
#6695=ORIENTED_EDGE ( 'NONE', *, *, #37469, .T. ) ;
#6696=CARTESIAN_POINT ( 'NONE',  ( 9.491735841231999871, 3.920043641733999884, -9.398198753036000497 ) ) ;
#6707=CARTESIAN_POINT ( 'NONE',  ( 11.09999999569000018, 9.179538081559000418, -6.556854281509999716 ) ) ;
#6715=CARTESIAN_POINT ( 'NONE',  ( 0.7338048310729522461, 2.699466831487369323, -1.587941003800196871 ) ) ;
#6719=CARTESIAN_POINT ( 'NONE',  ( 7.969305479088424349, 4.593434306755666441, -6.274929750779866033 ) ) ;
#6726=CARTESIAN_POINT ( 'NONE',  ( 6.711228317543000088, 3.668692617901999853, -8.939602259005999585 ) ) ;
#6730=CARTESIAN_POINT ( 'NONE',  ( 8.690229719593000723, 2.414630869937000046, -6.801495146585999407 ) ) ;
#6734=CARTESIAN_POINT ( 'NONE',  ( 5.399999746777999654, -12.99045401563999924, 1.690592933733000125 ) ) ;
#6736=EDGE_CURVE ( 'NONE', #33656, #1808, #25210, .T. ) ;
#6745=CARTESIAN_POINT ( 'NONE',  ( 6.999999085428001422, 12.01420426511556094, -3.456409902911533383 ) ) ;
#6759=LINE ( 'NONE', #60600, #18728 ) ;
#6768=CARTESIAN_POINT ( 'NONE',  ( 10.81746213571000048, 5.100000000000000533, 6.571291218949999902 ) ) ;
#6773=EDGE_CURVE ( 'NONE', #6658, #24788, #34685, .T. ) ;
#6777=CARTESIAN_POINT ( 'NONE',  ( 7.000000000000000000, 8.307879248642999315, 4.307879248643000203 ) ) ;
#6785=CARTESIAN_POINT ( 'NONE',  ( 8.921614158776000281, 3.251172436837000301, -6.320036569851000152 ) ) ;
#6786=CARTESIAN_POINT ( 'NONE',  ( -2.444943969992999916E-05, 2.899969545325999931, 0.000000000000000000 ) ) ;
#6789=CARTESIAN_POINT ( 'NONE',  ( 8.737764228571977654, 3.223862676119972903, -8.634700618639806535 ) ) ;
#6790=VECTOR ( 'NONE', #67621, 1000.000000000000000 ) ;
#6792=ORIENTED_EDGE ( 'NONE', *, *, #48925, .T. ) ;
#6796=ORIENTED_EDGE ( 'NONE', *, *, #28498, .T. ) ;
#6799=CARTESIAN_POINT ( 'NONE',  ( 2.750973465876000557, -3.500000000000000000, 0.000000000000000000 ) ) ;
#6804=CARTESIAN_POINT ( 'NONE',  ( 7.798175108423000879, 4.827257594231999960, -6.306127835448002372 ) ) ;
#6812=CARTESIAN_POINT ( 'NONE',  ( 10.85737917744000036, 2.754548910086000113, 8.976376585747001258 ) ) ;
#6813=CARTESIAN_POINT ( 'NONE',  ( 10.96332971959000169, 5.283550306828000309, -8.592773337476000250 ) ) ;
#6821=CARTESIAN_POINT ( 'NONE',  ( 11.09999999999999964, 4.000000000000000000, -7.500000000000000000 ) ) ;
#6825=CARTESIAN_POINT ( 'NONE',  ( 8.500189158773000742, 2.724453559418999582, -8.908010318766001134 ) ) ;
#6832=CARTESIAN_POINT ( 'NONE',  ( 6.999999691988000095, 13.87069231928999891, 4.225386915259999654 ) ) ;
#6844=CARTESIAN_POINT ( 'NONE',  ( 9.310554719594000161, 3.934138271021000222, -9.063586117809000697 ) ) ;
#6847=CARTESIAN_POINT ( 'NONE',  ( 0.7901652630780000575, -0.8195100712853999880, -3.441407140921999730 ) ) ;
#6848=CARTESIAN_POINT ( 'NONE',  ( 9.299999999999998934, 4.537600397704999899, 9.154563893594000135 ) ) ;
#6849=CARTESIAN_POINT ( 'NONE',  ( 2.256745668234000135, 2.821651784608999680, 1.942419289100000057 ) ) ;
#6854=CARTESIAN_POINT ( 'NONE',  ( 8.154704719592000828, 4.255646040929000229, 9.114085578076998928 ) ) ;
#6859=CARTESIAN_POINT ( 'NONE',  ( 7.590035841228000457, 5.397217548590999669, -7.528974776547999959 ) ) ;
#6862=CARTESIAN_POINT ( 'NONE',  ( 6.999998782146999332, 11.95749337870000062, 3.642574926947999892 ) ) ;
#6877=EDGE_LOOP ( 'NONE', ( #17403, #38876, #33635, #13754 ) ) ;
#6883=ORIENTED_EDGE ( 'NONE', *, *, #267, .F. ) ;
#6888=CARTESIAN_POINT ( 'NONE',  ( 5.000030787343000327, 2.099962892530999881, 0.000000000000000000 ) ) ;
#6899=CARTESIAN_POINT ( 'NONE',  ( 2.873654761058999973, 0.1588290254405000101, 3.211125886561999820 ) ) ;
#6901=CARTESIAN_POINT ( 'NONE',  ( 10.81905590578999998, 2.899999999999999911, -6.571291218949999902 ) ) ;
#6903=CARTESIAN_POINT ( 'NONE',  ( 9.099999999999999645, 0.000000000000000000, 11.84999999999999964 ) ) ;
#6905=ORIENTED_EDGE ( 'NONE', *, *, #68635, .F. ) ;
#6908=CARTESIAN_POINT ( 'NONE',  ( 11.20904666305999875, 5.937823941418000295, 7.147334722859000067 ) ) ;
#6911=CARTESIAN_POINT ( 'NONE',  ( 9.192115766384521436, 2.763712191446816568, 8.049223208410250407 ) ) ;
#6914=CARTESIAN_POINT ( 'NONE',  ( 10.50477421009230738, 2.640760156097457401, 6.397741617862033436 ) ) ;
#6929=CARTESIAN_POINT ( 'NONE',  ( 7.962142219590999659, 4.874567052833000069, 6.119507471270999588 ) ) ;
#6930=CARTESIAN_POINT ( 'NONE',  ( 9.243110841233001196, 4.112741311853999271, -5.603466076760000192 ) ) ;
#6941=EDGE_CURVE ( 'NONE', #15478, #115, #10498, .T. ) ;
#6942=B_SPLINE_CURVE_WITH_KNOTS ( 'NONE', 3,
 ( #14876, #25707, #24684, #41788, #9619, #47038 ),
 .UNSPECIFIED., .F., .F.,
 ( 4, 2, 4 ),
 ( 0.000000000000000000, 0.5000000000000005551, 1.000000000000000000 ),
 .UNSPECIFIED. ) ;
#6943=EDGE_CURVE ( 'NONE', #11525, #61746, #66019, .T. ) ;
#6950=ORIENTED_EDGE ( 'NONE', *, *, #26456, .T. ) ;
#6956=CARTESIAN_POINT ( 'NONE',  ( 7.544198296194000619, 2.929983868333001951, 6.556648683638004016 ) ) ;
#6959=CARTESIAN_POINT ( 'NONE',  ( 9.749220280410998640, 5.656948148960999845, -6.994239053114000626 ) ) ;
#6964=CARTESIAN_POINT ( 'NONE',  ( 9.273175939532153578, 2.820663304098465218, -8.179560065238094424 ) ) ;
#6967=CARTESIAN_POINT ( 'NONE',  ( 9.558834163536230832, 4.704973616088495625, 8.704082162066606898 ) ) ;
#6969=ORIENTED_EDGE ( 'NONE', *, *, #59509, .F. ) ;
#6975=CARTESIAN_POINT ( 'NONE',  ( 10.20918109782000016, 3.334760637131999772, -5.769467581755999497 ) ) ;
#6976=CARTESIAN_POINT ( 'NONE',  ( 8.518405616243800438, 5.127171463238822113, -6.752698291457244650 ) ) ;
#6983=CARTESIAN_POINT ( 'NONE',  ( 8.829017219593000121, 5.290207928847999064, 8.768105151414001597 ) ) ;
#6986=CARTESIAN_POINT ( 'NONE',  ( 7.350689587839424277, 3.996361938020618343, 6.125274922243029607 ) ) ;
#6991=CARTESIAN_POINT ( 'NONE',  ( 10.65050915380999896, 5.200037120669999346, 5.937706951697999891 ) ) ;
#6999=VECTOR ( 'NONE', #38668, 1000.000000000000000 ) ;
#7003=EDGE_CURVE ( 'NONE', #19885, #44936, #16722, .T. ) ;
#7004=EDGE_CURVE ( 'NONE', #62483, #61390, #703, .T. ) ;
#7005=CARTESIAN_POINT ( 'NONE',  ( 8.239948341229000661, 2.735218126362000124, 6.771983639047999937 ) ) ;
#7006=CARTESIAN_POINT ( 'NONE',  ( 10.34021053755999908, 4.202028620710000162, 9.459600235481000041 ) ) ;
#7009=CARTESIAN_POINT ( 'NONE',  ( 9.444964158775000840, 3.920043641733999884, -9.398198753036000497 ) ) ;
#7012=CARTESIAN_POINT ( 'NONE',  ( 8.335548698406999080, 5.102342278510997531, 6.653323484791000553 ) ) ;
#7018=CONICAL_SURFACE ( 'NONE', #2573, 12.44999944941000081, 0.7853981146832407223 ) ;
#7019=CARTESIAN_POINT ( 'NONE',  ( 1.400837695952000139, 2.565043520226999885, 2.270544068615000022 ) ) ;
#7023=CARTESIAN_POINT ( 'NONE',  ( 10.51293113580700123, 5.100000000000000533, 6.444141223116233164 ) ) ;
#7028=VERTEX_POINT ( 'NONE', #11186 ) ;
#7029=CARTESIAN_POINT ( 'NONE',  ( 7.406666666664500021, 2.820388375721751384, -6.820114376499287978 ) ) ;
#7031=CARTESIAN_POINT ( 'NONE',  ( 8.975133055567869889, 5.349981391149201571, 7.499992565666659949 ) ) ;
#7032=CARTESIAN_POINT ( 'NONE',  ( 9.716851002543000604, 2.832432432432000269, 6.822293592207000934 ) ) ;
#7034=VERTEX_POINT ( 'NONE', #55224 ) ;
#7047=CARTESIAN_POINT ( 'NONE',  ( 9.143660841233000269, 2.235961884443999459, -6.794506518623999902 ) ) ;
#7048=ORIENTED_EDGE ( 'NONE', *, *, #33791, .F. ) ;
#7051=CARTESIAN_POINT ( 'NONE',  ( 7.744301850232000461, 3.130385018321999890, 6.467396599055999395 ) ) ;
#7057=CARTESIAN_POINT ( 'NONE',  ( 9.657553581808000942, 5.333455947841000189, 6.049916795084000043 ) ) ;
#7060=FACE_OUTER_BOUND ( 'NONE', #67336, .T. ) ;
#7065=VERTEX_POINT ( 'NONE', #40186 ) ;
#7076=VERTEX_POINT ( 'NONE', #45088 ) ;
#7077=CARTESIAN_POINT ( 'NONE',  ( 6.892409439180999797, 3.668692617901999853, -8.939602259005999585 ) ) ;
#7078=DIRECTION ( 'NONE',  ( 1.000000000000000000, 0.000000000000000000, 0.000000000000000000 ) ) ;
#7081=CARTESIAN_POINT ( 'NONE',  ( 8.889129719593999113, 5.687930027805999877, -7.109876198051000351 ) ) ;
#7084=B_SPLINE_CURVE_WITH_KNOTS ( 'NONE', 3,
 ( #35109, #56421, #46278, #51511 ),
 .UNSPECIFIED., .F., .F.,
 ( 4, 4 ),
 ( 0.000000000000000000, 1.000000000000000000 ),
 .UNSPECIFIED. ) ;
#7086=EDGE_CURVE ( 'NONE', #8323, #32376, #35286, .T. ) ;
#7092=EDGE_CURVE ( 'NONE', #66190, #66492, #68481, .T. ) ;
#7099=CARTESIAN_POINT ( 'NONE',  ( 7.716851002542999716, 2.832432432432000269, 6.822293592207000934 ) ) ;
#7100=ORIENTED_EDGE ( 'NONE', *, *, #28896, .T. ) ;
#7105=B_SPLINE_CURVE_WITH_KNOTS ( 'NONE', 3,
 ( #11597, #1467, #54250, #65072 ),
 .UNSPECIFIED., .F., .F.,
 ( 4, 4 ),
 ( 0.000000000000000000, 0.1255288371561983085 ),
 .UNSPECIFIED. ) ;
#7123=ORIENTED_EDGE ( 'NONE', *, *, #28758, .T. ) ;
#7132=CARTESIAN_POINT ( 'NONE',  ( 0.1359928592618749876, 2.324556273228959184E-06, -3.136013406113613122 ) ) ;
#7138=CARTESIAN_POINT ( 'NONE',  ( 9.791229719590001324, 4.294368353031000396, -8.968663198664000191 ) ) ;
#7146=DIRECTION ( 'NONE',  ( -1.000000000000000000, 0.000000000000000000, 0.000000000000000000 ) ) ;
#7147=CARTESIAN_POINT ( 'NONE',  ( 8.450464158772000189, 3.789127741898000057, -9.388182174781999123 ) ) ;
#7150=CARTESIAN_POINT ( 'NONE',  ( 9.662441121991999893, 4.824173073626999653, -8.517602418144999632 ) ) ;
#7151=CARTESIAN_POINT ( 'NONE',  ( 4.500000000000000000, 0.000000000000000000, 0.000000000000000000 ) ) ;
#7152=VERTEX_POINT ( 'NONE', #46868 ) ;
#7155=CARTESIAN_POINT ( 'NONE',  ( 8.253230575588379025, 2.714951384259811196, 7.027308161653112784 ) ) ;
#7156=DIRECTION ( 'NONE',  ( 0.000000000000000000, 1.000000000000000000, 0.000000000000000000 ) ) ;
#7162=CARTESIAN_POINT ( 'NONE',  ( 10.48598278040999965, 5.506034726153999692, -7.274787238512000265 ) ) ;
#7164=DIRECTION ( 'NONE',  ( -0.8660254037844289376, 1.235977903561818058E-11, 0.5000000000000169864 ) ) ;
#7174=CARTESIAN_POINT ( 'NONE',  ( 9.933354719590999693, 5.639765292528999829, -8.059103558718000215 ) ) ;
#7197=CARTESIAN_POINT ( 'NONE',  ( 9.161379719595000637, 5.511689883260999956, -7.095113581311000672 ) ) ;
#7203=B_SPLINE_SURFACE_WITH_KNOTS ( 'NONE', 3, 3, ( 
 ( #27950, #54160, #11503, #5915, #53817, #336, #48926, #1034, #22346, #16750, #26575, #26915, #43683, #65336, #27257, #42645, #64980, #685, #17095, #11853, #5574, #17455, #38427, #47899, #59751, #21652, #6259, #63955, #59404, #54510, #48230, #33191, #42986, #60105, #34114 ),
 ( #64294, #21315, #6611, #21996, #43339, #16409, #49261, #16066, #48580, #53137, #37398, #64644, #38077, #32848, #1371, #22689, #27598, #38780, #44033, #37740, #12211, #59067, #10824, #5237, #58720, #32167, #53481, #11168, #32502, #40493, #29690, #7304, #8002, #23729, #18149 ),
 ( #61820, #24424, #33540, #45749, #6959, #44385, #54857, #55204, #29337, #28646, #28290, #39470, #13257, #60449, #56237, #49610, #67059, #2069, #44727, #49956, #40166, #61481, #50991, #23388, #34921, #45411, #34233, #66025, #2405, #2750, #45067, #3088, #19169, #66371, #65684 ),
 ( #8344, #17807, #66720, #1717, #55552, #60792, #12905, #23036, #18495, #39124, #39820, #55898, #61140, #7650, #12555, #28998, #50649, #33887, #50307, #34582, #24074, #18839, #13600, #52702, #47466, #25792, #25444, #52005, #31049, #42225, #30360, #36630, #67396, #47122, #30031 ) ),
 .UNSPECIFIED., .F., .F., .F.,
 ( 4, 4 ),
 ( 4, 1, 1, 1, 1, 1, 1, 1, 1, 1, 1, 1, 1, 1, 1, 1, 1, 1, 1, 1, 1, 1, 1, 1, 1, 1, 1, 1, 1, 1, 1, 1, 4 ),
 ( -0.1039370721279000015, 1.103937072127999963 ),
 ( -0.02000000000000000042, 0.01250000000000000069, 0.04499999999999999833, 0.07749999999999999944, 0.1100000000000000006, 0.1424999999999999878, 0.1749999999999999889, 0.2074999999999999900, 0.2399999999999999911, 0.2725000000000000200, 0.3049999999999999933, 0.3375000000000000222, 0.3699999999999999956, 0.4025000000000000244, 0.4349999999999999978, 0.4675000000000000266, 0.5000000000000000000, 0.5324999999999999734, 0.5649999999999999467, 0.5975000000000000311, 0.6300000000000000044, 0.6624999999999999778, 0.6949999999999999512, 0.7275000000000000355, 0.7600000000000000089, 0.7924999999999999822, 0.8249999999999999556, 0.8575000000000000400, 0.8900000000000000133, 0.9224999999999999867, 0.9549999999999999600, 0.9875000000000000444, 1.020000000000000018 ),
 .UNSPECIFIED. ) ;
#7204=CARTESIAN_POINT ( 'NONE',  ( 9.318998833837817131, 4.145059358747968048, 9.246721409219425425 ) ) ;
#7205=CARTESIAN_POINT ( 'NONE',  ( 2.828929061525000233, 0.2082079807930999893, 3.419278880862000047 ) ) ;
#7206=ORIENTED_EDGE ( 'NONE', *, *, #12277, .T. ) ;
#7208=FACE_OUTER_BOUND ( 'NONE', #56679, .T. ) ;
#7210=CARTESIAN_POINT ( 'NONE',  ( 7.962142219590999659, 4.874567052833000069, 6.119507471270999588 ) ) ;
#7213=CARTESIAN_POINT ( 'NONE',  ( 10.91096346280954599, 9.739945009095949402, 5.808747756428651599 ) ) ;
#7215=CARTESIAN_POINT ( 'NONE',  ( 11.00000177645999955, -1.199999999999999956, 9.776630298829998011 ) ) ;
#7223=ORIENTED_EDGE ( 'NONE', *, *, #43570, .T. ) ;
#7224=CARTESIAN_POINT ( 'NONE',  ( 10.94043540126313374, 9.310192335818811671, -6.236500861513892602 ) ) ;
#7231=FACE_BOUND ( 'NONE', #30639, .T. ) ;
#7239=CARTESIAN_POINT ( 'NONE',  ( 7.540822165042829539, 2.490019829878222790, -8.581199080916018573 ) ) ;
#7240=CARTESIAN_POINT ( 'NONE',  ( 5.000030787343001215, -1.679270695423617399, 1.290525307673965560 ) ) ;
#7244=VERTEX_POINT ( 'NONE', #45836 ) ;
#7248=CARTESIAN_POINT ( 'NONE',  ( 8.649364158774000444, 3.038023536984999939, -5.861661709981000001 ) ) ;
#7249=CARTESIAN_POINT ( 'NONE',  ( 3.551082810560999725, -2.917487451239999530, 1.705317907324000126 ) ) ;
#7253=CARTESIAN_POINT ( 'NONE',  ( 7.686616257283001907, 3.172402717919002413, -6.371572564913001280 ) ) ;
#7259=CARTESIAN_POINT ( 'NONE',  ( 10.25461802485000007, 2.860644035673999941, 6.604613005744999654 ) ) ;
#7263=CARTESIAN_POINT ( 'NONE',  ( 9.108372294250248302, 3.858766891214160832, 8.849156255801389648 ) ) ;
#7265=CARTESIAN_POINT ( 'NONE',  ( -15.86200481174999943, 2.399999999999999911, -6.571291218949999902 ) ) ;
#7266=CIRCLE ( 'NONE', #28490, 12.50000000000000000 ) ;
#7277=ORIENTED_EDGE ( 'NONE', *, *, #48695, .T. ) ;
#7279=ADVANCED_FACE ( 'NONE', ( #14376, #62588 ), #3518, .T. ) ;
#7281=CARTESIAN_POINT ( 'NONE',  ( 9.839810841229999383, 5.817107086401000160, -6.945352709928000579 ) ) ;
#7283=CARTESIAN_POINT ( 'NONE',  ( 3.442208132701131351, -1.604827515477729838, 2.835269537469987888 ) ) ;
#7285=CARTESIAN_POINT ( 'NONE',  ( 10.13339736671999880, 5.653645990693000556, 6.501823474484000442 ) ) ;
#7290=ORIENTED_EDGE ( 'NONE', *, *, #35829, .F. ) ;
#7301=ORIENTED_EDGE ( 'NONE', *, *, #39725, .T. ) ;
#7304=CARTESIAN_POINT ( 'NONE',  ( 8.316054719590999511, 3.826300099041999747, -9.055335252254000267 ) ) ;
#7311=VERTEX_POINT ( 'NONE', #3858 ) ;
#7313=CARTESIAN_POINT ( 'NONE',  ( 7.942841246801999766, 3.400849348593999899, -6.290208884758000885 ) ) ;
#7326=CARTESIAN_POINT ( 'NONE',  ( 8.545864158774001851, 3.856772556595000179, 5.521246073317000125 ) ) ;
#7327=ORIENTED_EDGE ( 'NONE', *, *, #49248, .T. ) ;
#7330=CARTESIAN_POINT ( 'NONE',  ( 8.225195096046167720, 2.649880853682612614, 7.500010424662513664 ) ) ;
#7331=CARTESIAN_POINT ( 'NONE',  ( 10.68375192593000023, 4.547306763790999184, -8.749120576764999768 ) ) ;
#7334=CARTESIAN_POINT ( 'NONE',  ( 9.347254965556000883, 4.028327103212000715, 9.469449669541999626 ) ) ;
#7344=AXIS2_PLACEMENT_3D ( 'NONE', #40946, #55656, #2850 ) ;
#7347=CARTESIAN_POINT ( 'NONE',  ( 7.764232780408999446, 4.628941086829000184, 5.991667691044999522 ) ) ;
#7348=CARTESIAN_POINT ( 'NONE',  ( 11.02286749330999882, 2.398743616553999924, 6.352468982205000891 ) ) ;
#7351=CARTESIAN_POINT ( 'NONE',  ( 8.947714158774999760, 3.854507394315999758, -9.394302886912999639 ) ) ;
#7358=ORIENTED_EDGE ( 'NONE', *, *, #45539, .T. ) ;
#7359=CARTESIAN_POINT ( 'NONE',  ( 1.543883544273999986, -2.789116823352000285, 1.988880583162999871 ) ) ;
#7362=VECTOR ( 'NONE', #30297, 1000.000000000000000 ) ;
#7364=DIRECTION ( 'NONE',  ( -0.7071067811865474617, -0.7071067811865474617, 9.304624505883612300E-09 ) ) ;
#7371=DIRECTION ( 'NONE',  ( 1.000000000000000000, 0.000000000000000000, 0.000000000000000000 ) ) ;
#7373=ORIENTED_EDGE ( 'NONE', *, *, #303, .F. ) ;
#7375=CARTESIAN_POINT ( 'NONE',  ( 11.13711610220999937, 5.336572488559999883, 5.178750058134000689 ) ) ;
#7380=CARTESIAN_POINT ( 'NONE',  ( 10.68797807636180863, 4.829546767829883791, -8.579382731882136071 ) ) ;
#7382=CARTESIAN_POINT ( 'NONE',  ( 9.681187238460999822, 2.612249048987000055, 7.804677627401999551 ) ) ;
#7386=CARTESIAN_POINT ( 'NONE',  ( 10.25000000000000000, 0.000000000000000000, 0.000000000000000000 ) ) ;
#7387=CARTESIAN_POINT ( 'NONE',  ( 7.000000000000000000, 10.80467225524999897, 3.475853594956999970 ) ) ;
#7388=CARTESIAN_POINT ( 'NONE',  ( 9.512931135678952543, 5.100000000000000533, 6.444141223441286925 ) ) ;
#7390=CARTESIAN_POINT ( 'NONE',  ( 8.596685841231000325, 2.141799395716999843, -7.895788736628000848 ) ) ;
#7398=EDGE_CURVE ( 'NONE', #21003, #16931, #63272, .T. ) ;
#7407=B_SPLINE_CURVE_WITH_KNOTS ( 'NONE', 3,
 ( #47850, #57988, #9738, #41562, #25483, #4145, #42597, #52392, #46812, #30734, #10086, #68805, #26521, #20927, #58326, #62871, #15340, #47156 ),
 .UNSPECIFIED., .F., .F.,
 ( 4, 2, 2, 2, 2, 2, 2, 2, 4 ),
 ( 0.000000000000000000, 0.1250000000000000555, 0.2500000000000001110, 0.3750000000000001665, 0.5000000000000002220, 0.6250000000000001110, 0.7500000000000001110, 0.8750000000000000000, 1.000000000000000000 ),
 .UNSPECIFIED. ) ;
#7410=CARTESIAN_POINT ( 'NONE',  ( 10.09999999999999964, 0.000000000000000000, -11.84999999999999964 ) ) ;
#7412=CARTESIAN_POINT ( 'NONE',  ( 8.224726226261992679, 8.026539296952000413, 4.869553275538997639 ) ) ;
#7421=CARTESIAN_POINT ( 'NONE',  ( 7.126409439180999783, 4.037115771921000018, -6.023232697733999608 ) ) ;
#7423=CARTESIAN_POINT ( 'NONE',  ( 10.59999999999999964, 4.599999999999999645, -4.756097560976000338 ) ) ;
#7427=CARTESIAN_POINT ( 'NONE',  ( 8.979720280412999855, 5.524776413195999325, -7.147585171405999915 ) ) ;
#7429=CARTESIAN_POINT ( 'NONE',  ( 11.07109161080999904, 7.831824785490000274, -6.601376317068999633 ) ) ;
#7434=CARTESIAN_POINT ( 'NONE',  ( 1.230140132541749809, -3.408904368339107815, 0.9161175952574674985 ) ) ;
#7443=VECTOR ( 'NONE', #49107, 1000.000000000000000 ) ;
#7449=DIRECTION ( 'NONE',  ( -1.000000000000000000, 0.000000000000000000, 0.000000000000000000 ) ) ;
#7454=LINE ( 'NONE', #38936, #20863 ) ;
#7456=CARTESIAN_POINT ( 'NONE',  ( 10.52052890781999928, 2.899999999999999911, 6.152188490330000370 ) ) ;
#7467=CARTESIAN_POINT ( 'NONE',  ( 3.500000000000000444, -2.306765131595603258, 2.202630344077171287 ) ) ;
#7471=DIRECTION ( 'NONE',  ( 0.000000000000000000, 0.000000000000000000, -1.000000000000000000 ) ) ;
#7476=CARTESIAN_POINT ( 'NONE',  ( 9.649770280412001355, 4.042991257420999851, -5.768106221333000327 ) ) ;
#7485=CYLINDRICAL_SURFACE ( 'NONE', #53278, 3.500000000000000000 ) ;
#7487=CARTESIAN_POINT ( 'NONE',  ( 8.848264158775000610, 5.751585344281000545, -8.235867044345999588 ) ) ;
#7488=EDGE_LOOP ( 'NONE', ( #41766, #52500, #33784, #50204 ) ) ;
#7490=CARTESIAN_POINT ( 'NONE',  ( 9.858847045824999711, 2.668090821818000169, -7.206973500459000093 ) ) ;
#7491=ORIENTED_EDGE ( 'NONE', *, *, #68326, .T. ) ;
#7502=CARTESIAN_POINT ( 'NONE',  ( 11.28109528040999976, 2.660125405577999924, -6.904121770750999865 ) ) ;
#7506=CARTESIAN_POINT ( 'NONE',  ( 3.452384183491000069, 1.140396268832999827, -3.309002319436000317 ) ) ;
#7513=CARTESIAN_POINT ( 'NONE',  ( 9.643864158774000828, 2.927176851028000293, -5.932007155957999878 ) ) ;
#7523=CARTESIAN_POINT ( 'NONE',  ( 7.335819197764073429, 2.649620978275905703, -7.146853263626653074 ) ) ;
#7533=CARTESIAN_POINT ( 'NONE',  ( 9.848670280409999478, 5.002683760508999988, -8.912673867568997821 ) ) ;
#7537=VECTOR ( 'NONE', #33347, 1000.000000000000000 ) ;
#7540=CARTESIAN_POINT ( 'NONE',  ( 9.355690472842169925, 3.345172699598239596, 9.147100720064839763 ) ) ;
#7541=CARTESIAN_POINT ( 'NONE',  ( 2.213837056856000185, 1.294680128176000089, 3.350772176593999951 ) ) ;
#7552=CARTESIAN_POINT ( 'NONE',  ( 7.938110841225999970, 3.563552687850000122, -6.172381771908999504 ) ) ;
#7557=VERTEX_POINT ( 'NONE', #65343 ) ;
#7565=CARTESIAN_POINT ( 'NONE',  ( 10.98895755164048005, 7.482542893969703179, -6.234366245063336365 ) ) ;
#7568=AXIS2_PLACEMENT_3D ( 'NONE', #62773, #41807, #14213 ) ;
#7569=CARTESIAN_POINT ( 'NONE',  ( 7.938589158768999177, 3.517942668285999996, -6.188254172171000711 ) ) ;
#7574=CARTESIAN_POINT ( 'NONE',  ( 9.091114158770999154, 3.762712042852999872, 8.787816121229999666 ) ) ;
#7583=CARTESIAN_POINT ( 'NONE',  ( 10.92594639468418194, 2.912972570981688492, -4.995424234945515352 ) ) ;
#7593=CARTESIAN_POINT ( 'NONE',  ( 0.1499942179680000542, -2.749953718116144863, 0.3599680999393964353 ) ) ;
#7594=CARTESIAN_POINT ( 'NONE',  ( 8.699089158774000907, 4.178200486578000472, -5.608493638783999202 ) ) ;
#7595=CARTESIAN_POINT ( 'NONE',  ( 3.083239578446000273, -1.700413634830000076, -2.728580140816999844 ) ) ;
#7602=VECTOR ( 'NONE', #59369, 1000.000000000000000 ) ;
#7605=CARTESIAN_POINT ( 'NONE',  ( 11.08992526467999973, 5.210543602612999869, 8.327598319864998544 ) ) ;
#7616=CARTESIAN_POINT ( 'NONE',  ( 0.8776366609678249997, 0.07532896536173545876, -3.521742350970665125 ) ) ;
#7618=CARTESIAN_POINT ( 'NONE',  ( 10.22094528040999961, 2.563078870232999851, -8.004103956955001209 ) ) ;
#7626=CARTESIAN_POINT ( 'NONE',  ( 8.745860841232000027, 4.178200486578000472, -5.608493638783999202 ) ) ;
#7628=CARTESIAN_POINT ( 'NONE',  ( 9.926176658771000305, 4.356412802752999802, -9.313960415320000408 ) ) ;
#7630=CARTESIAN_POINT ( 'NONE',  ( 10.22398792753999963, 5.507894434963000130, 6.589802269404000157 ) ) ;
#7634=CARTESIAN_POINT ( 'NONE',  ( 7.415011787918005304, 3.233093659812002585, 6.479723185591006462 ) ) ;
#7635=ORIENTED_EDGE ( 'NONE', *, *, #15398, .F. ) ;
#7636=CARTESIAN_POINT ( 'NONE',  ( 27.64127793187000037, 5.599999999999999645, -6.571291218949999902 ) ) ;
#7637=CARTESIAN_POINT ( 'NONE',  ( 1.271806799208249794, -3.408904368339104263, -0.9161175952574814874 ) ) ;
#7643=ORIENTED_EDGE ( 'NONE', *, *, #2538, .T. ) ;
#7646=EDGE_LOOP ( 'NONE', ( #6448, #41064, #57237, #20410, #7975, #65939, #64922, #22599, #43616, #55490 ) ) ;
#7648=ORIENTED_EDGE ( 'NONE', *, *, #23411, .T. ) ;
#7650=CARTESIAN_POINT ( 'NONE',  ( 9.392285841233000809, 5.775964236216999836, -8.174909295649001706 ) ) ;
#7653=CARTESIAN_POINT ( 'NONE',  ( 8.281372984174815599, 5.064944289833863245, 6.454156656949499471 ) ) ;
#7660=CARTESIAN_POINT ( 'NONE',  ( 7.560652572975699037, 4.656871241626066471, 8.697129146950519640 ) ) ;
#7670=AXIS2_PLACEMENT_3D ( 'NONE', #12659, #33991, #28399 ) ;
#7672=DIRECTION ( 'NONE',  ( 1.000000000000000000, 0.000000000000000000, 0.000000000000000000 ) ) ;
#7677=CARTESIAN_POINT ( 'NONE',  ( 7.866204719590000671, 4.580608786027000612, 9.213365309690999538 ) ) ;
#7678=ORIENTED_EDGE ( 'NONE', *, *, #2438, .F. ) ;
#7684=CARTESIAN_POINT ( 'NONE',  ( 7.319425230799852855, 3.475664936878117839, 6.226553775891153109 ) ) ;
#7695=CARTESIAN_POINT ( 'NONE',  ( 11.29622358543999994, 3.561657733933999648, 6.266050246368000565 ) ) ;
#7700=CARTESIAN_POINT ( 'NONE',  ( 8.251329719592000345, 5.773189794777000117, 7.141495931231999883 ) ) ;
#7701=CARTESIAN_POINT ( 'NONE',  ( 9.380783851237000093, 2.204242311415999911, 7.545378292079000460 ) ) ;
#7704=ADVANCED_FACE ( 'NONE', ( #51594, #52285 ), #20813, .T. ) ;
#7705=EDGE_LOOP ( 'NONE', ( #46413, #26130, #32641, #18078, #23436, #52952 ) ) ;
#7706=CARTESIAN_POINT ( 'NONE',  ( 9.933354719590999693, 5.639765292528999829, -8.059103558718000215 ) ) ;
#7714=CARTESIAN_POINT ( 'NONE',  ( 1.686929392597000144, -1.310877008326999826, -3.164872840607000359 ) ) ;
#7722=CARTESIAN_POINT ( 'NONE',  ( 7.936333771302000351, 5.123034328734999754, 6.721303713258000023 ) ) ;
#7724=CARTESIAN_POINT ( 'NONE',  ( 9.566490007895001924, 4.108964550738000376, 8.851615252874999840 ) ) ;
#7725=CARTESIAN_POINT ( 'NONE',  ( 10.95282897519000009, 5.154323752254000190, 5.175250089408000242 ) ) ;
#7727=CARTESIAN_POINT ( 'NONE',  ( 7.000000000000000000, 6.255435840762999966, -3.000000000000000000 ) ) ;
#7728=CARTESIAN_POINT ( 'NONE',  ( 0.5718663363677000122, 2.877489654231000227, -1.904074875451999826 ) ) ;
#7730=CARTESIAN_POINT ( 'NONE',  ( 1.917640132539666808, 1.762666431298152370, -3.058252359239900464 ) ) ;
#7737=CARTESIAN_POINT ( 'NONE',  ( 9.694386075239211920, 4.746878242517505342, -8.656463215293298319 ) ) ;
#7738=ADVANCED_FACE ( 'NONE', ( #46707 ), #3691, .F. ) ;
#7741=CARTESIAN_POINT ( 'NONE',  ( 8.602991695318323195, 4.582460011752433005, 5.856014114908588475 ) ) ;
#7744=B_SPLINE_CURVE_WITH_KNOTS ( 'NONE', 3,
 ( #69038, #21825, #58545, #43158 ),
 .UNSPECIFIED., .F., .F.,
 ( 4, 4 ),
 ( 0.000000000000000000, 1.000000000000000000 ),
 .UNSPECIFIED. ) ;
#7753=DIRECTION ( 'NONE',  ( 0.000000000000000000, 0.000000000000000000, -1.000000000000000000 ) ) ;
#7755=DIRECTION ( 'NONE',  ( 0.000000000000000000, 0.000000000000000000, 1.000000000000000000 ) ) ;
#7757=CARTESIAN_POINT ( 'NONE',  ( 10.99570321855695099, 5.445259508076459198, -7.243346639199888415 ) ) ;
#7761=CARTESIAN_POINT ( 'NONE',  ( 9.861802827889565748, 2.874603711571212639, -6.749639981086963836 ) ) ;
#7764=EDGE_CURVE ( 'NONE', #65548, #14966, #38328, .T. ) ;
#7779=B_SPLINE_SURFACE_WITH_KNOTS ( 'NONE', 3, 3, ( 
 ( #52914, #43465, #37861, #5357, #59185, #37514, #27037, #53252, #16190, #63732, #58496, #58839, #6039, #4659, #25998, #48349, #47329, #68986, #36837, #43109, #15163, #21099, #64072, #42424, #64412, #27376, #11286, #48703, #10598, #31940, #26696, #36485, #57807, #9915, #20753 ),
 ( #42080, #48011, #63390, #15512, #58156, #111, #21427, #42764, #44162, #28775, #28423, #16876, #1846, #17931, #39595, #49381, #22462, #27733, #64758, #22815, #54637, #23163, #65104, #39249, #7081, #13981, #23508, #44849, #6730, #30070, #60573, #11980, #65459, #38202, #3471 ),
 ( #28071, #60231, #66156, #1153, #12334, #38551, #33665, #44511, #35306, #65806, #56622, #33319, #12680, #54984, #11627, #49736, #59531, #34013, #18273, #60916, #59874, #32966, #2196, #55329, #7427, #1497, #50087, #54280, #8727, #6382, #49044, #17581, #51373, #24807, #43808 ),
 ( #38908, #17229, #63573, #62203, #35649, #10094, #56961, #14661, #67781, #31429, #46130, #62540, #25832, #41229, #26181, #37019, #57639, #14324, #31774, #52745, #35977, #51711, #63217, #15685, #5191, #36323, #20934, #58331, #68813, #9063, #15346, #4492, #30402, #57293, #9396 ) ),
 .UNSPECIFIED., .F., .F., .F.,
 ( 4, 4 ),
 ( 4, 1, 1, 1, 1, 1, 1, 1, 1, 1, 1, 1, 1, 1, 1, 1, 1, 1, 1, 1, 1, 1, 1, 1, 1, 1, 1, 1, 1, 1, 1, 1, 4 ),
 ( -0.1039370721279000015, 1.103937072127999963 ),
 ( -0.02000000000000000042, 0.01250000000000000069, 0.04499999999999999833, 0.07749999999999999944, 0.1100000000000000006, 0.1424999999999999878, 0.1749999999999999889, 0.2074999999999999900, 0.2399999999999999911, 0.2725000000000000200, 0.3049999999999999933, 0.3375000000000000222, 0.3699999999999999956, 0.4025000000000000244, 0.4349999999999999978, 0.4675000000000000266, 0.5000000000000000000, 0.5324999999999999734, 0.5649999999999999467, 0.5975000000000000311, 0.6300000000000000044, 0.6624999999999999778, 0.6949999999999999512, 0.7275000000000000355, 0.7600000000000000089, 0.7924999999999999822, 0.8249999999999999556, 0.8575000000000000400, 0.8900000000000000133, 0.9224999999999999867, 0.9549999999999999600, 0.9875000000000000444, 1.020000000000000018 ),
 .UNSPECIFIED. ) ;
#7780=DIRECTION ( 'NONE',  ( 0.000000000000000000, -1.000000000000000000, 0.000000000000000000 ) ) ;
#7781=CARTESIAN_POINT ( 'NONE',  ( 11.12723081016999949, 8.477322043720000977, -6.786959512705000641 ) ) ;
#7782=CARTESIAN_POINT ( 'NONE',  ( 8.137846616029218438, 4.829271229625343054, -8.579069916537873652 ) ) ;
#7783=FACE_OUTER_BOUND ( 'NONE', #5663, .T. ) ;
#7790=DIRECTION ( 'NONE',  ( -1.000000000000000000, 0.000000000000000000, 0.000000000000000000 ) ) ;
#7811=CARTESIAN_POINT ( 'NONE',  ( 6.999998782146999332, 0.000000000000000000, 0.000000000000000000 ) ) ;
#7814=ORIENTED_EDGE ( 'NONE', *, *, #65875, .T. ) ;
#7824=CARTESIAN_POINT ( 'NONE',  ( 8.424364158774000799, 3.292387953886000140, -6.294868737226000377 ) ) ;
#7831=ORIENTED_EDGE ( 'NONE', *, *, #27139, .T. ) ;
#7833=CARTESIAN_POINT ( 'NONE',  ( 2.728056799211040495, -2.150913519912213800, 2.798833948393621540 ) ) ;
#7834=CARTESIAN_POINT ( 'NONE',  ( 8.266329719591000824, 4.769017407621999993, -8.862909124839001507 ) ) ;
#7841=DIRECTION ( 'NONE',  ( -1.000000000000000000, 0.000000000000000000, 0.000000000000000000 ) ) ;
#7843=CARTESIAN_POINT ( 'NONE',  ( 8.897989158775001073, 4.990139824845000405, -9.121472988377998803 ) ) ;
#7845=CARTESIAN_POINT ( 'NONE',  ( 10.65649893244999902, 5.448184228579000532, -7.015214795518000201 ) ) ;
#7850=EDGE_CURVE ( 'NONE', #19641, #68613, #43525, .T. ) ;
#7857=EDGE_LOOP ( 'NONE', ( #17791, #42585, #22625, #62031, #54240 ) ) ;
#7859=CARTESIAN_POINT ( 'NONE',  ( 11.01605778040999972, 5.482856203356999636, -7.846408531951999166 ) ) ;
#7869=CARTESIAN_POINT ( 'NONE',  ( 9.684729719592999331, 2.370176859044999862, -6.912649125838000508 ) ) ;
#7879=EDGE_LOOP ( 'NONE', ( #13596, #49156, #25901, #14079, #37011 ) ) ;
#7881=CARTESIAN_POINT ( 'NONE',  ( 7.904992389751000381, 3.357074527946999787, -6.312906081255999169 ) ) ;
#7882=EDGE_CURVE ( 'NONE', #63419, #65344, #28895, .T. ) ;
#7888=DIRECTION ( 'NONE',  ( -1.000000000000000000, 0.000000000000000000, 0.000000000000000000 ) ) ;
#7890=CARTESIAN_POINT ( 'NONE',  ( 9.459729719592999686, 2.527713920559999661, -6.969421869128999525 ) ) ;
#7895=CARTESIAN_POINT ( 'NONE',  ( 2.261519006296000001, -0.8206105251038000592, 3.497205449952000222 ) ) ;
#7896=VERTEX_POINT ( 'NONE', #16253 ) ;
#7898=CARTESIAN_POINT ( 'NONE',  ( 9.365090231804463983, 2.650133164351947013, -7.500005474590564880 ) ) ;
#7904=CARTESIAN_POINT ( 'NONE',  ( 10.93892583729919110, 9.336001207588561002, 6.217743753063594170 ) ) ;
#7907=CARTESIAN_POINT ( 'NONE',  ( 10.66914689902456281, 4.353380376947314723, -8.814970433265305161 ) ) ;
#7912=ORIENTED_EDGE ( 'NONE', *, *, #11337, .F. ) ;
#7919=CARTESIAN_POINT ( 'NONE',  ( 10.97843137008999825, 5.235400103863000254, 6.782920672145000829 ) ) ;
#7920=AXIS2_PLACEMENT_3D ( 'NONE', #60918, #45193, #32968 ) ;
#7934=CARTESIAN_POINT ( 'NONE',  ( 6.904593832438223444, 5.247842549850568972, -8.795830109246409734 ) ) ;
#7941=ORIENTED_EDGE ( 'NONE', *, *, #13063, .F. ) ;
#7943=CARTESIAN_POINT ( 'NONE',  ( 8.929995280412999392, 5.030502105212999453, -6.322203460290999999 ) ) ;
#7944=CARTESIAN_POINT ( 'NONE',  ( 3.250907432355000015, 3.214334891372999881, -0.06787714083755000405 ) ) ;
#7946=CARTESIAN_POINT ( 'NONE',  ( 7.856038276909000473, 2.869044596334999753, -6.744487387516000076 ) ) ;
#7951=CARTESIAN_POINT ( 'NONE',  ( 10.84168637167000071, 2.681011538858999899, 6.554754637093000547 ) ) ;
#7955=CARTESIAN_POINT ( 'NONE',  ( 9.256664404737000140, 4.025830366070999311, 9.295863330698999505 ) ) ;
#7956=DIRECTION ( 'NONE',  ( 0.000000000000000000, 0.000000000000000000, -1.000000000000000000 ) ) ;
#7962=EDGE_CURVE ( 'NONE', #62147, #63419, #19948, .T. ) ;
#7966=CARTESIAN_POINT ( 'NONE',  ( 8.123290826992597857, 5.010513939749104750, -6.421869068174552275 ) ) ;
#7967=CARTESIAN_POINT ( 'NONE',  ( 5.500000000000000000, 12.78667792605000031, 2.345384795462000405 ) ) ;
#7970=EDGE_CURVE ( 'NONE', #65620, #25656, #61682, .T. ) ;
#7975=ORIENTED_EDGE ( 'NONE', *, *, #8016, .T. ) ;
#7976=CARTESIAN_POINT ( 'NONE',  ( 7.293864158771000028, 3.416213390569000197, 6.162512717529000206 ) ) ;
#7977=CARTESIAN_POINT ( 'NONE',  ( 8.406645280410000254, 3.807713920470999991, -9.221758713517999695 ) ) ;
#7978=CARTESIAN_POINT ( 'NONE',  ( 0.5181103717477000270, 3.205765437135000173, -1.404659375816999844 ) ) ;
#7979=CARTESIAN_POINT ( 'NONE',  ( 11.19050471959000070, 2.516756593394000152, -6.840361808223000217 ) ) ;
#7982=CARTESIAN_POINT ( 'NONE',  ( 10.27967883605999866, 5.739712809045000697, 7.774963411801000923 ) ) ;
#7986=CARTESIAN_POINT ( 'NONE',  ( 9.049999337612000261, 3.268496584495999908E-13, -12.44999944940996350 ) ) ;
#7989=ADVANCED_FACE ( 'NONE', ( #39658 ), #32998, .T. ) ;
#7998=ORIENTED_EDGE ( 'NONE', *, *, #46266, .F. ) ;
#8000=VERTEX_POINT ( 'NONE', #52894 ) ;
#8001=CARTESIAN_POINT ( 'NONE',  ( 11.08923508776216238, 3.836355264003908250, -9.039235091853335291 ) ) ;
#8002=CARTESIAN_POINT ( 'NONE',  ( 8.266329719591000824, 4.769017407621999993, -8.862909124839001507 ) ) ;
#8008=ORIENTED_EDGE ( 'NONE', *, *, #62724, .F. ) ;
#8010=EDGE_LOOP ( 'NONE', ( #66841, #69170, #45360 ) ) ;
#8013=VERTEX_POINT ( 'NONE', #439 ) ;
#8016=EDGE_CURVE ( 'NONE', #19886, #64076, #67491, .T. ) ;
#8025=CARTESIAN_POINT ( 'NONE',  ( 8.443892219592001425, 2.905861847853000057, 8.940690431604000565 ) ) ;
#8028=CARTESIAN_POINT ( 'NONE',  ( 9.299999999999998934, 4.537600397704999899, 9.154563893594000135 ) ) ;
#8033=CARTESIAN_POINT ( 'NONE',  ( 11.01665240710999960, 5.432459446251999502, 4.991866823696000210 ) ) ;
#8034=CARTESIAN_POINT ( 'NONE',  ( 9.719613305057999142, 5.967773797872000685, 7.406643507784999692 ) ) ;
#8035=DIRECTION ( 'NONE',  ( 0.000000000000000000, 0.8648648648648717963, 0.5020047465136829867 ) ) ;
#8039=CARTESIAN_POINT ( 'NONE',  ( 11.20563302462000088, 3.509134285281999777, 6.118194788334999856 ) ) ;
#8043=CARTESIAN_POINT ( 'NONE',  ( 7.802017219589999719, 5.638704226117999596, 8.266404648244000342 ) ) ;
#8044=CARTESIAN_POINT ( 'NONE',  ( 11.06923869026000062, 5.425682056982999768, 8.012911262916999178 ) ) ;
#8047=ORIENTED_EDGE ( 'NONE', *, *, #5822, .T. ) ;
#8051=ADVANCED_FACE ( 'NONE', ( #49362 ), #1475, .T. ) ;
#8060=CARTESIAN_POINT ( 'NONE',  ( 1.734611342038000048, 0.7023893950988999713, -3.352829814747000370 ) ) ;
#8065=CARTESIAN_POINT ( 'NONE',  ( 4.900006121742000786, -1.007237960741800276, -1.747572776708515407 ) ) ;
#8070=CARTESIAN_POINT ( 'NONE',  ( 9.240545280410998430, 4.158911560497999815, 5.873540104660999184 ) ) ;
#8072=CARTESIAN_POINT ( 'NONE',  ( 11.05576033064000185, 5.199216738862999954, 4.875271020876000172 ) ) ;
#8076=CARTESIAN_POINT ( 'NONE',  ( 0.6942448634807999452, 3.368557921162000479, -0.6219103594335000373 ) ) ;
#8078=LINE ( 'NONE', #55631, #60070 ) ;
#8081=CARTESIAN_POINT ( 'NONE',  ( 11.03856029907000114, 2.974095820320000083, 8.716122353065999917 ) ) ;
#8089=CARTESIAN_POINT ( 'NONE',  ( 8.259865135739552500, 5.282034867868143913, 8.692621038018929269 ) ) ;
#8096=CARTESIAN_POINT ( 'NONE',  ( 4.149992563291999836, 1.947893036340042183, -0.5234817089163682491 ) ) ;
#8098=CARTESIAN_POINT ( 'NONE',  ( 9.318724127987000116, 2.755029797911999978, 8.795125756257000660 ) ) ;
#8099=CARTESIAN_POINT ( 'NONE',  ( 10.09453415443000068, 5.362844031509000686, -7.550030311027999375 ) ) ;
#8104=DIRECTION ( 'NONE',  ( -1.000000000000000000, -8.790925318715999585E-10, -6.356715264083000235E-09 ) ) ;
#8109=CIRCLE ( 'NONE', #25968, 13.10000000000000320 ) ;
#8127=CARTESIAN_POINT ( 'NONE',  ( 0.01379484080271000009, 3.646234950436999966, -0.6383912046097000026 ) ) ;
#8156=CARTESIAN_POINT ( 'NONE',  ( 5.477523075960999854, 12.82224764859999766, 2.276049205300000100 ) ) ;
#8168=CARTESIAN_POINT ( 'NONE',  ( 8.709204462306734840, 2.899999999999999911, 6.662590550601094286 ) ) ;
#8174=CARTESIAN_POINT ( 'NONE',  ( 8.507804550190710913, 4.678883388517513175, 8.679043930491522119 ) ) ;
#8176=CARTESIAN_POINT ( 'NONE',  ( 9.211104719594999324, 5.462898983065000102, -8.055936939571999744 ) ) ;
#8182=CARTESIAN_POINT ( 'NONE',  ( 7.736620384918536431, 4.059907268619843634, -8.863659910720466328 ) ) ;
#8186=CARTESIAN_POINT ( 'NONE',  ( 10.76231429546999863, 3.259156861436999897, -8.644989069184999764 ) ) ;
#8193=DIRECTION ( 'NONE',  ( 1.000000000000000000, 0.000000000000000000, 0.000000000000000000 ) ) ;
#8194=EDGE_CURVE ( 'NONE', #58012, #10018, #68190, .T. ) ;
#8197=ORIENTED_EDGE ( 'NONE', *, *, #66834, .T. ) ;
#8199=AXIS2_PLACEMENT_3D ( 'NONE', #31658, #52977, #43867 ) ;
#8200=CARTESIAN_POINT ( 'NONE',  ( 10.84161084123000052, 2.641275823976000137, -7.444905437480000110 ) ) ;
#8207=CARTESIAN_POINT ( 'NONE',  ( 7.844724277266999835, 4.719412473309000156, 6.357657803787000184 ) ) ;
#8210=CARTESIAN_POINT ( 'NONE',  ( 9.883629719592001095, 5.656948148960999845, -6.994239053114000626 ) ) ;
#8211=DIRECTION ( 'NONE',  ( 1.000000000000000000, 0.000000000000000000, 0.000000000000000000 ) ) ;
#8222=ORIENTED_EDGE ( 'NONE', *, *, #18790, .T. ) ;
#8223=EDGE_CURVE ( 'NONE', #5660, #64040, #5414, .T. ) ;
#8224=CARTESIAN_POINT ( 'NONE',  ( 10.90000000000000036, 4.000000000000000000, 7.500000000000000000 ) ) ;
#8232=CARTESIAN_POINT ( 'NONE',  ( 9.740360841231000322, 4.047146749018000200, -5.600703114891000034 ) ) ;
#8237=CARTESIAN_POINT ( 'NONE',  ( 2.499928753500999523, 0.3043608712121999571, -3.579275528594000111 ) ) ;
#8246=CARTESIAN_POINT ( 'NONE',  ( 7.002195280409999611, 5.464161011425000325, -7.581039036848999935 ) ) ;
#8247=CARTESIAN_POINT ( 'NONE',  ( 10.42499241036494162, 5.349775919985349404, 7.500001834605750872 ) ) ;
#8254=DIRECTION ( 'NONE',  ( 1.000000000000000000, 0.000000000000000000, 0.000000000000000000 ) ) ;
#8268=AXIS2_PLACEMENT_3D ( 'NONE', #41183, #56915, #30355 ) ;
#8275=CARTESIAN_POINT ( 'NONE',  ( 3.500000000000000444, 3.257391245615596898, 1.180021364213383883 ) ) ;
#8276=EDGE_CURVE ( 'NONE', #34762, #24471, #42491, .T. ) ;
#8278=CYLINDRICAL_SURFACE ( 'NONE', #7568, 1.350000000000000533 ) ;
#8286=CARTESIAN_POINT ( 'NONE',  ( 9.590596677641999079, 2.445964682955000136, 7.841184989245001624 ) ) ;
#8289=CARTESIAN_POINT ( 'NONE',  ( 10.19741084123000086, 4.262870449202000422, -8.811513791423999820 ) ) ;
#8290=CARTESIAN_POINT ( 'NONE',  ( 3.215747102742000152, -0.1032237435928999997, -3.377807273626999951 ) ) ;
#8292=CARTESIAN_POINT ( 'NONE',  ( 7.858540647797734202, 2.846821975048335229, -6.797502970372296005 ) ) ;
#8294=ORIENTED_EDGE ( 'NONE', *, *, #53094, .T. ) ;
#8296=CARTESIAN_POINT ( 'NONE',  ( 10.56491664109999995, 4.212242527248999835, 8.933458498617000032 ) ) ;
#8297=DIRECTION ( 'NONE',  ( -0.8660254017760760092, -3.364876958529905008E-12, 0.5000000034785859748 ) ) ;
#8298=ADVANCED_FACE ( 'NONE', ( #56346 ), #38581, .F. ) ;
#8300=CARTESIAN_POINT ( 'NONE',  ( 10.80815748598999981, 2.937526572573000205, 8.948458885032000154 ) ) ;
#8301=CARTESIAN_POINT ( 'NONE',  ( 10.94166666666763987, 5.229667600279960915, 8.191470186740231085 ) ) ;
#8304=CARTESIAN_POINT ( 'NONE',  ( 10.95957739177982226, 2.825857471007950039, -6.683619889684592863 ) ) ;
#8308=CARTESIAN_POINT ( 'NONE',  ( 8.228368194308000483, 4.806758213781000322, 6.177034601037000527 ) ) ;
#8309=CARTESIAN_POINT ( 'NONE',  ( 10.18308278041000037, 2.953582937013000009, -8.606284720264998356 ) ) ;
#8313=CARTESIAN_POINT ( 'NONE',  ( 8.564919648097475857, 5.350116636189168773, -7.500005043868485544 ) ) ;
#8317=CARTESIAN_POINT ( 'NONE',  ( 8.860767219592000643, 2.935741164366000522, 6.259844213126999790 ) ) ;
#8318=ADVANCED_FACE ( 'NONE', ( #67418 ), #57619, .F. ) ;
#8320=CARTESIAN_POINT ( 'NONE',  ( 8.555820280412000045, 2.414630869937000046, -6.801495146585999407 ) ) ;
#8322=CARTESIAN_POINT ( 'NONE',  ( 10.15335165876999923, 3.144981324235999853, -5.860948306964999688 ) ) ;
#8323=VERTEX_POINT ( 'NONE', #52028 ) ;
#8329=DIRECTION ( 'NONE',  ( 1.000000000000000000, 0.000000000000000000, 0.000000000000000000 ) ) ;
#8330=ORIENTED_EDGE ( 'NONE', *, *, #7003, .T. ) ;
#8343=CARTESIAN_POINT ( 'NONE',  ( 11.08380555355736163, 3.999999927305438963, -9.033895164528459532 ) ) ;
#8344=CARTESIAN_POINT ( 'NONE',  ( 9.988985841228000595, 3.986577607995999806, -9.280166295424001177 ) ) ;
#8346=CYLINDRICAL_SURFACE ( 'NONE', #62312, 0.5000000000000002220 ) ;
#8349=CARTESIAN_POINT ( 'NONE',  ( 8.400073341230999802, 2.800103557244999930, 9.079946116129001155 ) ) ;
#8360=CARTESIAN_POINT ( 'NONE',  ( 9.140753410162000492, 5.100000000000000533, 6.175944241622000064 ) ) ;
#8365=EDGE_CURVE ( 'NONE', #69034, #8802, #68104, .T. ) ;
#8371=VERTEX_POINT ( 'NONE', #30718 ) ;
#8380=CARTESIAN_POINT ( 'NONE',  ( 9.848730799670999403, 2.769737997918999994, 6.441853401936000090 ) ) ;
#8382=B_SPLINE_CURVE_WITH_KNOTS ( 'NONE', 3,
 ( #22818, #44516, #54988, #13036, #34365, #64764, #55685, #59535, #65809, #50091, #7782, #29122, #11631, #33669 ),
 .UNSPECIFIED., .F., .F.,
 ( 4, 2, 2, 2, 2, 2, 4 ),
 ( 0.1253988501910747455, 0.3126983667838658665, 0.4063481250802616351, 0.4999978833766571817, 0.5936476416730528394, 0.6872973999694486080, 0.8745969165622392572 ),
 .UNSPECIFIED. ) ;
#8383=ORIENTED_EDGE ( 'NONE', *, *, #36136, .T. ) ;
#8386=CARTESIAN_POINT ( 'NONE',  ( 9.945533384955998812, 2.906048475816000121, 8.880389653997999844 ) ) ;
#8390=CARTESIAN_POINT ( 'NONE',  ( 7.518864158771000561, 3.206360348473000332, 5.681727837477000165 ) ) ;
#8391=CARTESIAN_POINT ( 'NONE',  ( 10.12550053024000007, 5.788811067708000024, 7.335561454339999621 ) ) ;
#8394=CARTESIAN_POINT ( 'NONE',  ( 9.544414158773999901, 2.173570076733999823, -8.023168429484000441 ) ) ;
#8396=CARTESIAN_POINT ( 'NONE',  ( 11.09998944727679060, 2.658360006774582285, 6.717872455900629092 ) ) ;
#8401=VERTEX_POINT ( 'NONE', #35289 ) ;
#8403=CARTESIAN_POINT ( 'NONE',  ( 1.443746307329000000, 3.563994061069000185, 0.4492161910706000127 ) ) ;
#8409=ADVANCED_FACE ( 'NONE', ( #19193 ), #23288, .T. ) ;
#8415=CARTESIAN_POINT ( 'NONE',  ( 9.497295280408998508, 3.734279507827999556, 8.942126004519000304 ) ) ;
#8419=CARTESIAN_POINT ( 'NONE',  ( 1.557293291478000219, 2.591090368091000240, -2.487991068387999771 ) ) ;
#8421=CARTESIAN_POINT ( 'NONE',  ( 0.7496340823758137484, 2.944778677366191921, -1.029289356940257694 ) ) ;
#8424=CARTESIAN_POINT ( 'NONE',  ( 9.701978494675000064, 3.399139198672999740, 6.026757051093999173 ) ) ;
#8432=CARTESIAN_POINT ( 'NONE',  ( 7.953337875888457198, 2.248440269089167387, 7.443232059063713102 ) ) ;
#8436=VERTEX_POINT ( 'NONE', #51690 ) ;
#8439=CARTESIAN_POINT ( 'NONE',  ( 11.04384236319999957, 1.600344243522999976, -5.035088906224999938 ) ) ;
#8441=CARTESIAN_POINT ( 'NONE',  ( 9.013423559847998590, 4.933953210258000155, 8.417881984655998906 ) ) ;
#8442=CARTESIAN_POINT ( 'NONE',  ( 6.949999692073999924, 11.00717859340000082, 1.432487142323000118 ) ) ;
#8449=EDGE_CURVE ( 'NONE', #26212, #2243, #51014, .T. ) ;
#8451=CARTESIAN_POINT ( 'NONE',  ( 7.662260841227999997, 2.688365364125000045, 8.140015608605001063 ) ) ;
#8470=AXIS2_PLACEMENT_3D ( 'NONE', #69011, #21124, #42450 ) ;
#8471=AXIS2_PLACEMENT_3D ( 'NONE', #20261, #25851, #52766 ) ;
#8473=CARTESIAN_POINT ( 'NONE',  ( 0.3839841414396000241, -0.8575131787502999758, -3.600995375387999964 ) ) ;
#8474=FACE_OUTER_BOUND ( 'NONE', #18888, .T. ) ;
#8484=ORIENTED_EDGE ( 'NONE', *, *, #58395, .F. ) ;
#8498=AXIS2_PLACEMENT_3D ( 'NONE', #6054, #44527, #11300 ) ;
#8499=DIRECTION ( 'NONE',  ( -1.000000000000000000, 0.000000000000000000, 0.000000000000000000 ) ) ;
#8500=CARTESIAN_POINT ( 'NONE',  ( 7.832795987768000678, 2.851255020980998811, 6.795938453665997692 ) ) ;
#8502=CARTESIAN_POINT ( 'NONE',  ( 0.8113901325419543564, -3.500000000000000888, -0.4581489286485119217 ) ) ;
#8503=VERTEX_POINT ( 'NONE', #9640 ) ;
#8509=CARTESIAN_POINT ( 'NONE',  ( 8.822164158776001130, 2.644017913812000131, -7.838184857420000817 ) ) ;
#8513=CARTESIAN_POINT ( 'NONE',  ( 4.000000000000000000, 1.321180510578203071, 1.719428477289353552 ) ) ;
#8518=CARTESIAN_POINT ( 'NONE',  ( 9.102795280413999990, 3.071719032003000116, -6.037263251225000182 ) ) ;
#8523=DIRECTION ( 'NONE',  ( 0.000000000000000000, 0.9916377111174247139, -0.1290528957048031888 ) ) ;
#8525=CARTESIAN_POINT ( 'NONE',  ( 7.858238185142895738, 2.638874411158420141, -7.614836700234859812 ) ) ;
#8529=ORIENTED_EDGE ( 'NONE', *, *, #62917, .T. ) ;
#8530=CARTESIAN_POINT ( 'NONE',  ( 10.95552360838999917, 4.744046441415999738, -9.198140387677000263 ) ) ;
#8540=CARTESIAN_POINT ( 'NONE',  ( 10.16008584122999991, 4.812959680871000678, -8.526582921144999716 ) ) ;
#8541=EDGE_CURVE ( 'NONE', #50591, #13432, #37530, .T. ) ;
#8553=CARTESIAN_POINT ( 'NONE',  ( 9.517835841233001304, 4.883347899767999323, -6.417062834774999835 ) ) ;
#8554=CARTESIAN_POINT ( 'NONE',  ( 9.265220490506111517, 5.204037557847910556, 8.765935439646369787 ) ) ;
#8561=DIRECTION ( 'NONE',  ( 1.000000000000000000, 0.000000000000000000, 0.000000000000000000 ) ) ;
#8564=AXIS2_PLACEMENT_3D ( 'NONE', #44284, #3329, #39368 ) ;
#8575=CARTESIAN_POINT ( 'NONE',  ( 2.395018178493999894, 1.174603829501999819, 3.040001730748000508 ) ) ;
#8576=ORIENTED_EDGE ( 'NONE', *, *, #63735, .T. ) ;
#8589=CARTESIAN_POINT ( 'NONE',  ( 7.803806111238657195, 2.990843308588816640, 6.553755180521002366 ) ) ;
#8599=CARTESIAN_POINT ( 'NONE',  ( 10.97977755915654541, 8.327332208918569734, -6.553115839673279375 ) ) ;
#8601=CARTESIAN_POINT ( 'NONE',  ( 7.640239158768000749, 5.144639763962000067, -8.301783154141999077 ) ) ;
#8602=AXIS2_PLACEMENT_3D ( 'NONE', #14176, #19066, #14858 ) ;
#8603=CYLINDRICAL_SURFACE ( 'NONE', #29780, 0.5000000000000000000 ) ;
#8618=CARTESIAN_POINT ( 'NONE',  ( 3.198890132544458531, -2.798833948393640192, 2.150913519912191152 ) ) ;
#8619=AXIS2_PLACEMENT_3D ( 'NONE', #5654, #32585, #27337 ) ;
#8622=ORIENTED_EDGE ( 'NONE', *, *, #62974, .F. ) ;
#8625=CARTESIAN_POINT ( 'NONE',  ( 9.757669403192000601, 4.489270656625000022, 5.986034819543999852 ) ) ;
#8627=CARTESIAN_POINT ( 'NONE',  ( 9.716735841232001292, 3.941185585667000169, -8.896279800194999865 ) ) ;
#8628=CARTESIAN_POINT ( 'NONE',  ( 3.229260370471000119, -3.128337010252999928, 1.990763144092999593 ) ) ;
#8635=CARTESIAN_POINT ( 'NONE',  ( 10.15902941591999920, 4.166415211384999040, 9.114163806478000396 ) ) ;
#8638=CARTESIAN_POINT ( 'NONE',  ( 10.00138108374000012, 3.855364958793999985, 5.709478909302000638 ) ) ;
#8641=AXIS2_PLACEMENT_3D ( 'NONE', #405, #37811, #11235 ) ;
#8642=CARTESIAN_POINT ( 'NONE',  ( 11.00624930493297882, 2.793750695071733681, -6.598047929500610032 ) ) ;
#8646=B_SPLINE_CURVE_WITH_KNOTS ( 'NONE', 3,
 ( #8343, #8001, #50990, #2749 ),
 .UNSPECIFIED., .F., .F.,
 ( 4, 4 ),
 ( 0.8675649130336897663, 1.000000000000000000 ),
 .UNSPECIFIED. ) ;
#8653=CARTESIAN_POINT ( 'NONE',  ( 8.642077642326000841, 2.899999999999999911, 6.463854830420999953 ) ) ;
#8655=EDGE_LOOP ( 'NONE', ( #21146, #13733, #16496, #42396, #28053, #51499 ) ) ;
#8657=CARTESIAN_POINT ( 'NONE',  ( 9.026926658770998202, 4.852728889087999598, 8.683917172082999514 ) ) ;
#8660=CARTESIAN_POINT ( 'NONE',  ( 10.20607971959000082, 2.622352165399999713, -6.528536464360000124 ) ) ;
#8661=ADVANCED_FACE ( 'NONE', ( #61939 ), #14400, .F. ) ;
#8664=CARTESIAN_POINT ( 'NONE',  ( 1.415556799207333905, -0.4581489286485083134, -3.500000000000000888 ) ) ;
#8676=ORIENTED_EDGE ( 'NONE', *, *, #5136, .F. ) ;
#8677=CARTESIAN_POINT ( 'NONE',  ( 2.855140132543084519, -0.9161175952574772685, -3.408904368339104707 ) ) ;
#8680=DIRECTION ( 'NONE',  ( -1.000000000000000000, 0.000000000000000000, -5.786858784138000079E-14 ) ) ;
#8689=CARTESIAN_POINT ( 'NONE',  ( 8.143323341229999457, 5.061727314042999915, 5.824077473724000420 ) ) ;
#8691=EDGE_CURVE ( 'NONE', #12641, #58572, #53251, .T. ) ;
#8693=CARTESIAN_POINT ( 'NONE',  ( 7.609170034105995128, 3.848214081969753231, 8.855880787058648451 ) ) ;
#8695=ADVANCED_FACE ( 'NONE', ( #62613 ), #16791, .F. ) ;
#8707=AXIS2_PLACEMENT_3D ( 'NONE', #51882, #25318, #19042 ) ;
#8715=CARTESIAN_POINT ( 'NONE',  ( 10.01597178489000051, 4.792666960550000077, -6.390258598531999290 ) ) ;
#8720=CARTESIAN_POINT ( 'NONE',  ( 10.43579914648999996, 2.587602126999999808, 6.390037244031000263 ) ) ;
#8722=ORIENTED_EDGE ( 'NONE', *, *, #64091, .T. ) ;
#8725=CARTESIAN_POINT ( 'NONE',  ( 9.646287586158999616, 2.591467678478000192, 6.760055064032999717 ) ) ;
#8727=CARTESIAN_POINT ( 'NONE',  ( 8.780820280412001466, 2.567871051582000241, -6.869011921437000012 ) ) ;
#8731=CARTESIAN_POINT ( 'NONE',  ( 7.775614158771000817, 4.636729845879000500, 9.378977473003999421 ) ) ;
#8732=CARTESIAN_POINT ( 'NONE',  ( 10.93227693248999977, 2.539877577705000000, 6.453611809651000009 ) ) ;
#8734=VERTEX_POINT ( 'NONE', #59435 ) ;
#8735=CARTESIAN_POINT ( 'NONE',  ( 10.06481084123000080, 5.336630274082000192, -7.092011739486999922 ) ) ;
#8743=CARTESIAN_POINT ( 'NONE',  ( 1.586792155651000291, -1.239015738333000050, 3.371748634333000094 ) ) ;
#8745=CARTESIAN_POINT ( 'NONE',  ( 8.374639158773000247, 2.721111233225000259, -6.936528696292000085 ) ) ;
#8757=ADVANCED_FACE ( 'NONE', ( #49642 ), #20673, .F. ) ;
#8758=CARTESIAN_POINT ( 'NONE',  ( 8.881823341230997926, 4.977909614887999545, 6.416776202806000029 ) ) ;
#8763=CARTESIAN_POINT ( 'NONE',  ( 1.271201594832999993, -1.239015738333000050, 3.371748634333000094 ) ) ;
#8765=DIRECTION ( 'NONE',  ( 1.000000000000000000, 0.000000000000000000, 0.000000000000000000 ) ) ;
#8768=CARTESIAN_POINT ( 'NONE',  ( 11.20563302462000088, 3.509134285281999777, 6.118194788334999856 ) ) ;
#8770=AXIS2_PLACEMENT_3D ( 'NONE', #47229, #30465, #13701 ) ;
#8771=DIRECTION ( 'NONE',  ( 1.000000000000000000, 0.000000000000000000, 0.000000000000000000 ) ) ;
#8772=CARTESIAN_POINT ( 'NONE',  ( 8.005415440112999548, 4.520303302631999642, -6.254081655062000422 ) ) ;
#8775=CARTESIAN_POINT ( 'NONE',  ( 8.114521557114207084, 4.828697020333564183, 5.952393600668290929 ) ) ;
#8779=ORIENTED_EDGE ( 'NONE', *, *, #44146, .F. ) ;
#8783=CARTESIAN_POINT ( 'NONE',  ( 10.62197831623999988, 5.779783227492000464, 7.256572995198999898 ) ) ;
#8784=CARTESIAN_POINT ( 'NONE',  ( 10.17309652395999997, 4.709165316578000748, -8.664874001714000684 ) ) ;
#8788=B_SPLINE_CURVE_WITH_KNOTS ( 'NONE', 3,
 ( #28790, #16890, #23523, #7099 ),
 .UNSPECIFIED., .F., .F.,
 ( 4, 4 ),
 ( 0.000000000000000000, 1.000000000000000000 ),
 .UNSPECIFIED. ) ;
#8791=CARTESIAN_POINT ( 'NONE',  ( 7.790635841228000125, 3.416213390569000197, 6.162512717529000206 ) ) ;
#8792=VERTEX_POINT ( 'NONE', #63564 ) ;
#8796=CARTESIAN_POINT ( 'NONE',  ( 5.500000000000000000, -12.43893545635000031, -2.828937028792000152 ) ) ;
#8801=DIRECTION ( 'NONE',  ( 1.000000000000000000, 0.000000000000000000, 0.000000000000000000 ) ) ;
#8802=VERTEX_POINT ( 'NONE', #5867 ) ;
#8803=VECTOR ( 'NONE', #23969, 1000.000000000000000 ) ;
#8805=LINE ( 'NONE', #51111, #5767 ) ;
#8812=CARTESIAN_POINT ( 'NONE',  ( 6.999999691988000095, -12.11716380430000051, 3.069905306952000146 ) ) ;
#8813=CARTESIAN_POINT ( 'NONE',  ( 7.976886985233497818, 5.078974948772304820, 8.328785302375242949 ) ) ;
#8817=CYLINDRICAL_SURFACE ( 'NONE', #3447, 1.350000000000000533 ) ;
#8819=CARTESIAN_POINT ( 'NONE',  ( 10.64556415877000006, 2.988929467935999895, -5.952329570726999641 ) ) ;
#8822=DIRECTION ( 'NONE',  ( -1.000000000000000000, 0.000000000000000000, 0.000000000000000000 ) ) ;
#8825=FACE_OUTER_BOUND ( 'NONE', #61080, .T. ) ;
#8832=CARTESIAN_POINT ( 'NONE',  ( 7.099999886593999499, 1.243449787579999883E-13, -1.714758320200999846E-13 ) ) ;
#8833=CARTESIAN_POINT ( 'NONE',  ( 6.899999691988000450, -12.20988339176000004, 3.111064831549000154 ) ) ;
#8834=ORIENTED_EDGE ( 'NONE', *, *, #32487, .F. ) ;
#8838=LINE ( 'NONE', #30510, #57789 ) ;
#8841=CARTESIAN_POINT ( 'NONE',  ( 2.750973465876000557, -3.500000000000000000, 0.000000000000000000 ) ) ;
#8843=CARTESIAN_POINT ( 'NONE',  ( 8.057199896074001444, 2.877672799700000450, 6.732802633655004421 ) ) ;
#8844=VECTOR ( 'NONE', #45624, 1000.000000000000000 ) ;
#8846=LINE ( 'NONE', #2905, #38248 ) ;
#8847=ORIENTED_EDGE ( 'NONE', *, *, #25959, .F. ) ;
#8854=CARTESIAN_POINT ( 'NONE',  ( 8.275189158773001097, 3.061731693614000438, -8.535706278603999664 ) ) ;
#8856=ORIENTED_EDGE ( 'NONE', *, *, #66872, .F. ) ;
#8862=CARTESIAN_POINT ( 'NONE',  ( 9.848670280409999478, 5.002683760508999988, -8.912673867568997821 ) ) ;
#8865=CARTESIAN_POINT ( 'NONE',  ( 8.940795537697701079, 5.100000000000000533, 6.662590550608718409 ) ) ;
#8867=ORIENTED_EDGE ( 'NONE', *, *, #59175, .F. ) ;
#8869=( BOUNDED_SURFACE ( )  B_SPLINE_SURFACE ( 3, 3, ( 
 ( #33592, #16803, #26968, #7012, #6311, #28003, #38130, #27309, #54211 ),
 ( #11908, #11220, #54566, #59115, #48633, #48283, #389, #32557, #21705 ),
 ( #17150, #22048, #53869, #38482, #735, #54909, #59457, #28346, #5970 ),
 ( #49663, #59805, #65387, #17508, #43394, #43737, #12263, #1772, #22398 ) ),
 .UNSPECIFIED., .F., .F., .F. ) 
 B_SPLINE_SURFACE_WITH_KNOTS ( ( 4, 4 ),
 ( 4, 1, 1, 1, 1, 1, 4 ),
 ( 0.000000000000000000, 1.000000000000000000 ),
 ( -0.004644144098274999473, 0.000000000000000000, 0.03269534097185999855, 0.06255479614191999937, 0.08986301827557000022, 0.1148786485006000058, 0.1342276000085000087 ),
 .UNSPECIFIED. ) 
 GEOMETRIC_REPRESENTATION_ITEM ( )  RATIONAL_B_SPLINE_SURFACE ( (
 ( 1.157365337832999996, 1.157365337832999996, 1.157365337832999996, 1.157365337832999996, 1.157365337832999996, 1.157365337832999996, 1.157365337832999996, 1.157365337832999996, 1.157365337832999996),
 ( 0.9475448873890999213, 0.9475448873890999213, 0.9475448873890999213, 0.9475448873890999213, 0.9475448873890999213, 0.9475448873890999213, 0.9475448873890999213, 0.9475448873890999213, 0.9475448873890999213),
 ( 0.9475448873890999213, 0.9475448873890999213, 0.9475448873890999213, 0.9475448873890999213, 0.9475448873890999213, 0.9475448873890999213, 0.9475448873890999213, 0.9475448873890999213, 0.9475448873890999213),
 ( 1.157365337832999996, 1.157365337832999996, 1.157365337832999996, 1.157365337832999996, 1.157365337832999996, 1.157365337832999996, 1.157365337832999996, 1.157365337832999996, 1.157365337832999996) ) ) 
 REPRESENTATION_ITEM ( '' )  SURFACE ( )  );
#8871=CARTESIAN_POINT ( 'NONE',  ( 9.436104719595000745, 5.619431609641999614, -8.115423117607999615 ) ) ;
#8874=CARTESIAN_POINT ( 'NONE',  ( 10.27571527605999968, 5.689443924112000062, -7.562019866568999049 ) ) ;
#8876=B_SPLINE_CURVE_WITH_KNOTS ( 'NONE', 3,
 ( #57492, #41085, #56477, #30261 ),
 .UNSPECIFIED., .F., .F.,
 ( 4, 4 ),
 ( 0.000000000000000000, 1.000000000000000000 ),
 .UNSPECIFIED. ) ;
#8881=CARTESIAN_POINT ( 'NONE',  ( 9.356851002546999752, 2.832432432432000269, -6.822293592207000934 ) ) ;
#8887=DIRECTION ( 'NONE',  ( 1.000000000000000000, 0.000000000000000000, 0.000000000000000000 ) ) ;
#8891=CARTESIAN_POINT ( 'NONE',  ( 10.12947109217999930, 5.100000000000000533, 6.152188490330000370 ) ) ;
#8893=VERTEX_POINT ( 'NONE', #6903 ) ;
#8895=CARTESIAN_POINT ( 'NONE',  ( 8.929995280412999392, 5.030502105212999453, -6.322203460290999999 ) ) ;
#8903=CARTESIAN_POINT ( 'NONE',  ( 10.31746213571000048, 5.100000000000000533, 6.571291218949999902 ) ) ;
#8904=ORIENTED_EDGE ( 'NONE', *, *, #4679, .T. ) ;
#8905=CARTESIAN_POINT ( 'NONE',  ( 7.387904567572019410, 3.170618095687768090, -6.421005598970153549 ) ) ;
#8908=CARTESIAN_POINT ( 'NONE',  ( 9.099999886593998610, 3.268496584495999908E-13, 3.613587358477999789E-14 ) ) ;
#8912=CARTESIAN_POINT ( 'NONE',  ( 8.497235841230001085, 3.789127741898000057, -9.388182174781999123 ) ) ;
#8918=B_SPLINE_SURFACE_WITH_KNOTS ( 'NONE', 3, 3, ( 
 ( #3829, #31119, #52422, #4518, #25855, #68489, #20613, #63245, #34988, #56303, #24488, #45811, #19232, #40559, #61886, #14002, #35330, #56645, #43664, #6238, #15370, #27579, #58019, #26207, #36698, #37040, #11150, #58355, #10121, #69184, #64275, #26553, #47879, #21296, #10457 ),
 ( #53462, #68840, #42626, #32484, #42295, #31452, #31799, #32824, #59383, #10803, #54140, #48905, #27236, #26898, #5556, #53798, #52771, #53115, #38059, #20958, #48561, #4866, #16047, #5217, #63936, #47535, #48210, #63594, #21633, #37719, #11484, #37378, #15712, #58700, #32147 ),
 ( #1013, #16392, #42968, #317, #59047, #5895, #665, #21976, #43318, #64621, #16730, #22322, #55531, #34213, #28624, #38407, #38759, #7630, #7982, #39104, #54489, #28977, #12536, #60769, #23709, #17431, #29315, #50284, #59731, #2385, #12190, #66005, #6589, #2049, #66351 ),
 ( #49937, #64961, #45044, #18471, #39797, #60085, #11832, #61120, #33865, #55180, #33519, #13237, #33172, #60428, #17074, #27931, #17785, #7285, #23368, #34563, #55876, #44708, #18128, #44363, #39450, #49240, #28269, #22667, #12884, #65663, #50628, #1349, #44010, #65315, #2729 ) ),
 .UNSPECIFIED., .F., .F., .F.,
 ( 4, 4 ),
 ( 4, 1, 1, 1, 1, 1, 1, 1, 1, 1, 1, 1, 1, 1, 1, 1, 1, 1, 1, 1, 1, 1, 1, 1, 1, 1, 1, 1, 1, 1, 1, 1, 4 ),
 ( -0.1039370721279000015, 1.103937072127999963 ),
 ( -0.01735257130020999988, 0.01084535706264999969, 0.03904328542550000031, 0.06724121378835999641, 0.09543914215121999944, 0.1236370705141000004, 0.1518349988768999959, 0.1800329272397999947, 0.2082308556026999935, 0.2364287839655000167, 0.2646267123283999601, 0.2928246406912000110, 0.3210225690540999821, 0.3492204974169000331, 0.3774184257798000042, 0.4056163541427000307, 0.4338142825054999707, 0.4620122108683999973, 0.4902101392311999928, 0.5184080675940999638, 0.5466059959569999904, 0.5748039243197999859, 0.6030018526827000125, 0.6311997810455000080, 0.6593977094084000345, 0.6875956377712000300, 0.7157935661340999456, 0.7439914944969999722, 0.7721894228597999676, 0.8003873512226999942, 0.8285852795854999897, 0.8567832079484000163, 0.8849811363112999318 ),
 .UNSPECIFIED. ) ;
#8919=DIRECTION ( 'NONE',  ( 1.000000000000000000, 0.000000000000000000, 0.000000000000000000 ) ) ;
#8920=CARTESIAN_POINT ( 'NONE',  ( 3.401112454814999797, -2.565134483810000088, 2.270441050239000003 ) ) ;
#8924=CYLINDRICAL_SURFACE ( 'NONE', #8602, 0.4999999999999998335 ) ;
#8927=ORIENTED_EDGE ( 'NONE', *, *, #19754, .T. ) ;
#8928=PLANE ( 'NONE',  #67887 ) ;
#8930=CARTESIAN_POINT ( 'NONE',  ( 10.96729999554885282, 8.729492799572236450, 6.507753220594684862 ) ) ;
#8933=CARTESIAN_POINT ( 'NONE',  ( 7.808141753486895986, 2.638822403986486265, -7.614799956045625429 ) ) ;
#8942=CARTESIAN_POINT ( 'NONE',  ( 8.404999999999999361, 5.190914425723000214, -8.768195054477999406 ) ) ;
#8944=CARTESIAN_POINT ( 'NONE',  ( 7.631379719587999766, 5.256485075641999849, -6.567055966373000153 ) ) ;
#8945=DIRECTION ( 'NONE',  ( 0.8660254037844289376, 0.000000000000000000, -0.5000000000000169864 ) ) ;
#8952=LINE ( 'NONE', #30293, #24740 ) ;
#8955=FACE_OUTER_BOUND ( 'NONE', #55282, .T. ) ;
#8956=CARTESIAN_POINT ( 'NONE',  ( 7.100000000000000533, 5.350000000000000533, -7.500000000000000000 ) ) ;
#8964=CARTESIAN_POINT ( 'NONE',  ( 9.869051220224999810, 5.575171928796999410, 7.724300137354000562 ) ) ;
#8965=AXIS2_PLACEMENT_3D ( 'NONE', #32511, #11862, #53827 ) ;
#8967=CARTESIAN_POINT ( 'NONE',  ( 9.327795280414001411, 3.161445734422999809, -6.178649910536000434 ) ) ;
#8968=CARTESIAN_POINT ( 'NONE',  ( 3.348254627038999676, 1.687100406436000011, -3.116347325074999564 ) ) ;
#8972=B_SPLINE_CURVE_WITH_KNOTS ( 'NONE', 3,
 ( #41048, #10947, #805, #53936 ),
 .UNSPECIFIED., .F., .F.,
 ( 4, 4 ),
 ( 0.000000000000000000, 1.000000000000000000 ),
 .UNSPECIFIED. ) ;
#8975=CARTESIAN_POINT ( 'NONE',  ( 10.35911162173837319, 5.698273092209690915, -7.916014385706306555 ) ) ;
#8978=CARTESIAN_POINT ( 'NONE',  ( 10.93227693248999977, 2.539877577705000000, 6.453611809651000009 ) ) ;
#8991=LINE ( 'NONE', #35910, #52817 ) ;
#8995=CARTESIAN_POINT ( 'NONE',  ( 0.2387948408026999980, 3.161455490150999914, -0.5535149012972000460 ) ) ;
#8997=CARTESIAN_POINT ( 'NONE',  ( 11.03905471959000018, 3.855072614532999875, -9.179480010827999692 ) ) ;
#9000=FACE_OUTER_BOUND ( 'NONE', #23145, .T. ) ;
#9003=CARTESIAN_POINT ( 'NONE',  ( 9.766851002543001314, 2.832432432432000269, 6.822293592207000934 ) ) ;
#9006=CARTESIAN_POINT ( 'NONE',  ( 6.970189158770000226, 3.332350081667999842, -9.278694849147001378 ) ) ;
#9015=ORIENTED_EDGE ( 'NONE', *, *, #68558, .F. ) ;
#9025=CARTESIAN_POINT ( 'NONE',  ( 9.041948341230998665, 2.707986230053999854, 5.994446745591000436 ) ) ;
#9029=CARTESIAN_POINT ( 'NONE',  ( 7.315000000000000391, 2.649999999999999911, -7.500000000000000000 ) ) ;
#9034=CARTESIAN_POINT ( 'NONE',  ( 8.644512467439003700, 8.815297989570002102, -6.028160447578001957 ) ) ;
#9042=VERTEX_POINT ( 'NONE', #26397 ) ;
#9046=CARTESIAN_POINT ( 'NONE',  ( 8.999999001754000361, 0.000000000000000000, 0.000000000000000000 ) ) ;
#9048=CARTESIAN_POINT ( 'NONE',  ( 9.870875237110999123, 2.904361819252000210, -8.563871667095998674 ) ) ;
#9049=AXIS2_PLACEMENT_3D ( 'NONE', #9046, #51359, #2776 ) ;
#9052=EDGE_CURVE ( 'NONE', #18020, #66620, #56809, .T. ) ;
#9055=CARTESIAN_POINT ( 'NONE',  ( 11.02786554143000153, 5.596226216413000110, 7.209502215883999199 ) ) ;
#9056=AXIS2_PLACEMENT_3D ( 'NONE', #60748, #61440, #13560 ) ;
#9058=ORIENTED_EDGE ( 'NONE', *, *, #37888, .F. ) ;
#9061=CARTESIAN_POINT ( 'NONE',  ( 9.667078842372998082, 4.541623431405000133, 5.824038024834000460 ) ) ;
#9063=CARTESIAN_POINT ( 'NONE',  ( 8.821685841230998193, 2.633142096252999664, -7.791134854666999843 ) ) ;
#9064=DIRECTION ( 'NONE',  ( 0.000000000000000000, 1.000000000000000000, 0.000000000000000000 ) ) ;
#9067=CARTESIAN_POINT ( 'NONE',  ( 7.647239158771000689, 5.850290547079999293, 6.784176679236000318 ) ) ;
#9068=CARTESIAN_POINT ( 'NONE',  ( 9.104014120666999332, 5.045862207587999748, 8.527865280865999154 ) ) ;
#9071=CARTESIAN_POINT ( 'NONE',  ( 9.974220280410998285, 5.496789211521000418, -7.043125396300999874 ) ) ;
#9072=CARTESIAN_POINT ( 'NONE',  ( -0.000000000000000000, -2.899969545325999931, 0.3811992978302040092 ) ) ;
#9076=CARTESIAN_POINT ( 'NONE',  ( 9.924988015501618577, 5.349815781279066762, 7.500001845592777272 ) ) ;
#9080=EDGE_CURVE ( 'NONE', #51168, #9263, #34078, .T. ) ;
#9081=CARTESIAN_POINT ( 'NONE',  ( 1.682156054532000011, -3.591455136169999562, 0.07279325410826999188 ) ) ;
#9083=CARTESIAN_POINT ( 'NONE',  ( 9.319414158774000256, 2.656512020013999997, -7.884832994446999699 ) ) ;
#9092=CARTESIAN_POINT ( 'NONE',  ( 7.545267219589999463, 2.302289264429000504, 6.875166305059000393 ) ) ;
#9097=CARTESIAN_POINT ( 'NONE',  ( 1.409474105092999974, -2.789116823352000285, 1.988880583162999871 ) ) ;
#9099=CARTESIAN_POINT ( 'NONE',  ( 0.9525933052797602718, -1.981538156914185667, 2.642344845388179486 ) ) ;
#9103=CARTESIAN_POINT ( 'NONE',  ( 10.42596030538999941, 5.042177533603999784, 8.702224267793999601 ) ) ;
#9105=CARTESIAN_POINT ( 'NONE',  ( 9.702711596877973577, 5.100000000000000533, 6.305985889537642386 ) ) ;
#9107=CARTESIAN_POINT ( 'NONE',  ( 5.399999732039999500, 13.10000000000000142, 0.000000000000000000 ) ) ;
#9108=CARTESIAN_POINT ( 'NONE',  ( 8.453783575583390331, 2.251044692578384687, 7.420277725347735220 ) ) ;
#9112=ORIENTED_EDGE ( 'NONE', *, *, #19795, .T. ) ;
#9116=CARTESIAN_POINT ( 'NONE',  ( 8.220491111160100672, 2.863432725431082737, 6.768885602738127893 ) ) ;
#9119=CARTESIAN_POINT ( 'NONE',  ( 10.37373942323999998, 2.215265813302000009, 7.703982730183001060 ) ) ;
#9120=CARTESIAN_POINT ( 'NONE',  ( 10.33022126302999943, 2.650190549566000087, -7.694579890082000162 ) ) ;
#9126=CARTESIAN_POINT ( 'NONE',  ( 8.304135841228999837, 3.650414032626000171, 6.083147621602999600 ) ) ;
#9127=ORIENTED_EDGE ( 'NONE', *, *, #29338, .T. ) ;
#9132=CARTESIAN_POINT ( 'NONE',  ( 8.374301491561006117, 10.15552111561999915, 5.491315164875996579 ) ) ;
#9143=DIRECTION ( 'NONE',  ( 1.000000000000000000, 0.000000000000000000, 0.000000000000000000 ) ) ;
#9147=CARTESIAN_POINT ( 'NONE',  ( 0.3100461241979999838, -2.634961698279000064, 2.360490016663000290 ) ) ;
#9153=B_SPLINE_CURVE_WITH_KNOTS ( 'NONE', 3,
 ( #7423, #34358, #2190, #50422, #43804, #65100, #17223, #38548, #3890, #14060 ),
 .UNSPECIFIED., .F., .F.,
 ( 4, 2, 2, 2, 4 ),
 ( 0.000000000000000000, 0.2500000000000000000, 0.5000000000000000000, 0.7500000000000000000, 1.000000000000000000 ),
 .UNSPECIFIED. ) ;
#9167=DIRECTION ( 'NONE',  ( -1.000000000000000000, 0.000000000000000000, 0.000000000000000000 ) ) ;
#9175=CARTESIAN_POINT ( 'NONE',  ( 2.605140132542667075, 0.9161175952574701631, 3.408904368339106927 ) ) ;
#9183=CARTESIAN_POINT ( 'NONE',  ( 11.09999999991999964, 8.127394258944999450, 6.728184650804999833 ) ) ;
#9184=CARTESIAN_POINT ( 'NONE',  ( 2.946806799211333594, 0.9161175952574844850, -3.408904368339102930 ) ) ;
#9185=CARTESIAN_POINT ( 'NONE',  ( 8.722714158775000115, 3.892978337449999771, -8.893414073324001023 ) ) ;
#9187=ORIENTED_EDGE ( 'NONE', *, *, #55258, .F. ) ;
#9191=DIRECTION ( 'NONE',  ( 1.000000000000000000, 0.000000000000000000, 0.000000000000000000 ) ) ;
#9197=FACE_OUTER_BOUND ( 'NONE', #28755, .T. ) ;
#9200=CARTESIAN_POINT ( 'NONE',  ( 9.476970280414001024, 5.511689883260999956, -7.095113581311000672 ) ) ;
#9202=CARTESIAN_POINT ( 'NONE',  ( 10.52343057594999998, 3.209665745824000105, -9.177097971982000502 ) ) ;
#9204=ORIENTED_EDGE ( 'NONE', *, *, #60921, .F. ) ;
#9209=ADVANCED_FACE ( 'NONE', ( #41710 ), #42288, .T. ) ;
#9214=ORIENTED_EDGE ( 'NONE', *, *, #5437, .T. ) ;
#9215=CARTESIAN_POINT ( 'NONE',  ( 10.27706886429732158, 2.899999999999999911, -6.444141223373538452 ) ) ;
#9216=CARTESIAN_POINT ( 'NONE',  ( 10.53871084122999946, 5.103389446345000025, -6.705205355781999721 ) ) ;
#9224=CARTESIAN_POINT ( 'NONE',  ( 9.128895280414001334, 3.880154689736000417, -9.060377011187000562 ) ) ;
#9227=CARTESIAN_POINT ( 'NONE',  ( 1.071806799208249839, 3.408904368339104263, 0.9161175952574878156 ) ) ;
#9232=CARTESIAN_POINT ( 'NONE',  ( 7.777243094059180351, 3.624681904425790968, 6.194791476713995770 ) ) ;
#9235=VECTOR ( 'NONE', #53368, 1000.000000000000000 ) ;
#9239=DIRECTION ( 'NONE',  ( -0.8987684456439055669, 0.000000000000000000, 0.4384236320214022764 ) ) ;
#9241=DIRECTION ( 'NONE',  ( 0.000000000000000000, 0.000000000000000000, -1.000000000000000000 ) ) ;
#9242=CARTESIAN_POINT ( 'NONE',  ( 9.093935841232999806, 2.156584729807999867, -7.959751745006000689 ) ) ;
#9248=CARTESIAN_POINT ( 'NONE',  ( 3.210384657052000268, 3.424905925778999993, 0.06955616133957001623 ) ) ;
#9249=EDGE_LOOP ( 'NONE', ( #48750, #45665, #35548, #3055 ) ) ;
#9252=ADVANCED_FACE ( 'NONE', ( #33985 ), #53912, .F. ) ;
#9253=DIRECTION ( 'NONE',  ( 0.000000000000000000, -0.7071067811865474617, -0.7071067811865474617 ) ) ;
#9257=LINE ( 'NONE', #52263, #58959 ) ;
#9263=VERTEX_POINT ( 'NONE', #16849 ) ;
#9265=ORIENTED_EDGE ( 'NONE', *, *, #55405, .F. ) ;
#9270=CARTESIAN_POINT ( 'NONE',  ( 8.547797334239181311, 2.488073269087734296, -8.392070911480191242 ) ) ;
#9271=CARTESIAN_POINT ( 'NONE',  ( 7.619022079480754606, 2.947662252026352459, 8.377606513860623494 ) ) ;
#9272=CARTESIAN_POINT ( 'NONE',  ( 7.142989158770000735, 5.116254232901999544, -8.340852485897000790 ) ) ;
#9275=ORIENTED_EDGE ( 'NONE', *, *, #67301, .F. ) ;
#9276=CARTESIAN_POINT ( 'NONE',  ( 2.230140132540584297, -3.408904368339107815, 0.9161175952574674985 ) ) ;
#9277=B_SPLINE_CURVE_WITH_KNOTS ( 'NONE', 3,
 ( #22225, #7881, #51217, #55778, #45292 ),
 .UNSPECIFIED., .F., .F.,
 ( 4, 1, 4 ),
 ( 0.000000000000000000, 0.5000000000000000000, 1.000000000000000000 ),
 .UNSPECIFIED. ) ;
#9280=DIRECTION ( 'NONE',  ( 0.000000000000000000, 0.000000000000000000, 1.000000000000000000 ) ) ;
#9283=AXIS2_PLACEMENT_3D ( 'NONE', #44615, #43213, #57394 ) ;
#9285=B_SPLINE_CURVE_WITH_KNOTS ( 'NONE', 3,
 ( #16895, #38224, #5716, #59204, #16209, #10970, #26368 ),
 .UNSPECIFIED., .F., .F.,
 ( 4, 1, 1, 1, 4 ),
 ( 0.000000000000000000, 0.2500000590475000006, 0.5000000002693999468, 0.7499999414914000351, 1.000000000000000000 ),
 .UNSPECIFIED. ) ;
#9290=FACE_OUTER_BOUND ( 'NONE', #29011, .T. ) ;
#9296=ORIENTED_EDGE ( 'NONE', *, *, #66539, .F. ) ;
#9297=CARTESIAN_POINT ( 'NONE',  ( 3.300973465876999580, -3.500000000000000000, 0.000000000000000000 ) ) ;
#9298=ORIENTED_EDGE ( 'NONE', *, *, #15779, .T. ) ;
#9299=CARTESIAN_POINT ( 'NONE',  ( 10.01533268956000100, 4.946987614118000032, 8.559212393557999121 ) ) ;
#9301=DIRECTION ( 'NONE',  ( -1.000000000000000000, 0.000000000000000000, 0.000000000000000000 ) ) ;
#9302=CARTESIAN_POINT ( 'NONE',  ( 8.640504719592000171, 2.305580295895999665, -7.860904109308999743 ) ) ;
#9303=CARTESIAN_POINT ( 'NONE',  ( 3.599756407902999999, -1.745607925010999928, 3.083988108660999927 ) ) ;
#9307=ORIENTED_EDGE ( 'NONE', *, *, #44625, .T. ) ;
#9309=CARTESIAN_POINT ( 'NONE',  ( 10.26947109217999810, 5.100000000000000533, -6.152188490330000370 ) ) ;
#9311=EDGE_CURVE ( 'NONE', #20987, #19641, #18221, .T. ) ;
#9313=CARTESIAN_POINT ( 'NONE',  ( 9.166073843917999397, 4.023333628930999772, 9.122276991855001071 ) ) ;
#9321=CARTESIAN_POINT ( 'NONE',  ( 0.4755637383194235568, 3.469857622234496120, -0.4961820259388217691 ) ) ;
#9327=CIRCLE ( 'NONE', #68515, 12.39999890530000037 ) ;
#9328=CARTESIAN_POINT ( 'NONE',  ( 0.7323805749852000391, 2.971343835407000089, -0.7711576440234000351 ) ) ;
#9330=CARTESIAN_POINT ( 'NONE',  ( 10.48598278040999965, 5.506034726153999692, -7.274787238512000265 ) ) ;
#9338=ORIENTED_EDGE ( 'NONE', *, *, #3732, .T. ) ;
#9347=ORIENTED_EDGE ( 'NONE', *, *, #23348, .T. ) ;
#9357=CARTESIAN_POINT ( 'NONE',  ( 8.913573341230998537, 2.550580605805000012, 8.854682662413999594 ) ) ;
#9366=CARTESIAN_POINT ( 'NONE',  ( 8.842615099866989681, 7.893622066425994177, -5.162893036762002730 ) ) ;
#9376=EDGE_LOOP ( 'NONE', ( #18571, #14377, #32930, #25442, #66746 ) ) ;
#9382=CARTESIAN_POINT ( 'NONE',  ( 7.996487690580179830, 5.313957503662987136, 7.853744048643257258 ) ) ;
#9383=CARTESIAN_POINT ( 'NONE',  ( 10.74708949327000163, 5.603142351927999698, -6.963341971584000589 ) ) ;
#9386=CYLINDRICAL_SURFACE ( 'NONE', #13818, 0.5000000000000004441 ) ;
#9387=CARTESIAN_POINT ( 'NONE',  ( 10.34520858566999912, 2.724123081339000052, 6.497325124886000225 ) ) ;
#9392=CARTESIAN_POINT ( 'NONE',  ( 10.44675156161000018, 2.885046387990999772, 8.863482298832000339 ) ) ;
#9395=B_SPLINE_CURVE_WITH_KNOTS ( 'NONE', 3,
 ( #38536, #60214, #59860, #28056, #33650, #1829, #17915, #49719, #39232, #23146, #44496, #35376, #67512, #13707, #28759, #24184, #51442, #13367 ),
 .UNSPECIFIED., .F., .F.,
 ( 4, 1, 2, 2, 1, 2, 2, 2, 2, 4 ),
 ( 0.000000000000000000, 0.1249999999999908962, 0.1874999999999859557, 0.2499999999999810152, 0.3749999999999767963, 0.4374999999999779066, 0.4999999999999790168, 0.6249999999999841238, 0.7499999999999892308, 1.000000000000000000 ),
 .UNSPECIFIED. ) ;
#9396=CARTESIAN_POINT ( 'NONE',  ( 8.622785841227999626, 5.189036231907000030, -8.048606212067999977 ) ) ;
#9397=CARTESIAN_POINT ( 'NONE',  ( 11.07072899110000108, 7.292403078108999459, -6.230988430885999740 ) ) ;
#9403=CARTESIAN_POINT ( 'NONE',  ( 10.59344747867000081, 5.297752619853000944, 8.474195539311001113 ) ) ;
#9405=VERTEX_POINT ( 'NONE', #65076 ) ;
#9406=CARTESIAN_POINT ( 'NONE',  ( 9.286929719595001131, 4.102804347295999854, -5.770625657082999460 ) ) ;
#9407=CARTESIAN_POINT ( 'NONE',  ( -0.000000000000000000, 1.781870588985605464, 2.319407620233724820 ) ) ;
#9413=CARTESIAN_POINT ( 'NONE',  ( 2.297248059201999482, -3.604362431180999859, -1.066289260138999939 ) ) ;
#9420=FACE_OUTER_BOUND ( 'NONE', #39938, .T. ) ;
#9426=CARTESIAN_POINT ( 'NONE',  ( 8.893204719592999297, 3.977267228909999730, 9.308925224542001331 ) ) ;
#9428=CARTESIAN_POINT ( 'NONE',  ( 10.91194340358000048, 5.022355073325999619, 4.912227978166000320 ) ) ;
#9432=CARTESIAN_POINT ( 'NONE',  ( 0.7848354242999000530, 3.204751743350000126, -0.5916681129576000231 ) ) ;
#9433=ORIENTED_EDGE ( 'NONE', *, *, #722, .T. ) ;
#9434=CYLINDRICAL_SURFACE ( 'NONE', #28852, 1.999999999999999778 ) ;
#9437=CARTESIAN_POINT ( 'NONE',  ( 11.29622358543999994, 3.561657733933999648, 6.266050246368000565 ) ) ;
#9448=FACE_OUTER_BOUND ( 'NONE', #3624, .T. ) ;
#9451=CARTESIAN_POINT ( 'NONE',  ( 8.199995020667000034, 2.894508905068999827, 6.645190348705000360 ) ) ;
#9452=AXIS2_PLACEMENT_3D ( 'NONE', #53334, #48774, #32021 ) ;
#9454=CARTESIAN_POINT ( 'NONE',  ( 9.104014120666999332, 5.045862207587999748, 8.527865280865999154 ) ) ;
#9455=CARTESIAN_POINT ( 'NONE',  ( 10.11859053700000111, 3.393394511985999618, -5.921995869926000466 ) ) ;
#9461=ADVANCED_FACE ( 'NONE', ( #35363 ), #16513, .T. ) ;
#9462=CARTESIAN_POINT ( 'NONE',  ( 7.598073341229000022, 3.554857159507999853, 8.889479859586000288 ) ) ;
#9463=EDGE_CURVE ( 'NONE', #39016, #53063, #29095, .T. ) ;
#9474=LINE ( 'NONE', #63646, #64930 ) ;
#9475=CARTESIAN_POINT ( 'NONE',  ( 10.90000000000000036, 0.2999999999999999889, 4.902439024389999567 ) ) ;
#9478=CARTESIAN_POINT ( 'NONE',  ( 6.899999691988000450, -12.43893545635000031, -2.828937028792000152 ) ) ;
#9483=EDGE_CURVE ( 'NONE', #28703, #29686, #30458, .T. ) ;
#9486=CARTESIAN_POINT ( 'NONE',  ( -0.1096015927428999892, -0.5648807336705999882, -3.658284285490000176 ) ) ;
#9492=CARTESIAN_POINT ( 'NONE',  ( 11.16750778041000025, 3.188704589882000118, -8.788663768996000769 ) ) ;
#9494=CARTESIAN_POINT ( 'NONE',  ( 10.14577299472025551, 2.689531466963051454, 7.995537948248067295 ) ) ;
#9496=B_SPLINE_CURVE_WITH_KNOTS ( 'NONE', 3,
 ( #22364, #1390, #42062, #46964, #44050 ),
 .UNSPECIFIED., .F., .F.,
 ( 4, 1, 4 ),
 ( 0.000000000000000000, 0.5000000000000000000, 1.000000000000000000 ),
 .UNSPECIFIED. ) ;
#9497=CARTESIAN_POINT ( 'NONE',  ( 10.11501430098066656, 5.350017391163124358, -7.499999134156894343 ) ) ;
#9500=CARTESIAN_POINT ( 'NONE',  ( 7.763719363403000173, 2.858336808333000079, 6.771132197038999934 ) ) ;
#9518=ADVANCED_FACE ( 'NONE', ( #55653 ), #27993, .T. ) ;
#9524=CARTESIAN_POINT ( 'NONE',  ( 4.950033214355999966, 0.000000000000000000, 0.000000000000000000 ) ) ;
#9528=CARTESIAN_POINT ( 'NONE',  ( 8.323770280408998801, 5.332332124071999857, -8.487089944253000340 ) ) ;
#9536=CARTESIAN_POINT ( 'NONE',  ( 4.149992563291999836, -1.947893036340040629, -0.5234817089163749104 ) ) ;
#9537=CARTESIAN_POINT ( 'NONE',  ( 9.857732874095237463, 2.650112054261821726, -7.624707679117006975 ) ) ;
#9544=CARTESIAN_POINT ( 'NONE',  ( 9.924495280410999598, 4.946705552514000459, -6.253848946732999181 ) ) ;
#9545=ADVANCED_FACE ( 'NONE', ( #23050 ), #31859, .F. ) ;
#9547=VECTOR ( 'NONE', #40057, 1000.000000000000000 ) ;
#9548=CARTESIAN_POINT ( 'NONE',  ( 10.98277660187000215, 2.518725482848000130, -8.314790074023999722 ) ) ;
#9555=CARTESIAN_POINT ( 'NONE',  ( 5.500000000000000000, 11.00717859340000082, -1.432487142323000118 ) ) ;
#9556=B_SPLINE_CURVE_WITH_KNOTS ( 'NONE', 3,
 ( #5997, #59486, #6694, #1457, #43769, #53897, #26658, #17182, #53215, #59834 ),
 .UNSPECIFIED., .F., .F.,
 ( 4, 2, 2, 2, 4 ),
 ( 0.000000000000000000, 0.1482977669950275301, 0.2224466504925418642, 0.2595210922412991561, 0.2965955339900564480 ),
 .UNSPECIFIED. ) ;
#9557=CYLINDRICAL_SURFACE ( 'NONE', #29092, 0.4999999999999998335 ) ;
#9561=DIRECTION ( 'NONE',  ( -1.000000000000000000, 0.000000000000000000, 0.000000000000000000 ) ) ;
#9569=ORIENTED_EDGE ( 'NONE', *, *, #4079, .F. ) ;
#9570=CARTESIAN_POINT ( 'NONE',  ( 9.865910841232000905, 2.685250982074999904, -7.026194612421999608 ) ) ;
#9572=CARTESIAN_POINT ( 'NONE',  ( 6.899999691988000450, -13.10000000000000142, 0.000000000000000000 ) ) ;
#9577=CARTESIAN_POINT ( 'NONE',  ( 7.827627258077122008, 4.479918276951376122, 6.205276188899031098 ) ) ;
#9587=CYLINDRICAL_SURFACE ( 'NONE', #823, 11.35000000000000142 ) ;
#9590=AXIS2_PLACEMENT_3D ( 'NONE', #39901, #18574, #3507 ) ;
#9592=CARTESIAN_POINT ( 'NONE',  ( 9.202182965154774408, 2.714244241234048616, 7.027734220012949784 ) ) ;
#9593=CARTESIAN_POINT ( 'NONE',  ( 0.1499942179680000265, -2.402872127494064536, -1.384928887584821133 ) ) ;
#9594=CARTESIAN_POINT ( 'NONE',  ( 3.353430505373999893, -0.8378046959084999301, 3.321581098373000529 ) ) ;
#9596=EDGE_CURVE ( 'NONE', #54370, #68077, #50794, .T. ) ;
#9597=EDGE_CURVE ( 'NONE', #25656, #49930, #6569, .T. ) ;
#9609=CARTESIAN_POINT ( 'NONE',  ( 7.801010157780201126, 2.973106524567316278, 6.575014448996248539 ) ) ;
#9613=EDGE_LOOP ( 'NONE', ( #8576, #85, #22098, #5763, #39661, #33629, #21717, #53218, #32869, #42767, #63276, #15 ) ) ;
#9617=ORIENTED_EDGE ( 'NONE', *, *, #46115, .T. ) ;
#9619=CARTESIAN_POINT ( 'NONE',  ( 7.965270188005331597, 3.582163548059296598, -6.202867177960278866 ) ) ;
#9620=CARTESIAN_POINT ( 'NONE',  ( 8.070045280407001087, 2.564091104321999826, -6.530737592441999695 ) ) ;
#9628=CARTESIAN_POINT ( 'NONE',  ( 9.179055905797000037, 2.899999999999999911, 6.571291218949999902 ) ) ;
#9629=B_SPLINE_CURVE_WITH_KNOTS ( 'NONE', 3,
 ( #29350, #23740, #7313, #39830, #61151 ),
 .UNSPECIFIED., .F., .F.,
 ( 4, 1, 4 ),
 ( 0.000000000000000000, 0.5000000000000000000, 1.000000000000000000 ),
 .UNSPECIFIED. ) ;
#9630=CARTESIAN_POINT ( 'NONE',  ( 9.082700812465912321, 2.899999999999999911, -6.316220168737575413 ) ) ;
#9633=CARTESIAN_POINT ( 'NONE',  ( 10.69357525437983725, 5.769078639290308175, 7.350227077746113835 ) ) ;
#9640=CARTESIAN_POINT ( 'NONE',  ( 8.455992358796999397, 5.100000000000000533, 6.571291218954000257 ) ) ;
#9641=VERTEX_POINT ( 'NONE', #18513 ) ;
#9644=CARTESIAN_POINT ( 'NONE',  ( 9.532678149083000818, 4.663044775770000427, 8.669813205957000335 ) ) ;
#9646=AXIS2_PLACEMENT_3D ( 'NONE', #1438, #11565, #39189 ) ;
#9648=CARTESIAN_POINT ( 'NONE',  ( 2.593749284444999859, -1.508056830049999908, 3.206819776970000202 ) ) ;
#9651=CARTESIAN_POINT ( 'NONE',  ( 8.082873386424997975, 5.111739203374999541, -6.679001318365999751 ) ) ;
#9654=EDGE_CURVE ( 'NONE', #36055, #66683, #19186, .T. ) ;
#9656=CARTESIAN_POINT ( 'NONE',  ( 10.52204676658863391, 2.851933436354328499, -8.818745687284273771 ) ) ;
#9660=CARTESIAN_POINT ( 'NONE',  ( 8.100000113405998903, 12.39999890530000037, 0.000000000000000000 ) ) ;
#9668=EDGE_LOOP ( 'NONE', ( #57220, #67380, #19225, #7912 ) ) ;
#9670=B_SPLINE_CURVE_WITH_KNOTS ( 'NONE', 3,
 ( #30520, #58117, #3928, #67910 ),
 .UNSPECIFIED., .F., .F.,
 ( 4, 4 ),
 ( 0.000000000000000000, 1.000000000000000000 ),
 .UNSPECIFIED. ) ;
#9671=CARTESIAN_POINT ( 'NONE',  ( 4.000000000000000000, 2.149963194831999491, -0.2827069376517958310 ) ) ;
#9675=CARTESIAN_POINT ( 'NONE',  ( 0.1153984072571000025, -0.4897778999536001043, -3.171902824723000336 ) ) ;
#9676=AXIS2_PLACEMENT_3D ( 'NONE', #40345, #19020, #18341 ) ;
#9678=CARTESIAN_POINT ( 'NONE',  ( 9.978904719591000116, 5.007782080444000528, -8.772599239991000886 ) ) ;
#9681=CARTESIAN_POINT ( 'NONE',  ( 8.623777853204000365, 5.100000000000000533, -6.534061169358333920 ) ) ;
#9686=CARTESIAN_POINT ( 'NONE',  ( 8.977760841230999489, 2.019067547072999957, 7.390982789861999969 ) ) ;
#9690=ADVANCED_FACE ( 'NONE', ( #61157 ), #66031, .F. ) ;
#9691=CARTESIAN_POINT ( 'NONE',  ( 7.467439158767000151, 3.394203523730999539, -9.300711568980998933 ) ) ;
#9693=AXIS2_PLACEMENT_3D ( 'NONE', #19233, #56304, #35670 ) ;
#9695=ORIENTED_EDGE ( 'NONE', *, *, #10872, .F. ) ;
#9701=ORIENTED_EDGE ( 'NONE', *, *, #2438, .T. ) ;
#9708=CARTESIAN_POINT ( 'NONE',  ( 7.346670280409000497, 2.374037589774999901, 8.293392681990997772 ) ) ;
#9711=CARTESIAN_POINT ( 'NONE',  ( 3.500000000000000000, -3.033011252059000018, -1.020217008720000207 ) ) ;
#9716=CARTESIAN_POINT ( 'NONE',  ( 7.245144510450004738, 10.37974071282999411, -4.936574216131997872 ) ) ;
#9728=CARTESIAN_POINT ( 'NONE',  ( 10.51140238467000110, 2.326714339996000191, -7.741210149842999932 ) ) ;
#9729=CARTESIAN_POINT ( 'NONE',  ( 8.664497909817340471, 5.045291088815394787, 6.188051271826346067 ) ) ;
#9734=CARTESIAN_POINT ( 'NONE',  ( 9.634020792350998619, 3.042978295541999945, 8.588098960242001922 ) ) ;
#9735=ORIENTED_EDGE ( 'NONE', *, *, #28774, .T. ) ;
#9738=CARTESIAN_POINT ( 'NONE',  ( 9.127723954448535792, 2.415158738379607595, -6.695780460953873359 ) ) ;
#9742=CARTESIAN_POINT ( 'NONE',  ( 10.72520610419000064, 5.521650664120000940, 6.612990918765000004 ) ) ;
#9744=CARTESIAN_POINT ( 'NONE',  ( 5.399998984437000438, 12.99045401563999924, 1.690592933733000125 ) ) ;
#9747=FACE_OUTER_BOUND ( 'NONE', #59032, .T. ) ;
#9750=CARTESIAN_POINT ( 'NONE',  ( 10.96291115433076868, 5.162911154333786889, -6.648309209566408917 ) ) ;
#9753=ORIENTED_EDGE ( 'NONE', *, *, #61642, .T. ) ;
#9754=CARTESIAN_POINT ( 'NONE',  ( 9.228345280414000484, 2.481540185810000132, -7.878707153279001396 ) ) ;
#9755=DIRECTION ( 'NONE',  ( 0.000000000000000000, 1.000000000000000000, 0.000000000000000000 ) ) ;
#9761=CARTESIAN_POINT ( 'NONE',  ( 2.397385296146999689, 3.036063727655999855, -1.493670828108000004 ) ) ;
#9762=CARTESIAN_POINT ( 'NONE',  ( 7.822385841228999048, 4.636729845879000500, 9.378977473003999421 ) ) ;
#9766=ORIENTED_EDGE ( 'NONE', *, *, #31012, .T. ) ;
#9771=FACE_OUTER_BOUND ( 'NONE', #20522, .T. ) ;
#9773=ORIENTED_EDGE ( 'NONE', *, *, #35829, .T. ) ;
#9774=CARTESIAN_POINT ( 'NONE',  ( 7.518864158771000561, 3.206360348473000332, 5.681727837477000165 ) ) ;
#9782=B_SPLINE_CURVE_WITH_KNOTS ( 'NONE', 3,
 ( #24328, #57163, #45661, #66967, #40401, #19073, #61723, #13843, #29939, #51243, #24672, #25350, #67993, #45992, #62745, #67305, #19421, #30269 ),
 .UNSPECIFIED., .F., .F.,
 ( 4, 2, 2, 2, 2, 2, 2, 2, 4 ),
 ( 0.000000000000000000, 0.1250000000000000000, 0.2500000000000000000, 0.3750000000000000000, 0.5000000000000000000, 0.6250000000000000000, 0.7500000000000000000, 0.8750000000000000000, 1.000000000000000000 ),
 .UNSPECIFIED. ) ;
#9784=CARTESIAN_POINT ( 'NONE',  ( 1.953914243537261619, -2.025123852575706707, 2.609090518642736889 ) ) ;
#9786=CARTESIAN_POINT ( 'NONE',  ( 9.843732751558000871, 4.115124343450999866, 9.466620196856998959 ) ) ;
#9787=CARTESIAN_POINT ( 'NONE',  ( 9.260906466624998501, 4.901388651757999426, 9.090324495507999814 ) ) ;
#9801=ADVANCED_FACE ( 'NONE', ( #1303 ), #6189, .T. ) ;
#9806=CARTESIAN_POINT ( 'NONE',  ( 10.74609776273999984, 4.263105564403999459, 9.276980853981999786 ) ) ;
#9807=CARTESIAN_POINT ( 'NONE',  ( 10.00074698269999907, 2.373893144840999891, -7.962435130300000274 ) ) ;
#9815=ORIENTED_EDGE ( 'NONE', *, *, #60490, .T. ) ;
#9816=B_SPLINE_CURVE_WITH_KNOTS ( 'NONE', 3,
 ( #2055, #22328, #16736, #60091, #49596 ),
 .UNSPECIFIED., .F., .F.,
 ( 4, 1, 4 ),
 ( 0.000000000000000000, 0.5000000000000000000, 1.000000000000000000 ),
 .UNSPECIFIED. ) ;
#9817=CARTESIAN_POINT ( 'NONE',  ( 11.09999999999999964, 4.000000000000000000, 7.500000000000000000 ) ) ;
#9818=CARTESIAN_POINT ( 'NONE',  ( 8.957462135714999718, 5.100000000000000533, -6.571291218949999902 ) ) ;
#9829=CARTESIAN_POINT ( 'NONE',  ( 8.200000304434999165, 12.49999969551000056, -3.568532357647000425E-10 ) ) ;
#9842=CARTESIAN_POINT ( 'NONE',  ( 7.805976048735002948, 2.918573024645998881, -6.499545638216004839 ) ) ;
#9843=CARTESIAN_POINT ( 'NONE',  ( 11.01605778040999972, 5.482856203356999636, -7.846408531951999166 ) ) ;
#9845=CARTESIAN_POINT ( 'NONE',  ( 9.991933421518185199, 4.976296783332229801, 8.591994908148388177 ) ) ;
#9847=LINE ( 'NONE', #58429, #60950 ) ;
#9848=ORIENTED_EDGE ( 'NONE', *, *, #63517, .F. ) ;
#9854=VECTOR ( 'NONE', #49171, 999.9999999999998863 ) ;
#9861=EDGE_CURVE ( 'NONE', #59329, #9965, #18735, .T. ) ;
#9879=B_SPLINE_CURVE_WITH_KNOTS ( 'NONE', 3,
 ( #3970, #2021, #35471, #8891 ),
 .UNSPECIFIED., .F., .F.,
 ( 4, 4 ),
 ( 0.000000000000000000, 1.000000000000000000 ),
 .UNSPECIFIED. ) ;
#9881=CARTESIAN_POINT ( 'NONE',  ( 9.450870280412999591, 2.928319778732999978, -8.861178115809998701 ) ) ;
#9889=CARTESIAN_POINT ( 'NONE',  ( 8.497235841230001085, 3.789127741898000057, -9.388182174781999123 ) ) ;
#9899=B_SPLINE_CURVE_WITH_KNOTS ( 'NONE', 3,
 ( #36067, #29817, #41657, #66849, #8813, #35730, #18963, #30156, #19995, #15089, #40622, #51122, #57382, #61954, #36413, #40289, #14068, #35392 ),
 .UNSPECIFIED., .F., .F.,
 ( 4, 2, 2, 2, 2, 2, 2, 2, 4 ),
 ( 0.1254918003289636208, 0.2191362172194401547, 0.3127806341099167442, 0.4064250510003932781, 0.5000694678908698121, 0.5937138847813465681, 0.6873583016718234351, 0.7810027185623000801, 0.8746471354527769471 ),
 .UNSPECIFIED. ) ;
#9900=CARTESIAN_POINT ( 'NONE',  ( 9.327795280414001411, 3.161445734422999809, -6.178649910536000434 ) ) ;
#9902=CARTESIAN_POINT ( 'NONE',  ( 10.91624242361999997, 5.459834480072999874, -8.642877574935999618 ) ) ;
#9914=FACE_OUTER_BOUND ( 'NONE', #68233, .T. ) ;
#9915=CARTESIAN_POINT ( 'NONE',  ( 8.367589158771000513, 5.461114003844000031, -8.582501063019000398 ) ) ;
#9921=ORIENTED_EDGE ( 'NONE', *, *, #13363, .F. ) ;
#9922=CARTESIAN_POINT ( 'NONE',  ( 8.970860841232001448, 4.131080973160000447, -6.108642999115999395 ) ) ;
#9924=CARTESIAN_POINT ( 'NONE',  ( 1.300973465874000201, -3.500000000000000000, 0.000000000000000000 ) ) ;
#9929=CARTESIAN_POINT ( 'NONE',  ( 8.878099260413335969, 2.921496745512210058, 8.876672705295140631 ) ) ;
#9932=CARTESIAN_POINT ( 'NONE',  ( 8.883148997460001084, 5.167567567567999731, 6.822293592207000934 ) ) ;
#9936=AXIS2_PLACEMENT_3D ( 'NONE', #47542, #20966, #63604 ) ;
#9939=DIRECTION ( 'NONE',  ( 1.000000000000000000, 0.000000000000000000, 0.000000000000000000 ) ) ;
#9940=EDGE_CURVE ( 'NONE', #35088, #10760, #11167, .T. ) ;
#9941=EDGE_CURVE ( 'NONE', #63357, #44911, #24307, .T. ) ;
#9943=CARTESIAN_POINT ( 'NONE',  ( 7.995237948509533510, 3.187523905036820704, -6.308808669286300130 ) ) ;
#9949=CARTESIAN_POINT ( 'NONE',  ( 3.544158303137000310, -1.635632129023999903, -3.009968172588000535 ) ) ;
#9959=CARTESIAN_POINT ( 'NONE',  ( 10.88834686957638631, 2.694378745199484282, -7.104278543674602098 ) ) ;
#9961=CARTESIAN_POINT ( 'NONE',  ( 7.771669714201605572, 2.830702833142050512, -8.205313987515433283 ) ) ;
#9965=VERTEX_POINT ( 'NONE', #39402 ) ;
#9966=EDGE_CURVE ( 'NONE', #36211, #62671, #42006, .T. ) ;
#9972=CARTESIAN_POINT ( 'NONE',  ( 6.944089158771000747, 3.609683333014999995, -6.158094852492999927 ) ) ;
#9980=DIRECTION ( 'NONE',  ( 1.077198146790999955E-09, 7.359447821342999600E-11, 1.000000000000000000 ) ) ;
#9981=ORIENTED_EDGE ( 'NONE', *, *, #56990, .T. ) ;
#9983=CARTESIAN_POINT ( 'NONE',  ( 10.85378311793296469, 3.372467802742289411, 9.158846416527032019 ) ) ;
#9986=CARTESIAN_POINT ( 'NONE',  ( 8.013720397008766483, 5.129092373936881444, -6.745135665648876788 ) ) ;
#9990=ORIENTED_EDGE ( 'NONE', *, *, #25501, .T. ) ;
#9993=CARTESIAN_POINT ( 'NONE',  ( 11.14994211610999919, 2.627136771666999771, 6.696094414592000277 ) ) ;
#9996=CARTESIAN_POINT ( 'NONE',  ( 3.306337663562000095, -0.1082433060725999929, -3.542063228793999485 ) ) ;
#9997=DIRECTION ( 'NONE',  ( 1.000000000000000000, 0.000000000000000000, 0.000000000000000000 ) ) ;
#10001=EDGE_CURVE ( 'NONE', #35521, #31036, #49555, .T. ) ;
#10005=CARTESIAN_POINT ( 'NONE',  ( 10.49760649485983954, 3.288391178207342502, -9.127049713605428494 ) ) ;
#10009=CARTESIAN_POINT ( 'NONE',  ( 11.02786554143000153, 5.596226216413000110, 7.209502215883999199 ) ) ;
#10018=VERTEX_POINT ( 'NONE', #55135 ) ;
#10020=CARTESIAN_POINT ( 'NONE',  ( 8.225464158772000545, 3.844886277615000125, -8.888911790991000927 ) ) ;
#10028=CARTESIAN_POINT ( 'NONE',  ( 10.14522028041000112, 3.576529456695000331, -8.962721799438000403 ) ) ;
#10031=CYLINDRICAL_SURFACE ( 'NONE', #14160, 0.4999999999999998335 ) ;
#10034=CARTESIAN_POINT ( 'NONE',  ( 7.218295280410000458, 4.773081973066999772, 8.927402469597002010 ) ) ;
#10037=CARTESIAN_POINT ( 'NONE',  ( 6.870739158771000277, 5.477119873501999692, -8.694708770948999188 ) ) ;
#10046=CARTESIAN_POINT ( 'NONE',  ( 9.457462135716001583, 5.100000000000000533, -6.571291218949999902 ) ) ;
#10047=CARTESIAN_POINT ( 'NONE',  ( 7.000000000000000000, 10.80467228076000019, -3.475853456584999890 ) ) ;
#10048=EDGE_LOOP ( 'NONE', ( #26734, #68870, #49326, #66479, #56771, #37347, #29267, #68258 ) ) ;
#10052=CARTESIAN_POINT ( 'NONE',  ( 2.300973465875999935, -3.500000000000000000, 0.000000000000000000 ) ) ;
#10057=CARTESIAN_POINT ( 'NONE',  ( 8.283079719592000956, 2.376526778640999815, 7.686980884243000745 ) ) ;
#10058=VERTEX_POINT ( 'NONE', #23321 ) ;
#10063=EDGE_LOOP ( 'NONE', ( #16335, #66900, #60267, #60210, #69133, #48590, #29114, #4596 ) ) ;
#10066=CARTESIAN_POINT ( 'NONE',  ( 9.670777473741994257, 8.576669611614002875, -6.497511528403997261 ) ) ;
#10068=LINE ( 'NONE', #270, #10698 ) ;
#10077=CARTESIAN_POINT ( 'NONE',  ( 4.900006121741999898, -2.000000000000000444, 0.2617993877991496299 ) ) ;
#10078=CARTESIAN_POINT ( 'NONE',  ( 9.898128230592000421, 2.965931985296999862, -6.610871072364999712 ) ) ;
#10081=CARTESIAN_POINT ( 'NONE',  ( 8.335548758400999958, 2.897657723982001166, -6.653323589456997311 ) ) ;
#10082=ADVANCED_FACE ( 'NONE', ( #29269 ), #50580, .F. ) ;
#10084=EDGE_CURVE ( 'NONE', #63350, #7311, #61204, .T. ) ;
#10085=VERTEX_POINT ( 'NONE', #26421 ) ;
#10086=CARTESIAN_POINT ( 'NONE',  ( 8.930139513018188424, 4.760571299603993722, -9.106213216995776349 ) ) ;
#10092=CARTESIAN_POINT ( 'NONE',  ( 10.50244247011999832, 2.268911387573000038, 7.824865741583000300 ) ) ;
#10094=CARTESIAN_POINT ( 'NONE',  ( 10.01508584123000034, 4.845406482350000488, -6.387189183984999907 ) ) ;
#10095=CARTESIAN_POINT ( 'NONE',  ( 11.04779087299999851, 9.995284108896999697, -5.683129190753000159 ) ) ;
#10100=CARTESIAN_POINT ( 'NONE',  ( 10.75109581085999899, 2.822145500011000063, 6.655897464539000552 ) ) ;
#10103=CARTESIAN_POINT ( 'NONE',  ( 8.548770280408998445, 5.203550244299999683, -8.391678825488000371 ) ) ;
#10104=CARTESIAN_POINT ( 'NONE',  ( 0.000000000000000000, 0.3800960799355100339, 2.899897457380500310 ) ) ;
#10113=VERTEX_POINT ( 'NONE', #68359 ) ;
#10115=CARTESIAN_POINT ( 'NONE',  ( 7.501448341228000416, 2.138190256467000339, 6.814770510101999967 ) ) ;
#10117=CARTESIAN_POINT ( 'NONE',  ( 8.623264158775000965, 5.288433695693000480, -8.041290150997999930 ) ) ;
#10120=ORIENTED_EDGE ( 'NONE', *, *, #60053, .F. ) ;
#10121=CARTESIAN_POINT ( 'NONE',  ( 11.01776904286000125, 4.914120883409999863, 8.587704221454000475 ) ) ;
#10127=CARTESIAN_POINT ( 'NONE',  ( 8.379704719592000473, 4.283000592898000392, 9.286795422009001655 ) ) ;
#10128=CARTESIAN_POINT ( 'NONE',  ( 9.957462135714001406, 5.100000000000000533, -6.571291218949999902 ) ) ;
#10133=EDGE_LOOP ( 'NONE', ( #1897, #43445, #5477, #46828, #29204 ) ) ;
#10136=FACE_OUTER_BOUND ( 'NONE', #64724, .T. ) ;
#10137=CARTESIAN_POINT ( 'NONE',  ( 10.13339736671999880, 5.653645990693000556, 6.501823474484000442 ) ) ;
#10145=B_SPLINE_CURVE_WITH_KNOTS ( 'NONE', 3,
 ( #52469, #25904, #10506, #15759, #42671, #37087, #4914, #52821, #68887, #52122, #15420 ),
 .UNSPECIFIED., .F., .F.,
 ( 4, 2, 1, 2, 2, 4 ),
 ( 0.000000000000000000, 0.2499999999999993339, 0.3749999999999968359, 0.4374999999999955591, 0.4999999999999942824, 1.000000000000000000 ),
 .UNSPECIFIED. ) ;
#10150=DIRECTION ( 'NONE',  ( 0.000000000000000000, 1.000000000000000000, 0.000000000000000000 ) ) ;
#10157=CARTESIAN_POINT ( 'NONE',  ( 11.15192953222999961, 2.359300361215999953, -6.636686939130999718 ) ) ;
#10164=B_SPLINE_CURVE_WITH_KNOTS ( 'NONE', 3,
 ( #40470, #9681, #14598, #40145 ),
 .UNSPECIFIED., .F., .F.,
 ( 4, 4 ),
 ( 0.000000000000000000, 1.000000000000000000 ),
 .UNSPECIFIED. ) ;
#10165=CARTESIAN_POINT ( 'NONE',  ( 7.700045280408999382, 3.346262376537000094, 6.002251090845000192 ) ) ;
#10166=B_SPLINE_CURVE_WITH_KNOTS ( 'NONE', 3,
 ( #12658, #2509, #7757, #49714, #59852, #66132, #60551, #32946, #33990, #44138 ),
 .UNSPECIFIED., .F., .F.,
 ( 4, 2, 2, 2, 4 ),
 ( 0.000000000000000000, 0.2168912282584224416, 0.4337824565168448832, 0.6506736847752673247, 0.8675649130336897663 ),
 .UNSPECIFIED. ) ;
#10169=CARTESIAN_POINT ( 'NONE',  ( 9.239025325185552973, 2.669691822737871423, 7.269879417777145747 ) ) ;
#10171=CARTESIAN_POINT ( 'NONE',  ( 8.962855452004999890, 10.45518530739999896, 4.395433839652001851 ) ) ;
#10178=VERTEX_POINT ( 'NONE', #15236 ) ;
#10185=CARTESIAN_POINT ( 'NONE',  ( 0.4829009740474999868, -3.219656052487999798, -1.007448552055000057 ) ) ;
#10191=CARTESIAN_POINT ( 'NONE',  ( 10.20607971959000082, 2.622352165399999713, -6.528536464360000124 ) ) ;
#10200=CARTESIAN_POINT ( 'NONE',  ( 9.595408426582343608, 2.229238661835026392, -7.375658712783358162 ) ) ;
#10215=CARTESIAN_POINT ( 'NONE',  ( 8.040182825300005831, 3.147885656133000420, 6.175979896252004053 ) ) ;
#10218=ADVANCED_FACE ( 'NONE', ( #8955 ), #54815, .T. ) ;
#10220=CARTESIAN_POINT ( 'NONE',  ( 3.500000000000000000, 0.000000000000000000, 0.000000000000000000 ) ) ;
#10222=CARTESIAN_POINT ( 'NONE',  ( 8.999999001754000361, -12.50000000000000000, 0.000000000000000000 ) ) ;
#10225=CARTESIAN_POINT ( 'NONE',  ( 8.614404719593999005, 5.030502105212999453, -6.322203460290999999 ) ) ;
#10232=CARTESIAN_POINT ( 'NONE',  ( 8.994485841233000656, 3.854507394315999758, -9.394302886912999639 ) ) ;
#10236=CARTESIAN_POINT ( 'NONE',  ( 10.98768472569999943, 5.449702578894000560, 4.945212061318999375 ) ) ;
#10240=CARTESIAN_POINT ( 'NONE',  ( 9.816185841232000442, 2.656512020013999997, -7.884832994446999699 ) ) ;
#10242=CARTESIAN_POINT ( 'NONE',  ( 2.500973465876000112, 3.500000000000000000, 0.000000000000000000 ) ) ;
#10247=B_SPLINE_CURVE_WITH_KNOTS ( 'NONE', 3,
 ( #20118, #68690, #41106, #62419, #20806, #14540, #25361, #33024, #38257, #6786 ),
 .UNSPECIFIED., .F., .F.,
 ( 4, 2, 2, 2, 4 ),
 ( 0.5000000000000000000, 0.6250000000000000000, 0.7500000000000000000, 0.8750000000000000000, 1.000000000000000000 ),
 .UNSPECIFIED. ) ;
#10248=DIRECTION ( 'NONE',  ( -1.000000000000000000, 0.000000000000000000, 0.000000000000000000 ) ) ;
#10249=ADVANCED_FACE ( 'NONE', ( #533 ), #61146, .F. ) ;
#10256=DIRECTION ( 'NONE',  ( 0.000000000000000000, 1.000000000000000000, 0.000000000000000000 ) ) ;
#10264=CARTESIAN_POINT ( 'NONE',  ( 10.85956136592000121, 5.063047012783000511, -5.179223560113999980 ) ) ;
#10266=CARTESIAN_POINT ( 'NONE',  ( 1.103056799208124827, 2.798833948393625981, 2.150913519912208471 ) ) ;
#10267=CARTESIAN_POINT ( 'NONE',  ( 0.000000000000000000, 0.000000000000000000, 0.000000000000000000 ) ) ;
#10268=CARTESIAN_POINT ( 'NONE',  ( 11.07925595036916633, 5.279255950369167394, 6.503434303641999925 ) ) ;
#10275=EDGE_CURVE ( 'NONE', #27749, #25016, #12405, .T. ) ;
#10279=LINE ( 'NONE', #31961, #24668 ) ;
#10286=VECTOR ( 'NONE', #31234, 1000.000000000000114 ) ;
#10294=CARTESIAN_POINT ( 'NONE',  ( 5.500000000000000000, -12.78667792605000031, 2.345384795463000049 ) ) ;
#10296=DIRECTION ( 'NONE',  ( 1.000000000000000000, 1.157371756818000115E-14, 6.365544662497999016E-14 ) ) ;
#10301=DIRECTION ( 'NONE',  ( 1.000000000000000000, 0.000000000000000000, 0.000000000000000000 ) ) ;
#10303=DIRECTION ( 'NONE',  ( 0.000000000000000000, -0.8648648648648720183, -0.5020047465136825426 ) ) ;
#10305=VERTEX_POINT ( 'NONE', #34083 ) ;
#10311=AXIS2_PLACEMENT_3D ( 'NONE', #547, #42850, #58582 ) ;
#10312=DIRECTION ( 'NONE',  ( -0.8231338744408063235, 0.000000000000000000, -0.5678473604306591982 ) ) ;
#10315=B_SPLINE_CURVE_WITH_KNOTS ( 'NONE', 3,
 ( #31461, #68848, #46852, #57670 ),
 .UNSPECIFIED., .F., .F.,
 ( 4, 4 ),
 ( 0.8745879739953518195, 1.000000000000000000 ),
 .UNSPECIFIED. ) ;
#10316=CARTESIAN_POINT ( 'NONE',  ( 6.885504719591000189, 2.696863807693000048, -8.366590973307999946 ) ) ;
#10318=CARTESIAN_POINT ( 'NONE',  ( 7.871384581343000342, 5.129340811002999878, 6.740051537885999977 ) ) ;
#10323=VERTEX_POINT ( 'NONE', #36046 ) ;
#10325=ORIENTED_EDGE ( 'NONE', *, *, #14526, .F. ) ;
#10329=DIRECTION ( 'NONE',  ( 0.000000000000000000, 0.000000000000000000, -1.000000000000000000 ) ) ;
#10336=EDGE_CURVE ( 'NONE', #13445, #57692, #55383, .T. ) ;
#10337=VERTEX_POINT ( 'NONE', #12406 ) ;
#10338=CARTESIAN_POINT ( 'NONE',  ( 9.353724647487000610, 2.823567847429000022, 9.032053040610000139 ) ) ;
#10341=CARTESIAN_POINT ( 'NONE',  ( 9.517835841233001304, 4.883347899767999323, -6.417062834774999835 ) ) ;
#10342=AXIS2_PLACEMENT_3D ( 'NONE', #47306, #68610, #62006 ) ;
#10350=CARTESIAN_POINT ( 'NONE',  ( 10.32652459277042212, 5.723289909120445884, -7.204243127669484714 ) ) ;
#10353=CARTESIAN_POINT ( 'NONE',  ( 10.97864812944000157, 5.273131703456000352, 7.958028903907000462 ) ) ;
#10365=CARTESIAN_POINT ( 'NONE',  ( 9.559179719593000613, 4.038835765825999680, -5.935509327774999733 ) ) ;
#10366=DIRECTION ( 'NONE',  ( -1.000000000000000000, 0.000000000000000000, 0.000000000000000000 ) ) ;
#10367=CARTESIAN_POINT ( 'NONE',  ( 10.09999999999999964, 0.000000000000000000, 11.84999999999999964 ) ) ;
#10371=CARTESIAN_POINT ( 'NONE',  ( 10.87947334122999976, 2.817426144593000004, -6.828668581221999823 ) ) ;
#10378=CARTESIAN_POINT ( 'NONE',  ( 7.282482780409000434, 3.448180532882000104, 9.222462917385000125 ) ) ;
#10381=CARTESIAN_POINT ( 'NONE',  ( 8.453079719590000707, 5.452311718892000059, -8.444358433472999081 ) ) ;
#10387=EDGE_LOOP ( 'NONE', ( #56927, #260, #62030, #55809 ) ) ;
#10392=EDGE_CURVE ( 'NONE', #35162, #57180, #37060, .T. ) ;
#10400=CARTESIAN_POINT ( 'NONE',  ( 8.860767219592000643, 2.935741164366000522, 6.259844213126999790 ) ) ;
#10402=CARTESIAN_POINT ( 'NONE',  ( 3.499999999999999556, -3.170392682610728041, -0.3463127203071835192 ) ) ;
#10403=CARTESIAN_POINT ( 'NONE',  ( 8.896432056425130241, 5.285622111567785275, 7.027794277398490053 ) ) ;
#10405=ORIENTED_EDGE ( 'NONE', *, *, #14607, .F. ) ;
#10419=CARTESIAN_POINT ( 'NONE',  ( 4.900006121741999898, 1.229093439949832334, 1.599333684796358401 ) ) ;
#10421=CARTESIAN_POINT ( 'NONE',  ( 10.48414939117999900, 4.098653981087000631, -9.351365234892998757 ) ) ;
#10424=CARTESIAN_POINT ( 'NONE',  ( 8.231600168468999001, 3.072304018142998139, -6.138007231110007567 ) ) ;
#10431=CARTESIAN_POINT ( 'NONE',  ( 10.35616100078999935, 2.777276096020000029, 8.995275123087999702 ) ) ;
#10433=CARTESIAN_POINT ( 'NONE',  ( 6.949999999999961986, 5.456597484868912495, -8.185422748483135891 ) ) ;
#10434=CONICAL_SURFACE ( 'NONE', #14888, 0.3062142749367001149, 0.7853981633972997312 ) ;
#10435=CARTESIAN_POINT ( 'NONE',  ( 11.06517113529999996, 8.815199625753001200, -6.641975173320999737 ) ) ;
#10439=CARTESIAN_POINT ( 'NONE',  ( 9.820199962102000413, 3.883325513302000154, 6.055618835924000187 ) ) ;
#10442=CARTESIAN_POINT ( 'NONE',  ( 9.169760841232999837, 4.728328492779000136, -8.692725459657999920 ) ) ;
#10445=CARTESIAN_POINT ( 'NONE',  ( 9.229794494861661036, 4.176538781553355228, -8.850125647912786775 ) ) ;
#10451=CARTESIAN_POINT ( 'NONE',  ( 8.014948341228999240, 2.280568568659000483, 6.510284508622999233 ) ) ;
#10453=CARTESIAN_POINT ( 'NONE',  ( 8.813304719595000947, 3.880154689736000417, -9.060377011187000562 ) ) ;
#10456=EDGE_LOOP ( 'NONE', ( #62577, #9701, #39880 ) ) ;
#10457=CARTESIAN_POINT ( 'NONE',  ( 11.29622358543999994, 3.561657733933999648, 6.266050246368000565 ) ) ;
#10462=ORIENTED_EDGE ( 'NONE', *, *, #66436, .T. ) ;
#10463=CARTESIAN_POINT ( 'NONE',  ( 9.406704719590001318, 3.705846972803000128, 9.096435887808000942 ) ) ;
#10473=CARTESIAN_POINT ( 'NONE',  ( 10.85737917744000036, 2.754548910086000113, 8.976376585747001258 ) ) ;
#10480=ADVANCED_FACE ( 'NONE', ( #26599 ), #37085, .F. ) ;
#10487=ORIENTED_EDGE ( 'NONE', *, *, #30154, .F. ) ;
#10493=CARTESIAN_POINT ( 'NONE',  ( 10.06843885510000014, 4.148608506723999945, 8.941445591976998841 ) ) ;
#10494=CARTESIAN_POINT ( 'NONE',  ( 10.69578011722000177, 5.505003832924999507, -7.759263776825999770 ) ) ;
#10498=LINE ( 'NONE', #20306, #55355 ) ;
#10500=CARTESIAN_POINT ( 'NONE',  ( 9.523698341228998387, 4.852728889087999598, 8.683917172082999514 ) ) ;
#10501=ORIENTED_EDGE ( 'NONE', *, *, #52556, .T. ) ;
#10503=CONICAL_SURFACE ( 'NONE', #8268, 12.49999584805000019, 0.7853981146832407223 ) ;
#10505=CARTESIAN_POINT ( 'NONE',  ( 9.242854517844085294, 2.682272565524075780, 7.207860447134208037 ) ) ;
#10506=CARTESIAN_POINT ( 'NONE',  ( 8.647846113052866102, 2.999226622549716392, -6.113461772567276853 ) ) ;
#10507=VECTOR ( 'NONE', #8680, 1000.000000000000000 ) ;
#10508=CARTESIAN_POINT ( 'NONE',  ( 10.21908538701999625, 9.735603468294996787, 6.344040641747004550 ) ) ;
#10509=DIRECTION ( 'NONE',  ( 1.000000000000000000, 0.000000000000000000, 0.000000000000000000 ) ) ;
#10510=CARTESIAN_POINT ( 'NONE',  ( 11.04779069327000052, 9.995291468210998787, 5.683114286574999952 ) ) ;
#10511=CIRCLE ( 'NONE', #2686, 2.000000000000000444 ) ;
#10521=CARTESIAN_POINT ( 'NONE',  ( 0.6748509817850999459, 2.983562695318000113, -1.348686013867999911 ) ) ;
#10528=CARTESIAN_POINT ( 'NONE',  ( 7.964620641636996901, 2.867893108869000507, -6.758951315555000505 ) ) ;
#10529=CARTESIAN_POINT ( 'NONE',  ( 10.35752971959000135, 5.367812128871999988, -6.514736131541999598 ) ) ;
#10533=LINE ( 'NONE', #30839, #46431 ) ;
#10536=CARTESIAN_POINT ( 'NONE',  ( 0.9764734890463999673, -3.085119672805999524, 1.050391531144999835 ) ) ;
#10537=CARTESIAN_POINT ( 'NONE',  ( 7.717918988116000634, 2.852331522235000083, 6.784355039830999523 ) ) ;
#10543=FACE_OUTER_BOUND ( 'NONE', #10581, .T. ) ;
#10560=CARTESIAN_POINT ( 'NONE',  ( 10.52052890781999928, 2.899999999999999911, 6.152188490330000370 ) ) ;
#10565=VECTOR ( 'NONE', #43956, 1000.000000000000000 ) ;
#10567=CARTESIAN_POINT ( 'NONE',  ( 8.655270280412999284, 4.162493982103000256, -5.775210092227999858 ) ) ;
#10572=ORIENTED_EDGE ( 'NONE', *, *, #44866, .F. ) ;
#10581=EDGE_LOOP ( 'NONE', ( #46918, #57769, #66926, #27673 ) ) ;
#10582=CARTESIAN_POINT ( 'NONE',  ( 8.517351160491474005, 5.205057563154839251, 8.206039936683215075 ) ) ;
#10584=EDGE_CURVE ( 'NONE', #27904, #32611, #54509, .T. ) ;
#10591=DIRECTION ( 'NONE',  ( 0.000000000000000000, 1.000000000000000000, 0.000000000000000000 ) ) ;
#10593=ORIENTED_EDGE ( 'NONE', *, *, #3647, .F. ) ;
#10598=CARTESIAN_POINT ( 'NONE',  ( 8.599639158772999892, 2.261390688294000029, -6.733978371730000134 ) ) ;
#10602=ORIENTED_EDGE ( 'NONE', *, *, #41654, .F. ) ;
#10604=CARTESIAN_POINT ( 'NONE',  ( 10.89182486572000030, 5.053346025730999891, -5.014777255665999078 ) ) ;
#10605=EDGE_CURVE ( 'NONE', #15028, #20142, #26156, .T. ) ;
#10606=CARTESIAN_POINT ( 'NONE',  ( 10.52462472184161157, 2.899999999999999911, -6.445686799303610215 ) ) ;
#10608=CARTESIAN_POINT ( 'NONE',  ( 1.259306799207500438, -3.058252359239909346, 1.762666431298136605 ) ) ;
#10609=DIRECTION ( 'NONE',  ( 1.000000000000000000, 0.000000000000000000, 0.000000000000000000 ) ) ;
#10615=ORIENTED_EDGE ( 'NONE', *, *, #5823, .T. ) ;
#10616=DIRECTION ( 'NONE',  ( 1.000000000000000000, 0.000000000000000000, -1.332267629588000161E-14 ) ) ;
#10619=CARTESIAN_POINT ( 'NONE',  ( 4.950033214355999966, 0.000000000000000000, 0.000000000000000000 ) ) ;
#10625=CARTESIAN_POINT ( 'NONE',  ( 7.100000000000000533, 5.326087788487999575, -7.247035225330000330 ) ) ;
#10630=CARTESIAN_POINT ( 'NONE',  ( 6.999999999999999112, 9.536570502379751346, -4.676103187607473011 ) ) ;
#10632=ORIENTED_EDGE ( 'NONE', *, *, #30154, .T. ) ;
#10636=CARTESIAN_POINT ( 'NONE',  ( 3.500000000000000000, -3.033011252059000018, -1.020217008720000207 ) ) ;
#10637=CARTESIAN_POINT ( 'NONE',  ( 1.696806799207916550, -0.9161175952574931447, 3.408904368339101598 ) ) ;
#10646=VERTEX_POINT ( 'NONE', #12239 ) ;
#10655=DIRECTION ( 'NONE',  ( -1.000000000000000000, 0.000000000000000000, 0.000000000000000000 ) ) ;
#10656=CARTESIAN_POINT ( 'NONE',  ( 7.721970280404999443, 5.390931070480998955, -6.467229401624000396 ) ) ;
#10667=EDGE_LOOP ( 'NONE', ( #65720, #39584, #29240, #25139 ) ) ;
#10672=CARTESIAN_POINT ( 'NONE',  ( 8.207992688182997654, 5.113487315348997697, -6.366574791658999644 ) ) ;
#10673=FACE_OUTER_BOUND ( 'NONE', #28299, .T. ) ;
#10674=CARTESIAN_POINT ( 'NONE',  ( 9.406851002546000373, 2.832432432432000269, -6.822293592207000934 ) ) ;
#10676=ORIENTED_EDGE ( 'NONE', *, *, #54147, .F. ) ;
#10679=CARTESIAN_POINT ( 'NONE',  ( 10.11260611051000069, 3.359887741436999864, 5.859127722154000573 ) ) ;
#10680=CARTESIAN_POINT ( 'NONE',  ( 10.87273915876999908, 5.407616985330000681, -8.698399706473999515 ) ) ;
#10686=AXIS2_PLACEMENT_3D ( 'NONE', #5972, #64696, #38838 ) ;
#10688=ORIENTED_EDGE ( 'NONE', *, *, #26456, .F. ) ;
#10693=CARTESIAN_POINT ( 'NONE',  ( 9.199602729599000384, 2.551394566582000145, 7.536605852160000119 ) ) ;
#10696=AXIS2_PLACEMENT_3D ( 'NONE', #23878, #3243, #67546 ) ;
#10698=VECTOR ( 'NONE', #37672, 1000.000000000000000 ) ;
#10707=LINE ( 'NONE', #225, #9235 ) ;
#10708=CARTESIAN_POINT ( 'NONE',  ( 10.99338701711408106, 6.182907969993329367, 5.102573636763008125 ) ) ;
#10710=CARTESIAN_POINT ( 'NONE',  ( 0.6339629568059000908, 0.7117304887930000490, 3.632629627798000360 ) ) ;
#10712=CARTESIAN_POINT ( 'NONE',  ( 3.029203535413000026, 3.757998461040000127, 0.07632091300853000027 ) ) ;
#10723=CARTESIAN_POINT ( 'NONE',  ( 7.946970280407001042, 5.256485075641999849, -6.567055966373000153 ) ) ;
#10728=B_SPLINE_CURVE_WITH_KNOTS ( 'NONE', 3,
 ( #12365, #61294, #33695, #54665 ),
 .UNSPECIFIED., .F., .F.,
 ( 4, 4 ),
 ( 0.000000000000000000, 1.000000000000000000 ),
 .UNSPECIFIED. ) ;
#10732=CARTESIAN_POINT ( 'NONE',  ( 11.10000000000000320, 2.488563452597234882, -8.216671174298946667 ) ) ;
#10735=CARTESIAN_POINT ( 'NONE',  ( 9.163298641743953254, 2.899999999999999911, -6.158784435141193114 ) ) ;
#10736=ORIENTED_EDGE ( 'NONE', *, *, #49392, .T. ) ;
#10743=CARTESIAN_POINT ( 'NONE',  ( 8.694607780412001219, 5.290207928847999064, 8.768105151414001597 ) ) ;
#10746=CIRCLE ( 'NONE', #6249, 3.199999999999999289 ) ;
#10753=DIRECTION ( 'NONE',  ( 0.000000000000000000, -1.000000000000000000, 0.000000000000000000 ) ) ;
#10760=VERTEX_POINT ( 'NONE', #48951 ) ;
#10766=CARTESIAN_POINT ( 'NONE',  ( 10.87696123885999810, 5.827079664135999870, -7.814747088295999511 ) ) ;
#10773=CARTESIAN_POINT ( 'NONE',  ( 10.68403803949000164, 5.436614310638000269, 8.578436083822998270 ) ) ;
#10774=CARTESIAN_POINT ( 'NONE',  ( 2.300973465875999935, -3.500000000000000000, 0.000000000000000000 ) ) ;
#10782=ADVANCED_FACE ( 'NONE', ( #59430 ), #32530, .T. ) ;
#10783=EDGE_CURVE ( 'NONE', #4475, #64347, #16113, .T. ) ;
#10784=CARTESIAN_POINT ( 'NONE',  ( 8.211023395313091555, 4.489943607116844149, -8.784467515373197699 ) ) ;
#10785=DIRECTION ( 'NONE',  ( 1.000000000000000000, 0.000000000000000000, -1.776356839443000099E-14 ) ) ;
#10786=AXIS2_PLACEMENT_3D ( 'NONE', #6417, #27767, #18307 ) ;
#10788=CARTESIAN_POINT ( 'NONE',  ( 8.871410841230998656, 2.721111233225000259, -6.936528696292000085 ) ) ;
#10791=CARTESIAN_POINT ( 'NONE',  ( 9.281866024821542993, 3.294723229065558368, -8.705120403943604757 ) ) ;
#10792=CARTESIAN_POINT ( 'NONE',  ( 8.205992358813000820, 3.399999999999999911, 6.138278517057000450 ) ) ;
#10794=ORIENTED_EDGE ( 'NONE', *, *, #6608, .T. ) ;
#10797=FACE_OUTER_BOUND ( 'NONE', #42084, .T. ) ;
#10798=CARTESIAN_POINT ( 'NONE',  ( 9.351420280414000530, 4.953415418491999844, -8.946479654552000227 ) ) ;
#10801=CARTESIAN_POINT ( 'NONE',  ( 2.310450118812109377, 2.961138536375865993, 1.358551000647025164 ) ) ;
#10803=CARTESIAN_POINT ( 'NONE',  ( 9.869051220224999810, 5.575171928796999410, 7.724300137354000562 ) ) ;
#10809=CARTESIAN_POINT ( 'NONE',  ( 9.059364158773000497, 4.192919163547999872, 5.525472271700999194 ) ) ;
#10817=ORIENTED_EDGE ( 'NONE', *, *, #33229, .F. ) ;
#10824=CARTESIAN_POINT ( 'NONE',  ( 8.763579719593998618, 4.815598936798999752, -8.835641302565999666 ) ) ;
#10825=CARTESIAN_POINT ( 'NONE',  ( 6.999999692086999126, -12.89129024276999935, 1.677687656890000101 ) ) ;
#10828=AXIS2_PLACEMENT_3D ( 'NONE', #1157, #44852, #1849 ) ;
#10831=CARTESIAN_POINT ( 'NONE',  ( 9.683745612763171806, 2.796157461452848825, 8.204744624355011950 ) ) ;
#10833=ORIENTED_EDGE ( 'NONE', *, *, #16868, .F. ) ;
#10838=CARTESIAN_POINT ( 'NONE',  ( 10.30204095393054509, 2.650238144765166837, -7.719132294906656533 ) ) ;
#10839=CARTESIAN_POINT ( 'NONE',  ( 10.26368708477999903, 4.794139572939999816, -8.804452601708000259 ) ) ;
#10843=CIRCLE ( 'NONE', #46586, 2.999989272562999965 ) ;
#10844=CARTESIAN_POINT ( 'NONE',  ( 9.040632417955841049, 4.918936971883569598, 8.488836720954758164 ) ) ;
#10846=CARTESIAN_POINT ( 'NONE',  ( 7.571670280409000142, 2.531201476950000195, 8.216704145297999418 ) ) ;
#10847=VERTEX_POINT ( 'NONE', #66400 ) ;
#10849=CARTESIAN_POINT ( 'NONE',  ( 11.00294879349999988, 5.167578603197999776, -4.969641262464000953 ) ) ;
#10850=CARTESIAN_POINT ( 'NONE',  ( 7.888294342220998345, 2.872416928457999674, -6.735169506715999788 ) ) ;
#10853=CARTESIAN_POINT ( 'NONE',  ( 10.95881151040999946, 8.162134461319000778, 6.507868381347999609 ) ) ;
#10856=FACE_OUTER_BOUND ( 'NONE', #27986, .T. ) ;
#10860=CARTESIAN_POINT ( 'NONE',  ( 10.10000011340999926, -1.190159082397999942E-13, -12.39999890530012117 ) ) ;
#10867=CARTESIAN_POINT ( 'NONE',  ( 0.4912272458363000083, -2.390579753276000030, 2.141564200098999837 ) ) ;
#10872=EDGE_CURVE ( 'NONE', #52078, #13783, #30275, .T. ) ;
#10874=CARTESIAN_POINT ( 'NONE',  ( 7.698447294381004724, 2.921226879009002797, -6.534475276641003916 ) ) ;
#10875=CARTESIAN_POINT ( 'NONE',  ( 10.39539221959000059, 5.667182949051000840, -7.250689098107000241 ) ) ;
#10879=CARTESIAN_POINT ( 'NONE',  ( 8.015378205837999204, 5.116433164263000322, -6.698485005943000559 ) ) ;
#10880=VERTEX_POINT ( 'NONE', #46462 ) ;
#10890=CARTESIAN_POINT ( 'NONE',  ( 10.22514748322308797, 2.649941783575544108, 7.500008211948054893 ) ) ;
#10896=CARTESIAN_POINT ( 'NONE',  ( 10.26685100253999927, 2.832432432432000269, 6.822293592207000934 ) ) ;
#10910=CARTESIAN_POINT ( 'NONE',  ( 9.839810841229999383, 5.817107086401000160, -6.945352709928000579 ) ) ;
#10927=VERTEX_POINT ( 'NONE', #8028 ) ;
#10929=CARTESIAN_POINT ( 'NONE',  ( 8.639360841228999277, 5.074768364528000397, -8.296267706722000312 ) ) ;
#10930=ORIENTED_EDGE ( 'NONE', *, *, #48616, .F. ) ;
#10931=CARTESIAN_POINT ( 'NONE',  ( 0.3034990810464371913, 3.062178106342674067, 1.095474795892486197 ) ) ;
#10941=EDGE_LOOP ( 'NONE', ( #13440, #60992, #66888, #61211, #37071, #38839, #59162, #66443, #32146 ) ) ;
#10947=CARTESIAN_POINT ( 'NONE',  ( 9.157839096883044760, 2.900038627299713401, -6.157793193892236339 ) ) ;
#10952=ORIENTED_EDGE ( 'NONE', *, *, #37520, .T. ) ;
#10953=ORIENTED_EDGE ( 'NONE', *, *, #38738, .T. ) ;
#10954=CARTESIAN_POINT ( 'NONE',  ( 11.04499918239000067, 5.245459939894999479, -5.176258674916000224 ) ) ;
#10959=CYLINDRICAL_SURFACE ( 'NONE', #3416, 3.500000000000000000 ) ;
#10970=CARTESIAN_POINT ( 'NONE',  ( 11.09999999999999964, 6.520421007963999926, -5.525576379744999933 ) ) ;
#10973=DIRECTION ( 'NONE',  ( 0.000000000000000000, 0.000000000000000000, -1.000000000000000000 ) ) ;
#10975=CARTESIAN_POINT ( 'NONE',  ( 7.207719739968999839, 8.269775584676999358, -4.413073181476000251 ) ) ;
#10985=CARTESIAN_POINT ( 'NONE',  ( 7.773264469372000107, 2.859518616742000141, 6.768376720750000075 ) ) ;
#10986=CARTESIAN_POINT ( 'NONE',  ( 10.28172590881818671, 3.320041345952004175, -8.679799923475062684 ) ) ;
#11002=CARTESIAN_POINT ( 'NONE',  ( 8.573539158775000502, 5.361622798585000460, -7.185294144754000634 ) ) ;
#11006=CARTESIAN_POINT ( 'NONE',  ( 7.174995280405999765, 4.580689680786999674, -5.867791741075000900 ) ) ;
#11007=EDGE_CURVE ( 'NONE', #23303, #14861, #14981, .T. ) ;
#11008=CARTESIAN_POINT ( 'NONE',  ( 8.799469176677469306, 2.649828231765675834, -7.761613174418741323 ) ) ;
#11023=FACE_OUTER_BOUND ( 'NONE', #46058, .T. ) ;
#11025=EDGE_LOOP ( 'NONE', ( #42994, #23800, #17011, #34112 ) ) ;
#11029=CARTESIAN_POINT ( 'NONE',  ( 9.465106464520001595, 2.290037071913000322, 6.601704384062999864 ) ) ;
#11036=CARTESIAN_POINT ( 'NONE',  ( 7.000000000000000000, 7.526486366024999874, -3.526486366024999874 ) ) ;
#11044=EDGE_CURVE ( 'NONE', #31394, #21003, #55695, .T. ) ;
#11048=CARTESIAN_POINT ( 'NONE',  ( 9.820199962102000413, 3.883325513302000154, 6.055618835924000187 ) ) ;
#11060=CARTESIAN_POINT ( 'NONE',  ( 9.369139158774000720, 2.685250982074999904, -7.026194612421999608 ) ) ;
#11061=DIRECTION ( 'NONE',  ( 0.000000000000000000, -1.000000000000000000, 0.000000000000000000 ) ) ;
#11063=CARTESIAN_POINT ( 'NONE',  ( 10.99249554219874447, 6.392256384488597121, 5.212998417364866022 ) ) ;
#11064=CARTESIAN_POINT ( 'NONE',  ( 0.4939139796827000106, -1.072119470989999934, 3.198702759649999727 ) ) ;
#11066=CARTESIAN_POINT ( 'NONE',  ( 10.57657334123000048, 5.344886503256999433, -7.298885378918000377 ) ) ;
#11067=ORIENTED_EDGE ( 'NONE', *, *, #34745, .F. ) ;
#11072=CARTESIAN_POINT ( 'NONE',  ( 7.860170280410000210, 2.263558315407000254, 8.007442119518000112 ) ) ;
#11075=CARTESIAN_POINT ( 'NONE',  ( 7.698345280408000590, 2.727583171400000062, -8.411095346025000197 ) ) ;
#11094=CARTESIAN_POINT ( 'NONE',  ( 7.320267219589999819, 2.466388272391000225, 6.935562100014999842 ) ) ;
#11098=CARTESIAN_POINT ( 'NONE',  ( 10.96499058814000094, 6.672045932937000323, -5.367166258627000808 ) ) ;
#11099=ORIENTED_EDGE ( 'NONE', *, *, #12185, .T. ) ;
#11109=ORIENTED_EDGE ( 'NONE', *, *, #54658, .T. ) ;
#11116=CARTESIAN_POINT ( 'NONE',  ( 4.900006121742000786, 1.947945353336632213, 0.5234957687185572972 ) ) ;
#11117=CARTESIAN_POINT ( 'NONE',  ( 9.947724669984761903, 5.285954009497370265, 7.027653896126389910 ) ) ;
#11119=CARTESIAN_POINT ( 'NONE',  ( 11.09999999999999964, 2.700000000000000178, -5.160242730539000178 ) ) ;
#11120=CARTESIAN_POINT ( 'NONE',  ( 7.893560293058006216, 2.859109450078002546, -6.778905949012001386 ) ) ;
#11121=CARTESIAN_POINT ( 'NONE',  ( 10.97864812944000157, 5.273131703456000352, 7.958028903907000462 ) ) ;
#11125=CARTESIAN_POINT ( 'NONE',  ( 10.99433665574000152, 3.697618584609999814, 5.729302299903000772 ) ) ;
#11130=CARTESIAN_POINT ( 'NONE',  ( 10.86280073406000035, 9.764482209271999835, -5.701704797273999148 ) ) ;
#11131=FACE_OUTER_BOUND ( 'NONE', #41863, .T. ) ;
#11133=CARTESIAN_POINT ( 'NONE',  ( 10.94076550314999885, 5.140765503144999471, -6.571291218949999902 ) ) ;
#11145=CARTESIAN_POINT ( 'NONE',  ( 7.539232780409000689, 4.696238830159999544, 5.830273622963999536 ) ) ;
#11146=CARTESIAN_POINT ( 'NONE',  ( 8.804445280412998898, 5.597201461420000967, -8.171008079894999554 ) ) ;
#11147=CARTESIAN_POINT ( 'NONE',  ( 10.56819717211696741, 5.125396288431045555, -6.749639981090855834 ) ) ;
#11148=CARTESIAN_POINT ( 'NONE',  ( 2.235213150975154495, 2.767678518585422687, -1.576253733361024256 ) ) ;
#11150=CARTESIAN_POINT ( 'NONE',  ( 10.90638722582999875, 5.227488226180000197, 6.784465725675999259 ) ) ;
#11161=CARTESIAN_POINT ( 'NONE',  ( 1.309336868148999855, 3.233448155534000001, 0.4075532224664999981 ) ) ;
#11167=B_SPLINE_CURVE_WITH_KNOTS ( 'NONE', 3,
 ( #26851, #966, #34164, #66652 ),
 .UNSPECIFIED., .F., .F.,
 ( 4, 4 ),
 ( 0.000000000000000000, 0.2468845652704700078 ),
 .UNSPECIFIED. ) ;
#11168=CARTESIAN_POINT ( 'NONE',  ( 8.514954719592999766, 3.207599814920999659, -6.150466394809999571 ) ) ;
#11169=CARTESIAN_POINT ( 'NONE',  ( 8.073148997456000231, 5.167567567567999731, -6.822293592207000934 ) ) ;
#11171=CARTESIAN_POINT ( 'NONE',  ( 9.179391679754937527, 4.176475755878279905, -8.849937275099289735 ) ) ;
#11179=CARTESIAN_POINT ( 'NONE',  ( 10.62697636434999993, 3.142921793056999924, 8.668445734229999644 ) ) ;
#11181=CARTESIAN_POINT ( 'NONE',  ( 10.64127413024999846, 2.258699798012000048, -6.863478635463000188 ) ) ;
#11186=CARTESIAN_POINT ( 'NONE',  ( 10.10000011340999926, -12.39999890530000037, 0.000000000000000000 ) ) ;
#11188=CARTESIAN_POINT ( 'NONE',  ( 7.737829719589999655, 5.687206835507000235, 6.847268999608999707 ) ) ;
#11192=CARTESIAN_POINT ( 'NONE',  ( 9.245063355149550688, 2.690443968828802657, 7.172286089387452712 ) ) ;
#11193=CARTESIAN_POINT ( 'NONE',  ( 7.910551708067999677, 2.874573263512000043, -6.728745899354000137 ) ) ;
#11196=CARTESIAN_POINT ( 'NONE',  ( 11.12341687003999979, 6.051695911142999762, 5.270624977622000884 ) ) ;
#11197=CARTESIAN_POINT ( 'NONE',  ( 11.06799838223999899, 8.464218156389000214, 6.698020382136999906 ) ) ;
#11201=ORIENTED_EDGE ( 'NONE', *, *, #41435, .T. ) ;
#11207=CARTESIAN_POINT ( 'NONE',  ( 8.315204322669442760, 2.904787293452365748, -6.552018845477737052 ) ) ;
#11212=CARTESIAN_POINT ( 'NONE',  ( 8.470295280410999439, 4.255646040929000229, 9.114085578076998928 ) ) ;
#11213=CARTESIAN_POINT ( 'NONE',  ( 9.575188572738724702, 5.349682312560990027, -7.676829535353270728 ) ) ;
#11217=CARTESIAN_POINT ( 'NONE',  ( 8.168244718249995984, 3.088031253505000961, -6.162676582372005996 ) ) ;
#11218=CARTESIAN_POINT ( 'NONE',  ( 11.33382334123000135, 2.642405149457999869, -7.577896731332000257 ) ) ;
#11219=CARTESIAN_POINT ( 'NONE',  ( 9.662398456551489545, 2.649938674315804210, 7.712117850346960957 ) ) ;
#11220=CARTESIAN_POINT ( 'NONE',  ( 8.354426260476000010, 5.125517035499999707, 6.367235573876004473 ) ) ;
#11222=CYLINDRICAL_SURFACE ( 'NONE', #16278, 0.5000000000000000000 ) ;
#11230=FACE_OUTER_BOUND ( 'NONE', #23479, .T. ) ;
#11235=DIRECTION ( 'NONE',  ( 0.000000000000000000, 1.000000000000000000, 0.000000000000000000 ) ) ;
#11249=CARTESIAN_POINT ( 'NONE',  ( 9.591185841232000797, 2.173570076733999823, -8.023168429484000441 ) ) ;
#11256=DIRECTION ( 'NONE',  ( 0.000000000000000000, 0.8648648648648717963, 0.5020047465136829867 ) ) ;
#11267=CARTESIAN_POINT ( 'NONE',  ( 8.672510841228998402, 4.686731264770999772, -8.717075579553000608 ) ) ;
#11269=CARTESIAN_POINT ( 'NONE',  ( 10.09133754351999990, 2.216715295763999727, -8.007133643737999407 ) ) ;
#11270=ORIENTED_EDGE ( 'NONE', *, *, #30786, .T. ) ;
#11273=CARTESIAN_POINT ( 'NONE',  ( 7.966901574931999797, 4.609574279519000228, -6.276317554486000816 ) ) ;
#11277=VECTOR ( 'NONE', #9239, 1000.000000000000000 ) ;
#11279=ORIENTED_EDGE ( 'NONE', *, *, #32405, .F. ) ;
#11280=CARTESIAN_POINT ( 'NONE',  ( 6.828228317543000081, 2.534482666265000184, -7.314862106114000007 ) ) ;
#11286=CARTESIAN_POINT ( 'NONE',  ( 8.699089158774000907, 4.178200486578000472, -5.608493638783999202 ) ) ;
#11291=CARTESIAN_POINT ( 'NONE',  ( 11.12988950457999948, 5.284594281680999650, -4.847983311486999902 ) ) ;
#11300=DIRECTION ( 'NONE',  ( 0.000000000000000000, -0.9916377111174247139, 0.1290528957048031888 ) ) ;
#11308=B_SPLINE_CURVE_WITH_KNOTS ( 'NONE', 3,
 ( #52232, #35818, #40374, #56456 ),
 .UNSPECIFIED., .F., .F.,
 ( 4, 4 ),
 ( 0.000000000000000000, 1.000000000000000000 ),
 .UNSPECIFIED. ) ;
#11316=VERTEX_POINT ( 'NONE', #33484 ) ;
#11328=CARTESIAN_POINT ( 'NONE',  ( 10.68360729283125465, 2.821290678667913276, 8.178873955024702269 ) ) ;
#11329=DIRECTION ( 'NONE',  ( -1.000000000000000000, 0.000000000000000000, 0.000000000000000000 ) ) ;
#11330=ORIENTED_EDGE ( 'NONE', *, *, #33500, .T. ) ;
#11333=ORIENTED_EDGE ( 'NONE', *, *, #43007, .T. ) ;
#11336=CARTESIAN_POINT ( 'NONE',  ( 8.142589158771000868, 5.074768364528000397, -8.296267706722000312 ) ) ;
#11337=EDGE_CURVE ( 'NONE', #38413, #31036, #5215, .T. ) ;
#11342=CARTESIAN_POINT ( 'NONE',  ( 7.961735841224999000, 4.624432025063999419, -9.294334464733999823 ) ) ;
#11346=ORIENTED_EDGE ( 'NONE', *, *, #6289, .F. ) ;
#11349=DIRECTION ( 'NONE',  ( 0.000000000000000000, 0.000000000000000000, 1.000000000000000000 ) ) ;
#11352=CARTESIAN_POINT ( 'NONE',  ( 11.09999999999999964, 2.899999999999999911, -4.467422426380999845 ) ) ;
#11364=CARTESIAN_POINT ( 'NONE',  ( 10.07770645819999977, 4.622041375574999833, 5.671348593713000596 ) ) ;
#11368=CARTESIAN_POINT ( 'NONE',  ( 9.221802827889732157, 2.874603711573444187, 6.749639981083119800 ) ) ;
#11389=EDGE_CURVE ( 'NONE', #19719, #58783, #45695, .T. ) ;
#11393=CARTESIAN_POINT ( 'NONE',  ( 8.424364158774000799, 3.292387953886000140, -6.294868737226000377 ) ) ;
#11396=AXIS2_PLACEMENT_3D ( 'NONE', #67178, #3550, #35723 ) ;
#11397=CARTESIAN_POINT ( 'NONE',  ( 0.3871700897145999853, -0.5648807336705999882, -3.658284285490000176 ) ) ;
#11400=CARTESIAN_POINT ( 'NONE',  ( 1.980200647714000173, 3.111577884474999500, -2.108416590332999885 ) ) ;
#11406=CARTESIAN_POINT ( 'NONE',  ( 8.860767219592000643, 2.935741164366000522, 6.259844213126999790 ) ) ;
#11410=CARTESIAN_POINT ( 'NONE',  ( 7.250820280410000152, 2.436157974829999961, -7.440523950196999969 ) ) ;
#11423=CARTESIAN_POINT ( 'NONE',  ( 10.98768472638000127, 7.408460511344000743, 6.159405790617999976 ) ) ;
#11425=DIRECTION ( 'NONE',  ( 0.000000000000000000, -0.7158784314710772145, -0.6982249432342778617 ) ) ;
#11429=CARTESIAN_POINT ( 'NONE',  ( 9.079732780410999737, 5.421534627450999899, 6.381126373995999579 ) ) ;
#11430=EDGE_CURVE ( 'NONE', #10178, #47578, #6567, .T. ) ;
#11434=CARTESIAN_POINT ( 'NONE',  ( 11.07202612390000063, 6.387422431570000114, -5.354923180025000562 ) ) ;
#11437=CARTESIAN_POINT ( 'NONE',  ( 0.4068495934470809372, -2.724938773265916492, -2.093043791803330222 ) ) ;
#11438=CARTESIAN_POINT ( 'NONE',  ( 8.383148997457999130, 5.167567567567999731, 6.822293592207000934 ) ) ;
#11439=DIRECTION ( 'NONE',  ( 0.000000000000000000, -0.9835907196275001096, -0.1804142351995999538 ) ) ;
#11451=CARTESIAN_POINT ( 'NONE',  ( 8.748814158775001459, 5.251032986819000214, -6.070151079272999795 ) ) ;
#11452=CARTESIAN_POINT ( 'NONE',  ( 10.28774346735000123, 5.077605961126000267, -5.991341245382999503 ) ) ;
#11456=CARTESIAN_POINT ( 'NONE',  ( 10.13049857835000012, 3.092060693447000297, 8.629378633793999498 ) ) ;
#11457=EDGE_LOOP ( 'NONE', ( #62556, #28157, #22428, #32132 ) ) ;
#11459=CARTESIAN_POINT ( 'NONE',  ( 9.538432183420001209, 5.620896541217999420, 7.423100299691999915 ) ) ;
#11462=CARTESIAN_POINT ( 'NONE',  ( 5.500000000000000000, 12.78667792605000031, -2.345384795462000405 ) ) ;
#11464=CARTESIAN_POINT ( 'NONE',  ( 7.100000000000168399, 3.318691773287608449, -8.707120243254404812 ) ) ;
#11466=DIRECTION ( 'NONE',  ( 0.000000000000000000, 0.000000000000000000, -1.000000000000000000 ) ) ;
#11468=EDGE_CURVE ( 'NONE', #13653, #51766, #15509, .T. ) ;
#11475=B_SPLINE_CURVE_WITH_KNOTS ( 'NONE', 3,
 ( #40287, #14411, #56714, #45874, #13721, #67526, #3221, #68207, #67872, #29471, #34706, #24550, #45538, #66847, #50780, #19296 ),
 .UNSPECIFIED., .F., .F.,
 ( 4, 2, 2, 2, 2, 2, 2, 4 ),
 ( 0.1254282067584606419, 0.2190722812470546343, 0.3127163557356486545, 0.4063604302242426192, 0.5000045047128366393, 0.6872926536900242356, 0.7809367281786182557, 0.8745808026672123869 ),
 .UNSPECIFIED. ) ;
#11477=ORIENTED_EDGE ( 'NONE', *, *, #39965, .T. ) ;
#11479=CARTESIAN_POINT ( 'NONE',  ( 8.218892219592001780, 3.011620138462000273, 8.801434747080000065 ) ) ;
#11480=CARTESIAN_POINT ( 'NONE',  ( 8.175739158770999992, 4.686731264770999772, -8.717075579553000608 ) ) ;
#11481=CARTESIAN_POINT ( 'NONE',  ( 10.61094409420999973, 5.100000000000000533, -6.571291218949999902 ) ) ;
#11484=CARTESIAN_POINT ( 'NONE',  ( 11.03856029907000114, 2.974095820320000083, 8.716122353065999917 ) ) ;
#11488=CARTESIAN_POINT ( 'NONE',  ( 7.428092358015002006, 3.524408735919001501, 6.653372890553997721 ) ) ;
#11500=CARTESIAN_POINT ( 'NONE',  ( 8.434803823919004628, 2.901237182992001173, 6.624660446101000133 ) ) ;
#11503=CARTESIAN_POINT ( 'NONE',  ( 9.667489158770999680, 4.808846957865000604, -8.639578604182998944 ) ) ;
#11508=CARTESIAN_POINT ( 'NONE',  ( 9.064883232718324635, 5.349954811645839747, -7.500006748065883855 ) ) ;
#11517=CARTESIAN_POINT ( 'NONE',  ( 10.97216345308000029, 2.857785899823000353, -4.994019200607999309 ) ) ;
#11518=FACE_OUTER_BOUND ( 'NONE', #30206, .T. ) ;
#11524=CARTESIAN_POINT ( 'NONE',  ( 7.802017219589999719, 5.638704226117999596, 8.266404648244000342 ) ) ;
#11525=VERTEX_POINT ( 'NONE', #30993 ) ;
#11527=ADVANCED_FACE ( 'NONE', ( #68716 ), #30642, .F. ) ;
#11530=CARTESIAN_POINT ( 'NONE',  ( 9.769471092180999960, 5.100000000000000533, -6.152188490330000370 ) ) ;
#11531=FACE_OUTER_BOUND ( 'NONE', #45918, .T. ) ;
#11535=CARTESIAN_POINT ( 'NONE',  ( 10.95622765495000195, 9.844278095421000074, 5.755901431881000008 ) ) ;
#11538=EDGE_LOOP ( 'NONE', ( #30026, #9307 ) ) ;
#11541=CARTESIAN_POINT ( 'NONE',  ( 9.903950872528001881, 5.205009505618999555, 6.747225973806000532 ) ) ;
#11542=CARTESIAN_POINT ( 'NONE',  ( 8.304100344616170304, 2.916767839732335776, -6.503809950610432544 ) ) ;
#11547=CARTESIAN_POINT ( 'NONE',  ( 8.791232780412000736, 5.095085596809999728, 6.286981168432999922 ) ) ;
#11553=CARTESIAN_POINT ( 'NONE',  ( 10.50084834123000022, 4.616783736607999344, -6.288082254674000282 ) ) ;
#11554=CARTESIAN_POINT ( 'NONE',  ( 0.000000000000000000, 2.899999999999999911, -7.500000000000000000 ) ) ;
#11556=CARTESIAN_POINT ( 'NONE',  ( 5.000000000000000000, 0.2999999999999999889, 3.149999999999999911 ) ) ;
#11565=DIRECTION ( 'NONE',  ( 1.000000000000000000, 0.000000000000000000, 0.000000000000000000 ) ) ;
#11570=DIRECTION ( 'NONE',  ( 1.000000000000000000, 0.000000000000000000, 0.000000000000000000 ) ) ;
#11573=CARTESIAN_POINT ( 'NONE',  ( 0.8468373879278999761, -2.423129934138000152, -2.873468012158999940 ) ) ;
#11576=CARTESIAN_POINT ( 'NONE',  ( 10.51655086620999846, 4.930662802525000110, 8.573584269714999095 ) ) ;
#11580=CARTESIAN_POINT ( 'NONE',  ( 7.933148997457998952, 5.167567567567999731, 6.822293592207000934 ) ) ;
#11585=EDGE_CURVE ( 'NONE', #6078, #60646, #46753, .T. ) ;
#11587=CARTESIAN_POINT ( 'NONE',  ( 7.424379198296266580, 2.348612827597222896, 8.058989540383295846 ) ) ;
#11591=B_SPLINE_CURVE_WITH_KNOTS ( 'NONE', 3,
 ( #17002, #27860, #46861, #20284 ),
 .UNSPECIFIED., .F., .F.,
 ( 4, 4 ),
 ( 0.000000000000000000, 1.000000000000000000 ),
 .UNSPECIFIED. ) ;
#11597=CARTESIAN_POINT ( 'NONE',  ( 8.383148997457999130, 5.167567567567999731, 6.822293592207000934 ) ) ;
#11604=CARTESIAN_POINT ( 'NONE',  ( 4.000000000000000888, -1.878608423871360289, -1.082950885222729198 ) ) ;
#11606=CARTESIAN_POINT ( 'NONE',  ( 8.821685841230998193, 2.633142096252999664, -7.791134854666999843 ) ) ;
#11607=ORIENTED_EDGE ( 'NONE', *, *, #32196, .T. ) ;
#11609=( NAMED_UNIT ( * ) PLANE_ANGLE_UNIT ( ) SI_UNIT ( $, .RADIAN. ) );
#11610=ORIENTED_EDGE ( 'NONE', *, *, #57045, .F. ) ;
#11611=CARTESIAN_POINT ( 'NONE',  ( 11.09999999999999964, 5.350000000000000533, -7.500000000000000000 ) ) ;
#11619=LINE ( 'NONE', #50079, #50428 ) ;
#11627=CARTESIAN_POINT ( 'NONE',  ( 9.476970280414001024, 5.511689883260999956, -7.095113581311000672 ) ) ;
#11628=DIRECTION ( 'NONE',  ( 1.000000000000000000, 0.000000000000000000, 0.000000000000000000 ) ) ;
#11631=CARTESIAN_POINT ( 'NONE',  ( 8.085754734272050825, 5.349973530442185599, -7.853162922483586605 ) ) ;
#11634=CARTESIAN_POINT ( 'NONE',  ( 6.899999691988000450, 12.99045401563999924, 1.690592933733000125 ) ) ;
#11643=ORIENTED_EDGE ( 'NONE', *, *, #47353, .F. ) ;
#11646=AXIS2_PLACEMENT_3D ( 'NONE', #2402, #13254, #44383 ) ;
#11648=ADVANCED_FACE ( 'NONE', ( #57895 ), #42508, .T. ) ;
#11650=ADVANCED_FACE ( 'NONE', ( #52645 ), #20146, .T. ) ;
#11664=CARTESIAN_POINT ( 'NONE',  ( 0.9780567992084204798, 2.150913519912206695, -2.798833948393626869 ) ) ;
#11672=CARTESIAN_POINT ( 'NONE',  ( 7.000000000000000000, 10.75808151192356732, 3.620680867180093188 ) ) ;
#11682=CARTESIAN_POINT ( 'NONE',  ( 9.418864158773999407, 3.210851187372000037, -6.346613542714999667 ) ) ;
#11683=EDGE_LOOP ( 'NONE', ( #45278, #5604, #47870, #12916 ) ) ;
#11686=CARTESIAN_POINT ( 'NONE',  ( 8.011460841224998575, 3.456780951359999854, -9.320567109458000488 ) ) ;
#11707=DIRECTION ( 'NONE',  ( 0.000000000000000000, 1.000000000000000000, 0.000000000000000000 ) ) ;
#11708=CARTESIAN_POINT ( 'NONE',  ( 11.15264221959000146, 2.317063201199000222, -7.596564358366999947 ) ) ;
#11716=VERTEX_POINT ( 'NONE', #43887 ) ;
#11717=CARTESIAN_POINT ( 'NONE',  ( 9.242342830452999536, 5.206708472530999998, 8.808826521083998884 ) ) ;
#11725=FACE_OUTER_BOUND ( 'NONE', #63244, .T. ) ;
#11734=CARTESIAN_POINT ( 'NONE',  ( 4.149992563291999836, 1.007210908820209028, 1.747525841223986243 ) ) ;
#11737=CARTESIAN_POINT ( 'NONE',  ( 9.550320280412000429, 2.370176859044999862, -6.912649125838000508 ) ) ;
#11742=CARTESIAN_POINT ( 'NONE',  ( 0.7079009740474999646, -3.376221432737999795, -1.056438743269999980 ) ) ;
#11743=AXIS2_PLACEMENT_3D ( 'NONE', #9555, #25643, #30896 ) ;
#11745=CARTESIAN_POINT ( 'NONE',  ( 10.17270667456000055, 4.650145611776999921, -8.655516756809999990 ) ) ;
#11746=VERTEX_POINT ( 'NONE', #48783 ) ;
#11751=CARTESIAN_POINT ( 'NONE',  ( 8.309482780410998970, 2.905861847853000057, 8.940690431604000565 ) ) ;
#11755=CARTESIAN_POINT ( 'NONE',  ( 8.005554719585999734, 4.569394889178999719, -9.136182695123999054 ) ) ;
#11760=CARTESIAN_POINT ( 'NONE',  ( -15.86200481174999943, 0.8000000000000000444, 3.149999999999999911 ) ) ;
#11761=CARTESIAN_POINT ( 'NONE',  ( 10.02314899745999988, 5.167567567567999731, -6.822293592207000934 ) ) ;
#11763=CARTESIAN_POINT ( 'NONE',  ( 11.09999999999999964, 2.274006712557999688, -7.281956340829000673 ) ) ;
#11774=VERTEX_POINT ( 'NONE', #27815 ) ;
#11775=DIRECTION ( 'NONE',  ( 0.000000000000000000, 0.000000000000000000, 1.000000000000000000 ) ) ;
#11780=CARTESIAN_POINT ( 'NONE',  ( 11.12484646121000154, 5.434138738817000380, -5.164717599857000074 ) ) ;
#11786=CARTESIAN_POINT ( 'NONE',  ( 8.286697165045001867, 5.451921732286531430, -6.342020349060414119 ) ) ;
#11797=VECTOR ( 'NONE', #54743, 1000.000000000000000 ) ;
#11798=CARTESIAN_POINT ( 'NONE',  ( 9.386379719595000282, 5.673443217382001080, -7.051790060464000476 ) ) ;
#11799=CARTESIAN_POINT ( 'NONE',  ( 10.60199294549000193, 2.164976235211999889, -7.764525279724000306 ) ) ;
#11807=CARTESIAN_POINT ( 'NONE',  ( 9.104014120666999332, 5.045862207587999748, 8.527865280865999154 ) ) ;
#11812=CARTESIAN_POINT ( 'NONE',  ( 10.43134583106436608, 2.301117676469145223, 7.915378199131434478 ) ) ;
#11816=SURFACE_STYLE_FILL_AREA ( #26880 ) ;
#11827=CARTESIAN_POINT ( 'NONE',  ( 8.887170280412000523, 2.193665972875999959, 7.400591513898000073 ) ) ;
#11828=CARTESIAN_POINT ( 'NONE',  ( 9.658629719592001450, 5.496789211521000418, -7.043125396300999874 ) ) ;
#11830=CARTESIAN_POINT ( 'NONE',  ( 10.60000000000016662, 3.352395157604608933, 4.756097560975663718 ) ) ;
#11832=CARTESIAN_POINT ( 'NONE',  ( 9.520797373037000355, 3.270552986600999912, 5.711478154812000163 ) ) ;
#11839=B_SPLINE_CURVE_WITH_KNOTS ( 'NONE', 3,
 ( #19103, #13190, #13869, #56168, #45685 ),
 .UNSPECIFIED., .F., .F.,
 ( 4, 1, 4 ),
 ( 0.8746155046758248286, 0.9972320922596067394, 1.000000000000000000 ),
 .UNSPECIFIED. ) ;
#11840=EDGE_CURVE ( 'NONE', #44223, #28596, #16214, .T. ) ;
#11853=CARTESIAN_POINT ( 'NONE',  ( 8.822164158776001130, 2.644017913812000131, -7.838184857420000817 ) ) ;
#11857=CARTESIAN_POINT ( 'NONE',  ( 7.952954263467808538, 4.709204723604079490, -6.291795282047308646 ) ) ;
#11859=ORIENTED_EDGE ( 'NONE', *, *, #42496, .T. ) ;
#11862=DIRECTION ( 'NONE',  ( 1.000000000000000000, 0.000000000000000000, 0.000000000000000000 ) ) ;
#11866=EDGE_CURVE ( 'NONE', #53988, #65371, #23248, .T. ) ;
#11868=CARTESIAN_POINT ( 'NONE',  ( 10.60199294549000193, 2.164976235211999889, -7.764525279724000306 ) ) ;
#11876=CARTESIAN_POINT ( 'NONE',  ( 9.021579719592999425, 2.193665972875999959, 7.400591513898000073 ) ) ;
#11881=CARTESIAN_POINT ( 'NONE',  ( 7.100000000000000533, 4.000000000000000000, 8.849999999999999645 ) ) ;
#11886=CARTESIAN_POINT ( 'NONE',  ( 10.96578430013000016, 7.637186626153999569, 6.308908953828000321 ) ) ;
#11895=CONICAL_SURFACE ( 'NONE', #770, 12.44999944941000081, 0.7853981146832407223 ) ;
#11896=B_SPLINE_CURVE_WITH_KNOTS ( 'NONE', 3,
 ( #65908, #18036, #60673, #12786 ),
 .UNSPECIFIED., .F., .F.,
 ( 4, 4 ),
 ( 0.000000000000000000, 1.000000000000000000 ),
 .UNSPECIFIED. ) ;
#11899=CARTESIAN_POINT ( 'NONE',  ( 7.464691113743000095, 4.351669901925999895, 8.977196921526999773 ) ) ;
#11903=CARTESIAN_POINT ( 'NONE',  ( 10.08477413932373246, 4.544730055193329399, -8.875862789218047055 ) ) ;
#11908=CARTESIAN_POINT ( 'NONE',  ( 8.361434368299004660, 5.126350915548002263, 6.365320234831002288 ) ) ;
#11913=CARTESIAN_POINT ( 'NONE',  ( 1.691702730658999787, 2.350777309937000403, -2.257240049571999752 ) ) ;
#11918=B_SPLINE_CURVE_WITH_KNOTS ( 'NONE', 3,
 ( #38493, #11920, #33261, #60859 ),
 .UNSPECIFIED., .F., .F.,
 ( 4, 4 ),
 ( 0.8744711836180196762, 1.000000000000000000 ),
 .UNSPECIFIED. ) ;
#11920=CARTESIAN_POINT ( 'NONE',  ( 7.961731591766461946, 5.351349901897397565, 7.263035046629775060 ) ) ;
#11926=CARTESIAN_POINT ( 'NONE',  ( 8.603645510037566169, 4.706833859774536499, 5.918599468013309384 ) ) ;
#11928=CARTESIAN_POINT ( 'NONE',  ( 10.17905590578999941, 2.899999999999999911, 6.571291218949999902 ) ) ;
#11929=CARTESIAN_POINT ( 'NONE',  ( 0.4812757755485000399, 3.010927365844000114, -1.992372462812000089 ) ) ;
#11932=CARTESIAN_POINT ( 'NONE',  ( 10.85069631730999973, 4.478098874537000285, 6.162039661770999821 ) ) ;
#11939=CARTESIAN_POINT ( 'NONE',  ( 9.865041550948095761, 2.650034642413356512, -7.500002425457249267 ) ) ;
#11942=CARTESIAN_POINT ( 'NONE',  ( 7.466031583599719745, 2.286618937992697997, 7.155872792181217079 ) ) ;
#11950=DIRECTION ( 'NONE',  ( -1.000000000000000000, 0.000000000000000000, 0.000000000000000000 ) ) ;
#11952=CARTESIAN_POINT ( 'NONE',  ( 9.194604681486000075, 5.157771204918000230, 8.637848577075999401 ) ) ;
#11962=ORIENTED_EDGE ( 'NONE', *, *, #67625, .T. ) ;
#11974=ORIENTED_EDGE ( 'NONE', *, *, #57682, .T. ) ;
#11975=CARTESIAN_POINT ( 'NONE',  ( 7.243409439180999776, 5.346164515353000191, -7.398308812559000636 ) ) ;
#11980=CARTESIAN_POINT ( 'NONE',  ( 8.541054719591000932, 3.807713920470999991, -9.221758713517999695 ) ) ;
#11999=AXIS2_PLACEMENT_3D ( 'NONE', #7215, #1624, #22939 ) ;
#12013=EDGE_CURVE ( 'NONE', #8503, #53057, #64216, .T. ) ;
#12014=CARTESIAN_POINT ( 'NONE',  ( 6.999999999999997335, 10.71083106425634490, -3.767558118307691828 ) ) ;
#12021=VERTEX_POINT ( 'NONE', #40029 ) ;
#12028=CARTESIAN_POINT ( 'NONE',  ( 7.000000000000000000, 8.619706073299337135, 4.541782559989387735 ) ) ;
#12035=VERTEX_POINT ( 'NONE', #55758 ) ;
#12039=CARTESIAN_POINT ( 'NONE',  ( 9.758079719591000512, 4.905765359186999852, -8.776126235875999271 ) ) ;
#12040=DIRECTION ( 'NONE',  ( -1.000000000000000000, 0.000000000000000000, 0.000000000000000000 ) ) ;
#12042=CARTESIAN_POINT ( 'NONE',  ( 7.912010841225000313, 5.556101987819999977, -8.589999141415001205 ) ) ;
#12049=ORIENTED_EDGE ( 'NONE', *, *, #62825, .F. ) ;
#12051=CARTESIAN_POINT ( 'NONE',  ( 8.865073590557452476, 2.650142864597553327, -7.500004675916596142 ) ) ;
#12057=CARTESIAN_POINT ( 'NONE',  ( 7.720595830382998237, 4.816914828557000483, -6.342622631669999400 ) ) ;
#12059=FACE_OUTER_BOUND ( 'NONE', #18215, .T. ) ;
#12061=VECTOR ( 'NONE', #41608, 1000.000000000000000 ) ;
#12064=EDGE_LOOP ( 'NONE', ( #1935, #64152, #33425, #33405, #21171, #68057, #40777, #45987 ) ) ;
#12066=CARTESIAN_POINT ( 'NONE',  ( 10.25880778041000063, 2.491777456852000139, -7.289938575364999451 ) ) ;
#12072=CYLINDRICAL_SURFACE ( 'NONE', #63172, 1.350000000000000533 ) ;
#12075=CARTESIAN_POINT ( 'NONE',  ( 9.345514158774999913, 5.775964236216999836, -8.174909295649001706 ) ) ;
#12089=CARTESIAN_POINT ( 'NONE',  ( 10.40537527825904007, 5.100000000000000533, -6.445686799541589629 ) ) ;
#12097=CARTESIAN_POINT ( 'NONE',  ( 9.798945280410000791, 5.639765292528999829, -8.059103558718000215 ) ) ;
#12100=AXIS2_PLACEMENT_3D ( 'NONE', #30961, #46697, #10312 ) ;
#12104=CARTESIAN_POINT ( 'NONE',  ( 2.023109259092000567, 1.242860124574000080, -3.147067557564999785 ) ) ;
#12106=AXIS2_PLACEMENT_3D ( 'NONE', #35111, #66214, #18336 ) ;
#12110=CARTESIAN_POINT ( 'NONE',  ( 8.477766462057999775, 2.899999999999999911, -6.558719934578999933 ) ) ;
#12111=CARTESIAN_POINT ( 'NONE',  ( 8.604017219593000476, 5.165497731316000873, 8.645531386060000045 ) ) ;
#12114=CARTESIAN_POINT ( 'NONE',  ( 7.309404719586999555, 4.580689680786999674, -5.867791741075000900 ) ) ;
#12117=CARTESIAN_POINT ( 'NONE',  ( 10.96876099447000108, 2.333339469804000199, 6.524055942683999021 ) ) ;
#12120=LINE ( 'NONE', #39040, #9854 ) ;
#12121=CARTESIAN_POINT ( 'NONE',  ( 10.05083014070727820, 5.349869709803526163, -7.263173528791787348 ) ) ;
#12122=ORIENTED_EDGE ( 'NONE', *, *, #6555, .T. ) ;
#12131=DIRECTION ( 'NONE',  ( -1.000000000000000000, 0.000000000000000000, 0.000000000000000000 ) ) ;
#12133=ORIENTED_EDGE ( 'NONE', *, *, #61833, .F. ) ;
#12134=CARTESIAN_POINT ( 'NONE',  ( 9.026926658770998202, 4.852728889087999598, 8.683917172082999514 ) ) ;
#12136=CARTESIAN_POINT ( 'NONE',  ( 10.06819717211483578, 5.125396288440276393, -6.749639981106758668 ) ) ;
#12140=AXIS2_PLACEMENT_3D ( 'NONE', #52196, #32264, #26323 ) ;
#12142=CARTESIAN_POINT ( 'NONE',  ( 7.242472165043829513, 4.622497589504547477, -5.750277660584385053 ) ) ;
#12144=DIRECTION ( 'NONE',  ( 1.000000000000000000, 0.000000000000000000, 0.000000000000000000 ) ) ;
#12147=AXIS2_PLACEMENT_3D ( 'NONE', #39883, #29402, #61882 ) ;
#12156=CARTESIAN_POINT ( 'NONE',  ( 2.670826577536000279, -1.894280328234999811, -2.798560188998999720 ) ) ;
#12164=CARTESIAN_POINT ( 'NONE',  ( 9.124700695083998170, 4.778663323155000420, 8.799742559280000265 ) ) ;
#12171=CARTESIAN_POINT ( 'NONE',  ( 10.29264778178926321, 4.710327358940427089, 9.125082257938260000 ) ) ;
#12174=DIRECTION ( 'NONE',  ( -1.000000000000000000, 0.000000000000000000, 0.000000000000000000 ) ) ;
#12182=VERTEX_POINT ( 'NONE', #63033 ) ;
#12184=CARTESIAN_POINT ( 'NONE',  ( 9.234510841229999656, 5.964723767581000757, 7.776480083716999836 ) ) ;
#12185=EDGE_CURVE ( 'NONE', #4475, #55227, #62699, .T. ) ;
#12186=CARTESIAN_POINT ( 'NONE',  ( 9.392285841233000809, 5.775964236216999836, -8.174909295649001706 ) ) ;
#12188=CARTESIAN_POINT ( 'NONE',  ( 10.71093936450548156, 3.092590697381819798, 4.810214324148986087 ) ) ;
#12190=CARTESIAN_POINT ( 'NONE',  ( 10.94796973825000030, 2.864322365205000054, 8.846249469408000721 ) ) ;
#12191=VECTOR ( 'NONE', #16719, 1000.000000000000000 ) ;
#12195=CARTESIAN_POINT ( 'NONE',  ( 7.656866975822993915, 3.528150633380001899, 6.493493947281997691 ) ) ;
#12202=FACE_OUTER_BOUND ( 'NONE', #22794, .T. ) ;
#12204=ORIENTED_EDGE ( 'NONE', *, *, #45645, .T. ) ;
#12208=CARTESIAN_POINT ( 'NONE',  ( 8.221179504219003675, 3.443168248977001245, 6.131664885159996636 ) ) ;
#12210=B_SPLINE_SURFACE_WITH_KNOTS ( 'NONE', 3, 3, ( 
 ( #37914, #54687, #58899, #59581, #21486, #16242, #43515, #11682, #49095, #17640, #38964, #27785, #64127, #37565, #1207, #60281, #43858, #6785, #59928, #49791, #33720, #21828, #64813, #42819, #11002, #17281, #43160, #1547, #12386, #55037, #38607, #59234, #33372, #11336, #32678 ),
 ( #6093, #7138, #12039, #65159, #48753, #858, #22175, #33022, #54334, #28123, #6436, #45244, #39302, #8176, #40001, #19349, #2580, #12736, #62002, #61314, #13770, #23908, #13085, #13435, #35103, #66894, #56765, #40671, #2923, #14115, #35439, #55732, #7834, #3270, #1900 ),
 ( #29525, #29170, #8862, #34416, #61656, #51174, #7476, #29866, #56415, #50142, #50478, #23221, #66551, #60972, #50827, #18669, #30200, #8518, #23560, #24601, #45921, #34756, #44568, #24251, #45589, #56066, #19006, #40333, #67233, #65860, #17983, #60625, #34066, #55382, #28831 ),
 ( #2247, #44901, #66204, #18326, #39649, #15138, #46957, #20725, #47302, #68606, #42053, #36459, #62342, #20381, #4634, #58469, #41708, #62677, #21070, #42401, #63359, #10232, #3945, #15821, #68957, #19700, #25973, #63709, #52886, #57778, #14459, #9889, #51505, #68260, #67575 ) ),
 .UNSPECIFIED., .F., .F., .F.,
 ( 4, 4 ),
 ( 4, 1, 1, 1, 1, 1, 1, 1, 1, 1, 1, 1, 1, 1, 1, 1, 1, 1, 1, 1, 1, 1, 1, 1, 1, 1, 1, 1, 1, 1, 1, 1, 4 ),
 ( -0.1039370721279000015, 1.103937072127999963 ),
 ( -0.02000000000000000042, 0.01250000000000000069, 0.04499999999999999833, 0.07749999999999999944, 0.1100000000000000006, 0.1424999999999999878, 0.1749999999999999889, 0.2074999999999999900, 0.2399999999999999911, 0.2725000000000000200, 0.3049999999999999933, 0.3375000000000000222, 0.3699999999999999956, 0.4025000000000000244, 0.4349999999999999978, 0.4675000000000000266, 0.5000000000000000000, 0.5324999999999999734, 0.5649999999999999467, 0.5975000000000000311, 0.6300000000000000044, 0.6624999999999999778, 0.6949999999999999512, 0.7275000000000000355, 0.7600000000000000089, 0.7924999999999999822, 0.8249999999999999556, 0.8575000000000000400, 0.8900000000000000133, 0.9224999999999999867, 0.9549999999999999600, 0.9875000000000000444, 1.020000000000000018 ),
 .UNSPECIFIED. ) ;
#12211=CARTESIAN_POINT ( 'NONE',  ( 8.863029719594999634, 2.990001567622999623, -8.695425648791999862 ) ) ;
#12215=DIRECTION ( 'NONE',  ( 0.000000000000000000, -0.8648648648648720183, -0.5020047465136825426 ) ) ;
#12226=CARTESIAN_POINT ( 'NONE',  ( 11.13711610230999938, 2.663427511852999974, -5.178750069089000263 ) ) ;
#12237=CARTESIAN_POINT ( 'NONE',  ( 8.379704719592000473, 4.283000592898000392, 9.286795422009001655 ) ) ;
#12239=CARTESIAN_POINT ( 'NONE',  ( 10.71685100253999856, 2.832432432432000269, 6.822293592207000934 ) ) ;
#12240=CARTESIAN_POINT ( 'NONE',  ( 5.399999746777999654, -13.10000000000000142, 0.000000000000000000 ) ) ;
#12241=CARTESIAN_POINT ( 'NONE',  ( 7.866682853741001402, 2.870179227930000021, -6.741414558537999646 ) ) ;
#12242=CARTESIAN_POINT ( 'NONE',  ( 10.40878363256000050, 3.093886843363999883, -6.480781753756000185 ) ) ;
#12245=CARTESIAN_POINT ( 'NONE',  ( 9.843732751558000871, 4.115124343450999866, 9.466620196856998959 ) ) ;
#12247=FACE_OUTER_BOUND ( 'NONE', #64405, .T. ) ;
#12252=DIRECTION ( 'NONE',  ( -1.000000000000000000, 0.000000000000000000, 0.000000000000000000 ) ) ;
#12256=CARTESIAN_POINT ( 'NONE',  ( 8.753448341231001351, 2.876288091423999660, 6.568897128359000526 ) ) ;
#12257=CARTESIAN_POINT ( 'NONE',  ( 10.65050915380999896, 5.200037120669999346, 5.937706951697999891 ) ) ;
#12260=CARTESIAN_POINT ( 'NONE',  ( 9.842764158772000727, 5.798263352390999437, -8.113145944980999502 ) ) ;
#12263=CARTESIAN_POINT ( 'NONE',  ( 7.690241772926001751, 4.592291064388997590, 6.438923047733998928 ) ) ;
#12268=LINE ( 'NONE', #27311, #1764 ) ;
#12271=CARTESIAN_POINT ( 'NONE',  ( 1.305473797069999886, 3.048238319583999711, -1.563029678068999839 ) ) ;
#12273=EDGE_CURVE ( 'NONE', #31943, #63357, #58638, .T. ) ;
#12276=CARTESIAN_POINT ( 'NONE',  ( 10.56577346846700038, 5.100000000000000533, 6.304440313576233024 ) ) ;
#12277=EDGE_CURVE ( 'NONE', #2331, #53988, #42422, .T. ) ;
#12279=CARTESIAN_POINT ( 'NONE',  ( 11.13509627278000025, 2.662095878336999899, 5.086083211022000228 ) ) ;
#12283=CARTESIAN_POINT ( 'NONE',  ( 7.437916666664375676, 3.170361928033863297, -6.420449762762457269 ) ) ;
#12285=CARTESIAN_POINT ( 'NONE',  ( 8.590472024761092840, 4.653241489312755164, 5.916299078424504643 ) ) ;
#12286=LINE ( 'NONE', #65050, #27980 ) ;
#12287=CARTESIAN_POINT ( 'NONE',  ( 0.6990182015430999041, 1.892658550137999995, 3.053125390820000007 ) ) ;
#12297=EDGE_LOOP ( 'NONE', ( #48229, #59762, #60515, #6361, #31195 ) ) ;
#12318=VERTEX_POINT ( 'NONE', #29117 ) ;
#12326=CARTESIAN_POINT ( 'NONE',  ( 10.01293113571299997, 5.100000000000000533, 6.444141223344916014 ) ) ;
#12329=CARTESIAN_POINT ( 'NONE',  ( 7.184909439180999335, 5.017953588770000195, -6.429833855306000601 ) ) ;
#12334=CARTESIAN_POINT ( 'NONE',  ( 9.974220280410998285, 5.496789211521000418, -7.043125396300999874 ) ) ;
#12341=DIRECTION ( 'NONE',  ( 0.000000000000000000, 1.000000000000000000, 0.000000000000000000 ) ) ;
#12347=FACE_OUTER_BOUND ( 'NONE', #31139, .T. ) ;
#12363=DIRECTION ( 'NONE',  ( 0.000000000000000000, 0.8304044637635152881, -0.5571610418556101063 ) ) ;
#12365=CARTESIAN_POINT ( 'NONE',  ( 6.899999691988000450, 12.20988339176000004, 3.111064831550000243 ) ) ;
#12373=CARTESIAN_POINT ( 'NONE',  ( 0.000000000000000000, -1.460905701137619417, -2.533699434756940594 ) ) ;
#12377=CARTESIAN_POINT ( 'NONE',  ( 4.900006121741999898, 1.747572776708514519, -1.007237960741801386 ) ) ;
#12378=CARTESIAN_POINT ( 'NONE',  ( 6.999999999999999112, 9.962435980213809827, 4.520115016280596976 ) ) ;
#12383=ORIENTED_EDGE ( 'NONE', *, *, #43570, .F. ) ;
#12384=CARTESIAN_POINT ( 'NONE',  ( 8.576923877145999242, 3.399999999999999911, 5.924121105096999962 ) ) ;
#12386=CARTESIAN_POINT ( 'NONE',  ( 8.374639158773000247, 2.721111233225000259, -6.936528696292000085 ) ) ;
#12392=ORIENTED_EDGE ( 'NONE', *, *, #37275, .T. ) ;
#12393=FACE_OUTER_BOUND ( 'NONE', #22356, .T. ) ;
#12395=ADVANCED_FACE ( 'NONE', ( #41312 ), #24546, .T. ) ;
#12397=CARTESIAN_POINT ( 'NONE',  ( 6.800000000000000711, 5.221516520829000640, -8.074802043613001246 ) ) ;
#12399=CARTESIAN_POINT ( 'NONE',  ( 10.88015784977000067, 2.793131772868000073, -6.864962922767000819 ) ) ;
#12405=CIRCLE ( 'NONE', #24678, 11.84999999999999964 ) ;
#12406=CARTESIAN_POINT ( 'NONE',  ( 11.09999803709000155, 0.4999945937327000545, 9.776630298829998011 ) ) ;
#12408=CARTESIAN_POINT ( 'NONE',  ( 11.01356641589999974, 2.786433584103999994, 6.253463831328000211 ) ) ;
#12413=CARTESIAN_POINT ( 'NONE',  ( 10.08211611373999972, 4.728047954991999369, -8.793974144431000894 ) ) ;
#12421=CLOSED_SHELL ( 'NONE', ( #40063, #58778, #43315, #51872, #17329, #31614, #16716, #43088, #34693, #29427, #24268, #2244, #3678, #11527, #64603, #50377, #7738, #32322, #59900, #23877, #10480, #8318, #15225, #48138, #53350, #36841, #64256, #68246, #1139, #17803, #3771, #48969, #49165, #63986, #63758, #63845, #8661, #65816, #37193, #51559, #42860, #52169, #407, #67864, #14746, #22247, #10218, #52128, #64853, #11648, #48611, #42663, #43841, #34773, #41128, #51329, #44724, #3269, #27277, #66911, #49792, #51104, #15698, #57455, #64451, #21209, #20448, #56753, #16643, #30073, #17077, #34610, #24457, #49883, #8757, #68809, #43003, #65500, #3853, #7279, #9801, #69087, #65421, #46139, #33899, #66232, #8409, #13024, #42054, #48010, #18626, #41152, #60241, #28256, #22079, #36222, #42319, #8051, #34335, #15582, #2013, #47935, #25335, #15078, #24185, #10782, #38855, #10249, #39786, #215, #41931, #58000, #10082, #4562, #21728, #24577, #28494, #61320, #21544, #40877, #45720, #54378, #58955, #5983, #47070, #35934, #7989, #42881, #33872, #36616, #64418, #32911, #51365, #19539, #4600, #9518, #1010, #29285, #47185, #61650, #43106, #5727, #14057, #9545, #56272, #30576, #54207, #12936, #19672, #40267, #25537, #67467, #38793, #18591, #4272, #16945, #45786, #43131, #37782, #55401, #17174, #23356, #13498, #32051, #20087, #44929, #53255, #40566, #16338, #30107, #29854, #19928, #18398, #35988, #19968, #9690, #66092, #33647, #54049, #35714, #8695, #24389, #47129, #63697, #65160, #11650, #38658, #49960, #54714, #44924, #49879, #12617, #34065, #25951, #1145, #62448, #64630, #59821, #28013, #48185, #37475, #57379, #68727, #16003, #14311, #53819, #30614, #8298, #25007, #45487, #59275, #56400, #18814, #30537, #9252, #25789, #64477, #44759, #33847, #31263, #23747, #55883, #49247, #47703, #5949, #14225, #18089, #48839, #66953, #65982, #16, #3568, #46921, #38459, #14366, #29775, #46965, #43795, #21682, #42415, #7704, #60137, #34357, #20230, #49001, #621, #5119, #25256, #55713, #32937, #41740, #928, #16334, #12395, #60301, #20663, #65705, #60139, #31489, #12987, #35387, #63024, #49195, #31930, #4894, #13197, #9461, #64602, #133, #66444, #53227, #43489, #13022, #41463, #67626, #19565, #24326, #2106, #35331, #25875, #63864, #6149, #3379, #45192, #37663, #24146, #53896, #29852, #14555, #18668, #33672, #58088, #63420, #24920, #9209, #60363 ) ) ;
#12425=CARTESIAN_POINT ( 'NONE',  ( 9.137754719594999742, 2.319062457810000311, -7.919229449146000022 ) ) ;
#12438=CARTESIAN_POINT ( 'NONE',  ( 8.266851002545999805, 2.832432432432000269, 6.822293592207000934 ) ) ;
#12443=CARTESIAN_POINT ( 'NONE',  ( 8.664129719593997692, 5.524776413195999325, -7.147585171405999915 ) ) ;
#12448=CARTESIAN_POINT ( 'NONE',  ( 2.929066298468999463, -2.590989723220999519, -2.488095879762999729 ) ) ;
#12455=CARTESIAN_POINT ( 'NONE',  ( 7.149100552923999707, 4.351669901925999895, 8.977196921526999773 ) ) ;
#12458=B_SPLINE_CURVE_WITH_KNOTS ( 'NONE', 3,
 ( #17627, #60614, #66883, #29512 ),
 .UNSPECIFIED., .F., .F.,
 ( 4, 4 ),
 ( 0.8155233265773513818, 1.000000000000000000 ),
 .UNSPECIFIED. ) ;
#12459=CARTESIAN_POINT ( 'NONE',  ( 8.335910841226001011, 2.603157881926999817, -7.543458285860999979 ) ) ;
#12461=DIRECTION ( 'NONE',  ( -0.000000000000000000, 1.000000000000000000, 0.000000000000000000 ) ) ;
#12468=AXIS2_PLACEMENT_3D ( 'NONE', #875, #16601, #38619 ) ;
#12471=CARTESIAN_POINT ( 'NONE',  ( 10.94809868027465960, 9.167339311643493360, -6.329225113183299278 ) ) ;
#12477=CARTESIAN_POINT ( 'NONE',  ( 8.898551658772998252, 5.146726419831999522, 6.597424767138000412 ) ) ;
#12479=EDGE_CURVE ( 'NONE', #23086, #53057, #50173, .T. ) ;
#12486=CARTESIAN_POINT ( 'NONE',  ( 8.336422165046002419, 5.855021065977306982, -7.410170379902396576 ) ) ;
#12491=EDGE_LOOP ( 'NONE', ( #2936, #61573, #19048 ) ) ;
#12495=CARTESIAN_POINT ( 'NONE',  ( 0.1499942179680000265, 2.678379783547567339, 0.7197945678028357941 ) ) ;
#12496=CARTESIAN_POINT ( 'NONE',  ( 10.03280471959000231, 3.987760651117999711, -9.123263301387000368 ) ) ;
#12497=CIRCLE ( 'NONE', #41532, 12.39999890530000037 ) ;
#12498=CARTESIAN_POINT ( 'NONE',  ( 3.467248883606000032, 0.03946336865253999987, 3.379145356818000323 ) ) ;
#12504=VERTEX_POINT ( 'NONE', #33889 ) ;
#12507=CARTESIAN_POINT ( 'NONE',  ( 9.447841622600000377, 5.447457912891000120, 7.431328695644999982 ) ) ;
#12512=AXIS2_PLACEMENT_3D ( 'NONE', #29123, #50092, #39599 ) ;
#12514=CARTESIAN_POINT ( 'NONE',  ( 10.43950453984525417, 2.266522852357361728, 7.738844268769847545 ) ) ;
#12519=CARTESIAN_POINT ( 'NONE',  ( 8.129547907574799837, 4.951600119927478616, -6.344532045157325939 ) ) ;
#12529=CARTESIAN_POINT ( 'NONE',  ( 7.191892219589999691, 3.501518846194999757, 9.055971388486000251 ) ) ;
#12530=CARTESIAN_POINT ( 'NONE',  ( 8.323770280408998801, 5.332332124071999857, -8.487089944253000340 ) ) ;
#12532=CARTESIAN_POINT ( 'NONE',  ( 10.72128915877000033, 4.673511966357999370, -5.778393480304000462 ) ) ;
#12536=CARTESIAN_POINT ( 'NONE',  ( 10.50244247011999832, 2.268911387573000038, 7.824865741583000300 ) ) ;
#12540=EDGE_LOOP ( 'NONE', ( #6595, #50957, #19934, #44009 ) ) ;
#12548=ORIENTED_EDGE ( 'NONE', *, *, #27146, .F. ) ;
#12549=CIRCLE ( 'NONE', #18141, 2.100000000000000533 ) ;
#12555=CARTESIAN_POINT ( 'NONE',  ( 9.342560841233000346, 5.835196551504000517, -7.008466539623000813 ) ) ;
#12557=CARTESIAN_POINT ( 'NONE',  ( 8.268352065779833282, 5.042535165667102248, 6.407252835108709021 ) ) ;
#12561=CARTESIAN_POINT ( 'NONE',  ( 9.304437359457891077, 2.650065539925081204, -7.676779421619798427 ) ) ;
#12572=CARTESIAN_POINT ( 'NONE',  ( 10.91624242361999997, 5.459834480072999874, -8.642877574935999618 ) ) ;
#12580=EDGE_LOOP ( 'NONE', ( #22524, #37938, #3917, #66367, #65335, #45485, #51328 ) ) ;
#12584=CARTESIAN_POINT ( 'NONE',  ( 10.90638722582999875, 5.227488226180000197, 6.784465725675999259 ) ) ;
#12589=CARTESIAN_POINT ( 'NONE',  ( 10.40227026081000083, 2.765684886876999649, 9.035354958280999327 ) ) ;
#12592=CARTESIAN_POINT ( 'NONE',  ( 2.286817272374999543, 2.922173510531999696, 1.340674101542000063 ) ) ;
#12596=FACE_OUTER_BOUND ( 'NONE', #12064, .T. ) ;
#12601=CARTESIAN_POINT ( 'NONE',  ( 8.175760841228999709, 2.599243720295000060, 7.909344432242998657 ) ) ;
#12602=CARTESIAN_POINT ( 'NONE',  ( 10.89874804681000064, 2.834828962328999502, 9.088465460431999432 ) ) ;
#12605=CARTESIAN_POINT ( 'NONE',  ( 9.635004719593998956, 2.334550724494000029, -7.977056617806000283 ) ) ;
#12613=CARTESIAN_POINT ( 'NONE',  ( 2.168522225066999987, 1.603576596796000064, -2.837084241009999896 ) ) ;
#12617=ADVANCED_FACE ( 'NONE', ( #34235 ), #8346, .T. ) ;
#12621=CARTESIAN_POINT ( 'NONE',  ( 11.05669207475000171, 2.810775113057000230, 4.849214660961000511 ) ) ;
#12624=VERTEX_POINT ( 'NONE', #66722 ) ;
#12629=CARTESIAN_POINT ( 'NONE',  ( 10.76947109217999810, 5.100000000000000533, -6.152188490330000370 ) ) ;
#12630=CARTESIAN_POINT ( 'NONE',  ( 1.275974932895000080, -3.758001540264999996, 0.07616889274500000806 ) ) ;
#12631=ORIENTED_EDGE ( 'NONE', *, *, #1799, .T. ) ;
#12634=CARTESIAN_POINT ( 'NONE',  ( 10.79500540879000070, 3.503955365545999623, 6.168588659884999714 ) ) ;
#12639=CARTESIAN_POINT ( 'NONE',  ( 0.5000220334827000235, 2.806761118207999672, -2.090954811877999919 ) ) ;
#12641=VERTEX_POINT ( 'NONE', #34923 ) ;
#12642=CARTESIAN_POINT ( 'NONE',  ( 7.327778877203178887, 3.954478523966745040, 9.238305800967093973 ) ) ;
#12644=AXIS2_PLACEMENT_3D ( 'NONE', #64268, #52416, #58347 ) ;
#12645=B_SPLINE_CURVE_WITH_KNOTS ( 'NONE', 3,
 ( #46321, #51893, #62048, #62388, #47005, #51219, #30928, #67281, #19399, #57141, #56812, #20426, #51552, #3991, #41755, #25327 ),
 .UNSPECIFIED., .F., .F.,
 ( 4, 2, 2, 1, 1, 2, 2, 2, 4 ),
 ( 0.000000000000000000, 0.2499999999999812372, 0.3749999999999744094, 0.4374999999999678035, 0.4687499999999645284, 0.4843749999999643618, 0.4999999999999642508, 0.7499999999999821254, 1.000000000000000000 ),
 .UNSPECIFIED. ) ;
#12653=CARTESIAN_POINT ( 'NONE',  ( 10.96080777006000062, 2.054568739078000306, 7.810084630238000258 ) ) ;
#12658=CARTESIAN_POINT ( 'NONE',  ( 10.97807333593999957, 5.235090452703000885, -6.783100406990000053 ) ) ;
#12659=CARTESIAN_POINT ( 'NONE',  ( -15.86200481174999943, 2.399999999999999911, -6.571291218949999902 ) ) ;
#12675=VERTEX_POINT ( 'NONE', #62162 ) ;
#12676=CARTESIAN_POINT ( 'NONE',  ( 7.313271682458000633, 2.788803157567000035, -8.345558963038001821 ) ) ;
#12677=CARTESIAN_POINT ( 'NONE',  ( 8.893038976302710452, 2.713248994154062732, -7.026754482570071403 ) ) ;
#12680=CARTESIAN_POINT ( 'NONE',  ( 9.576420280414000175, 4.861259245430999520, -8.806664389576001284 ) ) ;
#12683=CARTESIAN_POINT ( 'NONE',  ( 5.500000000000000000, 12.78667792605000031, -2.345384795462000405 ) ) ;
#12688=CARTESIAN_POINT ( 'NONE',  ( 10.90000000162999960, 2.899999999992999733, -5.160242739096000619 ) ) ;
#12694=VERTEX_POINT ( 'NONE', #25104 ) ;
#12702=LINE ( 'NONE', #27756, #50883 ) ;
#12736=CARTESIAN_POINT ( 'NONE',  ( 9.012204719595001023, 3.161445734422999809, -6.178649910536000434 ) ) ;
#12747=CARTESIAN_POINT ( 'NONE',  ( 10.10656234570999956, 4.887646627408000377, -6.257286147482000516 ) ) ;
#12749=VERTEX_POINT ( 'NONE', #37465 ) ;
#12756=EDGE_CURVE ( 'NONE', #9405, #14271, #32241, .T. ) ;
#12761=CARTESIAN_POINT ( 'NONE',  ( 10.92546721959000067, 5.641524285727999910, -7.883474821562000301 ) ) ;
#12773=CARTESIAN_POINT ( 'NONE',  ( 9.444964158775000840, 3.920043641733999884, -9.398198753036000497 ) ) ;
#12775=VECTOR ( 'NONE', #45320, 1000.000000000000114 ) ;
#12777=CARTESIAN_POINT ( 'NONE',  ( 10.93769906941999892, 2.936877991120999898, -4.920829195977000303 ) ) ;
#12779=CARTESIAN_POINT ( 'NONE',  ( 6.999999691988000095, -13.87069231928999891, 4.225386915259999654 ) ) ;
#12786=CARTESIAN_POINT ( 'NONE',  ( 7.871384581343000342, 5.129340811002999878, 6.740051537885999977 ) ) ;
#12789=CARTESIAN_POINT ( 'NONE',  ( 4.149992563292000725, 2.000000000000000000, 0.000000000000000000 ) ) ;
#12792=CARTESIAN_POINT ( 'NONE',  ( 9.587317385018980787, 5.286614015217494078, -7.026982148269482309 ) ) ;
#12793=CARTESIAN_POINT ( 'NONE',  ( 9.260829719593999698, 4.861259245430999520, -8.806664389576001284 ) ) ;
#12794=EDGE_CURVE ( 'NONE', #1019, #10847, #5946, .T. ) ;
#12797=AXIS2_PLACEMENT_3D ( 'NONE', #68069, #3415, #67384 ) ;
#12801=CARTESIAN_POINT ( 'NONE',  ( 3.215157995114000133, 1.238879411953999865, 3.371798807325999903 ) ) ;
#12804=CARTESIAN_POINT ( 'NONE',  ( 5.399998535875000449, 2.451372438371999805E-13, 6.461498003317998333E-14 ) ) ;
#12806=CARTESIAN_POINT ( 'NONE',  ( 8.347267219593000220, 2.741641653469999884, 6.457329666915000210 ) ) ;
#12807=ORIENTED_EDGE ( 'NONE', *, *, #30229, .T. ) ;
#12809=CARTESIAN_POINT ( 'NONE',  ( 10.95457883563474155, 9.034768305091144924, 6.398572458980741118 ) ) ;
#12810=EDGE_CURVE ( 'NONE', #3072, #33524, #63395, .T. ) ;
#12812=CARTESIAN_POINT ( 'NONE',  ( 10.67956456102485951, 4.176706786694609264, -8.849774126559262655 ) ) ;
#12813=AXIS2_PLACEMENT_3D ( 'NONE', #3291, #9561, #52214 ) ;
#12815=VERTEX_POINT ( 'NONE', #10896 ) ;
#12824=CARTESIAN_POINT ( 'NONE',  ( 10.92934437010315740, 9.489520708315478004, -6.090896311640516814 ) ) ;
#12826=DIRECTION ( 'NONE',  ( -1.000000000000000000, 1.776356839322000196E-14, -1.776356839322000196E-14 ) ) ;
#12827=CARTESIAN_POINT ( 'NONE',  ( 9.906851002540999929, 2.832432432432000269, -6.822293592207000934 ) ) ;
#12830=CARTESIAN_POINT ( 'NONE',  ( 8.577614158774000686, 3.981661882377999895, 8.959227447876999761 ) ) ;
#12834=ORIENTED_EDGE ( 'NONE', *, *, #25050, .F. ) ;
#12836=DIRECTION ( 'NONE',  ( 0.000000000000000000, -1.000000000000000000, 0.000000000000000000 ) ) ;
#12846=CARTESIAN_POINT ( 'NONE',  ( 6.999999691988000095, -1.332267629549999942E-14, 1.576516694967999966E-14 ) ) ;
#12848=CARTESIAN_POINT ( 'NONE',  ( 3.167073505399999878, 1.530628728318999876, -2.827318827580999727 ) ) ;
#12857=CARTESIAN_POINT ( 'NONE',  ( 10.50285691784999997, 5.158890929072000198, 8.369954994793999958 ) ) ;
#12863=CARTESIAN_POINT ( 'NONE',  ( 10.99161758052705196, 2.805470275078409514, -6.623309719462226575 ) ) ;
#12868=CARTESIAN_POINT ( 'NONE',  ( 0.8957314031238002849, 0.8639796672389500332, -3.414949893371867606 ) ) ;
#12869=CARTESIAN_POINT ( 'NONE',  ( 10.52384528040999889, 5.441915759804999198, -7.989632847918000103 ) ) ;
#12873=EDGE_CURVE ( 'NONE', #25668, #38871, #31848, .T. ) ;
#12879=CARTESIAN_POINT ( 'NONE',  ( 9.091114158770999154, 3.762712042852999872, 8.787816121229999666 ) ) ;
#12881=CARTESIAN_POINT ( 'NONE',  ( 0.6354672858397831803, 1.708930379032600699, 3.099689759355926277 ) ) ;
#12882=CARTESIAN_POINT ( 'NONE',  ( 10.00190165877000048, 2.729646201450000031, -8.843033333815998986 ) ) ;
#12884=CARTESIAN_POINT ( 'NONE',  ( 10.74599736040000053, 5.242718773683000322, 8.978699897073999736 ) ) ;
#12890=PLANE ( 'NONE',  #41094 ) ;
#12891=CARTESIAN_POINT ( 'NONE',  ( 1.355140132541249764, -0.9161175952574772685, -3.408904368339104707 ) ) ;
#12901=EDGE_CURVE ( 'NONE', #10058, #53044, #8078, .T. ) ;
#12903=ORIENTED_EDGE ( 'NONE', *, *, #4121, .T. ) ;
#12905=CARTESIAN_POINT ( 'NONE',  ( 9.740360841231000322, 4.047146749018000200, -5.600703114891000034 ) ) ;
#12911=ORIENTED_EDGE ( 'NONE', *, *, #19425, .T. ) ;
#12916=ORIENTED_EDGE ( 'NONE', *, *, #30125, .T. ) ;
#12921=CARTESIAN_POINT ( 'NONE',  ( 9.268025422169147376, 5.100000000000000533, 6.452077467066149374 ) ) ;
#12922=B_SPLINE_CURVE_WITH_KNOTS ( 'NONE', 3,
 ( #55981, #66811, #7388, #65767 ),
 .UNSPECIFIED., .F., .F.,
 ( 4, 4 ),
 ( 0.000000000000000000, 1.000000000000000000 ),
 .UNSPECIFIED. ) ;
#12929=CARTESIAN_POINT ( 'NONE',  ( 9.342517219591000455, 5.057081813675999626, 8.967637988488998957 ) ) ;
#12936=ADVANCED_FACE ( 'NONE', ( #55283 ), #44469, .F. ) ;
#12937=CARTESIAN_POINT ( 'NONE',  ( 11.07074944260999949, 5.433295094434000383, 5.078291584939999659 ) ) ;
#12938=EDGE_CURVE ( 'NONE', #3039, #2005, #36793, .T. ) ;
#12939=CARTESIAN_POINT ( 'NONE',  ( 10.18756025349000005, 5.387489739490000318, 8.640945789268998922 ) ) ;
#12946=CARTESIAN_POINT ( 'NONE',  ( 9.569805421428000614, 4.064052243276000453, 8.919241792616000808 ) ) ;
#12948=VECTOR ( 'NONE', #8104, 1000.000000000000000 ) ;
#12951=AXIS2_PLACEMENT_3D ( 'NONE', #35064, #19307, #29827 ) ;
#12952=CARTESIAN_POINT ( 'NONE',  ( 8.866801658774001282, 2.550580605805000012, 8.854682662413999594 ) ) ;
#12953=CARTESIAN_POINT ( 'NONE',  ( 10.09197164456000095, 3.841384681542000301, 5.536408945990000774 ) ) ;
#12956=CARTESIAN_POINT ( 'NONE',  ( 9.246064158776000852, 5.200883864107000321, -6.027780766890000308 ) ) ;
#12969=CARTESIAN_POINT ( 'NONE',  ( 1.214883236251000032, 2.900008637959000435, -1.487022697228999935 ) ) ;
#12974=CARTESIAN_POINT ( 'NONE',  ( 7.721047347516135417, 2.916517638618118635, 6.666908946472835495 ) ) ;
#12979=ORIENTED_EDGE ( 'NONE', *, *, #14606, .F. ) ;
#12981=CARTESIAN_POINT ( 'NONE',  ( 10.85939066991000068, 5.063022199667999601, 5.180095919022000395 ) ) ;
#12984=CARTESIAN_POINT ( 'NONE',  ( 1.466702730658999920, 2.711246897165000114, -2.603366577799000048 ) ) ;
#12986=CARTESIAN_POINT ( 'NONE',  ( 0.07497316781761000082, 0.000000000000000000, 0.000000000000000000 ) ) ;
#12987=ADVANCED_FACE ( 'NONE', ( #35001 ), #9434, .F. ) ;
#12994=CARTESIAN_POINT ( 'NONE',  ( 0.4921978635424994475, 2.476206882760971340, -2.521572608111618319 ) ) ;
#12998=CARTESIAN_POINT ( 'NONE',  ( 8.338298982574256613, 3.701651498039506549, 9.235001345112676674 ) ) ;
#13002=ORIENTED_EDGE ( 'NONE', *, *, #13050, .T. ) ;
#13007=CIRCLE ( 'NONE', #20821, 11.35000000000000675 ) ;
#13008=CARTESIAN_POINT ( 'NONE',  ( 10.27815081430999911, 5.521603098753999461, 8.751228458888000716 ) ) ;
#13009=CARTESIAN_POINT ( 'NONE',  ( 6.999999085428000534, 11.95749330617000084, -3.642574904853999929 ) ) ;
#13010=CYLINDRICAL_SURFACE ( 'NONE', #39514, 1.999999999999999778 ) ;
#13011=CARTESIAN_POINT ( 'NONE',  ( 4.000000000000000000, 0.000000000000000000, 0.000000000000000000 ) ) ;
#13013=CARTESIAN_POINT ( 'NONE',  ( 4.000000000000000000, -2.149963194832000379, -0.1424560705006995553 ) ) ;
#13022=ADVANCED_FACE ( 'NONE', ( #24501, #14014 ), #67134, .F. ) ;
#13024=ADVANCED_FACE ( 'NONE', ( #36016 ), #32185, .F. ) ;
#13029=ORIENTED_EDGE ( 'NONE', *, *, #3223, .F. ) ;
#13034=FACE_OUTER_BOUND ( 'NONE', #31437, .T. ) ;
#13035=CARTESIAN_POINT ( 'NONE',  ( 11.06794248424000138, 8.472325439733999985, -6.697655630924000292 ) ) ;
#13036=CARTESIAN_POINT ( 'NONE',  ( 8.242030379543560770, 3.170592169292434370, -8.579047363641327806 ) ) ;
#13037=CARTESIAN_POINT ( 'NONE',  ( 8.679055905797000037, 2.899999999999999911, 6.571291218949999902 ) ) ;
#13042=B_SPLINE_CURVE_WITH_KNOTS ( 'NONE', 3,
 ( #42559, #14024, #8772, #4795 ),
 .UNSPECIFIED., .F., .F.,
 ( 4, 4 ),
 ( 0.000000000000000000, 1.000000000000000000 ),
 .UNSPECIFIED. ) ;
#13050=EDGE_CURVE ( 'NONE', #29684, #9641, #25020, .T. ) ;
#13053=AXIS2_PLACEMENT_3D ( 'NONE', #66821, #45165, #23827 ) ;
#13063=EDGE_CURVE ( 'NONE', #1602, #37026, #68161, .T. ) ;
#13067=CARTESIAN_POINT ( 'NONE',  ( 10.93769906950999982, 5.063122007744000008, 4.920829195600999739 ) ) ;
#13076=CARTESIAN_POINT ( 'NONE',  ( 4.900006121741999898, 0.2617993877991493523, -1.999999999999999556 ) ) ;
#13077=CARTESIAN_POINT ( 'NONE',  ( 9.418864158773999407, 3.210851187372000037, -6.346613542714999667 ) ) ;
#13078=CARTESIAN_POINT ( 'NONE',  ( 10.25313817995482779, 2.714785337465412951, 7.027193780659266586 ) ) ;
#13079=ORIENTED_EDGE ( 'NONE', *, *, #47917, .F. ) ;
#13084=CARTESIAN_POINT ( 'NONE',  ( 2.686390132544208331, -0.4581489286485234680, 3.499999999999998668 ) ) ;
#13085=CARTESIAN_POINT ( 'NONE',  ( 8.763579719593998618, 4.815598936798999752, -8.835641302565999666 ) ) ;
#13087=CARTESIAN_POINT ( 'NONE',  ( 8.832537864289999874, 2.899999999999999911, 6.571291218949999902 ) ) ;
#13093=CARTESIAN_POINT ( 'NONE',  ( 9.047164158776000775, 2.156584729807999867, -7.959751745006000689 ) ) ;
#13096=CARTESIAN_POINT ( 'NONE',  ( 10.53865537815000053, 3.647234352455999584, -6.014129666051999834 ) ) ;
#13103=CARTESIAN_POINT ( 'NONE',  ( 9.152446624286001864, 2.899999999999999911, -6.169193161299999950 ) ) ;
#13114=CARTESIAN_POINT ( 'NONE',  ( 10.09249221959000131, 2.841614569232000065, -8.724659027040001291 ) ) ;
#13121=CARTESIAN_POINT ( 'NONE',  ( 2.000973465872999846, 3.500000000000000000, 0.000000000000000000 ) ) ;
#13125=CARTESIAN_POINT ( 'NONE',  ( 9.187479719595000205, 2.391443348526999912, -6.856688371964000162 ) ) ;
#13133=CARTESIAN_POINT ( 'NONE',  ( 2.550973465877000024, 3.500000000000000000, 0.000000000000000000 ) ) ;
#13135=ORIENTED_EDGE ( 'NONE', *, *, #68169, .T. ) ;
#13140=CARTESIAN_POINT ( 'NONE',  ( 4.149992563291998948, 1.229060429538527899, 1.599290730647371150 ) ) ;
#13143=CARTESIAN_POINT ( 'NONE',  ( 7.946129465983998941, 3.388696841564000195, -6.288310469962000049 ) ) ;
#13144=CARTESIAN_POINT ( 'NONE',  ( 8.804445280412998898, 5.597201461420000967, -8.171008079894999554 ) ) ;
#13152=CARTESIAN_POINT ( 'NONE',  ( 2.733565162642999979, 3.260648250327000230, 1.050234076676999972 ) ) ;
#13153=VERTEX_POINT ( 'NONE', #6252 ) ;
#13159=CARTESIAN_POINT ( 'NONE',  ( 8.385051658773999606, 4.977909614887999545, 6.416776202806000029 ) ) ;
#13160=CARTESIAN_POINT ( 'NONE',  ( 6.294818532647999849E-06, 2.999993704296999741, 7.007529276254001127E-10 ) ) ;
#13161=ORIENTED_EDGE ( 'NONE', *, *, #57825, .F. ) ;
#13163=CARTESIAN_POINT ( 'NONE',  ( 10.93804669887601833, 9.350510991039678643, 6.206837107818420129 ) ) ;
#13176=LINE ( 'NONE', #7919, #37160 ) ;
#13178=CARTESIAN_POINT ( 'NONE',  ( 7.789414158769000451, 2.892522941075999832, -8.352379580902999479 ) ) ;
#13186=ORIENTED_EDGE ( 'NONE', *, *, #52748, .F. ) ;
#13190=CARTESIAN_POINT ( 'NONE',  ( 10.68864630996109533, 2.651251715426289568, 7.268672106620575946 ) ) ;
#13197=ADVANCED_FACE ( 'NONE', ( #43677 ), #31031, .T. ) ;
#13200=ORIENTED_EDGE ( 'NONE', *, *, #55258, .T. ) ;
#13202=CARTESIAN_POINT ( 'NONE',  ( 9.228345280414000484, 2.481540185810000132, -7.878707153279001396 ) ) ;
#13203=CARTESIAN_POINT ( 'NONE',  ( 2.251656942761999680, 1.317797921594999755, -2.945325209437999803 ) ) ;
#13211=CARTESIAN_POINT ( 'NONE',  ( 10.93727498060999892, 5.425427353909999972, 7.240585962396000497 ) ) ;
#13215=CARTESIAN_POINT ( 'NONE',  ( 9.148115446195712153, 3.223534912153761756, 8.615607170735332332 ) ) ;
#13216=VECTOR ( 'NONE', #24924, 1000.000000000000114 ) ;
#13224=CARTESIAN_POINT ( 'NONE',  ( 10.67529528041000120, 3.066676902634999813, -8.703232886886000941 ) ) ;
#13229=CARTESIAN_POINT ( 'NONE',  ( 6.999999691988000095, 12.36734761319999798, -2.759114534468000368 ) ) ;
#13232=CARTESIAN_POINT ( 'NONE',  ( 8.924954719592001595, 4.158911560497999815, 5.873540104660999184 ) ) ;
#13235=CARTESIAN_POINT ( 'NONE',  ( 3.475528029604590952, -2.564910051950582748, 1.888346443232108207 ) ) ;
#13237=CARTESIAN_POINT ( 'NONE',  ( 9.799251915619999309, 4.057329420971000467, 9.430703183047999261 ) ) ;
#13242=DIRECTION ( 'NONE',  ( 0.8660254037844296038, 3.108624468950434369E-15, -0.5000000000000157652 ) ) ;
#13254=DIRECTION ( 'NONE',  ( 1.000000000000000000, 0.000000000000000000, 0.000000000000000000 ) ) ;
#13257=CARTESIAN_POINT ( 'NONE',  ( 9.351420280414000530, 4.953415418491999844, -8.946479654552000227 ) ) ;
#13260=CARTESIAN_POINT ( 'NONE',  ( 8.307732882202806479, 5.093561060909792104, 6.540202441368732522 ) ) ;
#13265=CARTESIAN_POINT ( 'NONE',  ( 7.597040668823413334, 4.060223358062168053, 8.863603326158687068 ) ) ;
#13267=VERTEX_POINT ( 'NONE', #23723 ) ;
#13277=CARTESIAN_POINT ( 'NONE',  ( 9.880016419786366910, 5.547192302291032107, -8.349494629669511170 ) ) ;
#13281=FACE_OUTER_BOUND ( 'NONE', #27340, .T. ) ;
#13283=CARTESIAN_POINT ( 'NONE',  ( 8.893204719592999297, 3.977267228909999730, 9.308925224542001331 ) ) ;
#13292=CARTESIAN_POINT ( 'NONE',  ( 11.12376201898999994, 5.751928413374999494, 5.182603196608999596 ) ) ;
#13293=B_SPLINE_CURVE_WITH_KNOTS ( 'NONE', 3,
 ( #6848, #18389, #7204, #34815, #7540, #1612, #43923, #65229, #17342, #66612, #55445, #66267, #28540, #38671, #28184 ),
 .UNSPECIFIED., .F., .F.,
 ( 4, 2, 1, 2, 2, 2, 2, 4 ),
 ( 0.000000000000000000, 0.1250000000000000833, 0.2500000000000001665, 0.3750000000000002220, 0.5000000000000003331, 0.6250000000000004441, 0.7500000000000004441, 1.000000000000000000 ),
 .UNSPECIFIED. ) ;
#13294=CARTESIAN_POINT ( 'NONE',  ( 9.691082467489000152, 5.335647408863999352, 8.701220655673999715 ) ) ;
#13300=CARTESIAN_POINT ( 'NONE',  ( 9.924742128742000347, 5.060458431729999873, 8.686130311522999747 ) ) ;
#13306=CARTESIAN_POINT ( 'NONE',  ( 7.737829719589999655, 5.687206835507000235, 6.847268999608999707 ) ) ;
#13307=CARTESIAN_POINT ( 'NONE',  ( 9.013423559847998590, 4.933953210258000155, 8.417881984655998906 ) ) ;
#13311=CARTESIAN_POINT ( 'NONE',  ( 8.848264158775000610, 5.751585344281000545, -8.235867044345999588 ) ) ;
#13315=CARTESIAN_POINT ( 'NONE',  ( 3.261349571466417352, -3.499999999999999556, -0.4563649592517093900 ) ) ;
#13319=CARTESIAN_POINT ( 'NONE',  ( 0.7809723532208000529, 2.290033430544000215, -2.273164938691999648 ) ) ;
#13322=LINE ( 'NONE', #17869, #13476 ) ;
#13324=CARTESIAN_POINT ( 'NONE',  ( 4.900006121742000786, -1.747572776708519404, -1.007237960741793170 ) ) ;
#13329=CARTESIAN_POINT ( 'NONE',  ( 8.662857780412000608, 2.741641653469999884, 6.457329666915000210 ) ) ;
#13330=CARTESIAN_POINT ( 'NONE',  ( 10.89212518207000002, 5.053080421413000067, 5.013248928177000074 ) ) ;
#13333=CARTESIAN_POINT ( 'NONE',  ( 2.029339447824000331, -2.164574875407999865, -2.655056891479000036 ) ) ;
#13335=CARTESIAN_POINT ( 'NONE',  ( 1.803056799206332883, -2.798833948393629978, -2.150913519912204031 ) ) ;
#13337=CARTESIAN_POINT ( 'NONE',  ( 10.59303303094000093, 2.436236667456999960, 7.793464546548000804 ) ) ;
#13343=CARTESIAN_POINT ( 'NONE',  ( 0.4609011837824754654, 0.5355237950841763572, -3.460879404214840527 ) ) ;
#13345=CARTESIAN_POINT ( 'NONE',  ( 8.360176255943175150, 3.240365764118005032, 9.085589947929626931 ) ) ;
#13346=ORIENTED_EDGE ( 'NONE', *, *, #61315, .F. ) ;
#13350=EDGE_LOOP ( 'NONE', ( #2650, #587, #4432, #35133 ) ) ;
#13354=CARTESIAN_POINT ( 'NONE',  ( 10.46432998405999903, 2.042755206296999582, 7.723699495214000343 ) ) ;
#13355=CARTESIAN_POINT ( 'NONE',  ( 9.937409415358999354, 3.510662261693000108, -6.227052446266999830 ) ) ;
#13363=EDGE_CURVE ( 'NONE', #69034, #61732, #1747, .T. ) ;
#13367=CARTESIAN_POINT ( 'NONE',  ( 10.59999999999999964, 3.399999999999999911, -4.756097560976000338 ) ) ;
#13376=ORIENTED_EDGE ( 'NONE', *, *, #2792, .T. ) ;
#13377=DIRECTION ( 'NONE',  ( 0.000000000000000000, 0.000000000000000000, -1.000000000000000000 ) ) ;
#13382=B_SPLINE_SURFACE_WITH_KNOTS ( 'NONE', 3, 3, ( 
 ( #34303, #14009, #35338, #12981 ),
 ( #7375, #39893, #7725, #50033 ),
 ( #23460, #44796, #66099, #39543 ),
 ( #50378, #61213, #55967, #13330 ),
 ( #34654, #8072, #26216, #51744 ),
 ( #14693, #47543, #62236, #9428 ) ),
 .UNSPECIFIED., .F., .F., .F.,
 ( 4, 1, 1, 4 ),
 ( 4, 4 ),
 ( -0.007877443071734000282, 0.000000000000000000, 0.07142857142856999519, 0.1006819380563999944 ),
 ( -0.1835627106809000209, 1.183562710543999863 ),
 .UNSPECIFIED. ) ;
#13385=CARTESIAN_POINT ( 'NONE',  ( 11.12486385074000061, 7.229995578275999257, -6.290807116501000884 ) ) ;
#13386=CARTESIAN_POINT ( 'NONE',  ( 0.05492698531792999939, 3.485378829570000114, 1.246872170512999922 ) ) ;
#13392=B_SPLINE_CURVE_WITH_KNOTS ( 'NONE', 3,
 ( #15439, #36069, #4244, #57385 ),
 .UNSPECIFIED., .F., .F.,
 ( 4, 4 ),
 ( 0.000000000000000000, 1.000000000000000000 ),
 .UNSPECIFIED. ) ;
#13393=CARTESIAN_POINT ( 'NONE',  ( 10.91060165877000188, 4.702351492776999820, -9.210043641106000933 ) ) ;
#13419=CARTESIAN_POINT ( 'NONE',  ( 0.8426401325419167199, -3.058252359239902685, -1.762666431298148595 ) ) ;
#13423=CARTESIAN_POINT ( 'NONE',  ( 10.59999999999999964, 3.399999999999999911, 4.756097560976000338 ) ) ;
#13425=CARTESIAN_POINT ( 'NONE',  ( 2.258651541363375426, -3.500000000000000000, -0.3376993977123544100 ) ) ;
#13426=AXIS2_PLACEMENT_3D ( 'NONE', #53733, #36974, #26135 ) ;
#13427=CARTESIAN_POINT ( 'NONE',  ( 9.658629719592001450, 5.496789211521000418, -7.043125396300999874 ) ) ;
#13432=VERTEX_POINT ( 'NONE', #26825 ) ;
#13435=CARTESIAN_POINT ( 'NONE',  ( 8.713854719593998155, 5.442817578555000146, -8.106149115450000053 ) ) ;
#13440=ORIENTED_EDGE ( 'NONE', *, *, #16306, .T. ) ;
#13441=CARTESIAN_POINT ( 'NONE',  ( 7.675811484805873164, 4.984677974768257691, -8.445524128177581247 ) ) ;
#13443=CARTESIAN_POINT ( 'NONE',  ( 9.693589158772999426, 4.047146749018000200, -5.600703114891000034 ) ) ;
#13445=VERTEX_POINT ( 'NONE', #37987 ) ;
#13446=CARTESIAN_POINT ( 'NONE',  ( 10.01597178489000051, 4.792666960550000077, -6.390258598531999290 ) ) ;
#13448=EDGE_CURVE ( 'NONE', #8401, #19244, #930, .T. ) ;
#13449=ORIENTED_EDGE ( 'NONE', *, *, #11430, .F. ) ;
#13452=CARTESIAN_POINT ( 'NONE',  ( 10.99335825053592330, 6.355322062518198756, -5.175304492146106661 ) ) ;
#13453=CARTESIAN_POINT ( 'NONE',  ( 7.936333771302000351, 5.123034328734999754, 6.721303713258000023 ) ) ;
#13454=DIRECTION ( 'NONE',  ( -1.000000000000000000, 0.000000000000000000, 0.000000000000000000 ) ) ;
#13456=ORIENTED_EDGE ( 'NONE', *, *, #28287, .F. ) ;
#13457=CARTESIAN_POINT ( 'NONE',  ( 10.47253786429000044, 2.899999999999999911, -6.571291218949999902 ) ) ;
#13458=CARTESIAN_POINT ( 'NONE',  ( 10.37239528041000014, 3.992345698584000235, -5.977238432995000572 ) ) ;
#13466=CARTESIAN_POINT ( 'NONE',  ( 7.836101299556240463, 4.962718242113793643, 6.493661227056148455 ) ) ;
#13469=CARTESIAN_POINT ( 'NONE',  ( 9.146614158775999925, 2.981992329588000423, -5.895876591910999664 ) ) ;
#13470=CARTESIAN_POINT ( 'NONE',  ( 9.137136214451835770, 5.220014052224821732, 6.249519307007754598 ) ) ;
#13476=VECTOR ( 'NONE', #60855, 1000.000000000000114 ) ;
#13479=CARTESIAN_POINT ( 'NONE',  ( 0.5929091678463546122, 3.086677832968792501, -1.352473734835327290 ) ) ;
#13495=CARTESIAN_POINT ( 'NONE',  ( 3.124567434295000279, 1.296329916925999859, 3.528159097347999928 ) ) ;
#13498=ADVANCED_FACE ( 'NONE', ( #35093 ), #44296, .T. ) ;
#13506=EDGE_CURVE ( 'NONE', #13445, #20297, #12120, .T. ) ;
#13507=CARTESIAN_POINT ( 'NONE',  ( 8.485085841226998937, 4.376386084436000523, -6.154119786874999498 ) ) ;
#13509=CARTESIAN_POINT ( 'NONE',  ( 7.773264469372000107, 2.859518616742000141, 6.768376720750000075 ) ) ;
#13518=CARTESIAN_POINT ( 'NONE',  ( 10.98911330520352791, 7.751816412315136517, -6.410483435660403018 ) ) ;
#13519=CARTESIAN_POINT ( 'NONE',  ( 8.266851002545999805, 2.832432432432000269, 6.822293592207000934 ) ) ;
#13520=VECTOR ( 'NONE', #52581, 1000.000000000000000 ) ;
#13524=ORIENTED_EDGE ( 'NONE', *, *, #15796, .T. ) ;
#13530=ORIENTED_EDGE ( 'NONE', *, *, #3726, .F. ) ;
#13534=CARTESIAN_POINT ( 'NONE',  ( 3.500000000000000000, 3.491196775144654207, 0.2719696052742964221 ) ) ;
#13539=ORIENTED_EDGE ( 'NONE', *, *, #63133, .T. ) ;
#13543=CARTESIAN_POINT ( 'NONE',  ( 9.088029719595001055, 2.881930053949999682, -8.823338183322999129 ) ) ;
#13544=CARTESIAN_POINT ( 'NONE',  ( 3.376658322786999733, 0.03754434462908000369, 3.214824333363999642 ) ) ;
#13550=ORIENTED_EDGE ( 'NONE', *, *, #26487, .F. ) ;
#13554=CARTESIAN_POINT ( 'NONE',  ( 9.910790522921001156, 3.869345236050000025, 5.882548872612999524 ) ) ;
#13557=CARTESIAN_POINT ( 'NONE',  ( 10.87021720923999979, 2.226038107033000202, 7.782753921296999167 ) ) ;
#13558=CARTESIAN_POINT ( 'NONE',  ( 9.218548476234555977, 2.654500937185336973, 7.609826956513907170 ) ) ;
#13560=DIRECTION ( 'NONE',  ( 0.000000000000000000, -1.000000000000000000, 0.000000000000000000 ) ) ;
#13564=CARTESIAN_POINT ( 'NONE',  ( 0.7871629501879499058, -3.165274489958428195, -1.545762285366434563 ) ) ;
#13572=CARTESIAN_POINT ( 'NONE',  ( 8.256676658772999389, 2.876288091423999660, 6.568897128359000526 ) ) ;
#13573=CARTESIAN_POINT ( 'NONE',  ( 8.646410841231000788, 2.261390688294000029, -6.733978371730000134 ) ) ;
#13576=CARTESIAN_POINT ( 'NONE',  ( 10.60770165877000082, 2.392327800351000011, -6.587345916039000215 ) ) ;
#13584=ORIENTED_EDGE ( 'NONE', *, *, #45806, .F. ) ;
#13585=CARTESIAN_POINT ( 'NONE',  ( 6.999999691988000095, -11.00717859340000082, 1.432487142323000118 ) ) ;
#13588=CARTESIAN_POINT ( 'NONE',  ( 1.500973465873999935, 3.500000000000000000, 0.000000000000000000 ) ) ;
#13593=ORIENTED_EDGE ( 'NONE', *, *, #54123, .T. ) ;
#13596=ORIENTED_EDGE ( 'NONE', *, *, #54129, .F. ) ;
#13600=CARTESIAN_POINT ( 'NONE',  ( 8.944760841233000193, 4.990139824845000405, -9.121472988377998803 ) ) ;
#13611=VERTEX_POINT ( 'NONE', #43941 ) ;
#13631=CARTESIAN_POINT ( 'NONE',  ( 9.414312736919001168, 3.941041961981000430, 5.878350450964999752 ) ) ;
#13637=CARTESIAN_POINT ( 'NONE',  ( 9.889842476439000052, 4.052276433608000161, 9.260531940735001299 ) ) ;
#13641=CARTESIAN_POINT ( 'NONE',  ( 8.443892219592001425, 2.905861847853000057, 8.940690431604000565 ) ) ;
#13642=CARTESIAN_POINT ( 'NONE',  ( 9.414312736919001168, 3.941041961981000430, 5.878350450964999752 ) ) ;
#13645=CARTESIAN_POINT ( 'NONE',  ( 8.997439158776000312, 2.773858540272000184, -8.951250717848999727 ) ) ;
#13650=CARTESIAN_POINT ( 'NONE',  ( 3.333982310585333231, -1.775032085411882177, -3.050824490492882735 ) ) ;
#13653=VERTEX_POINT ( 'NONE', #17717 ) ;
#13654=VECTOR ( 'NONE', #41711, 1000.000000000000000 ) ;
#13655=CARTESIAN_POINT ( 'NONE',  ( 1.491428256769000038, 2.689776413290000168, 2.380956047316999946 ) ) ;
#13657=CARTESIAN_POINT ( 'NONE',  ( 0.8933122983452270738, 3.086673542548771021, -1.352482486230435210 ) ) ;
#13659=CARTESIAN_POINT ( 'NONE',  ( 9.957462135714001406, 5.100000000000000533, -6.571291218949999902 ) ) ;
#13664=ORIENTED_EDGE ( 'NONE', *, *, #33962, .F. ) ;
#13665=CARTESIAN_POINT ( 'NONE',  ( 8.946010841230998878, 5.458692773671000253, 7.456452194274000078 ) ) ;
#13671=CARTESIAN_POINT ( 'NONE',  ( 1.218746307330000000, 3.398721108301999916, 0.4283847067656000318 ) ) ;
#13673=DIRECTION ( 'NONE',  ( 0.000000000000000000, 0.000000000000000000, -1.000000000000000000 ) ) ;
#13675=CARTESIAN_POINT ( 'NONE',  ( 10.11260611051000069, 3.359887741436999864, 5.859127722154000573 ) ) ;
#13684=CARTESIAN_POINT ( 'NONE',  ( 8.435568070370525362, 2.274764478101395149, 7.822608341263479481 ) ) ;
#13689=DIRECTION ( 'NONE',  ( -1.000000000000000000, 0.000000000000000000, 0.000000000000000000 ) ) ;
#13694=CARTESIAN_POINT ( 'NONE',  ( 10.99433665574000152, 3.697618584609999814, 5.729302299903000772 ) ) ;
#13695=CARTESIAN_POINT ( 'NONE',  ( 11.01002959534999981, 3.180718072098000171, -6.283812549199000230 ) ) ;
#13701=DIRECTION ( 'NONE',  ( 0.000000000000000000, 0.000000000000000000, 1.000000000000000000 ) ) ;
#13707=CARTESIAN_POINT ( 'NONE',  ( 10.63652412148805659, 3.218092512488175849, -4.773914205603903227 ) ) ;
#13716=DIRECTION ( 'NONE',  ( -1.000000000000000000, 0.000000000000000000, 0.000000000000000000 ) ) ;
#13717=DIRECTION ( 'NONE',  ( 1.000000000000000000, -1.776356839420000071E-14, 1.776356839420000071E-14 ) ) ;
#13721=CARTESIAN_POINT ( 'NONE',  ( 8.667306314937334832, 5.079264019707368405, -8.329425799205553815 ) ) ;
#13722=CARTESIAN_POINT ( 'NONE',  ( 0.1043854016219000064, 3.484641797009000008, -0.6100991035018999975 ) ) ;
#13723=CARTESIAN_POINT ( 'NONE',  ( -15.86200481174999943, 2.399999999999999911, -6.571291218949999902 ) ) ;
#13728=DIRECTION ( 'NONE',  ( 0.000000000000000000, 0.000000000000000000, -1.000000000000000000 ) ) ;
#13732=LINE ( 'NONE', #51132, #65379 ) ;
#13733=ORIENTED_EDGE ( 'NONE', *, *, #64064, .F. ) ;
#13746=CARTESIAN_POINT ( 'NONE',  ( 8.668612063652194166, 4.202134689404237733, 5.871184905935877829 ) ) ;
#13753=CARTESIAN_POINT ( 'NONE',  ( 0.8843067992085332785, -1.762666431298145930, -3.058252359239904905 ) ) ;
#13754=ORIENTED_EDGE ( 'NONE', *, *, #68169, .F. ) ;
#13755=CARTESIAN_POINT ( 'NONE',  ( 0.000000000000000000, -0.3800960799355100894, -2.899897457380500310 ) ) ;
#13769=VECTOR ( 'NONE', #29186, 1000.000000000000114 ) ;
#13770=CARTESIAN_POINT ( 'NONE',  ( 8.863029719594999634, 2.990001567622999623, -8.695425648791999862 ) ) ;
#13771=CARTESIAN_POINT ( 'NONE',  ( 7.931011803055000975, 3.387313518888000363, -6.297038610257000180 ) ) ;
#13776=CARTESIAN_POINT ( 'NONE',  ( 8.002383708823000319, 5.117451078405999887, -6.702236199791999915 ) ) ;
#13779=CARTESIAN_POINT ( 'NONE',  ( 8.500189158773000742, 2.724453559418999582, -8.908010318766001134 ) ) ;
#13780=ORIENTED_EDGE ( 'NONE', *, *, #5676, .T. ) ;
#13781=CARTESIAN_POINT ( 'NONE',  ( 10.46009300862000124, 2.565654508827999614, -6.975684004278000394 ) ) ;
#13783=VERTEX_POINT ( 'NONE', #10222 ) ;
#13803=EDGE_CURVE ( 'NONE', #24516, #11716, #3346, .T. ) ;
#13806=CARTESIAN_POINT ( 'NONE',  ( 10.11453584122999949, 5.322769172805999816, -7.951018786192998178 ) ) ;
#13807=CARTESIAN_POINT ( 'NONE',  ( 7.307500000000000107, 0.2999999999999999889, 3.149999999999999911 ) ) ;
#13808=CARTESIAN_POINT ( 'NONE',  ( 10.41164068750946825, 2.873222873834231805, -6.752018918838227357 ) ) ;
#13818=AXIS2_PLACEMENT_3D ( 'NONE', #40526, #61852, #62195 ) ;
#13823=CARTESIAN_POINT ( 'NONE',  ( 8.573148997459998810, 5.167567567567999731, -6.822293592207000934 ) ) ;
#13824=CARTESIAN_POINT ( 'NONE',  ( 9.491735841231999871, 3.920043641733999884, -9.398198753036000497 ) ) ;
#13841=CARTESIAN_POINT ( 'NONE',  ( 10.96031085658187720, 8.907343134533192597, 6.453647402135471722 ) ) ;
#13843=CARTESIAN_POINT ( 'NONE',  ( 1.605140132540249898, 0.9161175952574701631, 3.408904368339106927 ) ) ;
#13845=ORIENTED_EDGE ( 'NONE', *, *, #56376, .T. ) ;
#13853=ORIENTED_EDGE ( 'NONE', *, *, #14414, .T. ) ;
#13854=CARTESIAN_POINT ( 'NONE',  ( 10.94310967158117798, 9.262160174352873199, -6.269908194909642241 ) ) ;
#13869=CARTESIAN_POINT ( 'NONE',  ( 10.70259330317452751, 2.712330661039021429, 7.031802534341066391 ) ) ;
#13871=CARTESIAN_POINT ( 'NONE',  ( 3.073890132543958043, 2.150913519912194705, 2.798833948393636639 ) ) ;
#13878=CARTESIAN_POINT ( 'NONE',  ( 9.903950872528001881, 5.205009505618999555, 6.747225973806000532 ) ) ;
#13880=CARTESIAN_POINT ( 'NONE',  ( 9.816185841232000442, 2.656512020013999997, -7.884832994446999699 ) ) ;
#13882=CARTESIAN_POINT ( 'NONE',  ( 3.187343406994000095, -1.703486777756999970, 3.293594259118999723 ) ) ;
#13891=CARTESIAN_POINT ( 'NONE',  ( 10.81315553411000074, 3.756074350075000012, 6.071610008629000355 ) ) ;
#13894=CARTESIAN_POINT ( 'NONE',  ( 9.442843574488000158, 2.691255504502000129, 6.269523028052000235 ) ) ;
#13895=CARTESIAN_POINT ( 'NONE',  ( 10.98333333333433082, 4.339018939181010559, 8.912414555068393085 ) ) ;
#13896=CIRCLE ( 'NONE', #61896, 11.84999999999999964 ) ;
#13902=CARTESIAN_POINT ( 'NONE',  ( 0.8504945477338626825, -1.107043943361407212, -3.344068980614735231 ) ) ;
#13909=ORIENTED_EDGE ( 'NONE', *, *, #27306, .F. ) ;
#13910=AXIS2_PLACEMENT_3D ( 'NONE', #33715, #23215, #38601 ) ;
#13911=CARTESIAN_POINT ( 'NONE',  ( 8.064114158772998309, 4.228291488957999888, 8.941375734143997889 ) ) ;
#13912=AXIS2_PLACEMENT_3D ( 'NONE', #34607, #2428, #55920 ) ;
#13915=FACE_OUTER_BOUND ( 'NONE', #65509, .T. ) ;
#13916=VERTEX_POINT ( 'NONE', #63695 ) ;
#13934=CARTESIAN_POINT ( 'NONE',  ( 11.09999999999999964, 4.000000000000000000, -9.049999999997968558 ) ) ;
#13937=B_SPLINE_CURVE_WITH_KNOTS ( 'NONE', 3,
 ( #2506, #23830, #39570, #60204, #18248, #1470, #32943, #6707, #59502, #33641, #60894, #65077 ),
 .UNSPECIFIED., .F., .F.,
 ( 4, 1, 1, 1, 1, 1, 1, 1, 1, 4 ),
 ( 0.000000000000000000, 0.1111111144503000026, 0.2222222250406999944, 0.3333333356311999895, 0.4444444462216000091, 0.5555555568119999732, 0.6666666674023999928, 0.7777777779927999013, 0.8888888885832000319, 1.000000000000000000 ),
 .UNSPECIFIED. ) ;
#13949=ORIENTED_EDGE ( 'NONE', *, *, #7962, .F. ) ;
#13950=B_SPLINE_SURFACE_WITH_KNOTS ( 'NONE', 3, 3, ( 
 ( #43897, #57291, #25489, #46817, #59967, #23947, #55420, #7513, #33755, #50514, #54725, #12773, #17318, #12075, #39338, #34100, #44938, #13469, #34790, #23595, #39686, #65892, #28868, #1584, #49825, #44255, #61005, #18022, #55767, #22901, #6825, #38643, #24288, #56101, #60316 ),
 ( #33408, #2957, #2615, #7174, #8210, #28158, #29559, #50176, #7869, #65551, #66243, #18364, #40037, #55071, #2279, #49472, #17674, #38997, #13125, #12425, #1938, #34453, #28512, #23257, #44601, #50861, #61350, #29205, #60658, #45279, #66586, #18704, #45623, #24972, #29900 ),
 ( #68292, #45957, #61688, #19382, #51539, #46305, #30910, #30564, #19038, #3974, #20072, #41738, #3635, #24636, #51206, #66928, #67606, #56797, #25313, #67266, #41400, #9224, #15168, #25658, #46991, #8895, #31258, #62032, #14148, #57462, #40367, #4664, #14828, #4323, #30232 ),
 ( #20412, #40706, #52569, #13806, #19730, #51878, #35135, #41054, #9570, #26003, #62375, #35477, #63041, #14491, #56448, #8553, #35810, #57126, #36150, #46650, #52225, #3300, #67956, #62707, #36491, #57813, #9922, #37519, #48709, #461, #59189, #16196, #48355, #26701, #21435 ) ),
 .UNSPECIFIED., .F., .F., .F.,
 ( 4, 4 ),
 ( 4, 1, 1, 1, 1, 1, 1, 1, 1, 1, 1, 1, 1, 1, 1, 1, 1, 1, 1, 1, 1, 1, 1, 1, 1, 1, 1, 1, 1, 1, 1, 1, 4 ),
 ( -0.1039370721279000015, 1.103937072127999963 ),
 ( -0.02000000000000000042, 0.01250000000000000069, 0.04499999999999999833, 0.07749999999999999944, 0.1100000000000000006, 0.1424999999999999878, 0.1749999999999999889, 0.2074999999999999900, 0.2399999999999999911, 0.2725000000000000200, 0.3049999999999999933, 0.3375000000000000222, 0.3699999999999999956, 0.4025000000000000244, 0.4349999999999999978, 0.4675000000000000266, 0.5000000000000000000, 0.5324999999999999734, 0.5649999999999999467, 0.5975000000000000311, 0.6300000000000000044, 0.6624999999999999778, 0.6949999999999999512, 0.7275000000000000355, 0.7600000000000000089, 0.7924999999999999822, 0.8249999999999999556, 0.8575000000000000400, 0.8900000000000000133, 0.9224999999999999867, 0.9549999999999999600, 0.9875000000000000444, 1.020000000000000018 ),
 .UNSPECIFIED. ) ;
#13961=ORIENTED_EDGE ( 'NONE', *, *, #44983, .T. ) ;
#13962=ORIENTED_EDGE ( 'NONE', *, *, #54552, .T. ) ;
#13963=CARTESIAN_POINT ( 'NONE',  ( 10.31498017945866685, 2.650031506806222570, -7.499998780888569527 ) ) ;
#13965=CARTESIAN_POINT ( 'NONE',  ( 10.98277660187000215, 2.518725482848000130, -8.314790074023999722 ) ) ;
#13971=CARTESIAN_POINT ( 'NONE',  ( 9.166073843917999397, 4.023333628930999772, 9.122276991855001071 ) ) ;
#13972=EDGE_CURVE ( 'NONE', #24517, #29064, #9556, .T. ) ;
#13979=CARTESIAN_POINT ( 'NONE',  ( 9.442087588264000075, 4.742492734433000123, 8.809983635807000724 ) ) ;
#13981=CARTESIAN_POINT ( 'NONE',  ( 8.839404719593998649, 5.140767546012999567, -6.196177269779999719 ) ) ;
#13984=CARTESIAN_POINT ( 'NONE',  ( 8.829017219593000121, 5.290207928847999064, 8.768105151414001597 ) ) ;
#13985=CARTESIAN_POINT ( 'NONE',  ( 10.18756025349000005, 5.387489739490000318, 8.640945789268998922 ) ) ;
#13988=CARTESIAN_POINT ( 'NONE',  ( 10.16426084122999995, 4.808846957865000604, -8.639578604182998944 ) ) ;
#13997=CARTESIAN_POINT ( 'NONE',  ( 1.248245171504000162, -3.558193753575999985, 1.211459191638999844 ) ) ;
#13999=CARTESIAN_POINT ( 'NONE',  ( 9.645836745965350900, 5.376058781240163675, 6.376281615445395623 ) ) ;
#14002=CARTESIAN_POINT ( 'NONE',  ( 10.29378723213999969, 3.483632952461999999, 6.176337842045999338 ) ) ;
#14008=CARTESIAN_POINT ( 'NONE',  ( 7.352704719590999360, 4.773081973066999772, 8.927402469597002010 ) ) ;
#14009=CARTESIAN_POINT ( 'NONE',  ( 11.04467482866999894, 5.245201221631999644, 5.185341696387000709 ) ) ;
#14011=PLANE ( 'NONE',  #41492 ) ;
#14012=CARTESIAN_POINT ( 'NONE',  ( 2.077021397264999791, -0.2901351235585999944, -3.413359411422000278 ) ) ;
#14014=FACE_OUTER_BOUND ( 'NONE', #5319, .T. ) ;
#14017=CARTESIAN_POINT ( 'NONE',  ( 10.20319667131999886, 3.421760346951000287, 6.017732782098999422 ) ) ;
#14024=CARTESIAN_POINT ( 'NONE',  ( 7.990055090139000171, 4.541015240501000250, -6.262949957254000388 ) ) ;
#14025=CARTESIAN_POINT ( 'NONE',  ( 9.470944094206000585, 5.100000000000000533, 6.571291218949999902 ) ) ;
#14027=CARTESIAN_POINT ( 'NONE',  ( 7.528897780153962493, 3.013532217265934676, 6.036466769713773495 ) ) ;
#14031=ORIENTED_EDGE ( 'NONE', *, *, #57016, .T. ) ;
#14034=DIRECTION ( 'NONE',  ( 0.8480635683784220058, 0.000000000000000000, 0.5298945026977139872 ) ) ;
#14036=CARTESIAN_POINT ( 'NONE',  ( 10.53138775541999905, 5.607751175212000838, 7.280102404048999887 ) ) ;
#14037=CARTESIAN_POINT ( 'NONE',  ( 10.52662718686000076, 4.933722097448000277, -6.506013113666999637 ) ) ;
#14043=CARTESIAN_POINT ( 'NONE',  ( 8.179999999999999716, 4.924138593003999809, -8.484107647018999998 ) ) ;
#14048=CONICAL_SURFACE ( 'NONE', #53110, 12.37499919541000004, 0.7853980884875938484 ) ;
#14053=VERTEX_POINT ( 'NONE', #53561 ) ;
#14055=EDGE_CURVE ( 'NONE', #64129, #20386, #47975, .T. ) ;
#14057=ADVANCED_FACE ( 'NONE', ( #65062 ), #32252, .F. ) ;
#14060=CARTESIAN_POINT ( 'NONE',  ( 10.93769853197999886, 5.063116524846000388, -4.920828787216999345 ) ) ;
#14061=CARTESIAN_POINT ( 'NONE',  ( 8.331682176603999679, 5.101289360622999425, 6.607176324693000424 ) ) ;
#14064=AXIS2_PLACEMENT_3D ( 'NONE', #64660, #1733, #60811 ) ;
#14066=CARTESIAN_POINT ( 'NONE',  ( 0.1371912743484000052, 0.7117304887930000490, 3.632629627798000360 ) ) ;
#14068=CARTESIAN_POINT ( 'NONE',  ( 8.164556123749363792, 2.650750344902805811, 7.676799495578948473 ) ) ;
#14073=CARTESIAN_POINT ( 'NONE',  ( 10.75915165876999957, 5.387277012365999873, -6.278112168454999420 ) ) ;
#14076=DIRECTION ( 'NONE',  ( 0.000000000000000000, 0.000000000000000000, -1.000000000000000000 ) ) ;
#14079=ORIENTED_EDGE ( 'NONE', *, *, #55875, .F. ) ;
#14080=DIRECTION ( 'NONE',  ( 0.000000000000000000, 0.000000000000000000, -1.000000000000000000 ) ) ;
#14091=B_SPLINE_CURVE_WITH_KNOTS ( 'NONE', 3,
 ( #37541, #64791, #32317, #63764, #27066, #47704, #69014, #42454, #15875, #37206, #58524, #10630, #17615, #38939, #34394, #32999, #66527, #65838, #1877, #44192, #44879, #12014, #55360 ),
 .UNSPECIFIED., .F., .F.,
 ( 4, 2, 2, 2, 2, 2, 2, 2, 1, 2, 2, 4 ),
 ( 0.000000000000000000, 0.06249999999999983347, 0.1249999999999996669, 0.2499999999999977796, 0.3749999999999958922, 0.4374999999999949485, 0.4999999999999940048, 0.6249999999999936717, 0.6874999999999940048, 0.7187499999999945599, 0.7499999999999951150, 1.000000000000000000 ),
 .UNSPECIFIED. ) ;
#14093=CARTESIAN_POINT ( 'NONE',  ( 2.615556799209333594, 0.4581489286485002088, 3.500000000000001776 ) ) ;
#14105=CARTESIAN_POINT ( 'NONE',  ( 3.009306799211332262, 3.058252359239904905, -1.762666431298142600 ) ) ;
#14110=CARTESIAN_POINT ( 'NONE',  ( 4.000000000000000888, 2.040156275101110417, 0.6926574996740214596 ) ) ;
#14113=DIRECTION ( 'NONE',  ( 0.000000000000000000, -0.9565994702956990281, -0.2914059941558995726 ) ) ;
#14114=CARTESIAN_POINT ( 'NONE',  ( 2.550973465877000024, 3.500000000000000000, 0.000000000000000000 ) ) ;
#14115=CARTESIAN_POINT ( 'NONE',  ( 8.415504719592000527, 2.469361196073999842, -7.826019481986000059 ) ) ;
#14121=DIRECTION ( 'NONE',  ( 1.000000000000000000, 0.000000000000000000, 0.000000000000000000 ) ) ;
#14123=CARTESIAN_POINT ( 'NONE',  ( 8.839404719593998649, 5.140767546012999567, -6.196177269779999719 ) ) ;
#14125=CARTESIAN_POINT ( 'NONE',  ( 11.06133897141000055, 2.503910831767000023, -6.712778933675999760 ) ) ;
#14134=EDGE_CURVE ( 'NONE', #19777, #26667, #12922, .T. ) ;
#14137=CARTESIAN_POINT ( 'NONE',  ( 10.34939834122999969, 2.653159779809000085, -7.312415497503999440 ) ) ;
#14140=CIRCLE ( 'NONE', #55460, 2.999989272562999965 ) ;
#14148=CARTESIAN_POINT ( 'NONE',  ( 8.780820280412001466, 2.567871051582000241, -6.869011921437000012 ) ) ;
#14150=CARTESIAN_POINT ( 'NONE',  ( 9.229641524935605190, 5.653351949750144989, 8.124846574879386552 ) ) ;
#14160=AXIS2_PLACEMENT_3D ( 'NONE', #63510, #52340, #15285 ) ;
#14162=CARTESIAN_POINT ( 'NONE',  ( 6.999999691988000095, -13.87069231928999891, -4.225386915259999654 ) ) ;
#14168=CARTESIAN_POINT ( 'NONE',  ( 8.397785841227999981, 5.616457598545999907, -8.245813000738998255 ) ) ;
#14171=CARTESIAN_POINT ( 'NONE',  ( 0.1691085717929338428, 1.946941735042009070, -2.534826368309772260 ) ) ;
#14172=CARTESIAN_POINT ( 'NONE',  ( 3.258066606493000172, 2.789036351275000047, 1.988993390707999964 ) ) ;
#14176=CARTESIAN_POINT ( 'NONE',  ( 27.64127793187000037, 2.399999999999999911, 6.571291218949999902 ) ) ;
#14182=CARTESIAN_POINT ( 'NONE',  ( 0.7509734658760000015, -3.500000000000000000, 0.000000000000000000 ) ) ;
#14187=AXIS2_PLACEMENT_3D ( 'NONE', #17934, #60577, #34018 ) ;
#14190=CARTESIAN_POINT ( 'NONE',  ( 9.269471092183000138, 5.100000000000000533, -6.152188490330000370 ) ) ;
#14197=CARTESIAN_POINT ( 'NONE',  ( 8.558761214560396624, 2.378033399648631363, -8.172933946829649798 ) ) ;
#14199=CARTESIAN_POINT ( 'NONE',  ( 6.894364158771001172, 2.898440551356999961, -6.639986657414999272 ) ) ;
#14202=CARTESIAN_POINT ( 'NONE',  ( 3.452384183491000069, 1.140396268832999827, -3.309002319436000317 ) ) ;
#14208=CARTESIAN_POINT ( 'NONE',  ( 8.256966361271000920, 2.896784447077999758, 6.628744947585000880 ) ) ;
#14213=DIRECTION ( 'NONE',  ( 0.000000000000000000, 1.000000000000000000, 0.000000000000000000 ) ) ;
#14214=AXIS2_PLACEMENT_3D ( 'NONE', #49529, #1297, #11775 ) ;
#14222=CARTESIAN_POINT ( 'NONE',  ( 9.813360311708999362, 5.349397258738000538, 6.657026394682000081 ) ) ;
#14224=CARTESIAN_POINT ( 'NONE',  ( 10.07367028041000090, 4.905765359186999852, -8.776126235875999271 ) ) ;
#14225=ADVANCED_FACE ( 'NONE', ( #52095 ), #25880, .T. ) ;
#14226=CARTESIAN_POINT ( 'NONE',  ( 3.522679114812999668, 3.707222910410999717, -0.07828546188973999065 ) ) ;
#14235=CARTESIAN_POINT ( 'NONE',  ( 10.49785886974000171, 3.776281431161999880, 5.717632172928999168 ) ) ;
#14238=AXIS2_PLACEMENT_3D ( 'NONE', #57420, #67563, #25960 ) ;
#14239=EDGE_CURVE ( 'NONE', #30450, #16931, #3514, .T. ) ;
#14240=CARTESIAN_POINT ( 'NONE',  ( 6.999999691988000095, 12.11716380430000051, -3.069905306952000146 ) ) ;
#14249=FACE_OUTER_BOUND ( 'NONE', #14804, .T. ) ;
#14252=VERTEX_POINT ( 'NONE', #9107 ) ;
#14257=CARTESIAN_POINT ( 'NONE',  ( 10.62256721958999961, 2.471460423959999986, -8.210789473540000216 ) ) ;
#14267=CARTESIAN_POINT ( 'NONE',  ( 7.815514158766998953, 5.899700469177000528, -7.473738753146999869 ) ) ;
#14271=VERTEX_POINT ( 'NONE', #41961 ) ;
#14273=B_SPLINE_CURVE_WITH_KNOTS ( 'NONE', 3,
 ( #6536, #32430, #53747, #38005 ),
 .UNSPECIFIED., .F., .F.,
 ( 4, 4 ),
 ( 0.000000000000000000, 1.000000000000000000 ),
 .UNSPECIFIED. ) ;
#14287=CARTESIAN_POINT ( 'NONE',  ( 8.181107780410998842, 5.485785046334999748, 8.532070739720001740 ) ) ;
#14291=DIRECTION ( 'NONE',  ( -1.000000000000000000, 0.000000000000000000, 2.893429392025000534E-14 ) ) ;
#14299=CARTESIAN_POINT ( 'NONE',  ( 10.90000000296000060, 2.899999999990999999, 5.160242730682999657 ) ) ;
#14307=DIRECTION ( 'NONE',  ( 0.000000000000000000, 1.000000000000000000, 1.348567142399000110E-14 ) ) ;
#14308=AXIS2_PLACEMENT_3D ( 'NONE', #52602, #51571, #46339 ) ;
#14311=ADVANCED_FACE ( 'NONE', ( #25450 ), #57484, .F. ) ;
#14312=CARTESIAN_POINT ( 'NONE',  ( 10.02799997617999850, 3.452028386838999818, -6.074524158096999749 ) ) ;
#14316=CARTESIAN_POINT ( 'NONE',  ( 10.03490996941999924, 5.615906393494999982, 7.351455918368999143 ) ) ;
#14319=ORIENTED_EDGE ( 'NONE', *, *, #29731, .F. ) ;
#14322=CARTESIAN_POINT ( 'NONE',  ( 10.73931450027999901, 2.763002390638999994, 6.801034082888999244 ) ) ;
#14324=CARTESIAN_POINT ( 'NONE',  ( 9.418385841233000377, 3.251172436837000301, -6.320036569851000152 ) ) ;
#14329=CARTESIAN_POINT ( 'NONE',  ( 8.379704719592000473, 4.283000592898000392, 9.286795422009001655 ) ) ;
#14330=CARTESIAN_POINT ( 'NONE',  ( 9.910790522921001156, 3.869345236050000025, 5.882548872612999524 ) ) ;
#14333=CARTESIAN_POINT ( 'NONE',  ( 9.336654719594999818, 5.095038542659000136, -6.157541456184000062 ) ) ;
#14334=CARTESIAN_POINT ( 'NONE',  ( 0.000000000000000000, -1.781768641235091488, 2.319305672483670477 ) ) ;
#14335=DIRECTION ( 'NONE',  ( 1.000000000000000000, 0.000000000000000000, 0.000000000000000000 ) ) ;
#14340=CARTESIAN_POINT ( 'NONE',  ( 1.157654610683999996, -3.400502393318999950, 1.157769971473999959 ) ) ;
#14342=CARTESIAN_POINT ( 'NONE',  ( 10.02052890782000105, 2.899999999999999911, 6.152188490330000370 ) ) ;
#14344=CARTESIAN_POINT ( 'NONE',  ( 6.999999691988000095, 12.49999909016000110, -4.772673758002000880E-10 ) ) ;
#14347=DIRECTION ( 'NONE',  ( 1.000000000000000000, 0.000000000000000000, 0.000000000000000000 ) ) ;
#14350=ORIENTED_EDGE ( 'NONE', *, *, #29964, .T. ) ;
#14351=CARTESIAN_POINT ( 'NONE',  ( 8.855420280411999912, 5.633477595780999714, 7.451234169193000412 ) ) ;
#14356=FACE_OUTER_BOUND ( 'NONE', #38566, .T. ) ;
#14357=CARTESIAN_POINT ( 'NONE',  ( 1.838611650060999914, -0.2083462584559999942, 3.419270530009000275 ) ) ;
#14359=CARTESIAN_POINT ( 'NONE',  ( 1.810868395215021298, 2.997604546769242706, 1.386667885582162141 ) ) ;
#14363=CARTESIAN_POINT ( 'NONE',  ( 10.39106065309000115, 4.025321035224999733, 9.261125884460000179 ) ) ;
#14366=ADVANCED_FACE ( 'NONE', ( #7231, #54777 ), #55475, .T. ) ;
#14373=CARTESIAN_POINT ( 'NONE',  ( 8.150787273753783424, 5.419866027665010577, 6.461055956173178849 ) ) ;
#14374=ORIENTED_EDGE ( 'NONE', *, *, #58247, .T. ) ;
#14376=FACE_BOUND ( 'NONE', #11538, .T. ) ;
#14377=ORIENTED_EDGE ( 'NONE', *, *, #15221, .T. ) ;
#14378=ORIENTED_EDGE ( 'NONE', *, *, #7004, .T. ) ;
#14380=CARTESIAN_POINT ( 'NONE',  ( 8.460990129357115919, 3.502203120029797390, 5.991055485590817575 ) ) ;
#14382=CARTESIAN_POINT ( 'NONE',  ( 10.84168637167000071, 2.681011538858999899, 6.554754637093000547 ) ) ;
#14383=CARTESIAN_POINT ( 'NONE',  ( 10.73506130198999919, 5.202496273738000276, -8.441412224440000500 ) ) ;
#14394=CARTESIAN_POINT ( 'NONE',  ( 11.10000000011000054, 5.340540509194999785, -6.721892583407999666 ) ) ;
#14400=CYLINDRICAL_SURFACE ( 'NONE', #33350, 1.350000000000000533 ) ;
#14410=EDGE_CURVE ( 'NONE', #13783, #66620, #34156, .T. ) ;
#14411=CARTESIAN_POINT ( 'NONE',  ( 8.625655602088629692, 5.349651844363364717, -7.676783314127475499 ) ) ;
#14414=EDGE_CURVE ( 'NONE', #64893, #33797, #47956, .T. ) ;
#14425=CARTESIAN_POINT ( 'NONE',  ( 10.99999689388000057, 1.243449787579999883E-13, 0.000000000000000000 ) ) ;
#14426=CARTESIAN_POINT ( 'NONE',  ( 9.302064839073725722, 5.580009628946752898, -6.689794082201894199 ) ) ;
#14440=EDGE_CURVE ( 'NONE', #54722, #68545, #18419, .T. ) ;
#14449=CARTESIAN_POINT ( 'NONE',  ( 11.09999998388999920, 9.505740268506999158, 6.352095299649000104 ) ) ;
#14451=CARTESIAN_POINT ( 'NONE',  ( 8.871889158775999817, 2.702406276695999754, -6.981052078638000147 ) ) ;
#14456=ORIENTED_EDGE ( 'NONE', *, *, #38309, .F. ) ;
#14458=CARTESIAN_POINT ( 'NONE',  ( 2.696806799210917038, -0.9161175952574931447, 3.408904368339101598 ) ) ;
#14459=CARTESIAN_POINT ( 'NONE',  ( 8.546960841229999772, 2.724453559418999582, -8.908010318766001134 ) ) ;
#14465=ORIENTED_EDGE ( 'NONE', *, *, #10336, .T. ) ;
#14468=CARTESIAN_POINT ( 'NONE',  ( 8.590779719591999708, 2.836879604150999601, -8.783908972046001296 ) ) ;
#14472=CARTESIAN_POINT ( 'NONE',  ( 10.64127413024999846, 2.258699798012000048, -6.863478635463000188 ) ) ;
#14473=EDGE_LOOP ( 'NONE', ( #29970, #6552, #24755, #4462 ) ) ;
#14478=B_SPLINE_CURVE_WITH_KNOTS ( 'NONE', 3,
 ( #19778, #31307, #15216, #57174, #47385, #26404 ),
 .UNSPECIFIED., .F., .F.,
 ( 4, 2, 4 ),
 ( 0.000000000000000000, 0.5000000000000000000, 1.000000000000000000 ),
 .UNSPECIFIED. ) ;
#14483=CARTESIAN_POINT ( 'NONE',  ( 11.29596084123000210, 2.828872990872000059, -8.191118698770999629 ) ) ;
#14489=ORIENTED_EDGE ( 'NONE', *, *, #46396, .T. ) ;
#14491=CARTESIAN_POINT ( 'NONE',  ( 9.617285841233000454, 5.306366356490000769, -7.996450761531000317 ) ) ;
#14493=CARTESIAN_POINT ( 'NONE',  ( 10.61503919148293740, 5.349978903665603802, -7.499997722305280945 ) ) ;
#14494=CARTESIAN_POINT ( 'NONE',  ( 1.061390132541624842, 3.499999999999999112, 0.4581489286485193602 ) ) ;
#14499=CARTESIAN_POINT ( 'NONE',  ( 7.844724277266999835, 4.719412473309000156, 6.357657803787000184 ) ) ;
#14501=ORIENTED_EDGE ( 'NONE', *, *, #19446, .F. ) ;
#14502=LINE ( 'NONE', #9932, #13520 ) ;
#14508=CARTESIAN_POINT ( 'NONE',  ( 8.596685841231000325, 2.141799395716999843, -7.895788736628000848 ) ) ;
#14512=CARTESIAN_POINT ( 'NONE',  ( 9.050000000000000711, 0.000000000000000000, 4.000000000000000000 ) ) ;
#14517=CARTESIAN_POINT ( 'NONE',  ( 2.220184363877999889, 1.697856089507000066, -2.629976706909999518 ) ) ;
#14522=CARTESIAN_POINT ( 'NONE',  ( 8.898551658772998252, 5.146726419831999522, 6.597424767138000412 ) ) ;
#14526=EDGE_CURVE ( 'NONE', #2005, #25280, #25407, .T. ) ;
#14529=CARTESIAN_POINT ( 'NONE',  ( 0.5211625230349857807, 3.419518492017623146, 0.8791808744453025737 ) ) ;
#14531=CARTESIAN_POINT ( 'NONE',  ( 7.806464712881202139, 3.011078243462636639, 6.531313835357527964 ) ) ;
#14533=ORIENTED_EDGE ( 'NONE', *, *, #36662, .F. ) ;
#14535=ORIENTED_EDGE ( 'NONE', *, *, #19571, .T. ) ;
#14536=CARTESIAN_POINT ( 'NONE',  ( 9.449367199446873755, 4.457171844012795425, 8.907134314554838284 ) ) ;
#14540=CARTESIAN_POINT ( 'NONE',  ( -0.000000000000000000, 2.319407620233877587, -1.781870588985297932 ) ) ;
#14542=CARTESIAN_POINT ( 'NONE',  ( 7.979454719588000344, 2.702884610408000210, -6.624425519483001068 ) ) ;
#14545=ORIENTED_EDGE ( 'NONE', *, *, #54577, .F. ) ;
#14554=CARTESIAN_POINT ( 'NONE',  ( 10.70959604073516225, 5.759191062913065373, 7.715212687030478023 ) ) ;
#14555=ADVANCED_FACE ( 'NONE', ( #12393 ), #7485, .T. ) ;
#14556=DIRECTION ( 'NONE',  ( -1.000000000000000000, 0.000000000000000000, 0.000000000000000000 ) ) ;
#14563=VERTEX_POINT ( 'NONE', #1214 ) ;
#14564=CARTESIAN_POINT ( 'NONE',  ( 10.18240541510999897, 2.607737086676999994, 7.783408568367999436 ) ) ;
#14566=DIRECTION ( 'NONE',  ( 1.000000000000000000, 0.000000000000000000, 0.000000000000000000 ) ) ;
#14567=CARTESIAN_POINT ( 'NONE',  ( 9.675870280412999236, 3.031907308384000022, -8.729608011560001657 ) ) ;
#14568=B_SPLINE_CURVE_WITH_KNOTS ( 'NONE', 3,
 ( #1530, #54317, #55715, #49076 ),
 .UNSPECIFIED., .F., .F.,
 ( 4, 4 ),
 ( 0.000000000000000000, 1.000000000000000000 ),
 .UNSPECIFIED. ) ;
#14569=CARTESIAN_POINT ( 'NONE',  ( 2.635666247922999972, -2.915774638497000026, 2.013997748395000009 ) ) ;
#14575=CARTESIAN_POINT ( 'NONE',  ( 3.123890132544374421, 2.150913519912194261, 2.798833948393636195 ) ) ;
#14578=CARTESIAN_POINT ( 'NONE',  ( 10.31167969999000000, 2.874476822401000220, 8.900029516786000627 ) ) ;
#14592=ORIENTED_EDGE ( 'NONE', *, *, #44371, .T. ) ;
#14593=CARTESIAN_POINT ( 'NONE',  ( 10.72180282789423522, 2.874603711610002055, 6.749639981020137292 ) ) ;
#14596=CARTESIAN_POINT ( 'NONE',  ( 10.86460778041000097, 3.843601682313000367, -5.985271987931999327 ) ) ;
#14597=VERTEX_POINT ( 'NONE', #33379 ) ;
#14598=CARTESIAN_POINT ( 'NONE',  ( 8.636611612198999310, 5.100000000000000533, -6.496831119766667051 ) ) ;
#14606=EDGE_CURVE ( 'NONE', #18530, #45160, #58842, .T. ) ;
#14607=EDGE_CURVE ( 'NONE', #32433, #26116, #54640, .T. ) ;
#14608=CARTESIAN_POINT ( 'NONE',  ( 7.765789158767000266, 5.525377065333000104, -6.367402836891999485 ) ) ;
#14612=ORIENTED_EDGE ( 'NONE', *, *, #41907, .T. ) ;
#14615=EDGE_LOOP ( 'NONE', ( #64374, #5158, #2943, #6349 ) ) ;
#14616=LINE ( 'NONE', #41864, #51826 ) ;
#14617=VERTEX_POINT ( 'NONE', #50148 ) ;
#14619=CARTESIAN_POINT ( 'NONE',  ( 2.353056799209541250, -2.798833948393629534, -2.150913519912204031 ) ) ;
#14624=CARTESIAN_POINT ( 'NONE',  ( 7.282482780409000434, 3.448180532882000104, 9.222462917385000125 ) ) ;
#14626=CARTESIAN_POINT ( 'NONE',  ( 9.447682302133417309, 5.285671839984114939, 7.027659275301406439 ) ) ;
#14631=EDGE_CURVE ( 'NONE', #69130, #12504, #2253, .T. ) ;
#14634=CARTESIAN_POINT ( 'NONE',  ( 6.897224497904996809, 9.172783816707005045, -5.180261716721994425 ) ) ;
#14648=CARTESIAN_POINT ( 'NONE',  ( 10.05525296965999971, 5.223856410664000194, -6.898317050646999959 ) ) ;
#14649=DIRECTION ( 'NONE',  ( -1.000000000000000000, 0.000000000000000000, 0.000000000000000000 ) ) ;
#14653=CARTESIAN_POINT ( 'NONE',  ( 10.93227693248999977, 2.539877577705000000, 6.453611809651000009 ) ) ;
#14659=CARTESIAN_POINT ( 'NONE',  ( 10.98286939055999945, 3.998514186275999638, 9.091062412789998604 ) ) ;
#14661=CARTESIAN_POINT ( 'NONE',  ( 9.915635841230999503, 3.210851187372000037, -6.346613542714999667 ) ) ;
#14662=CARTESIAN_POINT ( 'NONE',  ( 11.12483609420999997, 7.237683487921999337, -6.298805210297000912 ) ) ;
#14667=CARTESIAN_POINT ( 'NONE',  ( 6.999999691988000095, -12.36734761319999798, -2.759114534468000368 ) ) ;
#14669=CARTESIAN_POINT ( 'NONE',  ( 10.46932803217000085, 4.988495740890000363, 6.213106455073000411 ) ) ;
#14672=CARTESIAN_POINT ( 'NONE',  ( 9.626145280412998773, 3.934138271021000222, -9.063586117809000697 ) ) ;
#14676=CARTESIAN_POINT ( 'NONE',  ( 10.72510394928502286, 2.650147065043140238, 7.500007457243191844 ) ) ;
#14679=CARTESIAN_POINT ( 'NONE',  ( 1.109972661243999958, -2.155162080922000012, 2.873869168568000010 ) ) ;
#14681=CARTESIAN_POINT ( 'NONE',  ( 9.717214158771000143, 3.990126737362999609, -8.809457313313998839 ) ) ;
#14690=CARTESIAN_POINT ( 'NONE',  ( 7.374100552923999352, 4.389299166881000858, 9.135259451319999613 ) ) ;
#14691=EDGE_CURVE ( 'NONE', #7034, #32067, #23139, .T. ) ;
#14693=CARTESIAN_POINT ( 'NONE',  ( 11.12916632831999841, 5.271622498040000160, 4.814907817406999690 ) ) ;
#14696=CARTESIAN_POINT ( 'NONE',  ( 0.7530474580061000678, 2.610614231003999919, -1.727479700733000056 ) ) ;
#14698=CARTESIAN_POINT ( 'NONE',  ( 2.204555053273437704, 1.932598637109171014, -2.448717497070831417 ) ) ;
#14699=EDGE_CURVE ( 'NONE', #55522, #8893, #34763, .T. ) ;
#14701=CARTESIAN_POINT ( 'NONE',  ( 10.27815081430999911, 5.521603098753999461, 8.751228458888000716 ) ) ;
#14702=CARTESIAN_POINT ( 'NONE',  ( 11.18706938844999854, 3.186790175674999670, 6.232702730851999995 ) ) ;
#14705=DIRECTION ( 'NONE',  ( 6.943145065999975329E-10, 0.7071067809470975574, -0.7071067814259974771 ) ) ;
#14711=EDGE_LOOP ( 'NONE', ( #60294, #50037, #44579, #59836 ) ) ;
#14714=VERTEX_POINT ( 'NONE', #62009 ) ;
#14719=CARTESIAN_POINT ( 'NONE',  ( 9.939321360490000146, 2.638097915594000309, 6.328629954376999933 ) ) ;
#14720=CARTESIAN_POINT ( 'NONE',  ( 10.65649893244999902, 5.448184228579000532, -7.015214795518000201 ) ) ;
#14727=EDGE_LOOP ( 'NONE', ( #23666, #16891, #57922, #43953, #6796, #34502 ) ) ;
#14735=CARTESIAN_POINT ( 'NONE',  ( 10.90000000000000036, 2.899999999999999911, 6.414037451299000381 ) ) ;
#14736=ORIENTED_EDGE ( 'NONE', *, *, #54577, .T. ) ;
#14746=ADVANCED_FACE ( 'NONE', ( #56772 ), #25290, .F. ) ;
#14752=EDGE_CURVE ( 'NONE', #8013, #33506, #63788, .T. ) ;
#14755=CARTESIAN_POINT ( 'NONE',  ( 11.24323278040999874, 2.479734175328000223, -7.587230544849999703 ) ) ;
#14757=CARTESIAN_POINT ( 'NONE',  ( 10.17500046684965120, 2.650307855385062972, 7.500001770945063484 ) ) ;
#14760=EDGE_LOOP ( 'NONE', ( #6475, #47201, #61149, #54519 ) ) ;
#14761=AXIS2_PLACEMENT_3D ( 'NONE', #57721, #68900, #58411 ) ;
#14765=CARTESIAN_POINT ( 'NONE',  ( 9.579111560609650411, 2.241182798226359463, -7.748722518521907965 ) ) ;
#14772=ORIENTED_EDGE ( 'NONE', *, *, #30234, .T. ) ;
#14788=CARTESIAN_POINT ( 'NONE',  ( 8.903895280414001689, 3.867331042029999999, -9.227339949050001877 ) ) ;
#14790=VERTEX_POINT ( 'NONE', #13776 ) ;
#14797=EDGE_CURVE ( 'NONE', #62021, #12694, #7084, .T. ) ;
#14801=CARTESIAN_POINT ( 'NONE',  ( 8.928197172114701985, 5.125396288430382086, 6.749639981089713636 ) ) ;
#14804=EDGE_LOOP ( 'NONE', ( #8722, #22956, #68350, #41810, #47489 ) ) ;
#14805=DIRECTION ( 'NONE',  ( 0.000000000000000000, -1.000000000000000000, 0.000000000000000000 ) ) ;
#14806=CARTESIAN_POINT ( 'NONE',  ( 8.458179719589999479, 5.332332124071999857, -8.487089944253000340 ) ) ;
#14809=CARTESIAN_POINT ( 'NONE',  ( 10.86493304757000011, 4.678466548873998931, -9.048467117372998914 ) ) ;
#14815=CARTESIAN_POINT ( 'NONE',  ( 8.567745549749458789, 3.352117218477321359, 5.929420214889738361 ) ) ;
#14817=CARTESIAN_POINT ( 'NONE',  ( 10.16052890781999984, 2.899999999999999911, -6.152188490330000370 ) ) ;
#14818=CARTESIAN_POINT ( 'NONE',  ( 10.76588584123000025, 3.166544027818999574, -8.574484964885998650 ) ) ;
#14820=FACE_OUTER_BOUND ( 'NONE', #19568, .T. ) ;
#14825=EDGE_CURVE ( 'NONE', #65344, #42751, #58139, .T. ) ;
#14828=CARTESIAN_POINT ( 'NONE',  ( 8.581920280410001212, 4.769017407621999993, -8.862909124839001507 ) ) ;
#14830=EDGE_CURVE ( 'NONE', #66075, #4878, #9496, .T. ) ;
#14832=CARTESIAN_POINT ( 'NONE',  ( 1.196806799207750238, -0.9161175952574931447, 3.408904368339101598 ) ) ;
#14846=DIRECTION ( 'NONE',  ( 0.000000000000000000, -1.000000000000000000, 0.000000000000000000 ) ) ;
#14852=CARTESIAN_POINT ( 'NONE',  ( 0.1889203238210994673, 2.786086813067528034, -1.606789352532954629 ) ) ;
#14854=CARTESIAN_POINT ( 'NONE',  ( 2.538064026817000052, -3.226256590673000080, 0.4610373736932000255 ) ) ;
#14858=DIRECTION ( 'NONE',  ( 0.000000000000000000, 0.8648648648648717963, 0.5020047465136829867 ) ) ;
#14859=CARTESIAN_POINT ( 'NONE',  ( 6.899999692186000289, 12.99045401582999837, -1.690592930688000095 ) ) ;
#14860=CARTESIAN_POINT ( 'NONE',  ( 10.35465597998896214, 2.649863840852023422, -7.676734101936348864 ) ) ;
#14861=VERTEX_POINT ( 'NONE', #1052 ) ;
#14863=CARTESIAN_POINT ( 'NONE',  ( 0.7094218594409307244, -3.054526701543303524, 1.768616831485774865 ) ) ;
#14867=ORIENTED_EDGE ( 'NONE', *, *, #27224, .T. ) ;
#14872=EDGE_CURVE ( 'NONE', #35486, #13916, #41003, .T. ) ;
#14876=CARTESIAN_POINT ( 'NONE',  ( 8.020125753392001400, 4.498951069075999953, -6.245588651729999441 ) ) ;
#14877=CARTESIAN_POINT ( 'NONE',  ( 8.277804719590999838, 4.529523339102000890, -8.867457431226998921 ) ) ;
#14885=CARTESIAN_POINT ( 'NONE',  ( 11.09999999999999964, 4.000000000000000000, 7.500000000000000000 ) ) ;
#14888=AXIS2_PLACEMENT_3D ( 'NONE', #17056, #12174, #11466 ) ;
#14894=CARTESIAN_POINT ( 'NONE',  ( 8.737804660583998739, 4.491756428607999396, -5.831236541471000123 ) ) ;
#14901=ORIENTED_EDGE ( 'NONE', *, *, #3138, .T. ) ;
#14902=CARTESIAN_POINT ( 'NONE',  ( 11.01776904286000125, 4.914120883409999863, 8.587704221454000475 ) ) ;
#14906=CARTESIAN_POINT ( 'NONE',  ( 2.558588954831999995, 3.370261330116000043, 1.546253863582000010 ) ) ;
#14912=DIRECTION ( 'NONE',  ( 1.000000000000000000, 0.000000000000000000, 0.000000000000000000 ) ) ;
#14916=CARTESIAN_POINT ( 'NONE',  ( 10.87521525736000072, 4.831064930369000088, 6.312796576761000367 ) ) ;
#14925=ORIENTED_EDGE ( 'NONE', *, *, #5349, .F. ) ;
#14934=CARTESIAN_POINT ( 'NONE',  ( 10.71315778041000044, 2.619207518211999819, -8.142085279690999045 ) ) ;
#14939=FACE_OUTER_BOUND ( 'NONE', #40026, .T. ) ;
#14941=ORIENTED_EDGE ( 'NONE', *, *, #55875, .T. ) ;
#14943=CARTESIAN_POINT ( 'NONE',  ( 8.064139158768000470, 2.101036793381999779, -7.559080181511999896 ) ) ;
#14947=VERTEX_POINT ( 'NONE', #28306 ) ;
#14948=CARTESIAN_POINT ( 'NONE',  ( 2.834306799209666661, -1.762666431298145708, -3.058252359239904461 ) ) ;
#14955=CARTESIAN_POINT ( 'NONE',  ( 2.467640132543333475, 1.762666431298152148, -3.058252359239900908 ) ) ;
#14961=CARTESIAN_POINT ( 'NONE',  ( 8.977760841230999489, 2.019067547072999957, 7.390982789861999969 ) ) ;
#14964=CARTESIAN_POINT ( 'NONE',  ( 8.883148997460001084, 5.167567567567999731, 6.822293592207000934 ) ) ;
#14966=VERTEX_POINT ( 'NONE', #17826 ) ;
#14970=CARTESIAN_POINT ( 'NONE',  ( 7.294908919857999052, 10.77487787641000239, -3.564476421554995778 ) ) ;
#14971=CARTESIAN_POINT ( 'NONE',  ( 2.490019101166500270, 3.500000000000001332, -0.4817981237446227194 ) ) ;
#14972=CARTESIAN_POINT ( 'NONE',  ( 8.433148997460000018, 5.167567567567999731, 6.822293592207000934 ) ) ;
#14981=LINE ( 'NONE', #20918, #19079 ) ;
#14983=CARTESIAN_POINT ( 'NONE',  ( 11.02205778663999958, 2.309481324353999554, -7.515673747780000191 ) ) ;
#14987=CARTESIAN_POINT ( 'NONE',  ( 9.261662452849000360, 2.944259351255000379, 6.507396354981000108 ) ) ;
#14995=CARTESIAN_POINT ( 'NONE',  ( 10.69030645188999884, 5.903031974240000146, 7.830710565751001440 ) ) ;
#14997=LINE ( 'NONE', #9744, #31706 ) ;
#14999=CARTESIAN_POINT ( 'NONE',  ( 9.317462135714000837, 5.100000000000000533, 6.571291218949999902 ) ) ;
#15007=CARTESIAN_POINT ( 'NONE',  ( 9.675870280412999236, 3.031907308384000022, -8.729608011560001657 ) ) ;
#15014=ORIENTED_EDGE ( 'NONE', *, *, #54531, .F. ) ;
#15015=CARTESIAN_POINT ( 'NONE',  ( 2.011156362556000055, 3.707157770482000014, -0.6207725330884000803 ) ) ;
#15017=CARTESIAN_POINT ( 'NONE',  ( 7.758198341228000672, 5.797099724369999763, 8.340484548805999765 ) ) ;
#15018=CARTESIAN_POINT ( 'NONE',  ( 9.906784761384550109, 2.482585475679351728, 8.418381271750890349 ) ) ;
#15028=VERTEX_POINT ( 'NONE', #65958 ) ;
#15029=CARTESIAN_POINT ( 'NONE',  ( 7.326301658771000369, 3.394842219570000097, 9.388954446285000088 ) ) ;
#15034=CARTESIAN_POINT ( 'NONE',  ( 1.786156362557000055, 3.214278412021000175, -0.5382386926684999962 ) ) ;
#15036=CARTESIAN_POINT ( 'NONE',  ( 2.182545538860289458, 1.234472752153680020, -2.960455995469124524 ) ) ;
#15038=CARTESIAN_POINT ( 'NONE',  ( 9.967852198058999136, 2.034774058634999605, 7.636878205663998997 ) ) ;
#15039=CARTESIAN_POINT ( 'NONE',  ( 9.409415556003999370, 2.113395950889999764, 7.914199712930999553 ) ) ;
#15042=CARTESIAN_POINT ( 'NONE',  ( 10.34920446230533564, 2.899999999999999911, -6.662590550568722847 ) ) ;
#15043=CARTESIAN_POINT ( 'NONE',  ( 11.04384236319999957, 1.600341926351999788, 5.035088906224999938 ) ) ;
#15045=AXIS2_PLACEMENT_3D ( 'NONE', #41389, #8887, #30221 ) ;
#15046=DIRECTION ( 'NONE',  ( 0.000000000000000000, 1.000000000000000000, 0.000000000000000000 ) ) ;
#15053=CIRCLE ( 'NONE', #54121, 13.10000000000000320 ) ;
#15056=CARTESIAN_POINT ( 'NONE',  ( 10.18756025349000005, 5.387489739490000318, 8.640945789268998922 ) ) ;
#15058=CARTESIAN_POINT ( 'NONE',  ( 10.23643409129999959, 5.517148499152000340, -6.754126239302999934 ) ) ;
#15062=CARTESIAN_POINT ( 'NONE',  ( 9.020069425496542337, 5.146911715855399194, 8.214611775107460545 ) ) ;
#15065=ORIENTED_EDGE ( 'NONE', *, *, #16001, .F. ) ;
#15078=ADVANCED_FACE ( 'NONE', ( #65271 ), #45346, .T. ) ;
#15088=CARTESIAN_POINT ( 'NONE',  ( 9.056630296855326279, 5.100000000000000533, 6.328714934328742103 ) ) ;
#15089=CARTESIAN_POINT ( 'NONE',  ( 8.060295491240845323, 3.823126980273178432, 8.848192560902505832 ) ) ;
#15094=CARTESIAN_POINT ( 'NONE',  ( 11.19050471959000070, 2.516756593394000152, -6.840361808223000217 ) ) ;
#15096=CARTESIAN_POINT ( 'NONE',  ( 9.928731151682097078, 5.349829198379457473, 7.563678851448849549 ) ) ;
#15098=CARTESIAN_POINT ( 'NONE',  ( 8.975133055567869889, 5.349981391149201571, 7.499992565666659949 ) ) ;
#15104=CARTESIAN_POINT ( 'NONE',  ( 8.856793857978997764, 5.100000000000000533, -6.339888365514000590 ) ) ;
#15109=CARTESIAN_POINT ( 'NONE',  ( 8.168183350545964672, 2.950618456246918875, 6.463661575758196776 ) ) ;
#15111=B_SPLINE_CURVE_WITH_KNOTS ( 'NONE', 3,
 ( #3612, #29532, #18902, #12974, #2132, #60510 ),
 .UNSPECIFIED., .F., .F.,
 ( 4, 2, 4 ),
 ( 0.000000000000000000, 0.5000000000000000000, 1.000000000000000000 ),
 .UNSPECIFIED. ) ;
#15112=B_SPLINE_CURVE_WITH_KNOTS ( 'NONE', 3,
 ( #50367, #61202, #13657, #50712 ),
 .UNSPECIFIED., .F., .F.,
 ( 4, 4 ),
 ( 0.000000000000000000, 1.000000000000000000 ),
 .UNSPECIFIED. ) ;
#15121=CARTESIAN_POINT ( 'NONE',  ( 7.415011787918005304, 3.233093659812002585, 6.479723185591006462 ) ) ;
#15131=CARTESIAN_POINT ( 'NONE',  ( 9.211104719594999324, 5.462898983065000102, -8.055936939571999744 ) ) ;
#15138=CARTESIAN_POINT ( 'NONE',  ( 9.790085841230000696, 5.149303692842000402, -5.987168472229000393 ) ) ;
#15143=CARTESIAN_POINT ( 'NONE',  ( 8.933148997457999840, 5.167567567567999731, 6.822293592207000934 ) ) ;
#15147=CARTESIAN_POINT ( 'NONE',  ( 9.883629719592001095, 5.656948148960999845, -6.994239053114000626 ) ) ;
#15149=CARTESIAN_POINT ( 'NONE',  ( 10.74708949327000163, 5.603142351927999698, -6.963341971584000589 ) ) ;
#15150=VERTEX_POINT ( 'NONE', #39754 ) ;
#15157=VERTEX_POINT ( 'NONE', #17742 ) ;
#15163=CARTESIAN_POINT ( 'NONE',  ( 8.997439158776000312, 2.773858540272000184, -8.951250717848999727 ) ) ;
#15167=ORIENTED_EDGE ( 'NONE', *, *, #39616, .T. ) ;
#15168=CARTESIAN_POINT ( 'NONE',  ( 9.079170280414000871, 4.815598936798999752, -8.835641302565999666 ) ) ;
#15170=CARTESIAN_POINT ( 'NONE',  ( 1.123890132541374820, 2.150913519912194261, 2.798833948393636195 ) ) ;
#15175=CARTESIAN_POINT ( 'NONE',  ( 8.667968151675525590, 5.621194584483597545, 6.797889474695828049 ) ) ;
#15193=CARTESIAN_POINT ( 'NONE',  ( 0.1499942179680000265, -1.384928887584815804, -2.402872127494067644 ) ) ;
#15194=CARTESIAN_POINT ( 'NONE',  ( 3.639522202018000030, 2.080217348686999923, -2.466622738429000261 ) ) ;
#15200=CARTESIAN_POINT ( 'NONE',  ( 3.500000000000001332, -0.7367456077618940169, 3.179724234113067372 ) ) ;
#15206=CARTESIAN_POINT ( 'NONE',  ( 7.564999999998999414, 5.349999999999999645, -7.500000000000000000 ) ) ;
#15215=ORIENTED_EDGE ( 'NONE', *, *, #29338, .F. ) ;
#15216=CARTESIAN_POINT ( 'NONE',  ( 8.267894473231022445, 3.183914367779229870, -6.154702421054330408 ) ) ;
#15218=DIRECTION ( 'NONE',  ( 0.000000000000000000, -1.000000000000000000, 0.000000000000000000 ) ) ;
#15219=CARTESIAN_POINT ( 'NONE',  ( 7.233579719589999790, 5.250007070404999254, -8.441605882928000071 ) ) ;
#15221=EDGE_CURVE ( 'NONE', #1019, #55375, #36126, .T. ) ;
#15223=ORIENTED_EDGE ( 'NONE', *, *, #61317, .T. ) ;
#15225=ADVANCED_FACE ( 'NONE', ( #9290 ), #8278, .F. ) ;
#15229=CARTESIAN_POINT ( 'NONE',  ( 9.101497196731600070, 2.899999999999999911, 6.350512455778112297 ) ) ;
#15234=CARTESIAN_POINT ( 'NONE',  ( 10.93769906941999892, 2.936877991120999898, -4.920829195977000303 ) ) ;
#15236=CARTESIAN_POINT ( 'NONE',  ( 6.999999691988000095, -12.89129024452999950, 1.677687644161999891 ) ) ;
#15240=CARTESIAN_POINT ( 'NONE',  ( 4.149992563292000725, 2.000000000000000000, 0.000000000000000000 ) ) ;
#15241=ORIENTED_EDGE ( 'NONE', *, *, #6401, .F. ) ;
#15245=ORIENTED_EDGE ( 'NONE', *, *, #63909, .F. ) ;
#15246=CARTESIAN_POINT ( 'NONE',  ( 9.520797373037000355, 3.270552986600999912, 5.711478154812000163 ) ) ;
#15248=DIRECTION ( 'NONE',  ( 0.000000000000000000, 1.000000000000000000, 0.000000000000000000 ) ) ;
#15250=CYLINDRICAL_SURFACE ( 'NONE', #29403, 0.4999999999999998335 ) ;
#15251=CARTESIAN_POINT ( 'NONE',  ( 2.768173772219000295, -3.696853176092000481, 0.2879355096300999506 ) ) ;
#15252=DIRECTION ( 'NONE',  ( 0.000000000000000000, 1.000000000000000000, 0.000000000000000000 ) ) ;
#15258=CARTESIAN_POINT ( 'NONE',  ( 10.43243243692329081, 4.711781382511952998, -9.127213014442659755 ) ) ;
#15261=CARTESIAN_POINT ( 'NONE',  ( 10.68903608760000168, 2.568976842941999905, 7.728092503410000091 ) ) ;
#15279=CARTESIAN_POINT ( 'NONE',  ( 0.4855877078939999647, -3.136585174263000209, 0.6804425983637999442 ) ) ;
#15282=CARTESIAN_POINT ( 'NONE',  ( 10.77401721959000014, 3.826866801954999620, -5.823193568970000733 ) ) ;
#15284=CARTESIAN_POINT ( 'NONE',  ( 8.869959105252339882, 2.899999999999999911, 6.481052078534832006 ) ) ;
#15285=DIRECTION ( 'NONE',  ( 0.000000000000000000, 0.8648648648648717963, -0.5020047465136829867 ) ) ;
#15289=CARTESIAN_POINT ( 'NONE',  ( 8.079135841228998416, 3.524748802314000340, 5.573833469815000718 ) ) ;
#15292=CARTESIAN_POINT ( 'NONE',  ( 7.019914158769999801, 2.417988323708999854, -8.552044326954000297 ) ) ;
#15296=CARTESIAN_POINT ( 'NONE',  ( 2.896806799209917127, 0.9161175952574848180, -3.408904368339103819 ) ) ;
#15298=VERTEX_POINT ( 'NONE', #41124 ) ;
#15300=CYLINDRICAL_SURFACE ( 'NONE', #13426, 0.4999999999999998335 ) ;
#15304=CARTESIAN_POINT ( 'NONE',  ( 2.311390132542709086, -3.500000000000000888, -0.4581489286485119217 ) ) ;
#15311=CARTESIAN_POINT ( 'NONE',  ( 7.448642219589999947, 4.628941086829000184, 5.991667691044999522 ) ) ;
#15319=CARTESIAN_POINT ( 'NONE',  ( 9.840759809372002564, 7.661537722051988908, -5.619389075507000619 ) ) ;
#15326=VERTEX_POINT ( 'NONE', #62437 ) ;
#15331=CARTESIAN_POINT ( 'NONE',  ( 4.900006121741999010, -2.000000000000000000, 0.000000000000000000 ) ) ;
#15332=CARTESIAN_POINT ( 'NONE',  ( 10.93146722582000052, 2.472885155055999817, -7.514158739122999364 ) ) ;
#15337=CARTESIAN_POINT ( 'NONE',  ( 10.93727498060999892, 5.425427353909999972, 7.240585962396000497 ) ) ;
#15340=CARTESIAN_POINT ( 'NONE',  ( 8.781951181944481988, 5.320239682019779259, -6.310370185644361918 ) ) ;
#15344=CARTESIAN_POINT ( 'NONE',  ( 9.465106464520001595, 2.290037071913000322, 6.601704384062999864 ) ) ;
#15346=CARTESIAN_POINT ( 'NONE',  ( 8.771960841230001193, 3.061731693614000438, -8.535706278603999664 ) ) ;
#15348=CARTESIAN_POINT ( 'NONE',  ( 10.85467598778999943, 9.827440234331000113, -5.589530524231999919 ) ) ;
#15350=CARTESIAN_POINT ( 'NONE',  ( 10.83837003704316615, 5.765189909578217531, -7.466044055516256606 ) ) ;
#15352=CARTESIAN_POINT ( 'NONE',  ( 10.44079719460000000, 5.435719122931000236, 7.303631812894000319 ) ) ;
#15354=LINE ( 'NONE', #5196, #60107 ) ;
#15357=CARTESIAN_POINT ( 'NONE',  ( 8.581920280410001212, 4.769017407621999993, -8.862909124839001507 ) ) ;
#15360=CARTESIAN_POINT ( 'NONE',  ( 3.479247788823166321, 3.398203023142295720, -0.9541934759467685101 ) ) ;
#15363=ORIENTED_EDGE ( 'NONE', *, *, #50107, .T. ) ;
#15364=CARTESIAN_POINT ( 'NONE',  ( 4.500000000000000000, -3.200000000000000178, 0.000000000000000000 ) ) ;
#15366=CARTESIAN_POINT ( 'NONE',  ( 9.021064158776001207, 4.883347899767999323, -6.417062834774999835 ) ) ;
#15367=CARTESIAN_POINT ( 'NONE',  ( 7.614999999996999946, 5.349999999999999645, -7.500000000000000000 ) ) ;
#15369=ORIENTED_EDGE ( 'NONE', *, *, #43595, .F. ) ;
#15370=CARTESIAN_POINT ( 'NONE',  ( 10.57224177473000104, 4.020426023752999178, 8.920668579831000145 ) ) ;
#15376=CARTESIAN_POINT ( 'NONE',  ( 9.342517219591000455, 5.057081813675999626, 8.967637988488998957 ) ) ;
#15377=AXIS2_PLACEMENT_3D ( 'NONE', #21583, #37670, #64226 ) ;
#15378=B_SPLINE_CURVE_WITH_KNOTS ( 'NONE', 3,
 ( #50812, #40654, #3254, #61637 ),
 .UNSPECIFIED., .F., .F.,
 ( 4, 4 ),
 ( 0.8745717919976516708, 1.000000000000000000 ),
 .UNSPECIFIED. ) ;
#15388=CARTESIAN_POINT ( 'NONE',  ( 10.02991192131000098, 2.506457833269999824, 6.215406506815000398 ) ) ;
#15389=CARTESIAN_POINT ( 'NONE',  ( 11.09647882763000126, 3.099775370665000196, 6.097099813297999660 ) ) ;
#15392=ORIENTED_EDGE ( 'NONE', *, *, #26124, .F. ) ;
#15393=CARTESIAN_POINT ( 'NONE',  ( 10.92799928937301246, 5.127999289373012637, -6.526892970107653014 ) ) ;
#15394=VECTOR ( 'NONE', #24651, 1000.000000000000000 ) ;
#15398=EDGE_CURVE ( 'NONE', #61732, #9405, #23619, .T. ) ;
#15406=EDGE_LOOP ( 'NONE', ( #52543, #40066, #51720, #18654, #29518 ) ) ;
#15408=CARTESIAN_POINT ( 'NONE',  ( 10.93727498060999892, 5.425427353909999972, 7.240585962396000497 ) ) ;
#15409=CARTESIAN_POINT ( 'NONE',  ( 10.07930935222999835, 2.718121894972999719, -6.397795030233000446 ) ) ;
#15410=CARTESIAN_POINT ( 'NONE',  ( 8.500383147356993518, 5.097359707274998541, 6.605634423517003029 ) ) ;
#15415=CARTESIAN_POINT ( 'NONE',  ( 7.443295280410000103, 4.698356649019999942, 8.789431186081998248 ) ) ;
#15420=CARTESIAN_POINT ( 'NONE',  ( 8.477766462057999775, 2.899999999999999911, -6.558719934578999933 ) ) ;
#15421=EDGE_CURVE ( 'NONE', #7028, #33691, #43298, .T. ) ;
#15422=CARTESIAN_POINT ( 'NONE',  ( 9.825984992304002574, 8.538414651508006159, 6.566328153291997261 ) ) ;
#15425=CARTESIAN_POINT ( 'NONE',  ( 10.90000037895999796, 0.2999996193951000034, 9.776630289319001577 ) ) ;
#15430=DIRECTION ( 'NONE',  ( -0.7071067811865474617, -0.7071067811865474617, 6.440236212535425163E-09 ) ) ;
#15435=CARTESIAN_POINT ( 'NONE',  ( 7.533885841228999958, 4.623631324973000112, 8.651459902566999816 ) ) ;
#15436=CARTESIAN_POINT ( 'NONE',  ( 9.616863785686895483, 5.079232767740477605, -8.329457163983990498 ) ) ;
#15437=VECTOR ( 'NONE', #50613, 1000.000000000000114 ) ;
#15439=CARTESIAN_POINT ( 'NONE',  ( 11.09999999999999964, 2.700000000000000178, -5.160242730539000178 ) ) ;
#15442=CARTESIAN_POINT ( 'NONE',  ( 9.888314158772001150, 5.105193280231000053, -8.895607399415000671 ) ) ;
#15444=CARTESIAN_POINT ( 'NONE',  ( 9.951050468514374359, 5.324162572649938419, 7.941948203265592809 ) ) ;
#15446=CARTESIAN_POINT ( 'NONE',  ( 8.082873386424997975, 5.111739203374999541, -6.679001318365999751 ) ) ;
#15447=ORIENTED_EDGE ( 'NONE', *, *, #22783, .T. ) ;
#15458=CARTESIAN_POINT ( 'NONE',  ( 8.154195026538843649, 3.087577394105698758, 6.292719520537814581 ) ) ;
#15462=DIRECTION ( 'NONE',  ( 1.000000000000000000, 1.776356839548999970E-14, 0.000000000000000000 ) ) ;
#15465=CARTESIAN_POINT ( 'NONE',  ( 8.587232097456750424, 5.014137595553737725, 6.171797112031566002 ) ) ;
#15478=VERTEX_POINT ( 'NONE', #32361 ) ;
#15479=CARTESIAN_POINT ( 'NONE',  ( 8.863029719594999634, 2.990001567622999623, -8.695425648791999862 ) ) ;
#15481=ORIENTED_EDGE ( 'NONE', *, *, #26841, .T. ) ;
#15493=ORIENTED_EDGE ( 'NONE', *, *, #36840, .T. ) ;
#15495=CARTESIAN_POINT ( 'NONE',  ( 9.626145280412998773, 3.934138271021000222, -9.063586117809000697 ) ) ;
#15497=CARTESIAN_POINT ( 'NONE',  ( 10.47212119989999835, 2.640756834784999896, -8.505248851866998194 ) ) ;
#15498=ORIENTED_EDGE ( 'NONE', *, *, #20682, .T. ) ;
#15509=CIRCLE ( 'NONE', #54583, 12.50000000000000000 ) ;
#15512=CARTESIAN_POINT ( 'NONE',  ( 9.933354719590999693, 5.639765292528999829, -8.059103558718000215 ) ) ;
#15515=ORIENTED_EDGE ( 'NONE', *, *, #54614, .T. ) ;
#15517=CARTESIAN_POINT ( 'NONE',  ( 10.91165258067000110, 5.022850734190000388, -4.913708377245000314 ) ) ;
#15538=CARTESIAN_POINT ( 'NONE',  ( 7.945634795641004722, 2.916734013644262991, -6.617471303626205170 ) ) ;
#15540=DIRECTION ( 'NONE',  ( 0.000000000000000000, 0.000000000000000000, -1.000000000000000000 ) ) ;
#15547=CARTESIAN_POINT ( 'NONE',  ( 5.399999746777999654, -12.99045401563999924, 1.690592933733000125 ) ) ;
#15551=FACE_OUTER_BOUND ( 'NONE', #48447, .T. ) ;
#15560=EDGE_CURVE ( 'NONE', #60354, #46704, #66216, .T. ) ;
#15561=B_SPLINE_CURVE_WITH_KNOTS ( 'NONE', 3,
 ( #8833, #30174, #56389, #61975, #33430 ),
 .UNSPECIFIED., .F., .F.,
 ( 4, 1, 4 ),
 ( 0.000000000000000000, 0.5000000000000000000, 1.000000000000000000 ),
 .UNSPECIFIED. ) ;
#15568=CARTESIAN_POINT ( 'NONE',  ( 8.514905693275615306, 2.973706675831895740, -8.924953531459744127 ) ) ;
#15569=CARTESIAN_POINT ( 'NONE',  ( 7.093264158770000272, 5.397217548590999669, -7.528974776547999959 ) ) ;
#15571=CARTESIAN_POINT ( 'NONE',  ( 9.477173644534087060, 5.064627895235314980, 8.332423391400503476 ) ) ;
#15574=CARTESIAN_POINT ( 'NONE',  ( 10.86123236735334530, 5.100000000000000533, -6.348362623949493688 ) ) ;
#15580=CARTESIAN_POINT ( 'NONE',  ( 10.64551289531389777, 5.370173726513001178, 6.373339187755826529 ) ) ;
#15582=ADVANCED_FACE ( 'NONE', ( #48034 ), #55623, .T. ) ;
#15587=VERTEX_POINT ( 'NONE', #2473 ) ;
#15589=ORIENTED_EDGE ( 'NONE', *, *, #68553, .F. ) ;
#15590=CARTESIAN_POINT ( 'NONE',  ( 9.388624299788999039, 4.079402096444999515, 9.259357173634999327 ) ) ;
#15591=CARTESIAN_POINT ( 'NONE',  ( 11.07691721959000120, 3.101894630379999906, -8.926552937604000704 ) ) ;
#15598=ORIENTED_EDGE ( 'NONE', *, *, #36861, .F. ) ;
#15601=DIRECTION ( 'NONE',  ( 1.000000000000000000, 0.000000000000000000, 1.736057635219000097E-14 ) ) ;
#15605=CARTESIAN_POINT ( 'NONE',  ( 10.44079719460000000, 5.435719122931000236, 7.303631812894000319 ) ) ;
#15617=CARTESIAN_POINT ( 'NONE',  ( 9.708354719591000048, 5.481267232667000222, -8.005061172455999241 ) ) ;
#15619=CARTESIAN_POINT ( 'NONE',  ( 6.899999691988000450, -13.87069231928999891, -4.225386915259999654 ) ) ;
#15622=CARTESIAN_POINT ( 'NONE',  ( 10.70920446231090040, 2.899999999999999911, 6.662590550528270761 ) ) ;
#15624=CARTESIAN_POINT ( 'NONE',  ( 10.80374834123000127, 2.766954612461999918, -8.073381085840999560 ) ) ;
#15630=CARTESIAN_POINT ( 'NONE',  ( 8.464260841230998977, 2.029098103856999735, 7.726995416028000108 ) ) ;
#15633=CARTESIAN_POINT ( 'NONE',  ( 8.486229719590999920, 4.901484321470999994, -8.891682961388999829 ) ) ;
#15636=ORIENTED_EDGE ( 'NONE', *, *, #1431, .F. ) ;
#15638=DIRECTION ( 'NONE',  ( 1.000000000000000000, 3.552713678493000424E-14, 8.881784196233999896E-14 ) ) ;
#15641=CARTESIAN_POINT ( 'NONE',  ( 6.916495184453999912, 12.19460085780000114, 3.104235911784000379 ) ) ;
#15650=CARTESIAN_POINT ( 'NONE',  ( 7.165489158771000788, 2.688365364125000045, 8.140015608605001063 ) ) ;
#15657=B_SPLINE_SURFACE_WITH_KNOTS ( 'NONE', 3, 3, ( 
 ( #54346, #50152, #12399, #34077, #18680, #8186, #2590, #35114, #1558, #28844, #45256, #23921, #40013, #44230, #66561, #66217, #55393, #56077, #29180, #39660, #39315, #61327, #34767, #34430, #13446, #40344, #23233, #49804, #7490, #56425, #28135, #65870, #33731, #55047, #7150 ),
 ( #65523, #22880, #55743, #60636, #17651, #50838, #50489, #24263, #28486, #45601, #7845, #38974, #1912, #13096, #66905, #13781, #49449, #60292, #29536, #44578, #19019, #2934, #61667, #17994, #12747, #18340, #2257, #23571, #44913, #60983, #30211, #68271, #52204, #4305, #3281 ),
 ( #36127, #57442, #14125, #20391, #9548, #4645, #25985, #14809, #42065, #20051, #15149, #30890, #25639, #20737, #3616, #51515, #35789, #15497, #36824, #46282, #35452, #56778, #8874, #19360, #47312, #45934, #24611, #46968, #41031, #67245, #31241, #41718, #68618, #62013, #63372 ),
 ( #67586, #36469, #41378, #52547, #3955, #63019, #57790, #8530, #9902, #29878, #24950, #51186, #19710, #62353, #40684, #14472, #67934, #57104, #9202, #30545, #51858, #25293, #46628, #62686, #37844, #16516, #59167, #63718, #48683, #11269, #54263, #6364, #64395, #22447, #441 ) ),
 .UNSPECIFIED., .F., .F., .F.,
 ( 4, 4 ),
 ( 4, 1, 1, 1, 1, 1, 1, 1, 1, 1, 1, 1, 1, 1, 1, 1, 1, 1, 1, 1, 1, 1, 1, 1, 1, 1, 1, 1, 1, 1, 1, 1, 4 ),
 ( -0.1039370721279000015, 1.103937072127999963 ),
 ( 0.1942321073450000157, 0.2199060843169000079, 0.2455800612886999967, 0.2712540382605999612, 0.2969280152323999777, 0.3226019922043000254, 0.3482759691761000420, 0.3739499461479999787, 0.3996239231197999953, 0.4252979000916999874, 0.4509718770635000040, 0.4766458540353999962, 0.5023198310072000128, 0.5279938079791000050, 0.5536677849509000771, 0.5793417619227999582, 0.6050157388945999193, 0.6306897158665000225, 0.6563636928382999836, 0.6820376698101999757, 0.7077116467820000478, 0.7333856237539000400, 0.7590596007256998901, 0.7847335776975999933, 0.8104075546693999543, 0.8360815316413000575, 0.8617555086131000186, 0.8874294855850000108, 0.9131034625568000829, 0.9387774395286999640, 0.9644514165004999251, 0.9901253934722999972, 1.015799370444000038 ),
 .UNSPECIFIED. ) ;
#15660=CARTESIAN_POINT ( 'NONE',  ( 11.40138360751001834, 9.883546562558999327, -5.506038862248998633 ) ) ;
#15661=CARTESIAN_POINT ( 'NONE',  ( 9.003209435578913400, 2.902877702504753632, 6.186420784426521990 ) ) ;
#15667=DIRECTION ( 'NONE',  ( -1.000000000000000000, 0.000000000000000000, 0.000000000000000000 ) ) ;
#15673=CARTESIAN_POINT ( 'NONE',  ( 4.900006121741999898, -1.747572776708515407, 1.007237960741799387 ) ) ;
#15674=CARTESIAN_POINT ( 'NONE',  ( 11.17811698873999937, 2.762452057009999962, -6.187198315927000536 ) ) ;
#15677=CARTESIAN_POINT ( 'NONE',  ( 7.733151861820001471, 2.920631402299000534, -6.523085346364998038 ) ) ;
#15678=CARTESIAN_POINT ( 'NONE',  ( 10.37873747135000002, 4.882725050998000249, 6.350806206758999650 ) ) ;
#15679=EDGE_LOOP ( 'NONE', ( #60078, #1953, #54089, #53951 ) ) ;
#15681=CARTESIAN_POINT ( 'NONE',  ( 9.967852198058999136, 2.034774058634999605, 7.636878205663998997 ) ) ;
#15683=CARTESIAN_POINT ( 'NONE',  ( 11.00366064676999933, 2.264078662261999941, 7.798351372501000078 ) ) ;
#15685=CARTESIAN_POINT ( 'NONE',  ( 9.120035841232999374, 5.288433695693000480, -8.041290150997999930 ) ) ;
#15693=CARTESIAN_POINT ( 'NONE',  ( 8.136848617591816435, 5.311482524923382798, -7.867489542080182474 ) ) ;
#15694=DIRECTION ( 'NONE',  ( -0.7071175914358266423, 0.000000000000000000, -0.7070959707719987053 ) ) ;
#15696=CARTESIAN_POINT ( 'NONE',  ( 9.020585841232000135, 4.920236664407999783, -6.448229650796999834 ) ) ;
#15698=ADVANCED_FACE ( 'NONE', ( #23372 ), #65621, .F. ) ;
#15702=CARTESIAN_POINT ( 'NONE',  ( 10.60000000000016662, 4.646670285053247085, 4.756097560975664607 ) ) ;
#15708=CARTESIAN_POINT ( 'NONE',  ( 8.962479719595000560, 2.546924812613000189, -6.918870225297999887 ) ) ;
#15712=CARTESIAN_POINT ( 'NONE',  ( 11.14994211610999919, 2.627136771666999771, 6.696094414592000277 ) ) ;
#15718=CARTESIAN_POINT ( 'NONE',  ( 8.315517219592001297, 5.485785046334999748, 8.532070739720001740 ) ) ;
#15720=EDGE_CURVE ( 'NONE', #523, #54836, #16488, .T. ) ;
#15724=CARTESIAN_POINT ( 'NONE',  ( 8.406851002545000284, 2.832432432432000269, -6.822293592207000934 ) ) ;
#15725=CARTESIAN_POINT ( 'NONE',  ( 1.929202210879999990, -0.1982148001128000159, 3.252998300308999724 ) ) ;
#15729=CARTESIAN_POINT ( 'NONE',  ( 10.80168826891999956, 3.998196217194999846, 9.431555066626000183 ) ) ;
#15731=ORIENTED_EDGE ( 'NONE', *, *, #66773, .F. ) ;
#15732=SHAPE_REPRESENTATION ( 'Negative Post', ( #9676 ), #67766 ) ;
#15740=ORIENTED_EDGE ( 'NONE', *, *, #62988, .F. ) ;
#15742=FACE_OUTER_BOUND ( 'NONE', #53142, .T. ) ;
#15744=ORIENTED_EDGE ( 'NONE', *, *, #55596, .T. ) ;
#15745=LINE ( 'NONE', #30454, #50637 ) ;
#15747=CARTESIAN_POINT ( 'NONE',  ( 11.09999999999999964, 7.281355511280001025, -6.286510895624999762 ) ) ;
#15748=CARTESIAN_POINT ( 'NONE',  ( 9.949437606643998677, 2.508497579857000392, -7.171862210735000076 ) ) ;
#15749=CARTESIAN_POINT ( 'NONE',  ( 7.800985831153996131, 4.602212482482000766, 6.372454311207003563 ) ) ;
#15752=EDGE_CURVE ( 'NONE', #58126, #32166, #65341, .T. ) ;
#15755=CARTESIAN_POINT ( 'NONE',  ( 7.673642219589999591, 4.696238830159999544, 5.830273622963999536 ) ) ;
#15758=DIRECTION ( 'NONE',  ( 0.000000000000000000, 1.000000000000000000, 0.000000000000000000 ) ) ;
#15759=CARTESIAN_POINT ( 'NONE',  ( 8.628315327349485031, 2.973711298499293942, -6.169547619358109358 ) ) ;
#15761=AXIS2_PLACEMENT_3D ( 'NONE', #19958, #36375, #68519 ) ;
#15762=CARTESIAN_POINT ( 'NONE',  ( 10.96506373917000055, 6.669401756511000201, 5.364506396814999967 ) ) ;
#15763=CARTESIAN_POINT ( 'NONE',  ( 10.95087180411999839, 9.916154023254000194, 5.627633586593999482 ) ) ;
#15769=CARTESIAN_POINT ( 'NONE',  ( 8.828853474160295534, 2.650682855974121122, -7.263274753612249945 ) ) ;
#15773=CARTESIAN_POINT ( 'NONE',  ( 0.2033022342298000107, 1.141789477572999978, -2.999605631121999849 ) ) ;
#15779=EDGE_CURVE ( 'NONE', #10880, #39380, #46165, .T. ) ;
#15780=CARTESIAN_POINT ( 'NONE',  ( 10.47111721959000086, 5.170640285885000687, -8.712953516124999354 ) ) ;
#15784=CARTESIAN_POINT ( 'NONE',  ( 8.967236468531000426, 5.342667293695661179, 7.360013885755487983 ) ) ;
#15787=CYLINDRICAL_SURFACE ( 'NONE', #5452, 11.35000000000000142 ) ;
#15788=CARTESIAN_POINT ( 'NONE',  ( 9.660528907822998335, 2.899999999999999911, -6.152188490330000370 ) ) ;
#15790=CARTESIAN_POINT ( 'NONE',  ( 8.999999001754000361, 3.268496584495999908E-13, -12.49999978039651083 ) ) ;
#15794=B_SPLINE_CURVE_WITH_KNOTS ( 'NONE', 3,
 ( #65487, #1875, #57408, #3920 ),
 .UNSPECIFIED., .F., .F.,
 ( 4, 4 ),
 ( 0.000000000000000000, 1.000000000000000000 ),
 .UNSPECIFIED. ) ;
#15796=EDGE_CURVE ( 'NONE', #18020, #52078, #61804, .T. ) ;
#15800=CARTESIAN_POINT ( 'NONE',  ( 10.98768472639999949, 5.139096889661000311, -4.945212061661000469 ) ) ;
#15808=CARTESIAN_POINT ( 'NONE',  ( 9.771640687503566625, 2.873222873816650313, 6.752018918868516018 ) ) ;
#15813=CARTESIAN_POINT ( 'NONE',  ( 8.854170280414001226, 4.902869380824999901, -8.978557145469999057 ) ) ;
#15817=B_SPLINE_CURVE_WITH_KNOTS ( 'NONE', 3,
 ( #25949, #5990, #26650, #5645, #63688, #4966 ),
 .UNSPECIFIED., .F., .F.,
 ( 4, 2, 4 ),
 ( 0.000000000000000000, 0.5000000000000000000, 1.000000000000000000 ),
 .UNSPECIFIED. ) ;
#15821=CARTESIAN_POINT ( 'NONE',  ( 8.895035841232999729, 5.751585344281000545, -8.235867044345999588 ) ) ;
#15828=CARTESIAN_POINT ( 'NONE',  ( 8.684028039623227002, 2.794631556210644074, 8.206409581471232784 ) ) ;
#15829=ORIENTED_EDGE ( 'NONE', *, *, #38738, .F. ) ;
#15830=LINE ( 'NONE', #10242, #187 ) ;
#15831=( NAMED_UNIT ( * ) SI_UNIT ( $, .STERADIAN. ) SOLID_ANGLE_UNIT ( ) );
#15832=VERTEX_POINT ( 'NONE', #62482 ) ;
#15843=CIRCLE ( 'NONE', #11396, 12.49999909016000110 ) ;
#15844=FACE_OUTER_BOUND ( 'NONE', #31717, .T. ) ;
#15849=VERTEX_POINT ( 'NONE', #3412 ) ;
#15850=CARTESIAN_POINT ( 'NONE',  ( 11.04471440281000127, 5.245236777044000043, -5.184237567191000373 ) ) ;
#15853=CARTESIAN_POINT ( 'NONE',  ( 0.1499942179679999987, 2.750000000000000000, 0.000000000000000000 ) ) ;
#15856=CARTESIAN_POINT ( 'NONE',  ( 11.03776785110999903, 5.237767851104999650, 6.571291218949999902 ) ) ;
#15859=CARTESIAN_POINT ( 'NONE',  ( 8.453116750410908153, 5.099910069830336568, -6.561598178278856608 ) ) ;
#15875=CARTESIAN_POINT ( 'NONE',  ( 6.999999999999999112, 9.168025982482129521, -4.705522764150024351 ) ) ;
#15877=VERTEX_POINT ( 'NONE', #40475 ) ;
#15880=CARTESIAN_POINT ( 'NONE',  ( 6.899999692059999745, 12.99045401434999825, 1.690592943097000145 ) ) ;
#15882=CARTESIAN_POINT ( 'NONE',  ( 1.655140132541082831, 0.9161175952574702741, 3.408904368339106927 ) ) ;
#15891=AXIS2_PLACEMENT_3D ( 'NONE', #6542, #23322, #44998 ) ;
#15899=ORIENTED_EDGE ( 'NONE', *, *, #47275, .T. ) ;
#15901=CARTESIAN_POINT ( 'NONE',  ( 7.663385841224000572, 2.462963193532999640, -6.383277393009000100 ) ) ;
#15903=CARTESIAN_POINT ( 'NONE',  ( 7.364999999998000035, 2.649999999999999911, -7.500000000000000000 ) ) ;
#15917=CARTESIAN_POINT ( 'NONE',  ( 7.171515396205728088, 4.321096043748422488, -8.846445178760147243 ) ) ;
#15919=EDGE_CURVE ( 'NONE', #26552, #7028, #55587, .T. ) ;
#15920=B_SPLINE_SURFACE_WITH_KNOTS ( 'NONE', 3, 3, ( 
 ( #23484, #33639, #54606, #49354, #60202, #2502, #44824, #7057, #39568, #29442, #50748, #65432, #2845, #39920, #60892, #65777, #28392, #13008, #34334, #24172, #13354, #33291, #59847, #55652, #29094, #1816, #1468, #44486, #12653, #50403, #22784, #23135, #44133, #34680, #17554 ),
 ( #11952, #61238, #55994, #8098, #17903, #38880, #54955, #39220, #60546, #30127, #67155, #45844, #35023, #14719, #3867, #57019, #25550, #15056, #35702, #57350, #9119, #30456, #19963, #56684, #8783, #62933, #9806, #25201, #51430, #36034, #13694, #40258, #57696, #67500, #68525 ),
 ( #9454, #51091, #29789, #31155, #4212, #40940, #41287, #62261, #19267, #36380, #30796, #52109, #46875, #46536, #40596, #62595, #61578, #61921, #3526, #24862, #68183, #41627, #20301, #52457, #14036, #4552, #51769, #3194, #67842, #14382, #25893, #35362, #46190, #47222, #56338 ),
 ( #8441, #24521, #19618, #26588, #37075, #48243, #42998, #32860, #43356, #63278, #54173, #26929, #16424, #58386, #64306, #27612, #32516, #696, #10493, #7, #37753, #5929, #4901, #53149, #20647, #59079, #53832, #11179, #48940, #6271, #41972, #27271, #15408, #36734, #48594 ) ),
 .UNSPECIFIED., .F., .F., .F.,
 ( 4, 4 ),
 ( 4, 1, 1, 1, 1, 1, 1, 1, 1, 1, 1, 1, 1, 1, 1, 1, 1, 1, 1, 1, 1, 1, 1, 1, 1, 1, 1, 1, 1, 1, 1, 1, 4 ),
 ( -0.1039370721279000015, 1.103937072127999963 ),
 ( -0.01933701211302999920, 0.01208563257065999909, 0.04350827725433999843, 0.07493092193802000645, 0.1063535666217000075, 0.1377762113054000204, 0.1691988559891000055, 0.2006215006727000150, 0.2320441453564000001, 0.2634667900400999851, 0.2948894347238000258, 0.3263120794074999553, 0.3577347240911999959, 0.3891573687748000054, 0.4205800134584999905, 0.4520026581421999756, 0.4834253028259000162, 0.5148479475096000568, 0.5462705921932000663, 0.5776932368768999959, 0.6091158815606000365, 0.6405385262443000771, 0.6719611709280000067, 0.7033838156117000473, 0.7348064602953000568, 0.7662291049789999864, 0.7976517496627000270, 0.8290743943464000676, 0.8604970390300999972, 0.8919196837138000378, 0.9233423283974000473, 0.9547649730810999769, 0.9861876177648000175 ),
 .UNSPECIFIED. ) ;
#15924=CARTESIAN_POINT ( 'NONE',  ( 9.743561007103998861, 5.287400066955999733, 8.939966147452000911 ) ) ;
#15926=CARTESIAN_POINT ( 'NONE',  ( 10.94846415877000112, 3.841064079579000090, -9.341816855317999213 ) ) ;
#15927=B_SPLINE_CURVE_WITH_KNOTS ( 'NONE', 3,
 ( #52355, #43245, #63171, #15641, #57949 ),
 .UNSPECIFIED., .F., .F.,
 ( 4, 1, 4 ),
 ( 0.000000000000000000, 0.5000000000000000000, 1.000000000000000000 ),
 .UNSPECIFIED. ) ;
#15928=CARTESIAN_POINT ( 'NONE',  ( 11.09999999999999964, 4.000000000000000000, 7.500000000000000000 ) ) ;
#15929=CARTESIAN_POINT ( 'NONE',  ( 9.269210841233000764, 3.098073081301000009, -8.567513114264999174 ) ) ;
#15931=CARTESIAN_POINT ( 'NONE',  ( 10.59999999999999964, 4.599999999999999645, 4.756097560976000338 ) ) ;
#15935=EDGE_LOOP ( 'NONE', ( #68857, #38589, #38889, #34377 ) ) ;
#15942=CARTESIAN_POINT ( 'NONE',  ( 10.99933470386000067, 5.081013421858999735, 8.239043921879998678 ) ) ;
#15954=CARTESIAN_POINT ( 'NONE',  ( 9.219964158774999419, 3.941185585667000169, -8.896279800194999865 ) ) ;
#15958=CARTESIAN_POINT ( 'NONE',  ( 0.7186698601468000103, 2.838478058858999731, -1.283102133118000143 ) ) ;
#15961=CARTESIAN_POINT ( 'NONE',  ( 2.504702091563999478, 3.604403478001999783, -1.066139224190999935 ) ) ;
#15963=DIRECTION ( 'NONE',  ( -1.000000000000000000, 0.000000000000000000, 0.000000000000000000 ) ) ;
#15967=CARTESIAN_POINT ( 'NONE',  ( 7.603420280409000753, 5.687206835507000235, 6.847268999608999707 ) ) ;
#15971=CARTESIAN_POINT ( 'NONE',  ( 6.961329719590000131, 5.346927244140000646, -8.589407719218000281 ) ) ;
#15983=DIRECTION ( 'NONE',  ( 1.000000000000000000, 0.000000000000000000, 0.000000000000000000 ) ) ;
#15984=CARTESIAN_POINT ( 'NONE',  ( 7.924878289113897800, 5.349357204871084903, 7.500005630225526687 ) ) ;
#15989=CARTESIAN_POINT ( 'NONE',  ( 8.411454719592999396, 3.882020551409000042, 5.870058896428999695 ) ) ;
#15993=CARTESIAN_POINT ( 'NONE',  ( 11.02144803208000035, 6.131092151569999871, -5.118571239882999890 ) ) ;
#15996=CARTESIAN_POINT ( 'NONE',  ( 6.032801325126996517, 9.323366446862999979, -4.734513139768997902 ) ) ;
#15997=CARTESIAN_POINT ( 'NONE',  ( 7.906851002540999929, 2.832432432432000269, -6.822293592207000934 ) ) ;
#16001=EDGE_CURVE ( 'NONE', #47667, #58927, #36265, .T. ) ;
#16003=ADVANCED_FACE ( 'NONE', ( #63160 ), #48039, .F. ) ;
#16004=CARTESIAN_POINT ( 'NONE',  ( 10.90000154029999990, 0.000000000000000000, 0.000000000000000000 ) ) ;
#16013=CARTESIAN_POINT ( 'NONE',  ( 11.03408597791999846, 2.992846905312999795, -9.056576857348998644 ) ) ;
#16021=CARTESIAN_POINT ( 'NONE',  ( 2.155140132542666453, 0.9161175952574702741, 3.408904368339106927 ) ) ;
#16029=CARTESIAN_POINT ( 'NONE',  ( 10.25461802485000007, 2.860644035673999941, 6.604613005744999654 ) ) ;
#16035=CARTESIAN_POINT ( 'NONE',  ( 9.323523248789006956, 2.820543420478710761, -8.179640942048592933 ) ) ;
#16043=CARTESIAN_POINT ( 'NONE',  ( 9.600045280412000892, 3.021734963141999852, -6.070209284876999511 ) ) ;
#16047=CARTESIAN_POINT ( 'NONE',  ( 10.59303303094000093, 2.436236667456999960, 7.793464546548000804 ) ) ;
#16053=CARTESIAN_POINT ( 'NONE',  ( 9.316114158771000575, 3.677414437776999723, 9.250745771096999803 ) ) ;
#16059=CARTESIAN_POINT ( 'NONE',  ( 1.690792463676000112, 0.6682336154344999946, -3.189788463028000454 ) ) ;
#16066=CARTESIAN_POINT ( 'NONE',  ( 9.509454719593000149, 3.116293075258000478, -6.208411413796000033 ) ) ;
#16080=CARTESIAN_POINT ( 'NONE',  ( 10.51140238467000110, 2.326714339996000191, -7.741210149842999932 ) ) ;
#16081=CARTESIAN_POINT ( 'NONE',  ( 8.196365526475007712, 5.108366921470007149, 6.411205986879997099 ) ) ;
#16086=DIRECTION ( 'NONE',  ( -1.000000000000000000, 0.000000000000000000, 0.000000000000000000 ) ) ;
#16090=CARTESIAN_POINT ( 'NONE',  ( 8.727045280411999784, 3.882020551409000042, 5.870058896428999695 ) ) ;
#16092=CIRCLE ( 'NONE', #26128, 2.100000000000000977 ) ;
#16097=AXIS2_PLACEMENT_3D ( 'NONE', #62000, #9191, #14113 ) ;
#16100=CARTESIAN_POINT ( 'NONE',  ( 11.07109548961999934, 7.377812892753000007, 6.318590435936999761 ) ) ;
#16105=B_SPLINE_CURVE_WITH_KNOTS ( 'NONE', 3,
 ( #53996, #47735, #59587, #37570, #10318 ),
 .UNSPECIFIED., .F., .F.,
 ( 4, 1, 4 ),
 ( 0.000000000000000000, 0.5000000000000000000, 1.000000000000000000 ),
 .UNSPECIFIED. ) ;
#16107=CARTESIAN_POINT ( 'NONE',  ( 11.00000005150999982, -4.755975669291000300E-06, 1.428076682242000113E-06 ) ) ;
#16113=B_SPLINE_CURVE_WITH_KNOTS ( 'NONE', 3,
 ( #48605, #49286, #24450, #13963 ),
 .UNSPECIFIED., .F., .F.,
 ( 4, 4 ),
 ( 0.000000000000000000, 0.2126015446065814829 ),
 .UNSPECIFIED. ) ;
#16115=CARTESIAN_POINT ( 'NONE',  ( 9.773145834241621088, 2.820529238741949385, -8.179623275354476419 ) ) ;
#16118=CARTESIAN_POINT ( 'NONE',  ( 8.368323341230000878, 4.780986922229000236, 6.267222470044999660 ) ) ;
#16120=CARTESIAN_POINT ( 'NONE',  ( 8.220124669774001802, 3.381964873247001790, -6.130490311850000928 ) ) ;
#16121=CARTESIAN_POINT ( 'NONE',  ( 11.26847444708000090, 2.565620268983000329, -7.116623294300999270 ) ) ;
#16126=ORIENTED_EDGE ( 'NONE', *, *, #9861, .T. ) ;
#16129=CARTESIAN_POINT ( 'NONE',  ( 9.041074696475142503, 2.899999999999999911, 6.201633003104277897 ) ) ;
#16131=LINE ( 'NONE', #37456, #39664 ) ;
#16142=LINE ( 'NONE', #63334, #66728 ) ;
#16155=CARTESIAN_POINT ( 'NONE',  ( 9.939260841229000221, 5.099602161831000124, -9.049221499261999924 ) ) ;
#16169=EDGE_LOOP ( 'NONE', ( #43529, #24211, #32961, #68533 ) ) ;
#16172=CARTESIAN_POINT ( 'NONE',  ( 9.915635841230999503, 3.210851187372000037, -6.346613542714999667 ) ) ;
#16174=CARTESIAN_POINT ( 'NONE',  ( 0.1801026475008349892, 1.156975259834909453, -3.039500339280597263 ) ) ;
#16175=ORIENTED_EDGE ( 'NONE', *, *, #55596, .F. ) ;
#16181=CARTESIAN_POINT ( 'NONE',  ( 27.64127793187000037, 11.00717859340000082, -1.432487142323000118 ) ) ;
#16186=EDGE_CURVE ( 'NONE', #65344, #19244, #20102, .T. ) ;
#16190=CARTESIAN_POINT ( 'NONE',  ( 9.594139158774000364, 2.212639797530000063, -6.855876382544999537 ) ) ;
#16191=VECTOR ( 'NONE', #25990, 1000.000000000000114 ) ;
#16196=CARTESIAN_POINT ( 'NONE',  ( 8.722235841230000730, 3.844886277615000125, -8.888911790991000927 ) ) ;
#16204=CARTESIAN_POINT ( 'NONE',  ( 2.040019101166500093, 3.500000000000000888, -0.4817981237446227749 ) ) ;
#16209=CARTESIAN_POINT ( 'NONE',  ( 11.09999999999999964, 6.361341001828001218, -5.393275588238999774 ) ) ;
#16211=EDGE_CURVE ( 'NONE', #14714, #43600, #24363, .T. ) ;
#16214=CIRCLE ( 'NONE', #66477, 12.99999867215000116 ) ;
#16215=CARTESIAN_POINT ( 'NONE',  ( 11.02452225494999993, 2.775477745048999800, -6.571291218949999902 ) ) ;
#16220=CARTESIAN_POINT ( 'NONE',  ( 0.1499942179680000542, -2.749953718116142198, -0.3599680999394080372 ) ) ;
#16224=CARTESIAN_POINT ( 'NONE',  ( 5.399998984437000438, -12.98068687585000092, 1.765643277146000001 ) ) ;
#16226=CARTESIAN_POINT ( 'NONE',  ( 1.665556799207791983, 0.4581489286485003198, 3.500000000000000444 ) ) ;
#16227=EDGE_LOOP ( 'NONE', ( #35972, #36248, #57866 ) ) ;
#16232=CARTESIAN_POINT ( 'NONE',  ( 8.819055905797000605, 2.899999999999999911, -6.571291218949999902 ) ) ;
#16235=ORIENTED_EDGE ( 'NONE', *, *, #5592, .T. ) ;
#16238=ORIENTED_EDGE ( 'NONE', *, *, #53369, .F. ) ;
#16242=CARTESIAN_POINT ( 'NONE',  ( 9.518314158773000244, 4.845406482350000488, -6.387189183984999907 ) ) ;
#16253=CARTESIAN_POINT ( 'NONE',  ( 9.573148997458000409, 5.167567567567999731, -6.822293592207000934 ) ) ;
#16261=CARTESIAN_POINT ( 'NONE',  ( 8.021466877102001902, 5.126313762262000751, -6.742875694880997806 ) ) ;
#16265=B_SPLINE_CURVE_WITH_KNOTS ( 'NONE', 3,
 ( #1604, #66261, #13143, #40058, #18041 ),
 .UNSPECIFIED., .F., .F.,
 ( 4, 1, 4 ),
 ( 0.000000000000000000, 0.5000000000000000000, 1.000000000000000000 ),
 .UNSPECIFIED. ) ;
#16268=EDGE_LOOP ( 'NONE', ( #33057, #3954 ) ) ;
#16269=CARTESIAN_POINT ( 'NONE',  ( 10.44675156161000018, 2.885046387990999772, 8.863482298832000339 ) ) ;
#16274=CARTESIAN_POINT ( 'NONE',  ( 10.02462472190973486, 2.899999999999999911, -6.445686799157789082 ) ) ;
#16278=AXIS2_PLACEMENT_3D ( 'NONE', #1086, #737, #59118 ) ;
#16280=VERTEX_POINT ( 'NONE', #63770 ) ;
#16285=CARTESIAN_POINT ( 'NONE',  ( 10.37873747135000002, 4.882725050998000249, 6.350806206758999650 ) ) ;
#16300=ORIENTED_EDGE ( 'NONE', *, *, #47968, .F. ) ;
#16301=CARTESIAN_POINT ( 'NONE',  ( 0.5350461241980000171, -2.512770725774000180, 2.251027108384000108 ) ) ;
#16303=CARTESIAN_POINT ( 'NONE',  ( 11.35906500789999996, 2.719101288111000159, -7.157645240044000268 ) ) ;
#16306=EDGE_CURVE ( 'NONE', #25126, #9641, #31923, .T. ) ;
#16311=CARTESIAN_POINT ( 'NONE',  ( 9.362885841227999606, 3.677414437776999723, 9.250745771096999803 ) ) ;
#16312=VERTEX_POINT ( 'NONE', #10985 ) ;
#16314=CARTESIAN_POINT ( 'NONE',  ( 7.209954719586999516, 2.634456420141999988, -6.433888043919999689 ) ) ;
#16318=DIRECTION ( 'NONE',  ( 0.000000000000000000, 0.9916377111174247139, 0.1290528957048031888 ) ) ;
#16331=ORIENTED_EDGE ( 'NONE', *, *, #23754, .T. ) ;
#16332=CARTESIAN_POINT ( 'NONE',  ( 9.015545280411000562, 4.175915362023999933, 5.699506188181000077 ) ) ;
#16333=EDGE_CURVE ( 'NONE', #8503, #23086, #28586, .T. ) ;
#16334=ADVANCED_FACE ( 'NONE', ( #27769 ), #496, .T. ) ;
#16335=ORIENTED_EDGE ( 'NONE', *, *, #58247, .F. ) ;
#16338=ADVANCED_FACE ( 'NONE', ( #21811 ), #22499, .T. ) ;
#16340=CARTESIAN_POINT ( 'NONE',  ( 11.01665246377999985, 5.432467678272000278, -4.991868250041999744 ) ) ;
#16344=CARTESIAN_POINT ( 'NONE',  ( 8.983146706529641534, 2.899999999999999911, 6.231099004629861327 ) ) ;
#16345=CARTESIAN_POINT ( 'NONE',  ( 8.475341021510232054, 5.350570349241480450, 7.499981640446101494 ) ) ;
#16352=ORIENTED_EDGE ( 'NONE', *, *, #36928, .F. ) ;
#16354=FACE_OUTER_BOUND ( 'NONE', #14615, .T. ) ;
#16355=CARTESIAN_POINT ( 'NONE',  ( 9.975298369746390392, 5.350379160513678123, 7.499985214262784083 ) ) ;
#16358=PLANE ( 'NONE',  #60699 ) ;
#16360=CARTESIAN_POINT ( 'NONE',  ( 10.31667774810000004, 3.819530253758000260, 6.062195927068000145 ) ) ;
#16363=CARTESIAN_POINT ( 'NONE',  ( 11.27110638630999873, 5.469603964121000139, 8.504707115835000053 ) ) ;
#16364=CARTESIAN_POINT ( 'NONE',  ( 2.092640132542666898, 3.058252359239899132, 1.762666431298155034 ) ) ;
#16373=CARTESIAN_POINT ( 'NONE',  ( 10.50285691784999997, 5.158890929072000198, 8.369954994793999958 ) ) ;
#16375=AXIS2_PLACEMENT_3D ( 'NONE', #2561, #45225, #66187 ) ;
#16376=VERTEX_POINT ( 'NONE', #59566 ) ;
#16377=DIRECTION ( 'NONE',  ( 0.7071067811865475727, -0.7071067811865475727, 0.000000000000000000 ) ) ;
#16380=CARTESIAN_POINT ( 'NONE',  ( 11.09999999999999964, 5.299316147296000423, -5.124965750789000296 ) ) ;
#16384=CARTESIAN_POINT ( 'NONE',  ( 7.448642219589999947, 4.628941086829000184, 5.991667691044999522 ) ) ;
#16385=CARTESIAN_POINT ( 'NONE',  ( 8.233179719589999834, 5.203550244299999683, -8.391678825488000371 ) ) ;
#16387=CARTESIAN_POINT ( 'NONE',  ( 10.59999999999999964, 3.399999999999999911, 4.756097560976000338 ) ) ;
#16388=EDGE_CURVE ( 'NONE', #1808, #25355, #16572, .T. ) ;
#16391=B_SPLINE_CURVE_WITH_KNOTS ( 'NONE', 3,
 ( #32122, #48537, #49913, #49565, #13558, #45022, #66327, #23344, #40126, #44342, #2365, #6911, #1676, #28957, #23686, #34541, #3045, #24378, #13215, #55854, #65638, #7263, #29294, #61438, #45366 ),
 .UNSPECIFIED., .F., .F.,
 ( 4, 2, 2, 1, 1, 1, 2, 2, 2, 2, 2, 2, 2, 4 ),
 ( 0.1993834124056478585, 0.2494219491302857028, 0.2525493576755761804, 0.2556767662208666025, 0.2619315833114475578, 0.2744412174926094683, 0.2994604858549331228, 0.3995375593042285178, 0.4996146327535239129, 0.5496531694781714439, 0.5996917062028190859, 0.7998458531014098760, 0.8999229265507049380, 1.000000000000000000 ),
 .UNSPECIFIED. ) ;
#16392=CARTESIAN_POINT ( 'NONE',  ( 9.351497027444999333, 4.821940693094999730, 8.950154065657999425 ) ) ;
#16398=CARTESIAN_POINT ( 'NONE',  ( 8.032364158772001161, 3.524748802314000340, 5.573833469815000718 ) ) ;
#16403=CARTESIAN_POINT ( 'NONE',  ( 1.643110514234999986, -1.247131703260000002, -3.010971457459999723 ) ) ;
#16404=ORIENTED_EDGE ( 'NONE', *, *, #14830, .T. ) ;
#16408=EDGE_LOOP ( 'NONE', ( #54488, #38517, #18067, #45185 ) ) ;
#16409=CARTESIAN_POINT ( 'NONE',  ( 9.608904719592000987, 4.946705552514000459, -6.253848946732999181 ) ) ;
#16412=EDGE_CURVE ( 'NONE', #23153, #45049, #25264, .T. ) ;
#16413=ORIENTED_EDGE ( 'NONE', *, *, #31798, .T. ) ;
#16414=CARTESIAN_POINT ( 'NONE',  ( 3.999971066382000284, 2.149963194831999935, 0.000000000000000000 ) ) ;
#16418=ORIENTED_EDGE ( 'NONE', *, *, #48179, .F. ) ;
#16421=ORIENTED_EDGE ( 'NONE', *, *, #46204, .F. ) ;
#16424=CARTESIAN_POINT ( 'NONE',  ( 9.696080515601000371, 2.554416243104999928, 7.600685069647000525 ) ) ;
#16425=CARTESIAN_POINT ( 'NONE',  ( 10.98435102962999999, 2.894555727676000334, -4.879788070431000158 ) ) ;
#16430=CARTESIAN_POINT ( 'NONE',  ( 6.999999085428001422, -12.01420426511556094, 3.456409902911533383 ) ) ;
#16432=CARTESIAN_POINT ( 'NONE',  ( 8.598670280411999656, 2.376526778640999815, 7.686980884243000745 ) ) ;
#16440=CARTESIAN_POINT ( 'NONE',  ( 11.07074946250000025, 6.638246904777000523, 5.577396945824999897 ) ) ;
#16441=CARTESIAN_POINT ( 'NONE',  ( 11.07111654620999985, 7.823241544734999664, 6.598400448272999874 ) ) ;
#16442=AXIS2_PLACEMENT_3D ( 'NONE', #41374, #66901, #14805 ) ;
#16444=DIRECTION ( 'NONE',  ( 0.000000000000000000, 0.8648648648648717963, -0.5020047465136829867 ) ) ;
#16445=ORIENTED_EDGE ( 'NONE', *, *, #57682, .F. ) ;
#16449=CARTESIAN_POINT ( 'NONE',  ( 8.293430908490591946, 2.934198963169226015, -6.452279353973301212 ) ) ;
#16459=CARTESIAN_POINT ( 'NONE',  ( 10.71315778041000044, 2.619207518211999819, -8.142085279690999045 ) ) ;
#16473=CONICAL_SURFACE ( 'NONE', #26576, 0.4311160744474001327, 0.7853981633972997312 ) ;
#16475=DIRECTION ( 'NONE',  ( 0.000000000000000000, -0.5592907522138691467, 0.8289715643422543856 ) ) ;
#16476=CARTESIAN_POINT ( 'NONE',  ( 10.81746213571000048, 5.100000000000000533, 6.571291218949999902 ) ) ;
#16482=VECTOR ( 'NONE', #16914, 1000.000000000000000 ) ;
#16484=CARTESIAN_POINT ( 'NONE',  ( 6.899999691988000450, -11.00717859340000082, -1.432487142323000118 ) ) ;
#16488=CIRCLE ( 'NONE', #38813, 0.4999999999999996114 ) ;
#16496=ORIENTED_EDGE ( 'NONE', *, *, #65528, .F. ) ;
#16497=CARTESIAN_POINT ( 'NONE',  ( 11.09999999999999964, 5.449702574547000467, 5.124965750789000296 ) ) ;
#16513=CONICAL_SURFACE ( 'NONE', #19863, 1.949999999913999860, 0.7853981633972997312 ) ;
#16515=ORIENTED_EDGE ( 'NONE', *, *, #4010, .F. ) ;
#16516=CARTESIAN_POINT ( 'NONE',  ( 10.24846228258000025, 4.234133568259999869, -5.660851473941000300 ) ) ;
#16521=VECTOR ( 'NONE', #43408, 1000.000000000000000 ) ;
#16538=VERTEX_POINT ( 'NONE', #28031 ) ;
#16548=CARTESIAN_POINT ( 'NONE',  ( 8.341176297635993109, 4.893934000596881440, -6.169995681351899464 ) ) ;
#16566=DIRECTION ( 'NONE',  ( 1.000000000000000000, 0.000000000000000000, 0.000000000000000000 ) ) ;
#16570=CARTESIAN_POINT ( 'NONE',  ( 5.407309473666999544, -12.95251760905999916, 1.915207572622000143 ) ) ;
#16571=AXIS2_PLACEMENT_3D ( 'NONE', #21711, #48289, #68921 ) ;
#16572=LINE ( 'NONE', #33356, #41259 ) ;
#16573=DIRECTION ( 'NONE',  ( 0.8843050080896810439, -0.1786786090465959931, -0.4313682966290904863 ) ) ;
#16580=CARTESIAN_POINT ( 'NONE',  ( 7.650096249917202940, 4.657077951104835023, -8.696453622792276406 ) ) ;
#16590=AXIS2_PLACEMENT_3D ( 'NONE', #3787, #57272, #51355 ) ;
#16595=CARTESIAN_POINT ( 'NONE',  ( 9.457108735800074939, 5.237413963666066152, 8.039587586354246085 ) ) ;
#16600=ORIENTED_EDGE ( 'NONE', *, *, #59093, .F. ) ;
#16601=DIRECTION ( 'NONE',  ( -1.000000000000000000, 0.000000000000000000, 0.000000000000000000 ) ) ;
#16602=CARTESIAN_POINT ( 'NONE',  ( 8.474485200571999499, 5.100000000000000533, 6.560614371780999043 ) ) ;
#16609=CARTESIAN_POINT ( 'NONE',  ( 7.225316516319210791, 3.408784923954944812, -8.751707459018776447 ) ) ;
#16614=CARTESIAN_POINT ( 'NONE',  ( 10.05691520198999989, 2.453477278391000382, 6.657104391228999773 ) ) ;
#16615=CARTESIAN_POINT ( 'NONE',  ( 10.22907665877000127, 4.838498214728000235, -5.852435699035000383 ) ) ;
#16618=CARTESIAN_POINT ( 'NONE',  ( 3.690346968721999854, -1.826556930874999818, 3.227001764767000402 ) ) ;
#16622=ORIENTED_EDGE ( 'NONE', *, *, #26124, .T. ) ;
#16638=CYLINDRICAL_SURFACE ( 'NONE', #23225, 1.350000000000000533 ) ;
#16641=CARTESIAN_POINT ( 'NONE',  ( 8.871889158775999817, 2.702406276695999754, -6.981052078638000147 ) ) ;
#16643=ADVANCED_FACE ( 'NONE', ( #37470 ), #16829, .T. ) ;
#16644=CARTESIAN_POINT ( 'NONE',  ( 8.266851002545999805, 2.832432432432000269, 6.822293592207000934 ) ) ;
#16646=CARTESIAN_POINT ( 'NONE',  ( 0.5022402514714999766, 2.306917309723999665, 2.681989686974000087 ) ) ;
#16648=CARTESIAN_POINT ( 'NONE',  ( 2.266292344358999955, -3.720972690152000162, 0.5317331180723999795 ) ) ;
#16650=CARTESIAN_POINT ( 'NONE',  ( 6.999999691988000095, 13.87069231928999891, -4.225386915259999654 ) ) ;
#16654=CARTESIAN_POINT ( 'NONE',  ( 8.796579719592999780, 2.368264398678999516, 7.410200237937000445 ) ) ;
#16655=EDGE_LOOP ( 'NONE', ( #30989, #16413, #64911, #68092, #8008, #29314 ) ) ;
#16657=CARTESIAN_POINT ( 'NONE',  ( 7.598895280409000641, 4.462983737834999687, -8.994919855354998717 ) ) ;
#16669=ORIENTED_EDGE ( 'NONE', *, *, #7850, .T. ) ;
#16676=CARTESIAN_POINT ( 'NONE',  ( 8.732392219593000604, 2.806082850903000026, 8.615880516515998622 ) ) ;
#16680=CARTESIAN_POINT ( 'NONE',  ( 10.97046361309999973, 6.164149261029999494, -5.039793574291000056 ) ) ;
#16683=CARTESIAN_POINT ( 'NONE',  ( 0.4200574278457634425, -2.102383120260660210, -2.734278034550727376 ) ) ;
#16690=VERTEX_POINT ( 'NONE', #64026 ) ;
#16694=CARTESIAN_POINT ( 'NONE',  ( 9.635004719593998956, 2.334550724494000029, -7.977056617806000283 ) ) ;
#16695=CARTESIAN_POINT ( 'NONE',  ( 10.64127413024999846, 2.258699798012000048, -6.863478635463000188 ) ) ;
#16703=CARTESIAN_POINT ( 'NONE',  ( 10.34021053755999908, 4.202028620710000162, 9.459600235481000041 ) ) ;
#16704=B_SPLINE_CURVE_WITH_KNOTS ( 'NONE', 3,
 ( #43055, #12285, #11926, #33266 ),
 .UNSPECIFIED., .F., .F.,
 ( 4, 4 ),
 ( 0.000000000000000000, 1.000000000000000000 ),
 .UNSPECIFIED. ) ;
#16707=CARTESIAN_POINT ( 'NONE',  ( 5.440293001548999641, 12.88483958404999896, -2.133988467673999967 ) ) ;
#16709=CARTESIAN_POINT ( 'NONE',  ( 10.19474327641866473, 5.745204535562014492, 7.382935988871072830 ) ) ;
#16714=CARTESIAN_POINT ( 'NONE',  ( 9.120035841232999374, 5.288433695693000480, -8.041290150997999930 ) ) ;
#16716=ADVANCED_FACE ( 'NONE', ( #37817 ), #63606, .T. ) ;
#16719=DIRECTION ( 'NONE',  ( 1.000000000000000000, 0.000000000000000000, 0.000000000000000000 ) ) ;
#16722=B_SPLINE_CURVE_WITH_KNOTS ( 'NONE', 3,
 ( #17828, #23055, #16430, #65706 ),
 .UNSPECIFIED., .F., .F.,
 ( 4, 4 ),
 ( 0.000000000000000000, 1.000000000000000000 ),
 .UNSPECIFIED. ) ;
#16724=CARTESIAN_POINT ( 'NONE',  ( 9.079732780410999737, 5.421534627450999899, 6.381126373995999579 ) ) ;
#16725=CARTESIAN_POINT ( 'NONE',  ( 9.360279719594000625, 3.031907308384000022, -8.729608011560001657 ) ) ;
#16727=CARTESIAN_POINT ( 'NONE',  ( 2.939204570973131148, -1.496697095495769902, 2.893778235148168676 ) ) ;
#16730=CARTESIAN_POINT ( 'NONE',  ( 9.834151567923001380, 5.173929249342999803, 8.813048229486998508 ) ) ;
#16734=CARTESIAN_POINT ( 'NONE',  ( 7.722357335211003537, 2.834201928695000650, 6.826641520477001457 ) ) ;
#16736=CARTESIAN_POINT ( 'NONE',  ( 8.391562694006999834, 2.899763935154999750, -6.589890517430999850 ) ) ;
#16747=CARTESIAN_POINT ( 'NONE',  ( 7.411012926802005296, 3.233242541571998085, 6.481873309613996881 ) ) ;
#16749=ORIENTED_EDGE ( 'NONE', *, *, #53094, .F. ) ;
#16750=CARTESIAN_POINT ( 'NONE',  ( 9.319414158774000256, 2.656512020013999997, -7.884832994446999699 ) ) ;
#16753=CARTESIAN_POINT ( 'NONE',  ( 9.262755466223577372, 2.920626183394224196, -8.329572976240578797 ) ) ;
#16762=CARTESIAN_POINT ( 'NONE',  ( 11.11264834745999863, 2.146077493652999824, -7.517188756437000130 ) ) ;
#16763=CARTESIAN_POINT ( 'NONE',  ( 7.729292060080003246, 5.085123327752999245, 6.553315682963002153 ) ) ;
#16769=CARTESIAN_POINT ( 'NONE',  ( 9.112170280412000167, 2.368264398678999516, 7.410200237937000445 ) ) ;
#16782=B_SPLINE_CURVE_WITH_KNOTS ( 'NONE', 3,
 ( #35626, #68098, #62175, #41541, #14971, #24094 ),
 .UNSPECIFIED., .F., .F.,
 ( 4, 2, 4 ),
 ( 0.000000000000000000, 0.5000000000000000000, 1.000000000000000000 ),
 .UNSPECIFIED. ) ;
#16787=CARTESIAN_POINT ( 'NONE',  ( 10.18240541510999897, 2.607737086676999994, 7.783408568367999436 ) ) ;
#16790=CARTESIAN_POINT ( 'NONE',  ( 8.288209573716871503, 2.946091060167179698, -6.424054805521736355 ) ) ;
#16791=B_SPLINE_SURFACE_WITH_KNOTS ( 'NONE', 3, 3, ( 
 ( #21346, #15763, #6288, #42345 ),
 ( #27635, #37425, #10510, #37090 ),
 ( #53850, #11535, #5948, #43374 ),
 ( #367, #32199, #59782, #43017 ),
 ( #63644, #64674, #58748, #58405 ),
 ( #26948, #1065, #21009, #715 ),
 ( #68891, #54189, #26605, #32877 ),
 ( #48956, #48259, #11197, #21681 ),
 ( #10853, #22376, #31850, #38109 ),
 ( #53165, #47587, #16441, #27290 ),
 ( #11886, #53512, #43717, #25 ),
 ( #52824, #65010, #16100, #4920 ),
 ( #32535, #17129, #38463, #59096 ),
 ( #64320, #48610, #47926, #5601 ) ),
 .UNSPECIFIED., .F., .F., .F.,
 ( 4, 1, 1, 1, 1, 1, 1, 1, 1, 1, 1, 4 ),
 ( 4, 4 ),
 ( -0.008665511476623999690, 0.000000000000000000, 0.1111111111111000027, 0.2222222222222000054, 0.3333333333333000081, 0.4444444444444000109, 0.5555555555555999891, 0.6666666666667000474, 0.7777777777777999946, 0.8888888888888999418, 1.000000000000000000, 1.011507985605999860 ),
 ( -0.2206650672664999813, 1.220665067267000081 ),
 .UNSPECIFIED. ) ;
#16794=CARTESIAN_POINT ( 'NONE',  ( 8.368323341230000878, 4.780986922229000236, 6.267222470044999660 ) ) ;
#16795=CARTESIAN_POINT ( 'NONE',  ( 9.710633014819311626, 3.646661381981713301, -8.850710600599320799 ) ) ;
#16799=CARTESIAN_POINT ( 'NONE',  ( 11.07484075165016613, 2.725159248349832364, -6.497852970900666492 ) ) ;
#16801=CARTESIAN_POINT ( 'NONE',  ( 10.61443584123000150, 5.287628373050000441, -7.937241318065001217 ) ) ;
#16802=CARTESIAN_POINT ( 'NONE',  ( 9.525000000000000355, 4.417172942406000224, 8.783926296998000538 ) ) ;
#16803=CARTESIAN_POINT ( 'NONE',  ( 8.493369886551995762, 5.097498803759001440, 6.607670056088003285 ) ) ;
#16815=DIRECTION ( 'NONE',  ( 0.000000000000000000, 0.000000000000000000, -1.000000000000000000 ) ) ;
#16816=ORIENTED_EDGE ( 'NONE', *, *, #17941, .F. ) ;
#16819=CARTESIAN_POINT ( 'NONE',  ( 7.000000000000000000, 8.307879248642999315, 4.307879248643000203 ) ) ;
#16821=CARTESIAN_POINT ( 'NONE',  ( 0.8897459993062000194, -3.461062994654999780, -0.9617132324576000979 ) ) ;
#16824=VECTOR ( 'NONE', #44336, 1000.000000000000000 ) ;
#16826=CARTESIAN_POINT ( 'NONE',  ( 10.18240541510999897, 2.607737086676999994, 7.783408568367999436 ) ) ;
#16829=CYLINDRICAL_SURFACE ( 'NONE', #34591, 0.4999999999999998335 ) ;
#16831=CARTESIAN_POINT ( 'NONE',  ( 7.844724277266999835, 4.719412473309000156, 6.357657803787000184 ) ) ;
#16832=CARTESIAN_POINT ( 'NONE',  ( 9.832537864288001472, 2.899999999999999911, 6.571291218949999902 ) ) ;
#16836=B_SPLINE_CURVE_WITH_KNOTS ( 'NONE', 3,
 ( #12408, #45606, #2263, #17658 ),
 .UNSPECIFIED., .F., .F.,
 ( 4, 4 ),
 ( 0.000000000000000000, 1.000000000000000000 ),
 .UNSPECIFIED. ) ;
#16838=CARTESIAN_POINT ( 'NONE',  ( 7.402683226288421459, 2.556880117659619867, 8.471723903841693826 ) ) ;
#16849=CARTESIAN_POINT ( 'NONE',  ( 8.832537864289999874, 2.899999999999999911, 6.571291218949999902 ) ) ;
#16855=CARTESIAN_POINT ( 'NONE',  ( 9.318935841232999451, 2.644017913812000131, -7.838184857420000817 ) ) ;
#16858=ORIENTED_EDGE ( 'NONE', *, *, #49582, .T. ) ;
#16867=CARTESIAN_POINT ( 'NONE',  ( 7.862706706567756498, 3.149338860038144006, -6.385288329380975014 ) ) ;
#16868=EDGE_CURVE ( 'NONE', #47736, #12318, #47638, .T. ) ;
#16872=CARTESIAN_POINT ( 'NONE',  ( 7.405090560819000522, 5.321245676936000812, -7.068438969505000280 ) ) ;
#16873=CARTESIAN_POINT ( 'NONE',  ( 8.906851002547000462, 2.832432432432000269, -6.822293592207000934 ) ) ;
#16876=CARTESIAN_POINT ( 'NONE',  ( 9.535554719593998030, 3.927090956378999742, -9.230892435423001530 ) ) ;
#16881=AXIS2_PLACEMENT_3D ( 'NONE', #18258, #34346, #29800 ) ;
#16890=CARTESIAN_POINT ( 'NONE',  ( 7.717562992925000032, 2.846244489068278316, 6.797277731627717756 ) ) ;
#16891=ORIENTED_EDGE ( 'NONE', *, *, #16211, .F. ) ;
#16895=CARTESIAN_POINT ( 'NONE',  ( 11.09999999999999964, 5.449702572737000317, -5.124965750789000296 ) ) ;
#16898=DIRECTION ( 'NONE',  ( -0.8660254037844288266, 0.000000000000000000, -0.5000000000000169864 ) ) ;
#16909=CARTESIAN_POINT ( 'NONE',  ( 0.9468067992084583384, 0.9161175952574844850, -3.408904368339102930 ) ) ;
#16911=CARTESIAN_POINT ( 'NONE',  ( 10.83253786428999987, 2.899999999999999911, 6.571291218949999902 ) ) ;
#16914=DIRECTION ( 'NONE',  ( 1.000000000000000000, -1.210302035963000169E-10, 1.972161209128000006E-09 ) ) ;
#16915=CARTESIAN_POINT ( 'NONE',  ( 10.47530200610849604, 5.350262918594154371, 7.499984559551275964 ) ) ;
#16917=VERTEX_POINT ( 'NONE', #66456 ) ;
#16918=FACE_OUTER_BOUND ( 'NONE', #57874, .T. ) ;
#16927=AXIS2_PLACEMENT_3D ( 'NONE', #5268, #47240, #42347 ) ;
#16928=CARTESIAN_POINT ( 'NONE',  ( 7.423620280405000216, 3.447598131391000020, -9.141997724497999300 ) ) ;
#16930=CARTESIAN_POINT ( 'NONE',  ( 9.468459139564425087, 5.148170612271298907, 8.212595183817528621 ) ) ;
#16931=VERTEX_POINT ( 'NONE', #29425 ) ;
#16942=CIRCLE ( 'NONE', #43762, 1.349999999999999867 ) ;
#16945=ADVANCED_FACE ( 'NONE', ( #50733 ), #45492, .F. ) ;
#16952=CARTESIAN_POINT ( 'NONE',  ( 11.19050471959000070, 2.516756593394000152, -6.840361808223000217 ) ) ;
#16953=CARTESIAN_POINT ( 'NONE',  ( 4.500000125099000492, 1.829647544581999737E-13, 0.000000000000000000 ) ) ;
#16958=ORIENTED_EDGE ( 'NONE', *, *, #31575, .T. ) ;
#16960=CARTESIAN_POINT ( 'NONE',  ( 9.910633732652998518, 2.107262079134000210, 7.885285091859000062 ) ) ;
#16966=EDGE_CURVE ( 'NONE', #5467, #23807, #15927, .T. ) ;
#16968=DIRECTION ( 'NONE',  ( 0.000000000000000000, -0.8648648648648720183, -0.5020047465136825426 ) ) ;
#16973=CARTESIAN_POINT ( 'NONE',  ( 7.564999999998999414, 5.349999999999999645, -7.500000000000000000 ) ) ;
#16979=ORIENTED_EDGE ( 'NONE', *, *, #23916, .F. ) ;
#16981=CARTESIAN_POINT ( 'NONE',  ( 8.523814158775000038, 4.920236664407999783, -6.448229650796999834 ) ) ;
#16983=DIRECTION ( 'NONE',  ( 1.000000000000000000, 0.000000000000000000, 0.000000000000000000 ) ) ;
#16985=CARTESIAN_POINT ( 'NONE',  ( 0.3293854016218999980, 3.323048643578999872, -0.5818070024050000510 ) ) ;
#16988=CARTESIAN_POINT ( 'NONE',  ( 3.076885484853999930, 3.060286776641000017, 2.182434864853000089 ) ) ;
#16997=CARTESIAN_POINT ( 'NONE',  ( 8.052732780410000402, 4.968147183437999992, 5.971792472497999604 ) ) ;
#17000=CARTESIAN_POINT ( 'NONE',  ( 8.444220280407998658, 5.223492654083000453, -6.524203877525000195 ) ) ;
#17002=CARTESIAN_POINT ( 'NONE',  ( 10.88314899746000108, 5.167567567567999731, 6.822293592207000934 ) ) ;
#17004=ORIENTED_EDGE ( 'NONE', *, *, #64541, .F. ) ;
#17011=ORIENTED_EDGE ( 'NONE', *, *, #10001, .F. ) ;
#17013=CARTESIAN_POINT ( 'NONE',  ( 7.197921422182000484, 8.271573195358998376, 4.408111321959999884 ) ) ;
#17015=CARTESIAN_POINT ( 'NONE',  ( 8.174990947233153449, 2.650692654198087972, 7.500004443805798005 ) ) ;
#17018=CARTESIAN_POINT ( 'NONE',  ( 8.320864158774000430, 3.894644548817000285, 6.044465307984999924 ) ) ;
#17024=CARTESIAN_POINT ( 'NONE',  ( 11.07206066007000089, 5.780045616399000608, -5.100130972279999675 ) ) ;
#17028=CARTESIAN_POINT ( 'NONE',  ( 7.689997165042062655, 3.420006650669772608, -5.735732650232894692 ) ) ;
#17038=VECTOR ( 'NONE', #16573, 1000.000000000000000 ) ;
#17040=CARTESIAN_POINT ( 'NONE',  ( 9.585279719593998493, 2.928319778732999978, -8.861178115809998701 ) ) ;
#17047=CARTESIAN_POINT ( 'NONE',  ( 10.07314899745999881, 5.167567567567999731, -6.822293592207000934 ) ) ;
#17048=CARTESIAN_POINT ( 'NONE',  ( 11.02286749330999882, 2.398743616553999924, 6.352468982205000891 ) ) ;
#17050=EDGE_CURVE ( 'NONE', #30347, #7557, #55191, .T. ) ;
#17056=CARTESIAN_POINT ( 'NONE',  ( 11.09378572506000005, 2.399999999999999911, 6.571291218949999902 ) ) ;
#17061=CARTESIAN_POINT ( 'NONE',  ( 8.722235841230000730, 3.844886277615000125, -8.888911790991000927 ) ) ;
#17066=ORIENTED_EDGE ( 'NONE', *, *, #46591, .F. ) ;
#17069=CARTESIAN_POINT ( 'NONE',  ( 7.860170280410000210, 2.263558315407000254, 8.007442119518000112 ) ) ;
#17070=CARTESIAN_POINT ( 'NONE',  ( 9.848670280409999478, 5.002683760508999988, -8.912673867568997821 ) ) ;
#17071=CARTESIAN_POINT ( 'NONE',  ( 4.933367189779430895, -2.033301450227492424, 8.777104316792798490E-10 ) ) ;
#17072=CARTESIAN_POINT ( 'NONE',  ( 6.999999691988000095, 11.00717859340000082, 1.432487142323000118 ) ) ;
#17074=CARTESIAN_POINT ( 'NONE',  ( 9.966324641169999055, 2.303991951421000106, 6.575630951545000435 ) ) ;
#17077=ADVANCED_FACE ( 'NONE', ( #20541 ), #15300, .T. ) ;
#17079=CARTESIAN_POINT ( 'NONE',  ( 8.500493705215999896, 2.902642539927001941, 6.605602875546000341 ) ) ;
#17081=CARTESIAN_POINT ( 'NONE',  ( 11.09999999999999964, 5.299999999254000116, 5.148510364898998937 ) ) ;
#17088=ORIENTED_EDGE ( 'NONE', *, *, #50129, .F. ) ;
#17091=CARTESIAN_POINT ( 'NONE',  ( 7.911791375976998886, 3.505433841991000499, 6.324291089890995643 ) ) ;
#17095=CARTESIAN_POINT ( 'NONE',  ( 8.871889158775999817, 2.702406276695999754, -6.981052078638000147 ) ) ;
#17099=B_SPLINE_CURVE_WITH_KNOTS ( 'NONE', 3,
 ( #11423, #37655, #42562, #601, #37996, #63870, #17013, #32764 ),
 .UNSPECIFIED., .F., .F.,
 ( 4, 1, 1, 1, 1, 4 ),
 ( 0.000000000000000000, 0.2000000000000000111, 0.4000000000000000222, 0.5999999999999999778, 0.8000000000000000444, 1.000000000000000000 ),
 .UNSPECIFIED. ) ;
#17103=ORIENTED_EDGE ( 'NONE', *, *, #54129, .T. ) ;
#17109=CARTESIAN_POINT ( 'NONE',  ( 10.17284693385832206, 4.293232846717514484, -8.835933254752031729 ) ) ;
#17110=CARTESIAN_POINT ( 'NONE',  ( 11.12983972340999905, 2.716185796578999945, -4.845726974617000415 ) ) ;
#17112=CARTESIAN_POINT ( 'NONE',  ( 11.09999999999999964, 5.350000000000000533, 7.500000000000000000 ) ) ;
#17118=CARTESIAN_POINT ( 'NONE',  ( 8.289114158772999730, 4.310355144869000732, 9.459505265942000918 ) ) ;
#17124=CARTESIAN_POINT ( 'NONE',  ( 7.163103445601981534, 3.030767263943030976, 8.474512546327412466 ) ) ;
#17129=CARTESIAN_POINT ( 'NONE',  ( 11.01668711954999935, 7.361592993461999690, 6.178312432500000284 ) ) ;
#17136=EDGE_CURVE ( 'NONE', #30347, #44476, #5565, .T. ) ;
#17142=CARTESIAN_POINT ( 'NONE',  ( 8.983795280412000039, 3.979464555644999901, 9.134076336209998814 ) ) ;
#17143=CARTESIAN_POINT ( 'NONE',  ( 9.471374412057000924, 2.030666183831999927, 7.549764512038000142 ) ) ;
#17145=ORIENTED_EDGE ( 'NONE', *, *, #31882, .F. ) ;
#17150=CARTESIAN_POINT ( 'NONE',  ( 8.251334741087001490, 4.957169262993001091, 6.172567036706003485 ) ) ;
#17155=CARTESIAN_POINT ( 'NONE',  ( 1.548656882336000074, -2.727979478513999911, -1.783091295463999915 ) ) ;
#17164=VECTOR ( 'NONE', #2282, 1000.000000000000114 ) ;
#17167=VECTOR ( 'NONE', #26255, 1000.000000000000114 ) ;
#17169=CARTESIAN_POINT ( 'NONE',  ( 0.7991554384871001337, -3.621562729233000599, -1.006310721376000084 ) ) ;
#17170=DIRECTION ( 'NONE',  ( 1.000000000000000000, 0.000000000000000000, 5.031225091942999521E-14 ) ) ;
#17174=ADVANCED_FACE ( 'NONE', ( #23305 ), #59318, .T. ) ;
#17182=CARTESIAN_POINT ( 'NONE',  ( 9.421209229099421378, 5.348866595988766015, 7.442183899411809911 ) ) ;
#17186=ORIENTED_EDGE ( 'NONE', *, *, #66755, .T. ) ;
#17202=ORIENTED_EDGE ( 'NONE', *, *, #23270, .F. ) ;
#17204=CARTESIAN_POINT ( 'NONE',  ( 9.965360841230999966, 4.034680274230000308, -6.102912434217000026 ) ) ;
#17209=( LENGTH_UNIT ( ) NAMED_UNIT ( * ) SI_UNIT ( .MILLI., .METRE. ) );
#17217=B_SPLINE_SURFACE_WITH_KNOTS ( 'NONE', 3, 3, ( 
 ( #47452, #41514, #4440, #25433, #56909, #68409, #26126, #35926, #14943, #62149, #63163, #4784, #51656, #14267, #14608, #57239, #51993, #57941, #36268, #24751, #9691, #47110, #68758, #46766, #30349, #35595, #46076, #62824, #20530, #15292, #9006, #31376, #10037, #52688, #42214 ),
 ( #63519, #15633, #10381, #31719, #3752, #27161, #48482, #42549, #22249, #589, #48828, #11755, #5486, #17356, #69112, #53725, #37983, #21220, #5824, #64886, #60003, #64199, #26821, #33096, #42892, #12114, #63857, #16314, #48139, #937, #37641, #43585, #15971, #26473, #58972 ),
 ( #6513, #43236, #54413, #6161, #17000, #21898, #54064, #32410, #64542, #27502, #1277, #37300, #58622, #38329, #10723, #21556, #241, #59659, #53041, #11075, #32751, #16657, #27858, #43935, #59309, #32069, #38682, #49166, #11410, #53385, #22592, #65239, #5135, #47806, #8246 ),
 ( #18744, #2312, #39035, #1622, #54758, #13507, #34491, #44972, #12459, #50897, #2993, #29243, #49509, #45317, #65587, #33793, #7552, #66276, #55804, #66622, #39373, #40075, #23634, #6859, #22937, #56138, #1975, #18400, #17712, #61386, #66965, #50553, #34826, #28906, #55455 ) ),
 .UNSPECIFIED., .F., .F., .F.,
 ( 4, 4 ),
 ( 4, 1, 1, 1, 1, 1, 1, 1, 1, 1, 1, 1, 1, 1, 1, 1, 1, 1, 1, 1, 1, 1, 1, 1, 1, 1, 1, 1, 1, 1, 1, 1, 4 ),
 ( -0.1039370721279000015, 1.103937072127999963 ),
 ( -0.01999999999998999800, 0.01250000000001000137, 0.04499999999999999833, 0.07749999999999999944, 0.1100000000000000006, 0.1424999999999999878, 0.1749999999999999889, 0.2074999999999999900, 0.2399999999999999911, 0.2725000000000000200, 0.3049999999999999933, 0.3375000000000000222, 0.3699999999999999956, 0.4025000000000000244, 0.4349999999999999978, 0.4675000000000000266, 0.5000000000000000000, 0.5324999999999999734, 0.5649999999999999467, 0.5975000000000000311, 0.6300000000000000044, 0.6624999999999999778, 0.6949999999999999512, 0.7275000000000000355, 0.7600000000000000089, 0.7924999999999999822, 0.8249999999999999556, 0.8575000000000000400, 0.8900000000000000133, 0.9224999999999999867, 0.9549999999999999600, 0.9875000000000000444, 1.020000000000000018 ),
 .UNSPECIFIED. ) ;
#17222=CARTESIAN_POINT ( 'NONE',  ( 7.042728317542000127, 5.321245676936000812, -7.068438969505000280 ) ) ;
#17223=CARTESIAN_POINT ( 'NONE',  ( 10.74549835728371150, 4.944659509662737484, -4.827072369406659291 ) ) ;
#17229=CARTESIAN_POINT ( 'NONE',  ( 10.19741084123000086, 4.262870449202000422, -8.811513791423999820 ) ) ;
#17232=VERTEX_POINT ( 'NONE', #46696 ) ;
#17237=DIRECTION ( 'NONE',  ( 1.000000000000000000, 0.000000000000000000, 0.000000000000000000 ) ) ;
#17242=FACE_OUTER_BOUND ( 'NONE', #59087, .T. ) ;
#17251=DIRECTION ( 'NONE',  ( -1.000000000000000000, -1.776356839247999994E-14, 0.000000000000000000 ) ) ;
#17252=CARTESIAN_POINT ( 'NONE',  ( 5.407309682995999900, -12.95251760905999916, -1.915207572622000143 ) ) ;
#17255=DIRECTION ( 'NONE',  ( 0.000000000000000000, -1.000000000000000000, 0.000000000000000000 ) ) ;
#17257=CARTESIAN_POINT ( 'NONE',  ( 6.999999999999999112, 6.725428974790256476, 3.045254342161083816 ) ) ;
#17265=CARTESIAN_POINT ( 'NONE',  ( 0.9363901325418041433, 0.4581489286485155299, -3.499999999999999556 ) ) ;
#17266=ORIENTED_EDGE ( 'NONE', *, *, #12756, .T. ) ;
#17271=CARTESIAN_POINT ( 'NONE',  ( 4.900006121741999898, -6.122517096885939548E-17, -1.999970730383187734 ) ) ;
#17274=ORIENTED_EDGE ( 'NONE', *, *, #5903, .F. ) ;
#17281=CARTESIAN_POINT ( 'NONE',  ( 8.523814158775000038, 4.920236664407999783, -6.448229650796999834 ) ) ;
#17284=CARTESIAN_POINT ( 'NONE',  ( 7.464485841224999696, 4.562063799276000253, -9.314837681783000534 ) ) ;
#17294=EDGE_CURVE ( 'NONE', #58219, #30029, #21826, .T. ) ;
#17296=ORIENTED_EDGE ( 'NONE', *, *, #26066, .F. ) ;
#17301=CARTESIAN_POINT ( 'NONE',  ( 8.090553154006000725, 4.882634821118998047, -6.178046870599000151 ) ) ;
#17302=CARTESIAN_POINT ( 'NONE',  ( 8.411640687506832137, 2.873222873817933731, -6.752018918866305341 ) ) ;
#17307=CARTESIAN_POINT ( 'NONE',  ( 11.00588826681000043, 3.012760565655999923, 5.961496895743000124 ) ) ;
#17308=CARTESIAN_POINT ( 'NONE',  ( 10.52384528040999889, 5.441915759804999198, -7.989632847918000103 ) ) ;
#17318=CARTESIAN_POINT ( 'NONE',  ( 9.395239158775000377, 5.045571591548999812, -9.086294919530001124 ) ) ;
#17329=ADVANCED_FACE ( 'NONE', ( #29537 ), #50153, .T. ) ;
#17332=CARTESIAN_POINT ( 'NONE',  ( 6.966776889526476779, -12.39113590211060156, -2.782306601751617592 ) ) ;
#17336=CARTESIAN_POINT ( 'NONE',  ( 3.427367260881082789, 2.126417870048149528, -2.817200031586805764 ) ) ;
#17337=CARTESIAN_POINT ( 'NONE',  ( 9.301695280414000067, 5.619431609641999614, -8.115423117607999615 ) ) ;
#17340=CARTESIAN_POINT ( 'NONE',  ( 0.9135616966234998415, 3.275095586319999974, -0.8499908244220999443 ) ) ;
#17342=CARTESIAN_POINT ( 'NONE',  ( 9.419900841099883237, 2.377805712834746288, 8.156167515375480903 ) ) ;
#17343=CARTESIAN_POINT ( 'NONE',  ( 3.119794096232999969, 3.591452193409999882, 0.07293853716477999294 ) ) ;
#17346=EDGE_CURVE ( 'NONE', #67708, #68916, #33020, .T. ) ;
#17351=CARTESIAN_POINT ( 'NONE',  ( 7.384454719589999883, 3.346262376537000094, 6.002251090845000192 ) ) ;
#17354=EDGE_CURVE ( 'NONE', #8802, #37404, #45175, .T. ) ;
#17356=CARTESIAN_POINT ( 'NONE',  ( 7.906104719586000584, 5.732261791031000087, -7.476053406707000804 ) ) ;
#17358=CARTESIAN_POINT ( 'NONE',  ( 9.966324641169999055, 2.303991951421000106, 6.575630951545000435 ) ) ;
#17374=CARTESIAN_POINT ( 'NONE',  ( 8.641801658773999861, 2.933833973450999721, 8.496479443567000800 ) ) ;
#17383=CARTESIAN_POINT ( 'NONE',  ( 10.93769906941999892, 2.936877991120999898, -4.920829195977000303 ) ) ;
#17385=CARTESIAN_POINT ( 'NONE',  ( 7.100000000000000533, 0.000000000000000000, 0.000000000000000000 ) ) ;
#17393=AXIS2_PLACEMENT_3D ( 'NONE', #38931, #7449, #28800 ) ;
#17395=CARTESIAN_POINT ( 'NONE',  ( 2.419324796670999866, 1.946756166963000023, 2.762316150676000337 ) ) ;
#17403=ORIENTED_EDGE ( 'NONE', *, *, #23689, .F. ) ;
#17405=CARTESIAN_POINT ( 'NONE',  ( 1.908466522725666525, -0.7663246491380455439, -3.431732421873642025 ) ) ;
#17407=CARTESIAN_POINT ( 'NONE',  ( 10.62197831623999988, 5.779783227492000464, 7.256572995198999898 ) ) ;
#17412=DIRECTION ( 'NONE',  ( 0.000000000000000000, 0.8648648648648717963, -0.5020047465136829867 ) ) ;
#17425=CARTESIAN_POINT ( 'NONE',  ( 7.705392219590000202, 3.245534453799999941, 8.949623695221001540 ) ) ;
#17426=CIRCLE ( 'NONE', #12951, 1.550000000000000044 ) ;
#17427=CARTESIAN_POINT ( 'NONE',  ( 9.790085841230000696, 5.149303692842000402, -5.987168472229000393 ) ) ;
#17428=DIRECTION ( 'NONE',  ( -1.000000000000000000, -1.776356839370000173E-14, 0.000000000000000000 ) ) ;
#17429=CARTESIAN_POINT ( 'NONE',  ( 3.064955461405348469, -2.879526833223610804, -1.523935657190285564 ) ) ;
#17431=CARTESIAN_POINT ( 'NONE',  ( 10.66951519566999806, 4.592673277375999952, 5.841403042559999648 ) ) ;
#17435=CARTESIAN_POINT ( 'NONE',  ( 7.726096713366001900, 2.834812733921999062, 6.825604963486997079 ) ) ;
#17440=LINE ( 'NONE', #13160, #66251 ) ;
#17445=CIRCLE ( 'NONE', #53174, 12.49999909015999577 ) ;
#17451=ORIENTED_EDGE ( 'NONE', *, *, #3074, .F. ) ;
#17452=CARTESIAN_POINT ( 'NONE',  ( 7.528515907654997896, 3.227039430994999236, 6.419564954296006931 ) ) ;
#17455=CARTESIAN_POINT ( 'NONE',  ( 8.722714158775000115, 3.892978337449999771, -8.893414073324001023 ) ) ;
#17460=EDGE_CURVE ( 'NONE', #10760, #59329, #2921, .T. ) ;
#17462=CARTESIAN_POINT ( 'NONE',  ( 10.99999999839000075, 0.3999999983917999491, 7.388315149414999894 ) ) ;
#17464=ORIENTED_EDGE ( 'NONE', *, *, #60921, .T. ) ;
#17465=CARTESIAN_POINT ( 'NONE',  ( 9.579652738407363088, 4.352972272612339211, 8.851639610528335922 ) ) ;
#17471=CARTESIAN_POINT ( 'NONE',  ( 9.934212804449000345, 5.120437537252000126, -8.883398686237999442 ) ) ;
#17478=CARTESIAN_POINT ( 'NONE',  ( 8.353301658773000682, 2.800103557244999930, 9.079946116129001155 ) ) ;
#17483=DIRECTION ( 'NONE',  ( -1.000000000000000000, 0.000000000000000000, 0.000000000000000000 ) ) ;
#17485=AXIS2_PLACEMENT_3D ( 'NONE', #9524, #25616, #61990 ) ;
#17487=CARTESIAN_POINT ( 'NONE',  ( 11.07126769815000067, 5.548036418162999972, 5.077736284810999479 ) ) ;
#17492=ORIENTED_EDGE ( 'NONE', *, *, #47754, .T. ) ;
#17499=VERTEX_POINT ( 'NONE', #35102 ) ;
#17501=CARTESIAN_POINT ( 'NONE',  ( 8.304135841228999837, 3.650414032626000171, 6.083147621602999600 ) ) ;
#17502=FACE_OUTER_BOUND ( 'NONE', #59621, .T. ) ;
#17508=CARTESIAN_POINT ( 'NONE',  ( 8.064674013518999374, 4.643178316509001036, 6.221316387655001279 ) ) ;
#17513=ORIENTED_EDGE ( 'NONE', *, *, #28685, .T. ) ;
#17514=CARTESIAN_POINT ( 'NONE',  ( 1.930112477862999887, -1.998287707672000035, 2.574515877127999897 ) ) ;
#17520=CARTESIAN_POINT ( 'NONE',  ( 10.97197891481999932, 2.857467565480000360, 4.995747414879000203 ) ) ;
#17521=CARTESIAN_POINT ( 'NONE',  ( 11.09999999999999964, 5.449702574547000467, 5.124965750789000296 ) ) ;
#17524=CARTESIAN_POINT ( 'NONE',  ( 7.542083333330625194, 4.829638071966136259, -6.420449762762456380 ) ) ;
#17528=CARTESIAN_POINT ( 'NONE',  ( 9.179055905797000037, 2.899999999999999911, 6.571291218949999902 ) ) ;
#17530=CARTESIAN_POINT ( 'NONE',  ( 0.5607456912831000340, 3.437215509016000148, 1.521310954037999874 ) ) ;
#17531=CARTESIAN_POINT ( 'NONE',  ( 1.928056799206333327, 2.150913519912206695, -2.798833948393627313 ) ) ;
#17540=CARTESIAN_POINT ( 'NONE',  ( 10.59999999999999964, 4.599999999999999645, 4.756097560976000338 ) ) ;
#17544=CARTESIAN_POINT ( 'NONE',  ( 9.442010841233001273, 5.045571591548999812, -9.086294919530001124 ) ) ;
#17554=CARTESIAN_POINT ( 'NONE',  ( 11.27110638630999873, 5.469603964121000139, 8.504707115835000053 ) ) ;
#17555=DIRECTION ( 'NONE',  ( 0.000000000000000000, 1.000000000000000000, 0.000000000000000000 ) ) ;
#17564=CARTESIAN_POINT ( 'NONE',  ( -15.86200481174999943, 5.599999999999999645, 6.571291218949999902 ) ) ;
#17572=ORIENTED_EDGE ( 'NONE', *, *, #58583, .T. ) ;
#17576=CARTESIAN_POINT ( 'NONE',  ( 7.157271682457999162, 5.172411450403999744, -8.246583185469999577 ) ) ;
#17577=CARTESIAN_POINT ( 'NONE',  ( 8.865073590557452476, 2.650142864597553327, -7.500004675916596142 ) ) ;
#17581=CARTESIAN_POINT ( 'NONE',  ( 8.631645280409999899, 3.826300099041999747, -9.055335252254000267 ) ) ;
#17582=MECHANICAL_DESIGN_GEOMETRIC_PRESENTATION_REPRESENTATION('',(#18685),#47728);
#17583=FACE_OUTER_BOUND ( 'NONE', #58822, .T. ) ;
#17598=ORIENTED_EDGE ( 'NONE', *, *, #25440, .F. ) ;
#17604=CARTESIAN_POINT ( 'NONE',  ( 10.35685100253999913, 2.832432432432000269, -6.822293592207000934 ) ) ;
#17607=UNCERTAINTY_MEASURE_WITH_UNIT (LENGTH_MEASURE( 1.000000000000000082E-05 ), #17209, 'distance_accuracy_value', 'NONE');
#17615=CARTESIAN_POINT ( 'NONE',  ( 6.999999999999998224, 9.596681707279657303, -4.662612261201800834 ) ) ;
#17616=CYLINDRICAL_SURFACE ( 'NONE', #32829, 13.10000000000000142 ) ;
#17617=B_SPLINE_CURVE_WITH_KNOTS ( 'NONE', 3,
 ( #19832, #36599, #40807, #46750, #51302, #67364, #68055, #36250, #9671, #47436 ),
 .UNSPECIFIED., .F., .F.,
 ( 4, 2, 2, 2, 4 ),
 ( 0.5000000000000000000, 0.6250000000000000000, 0.7500000000000000000, 0.8750000000000000000, 1.000000000000000000 ),
 .UNSPECIFIED. ) ;
#17620=FACE_OUTER_BOUND ( 'NONE', #20735, .T. ) ;
#17621=CARTESIAN_POINT ( 'NONE',  ( 8.434520297147999557, 5.100000003584000297, 6.577489351425000130 ) ) ;
#17623=ORIENTED_EDGE ( 'NONE', *, *, #23580, .F. ) ;
#17627=CARTESIAN_POINT ( 'NONE',  ( 8.365056901398830291, 2.650139792115765669, -7.500003826568613086 ) ) ;
#17634=DIRECTION ( 'NONE',  ( 0.000000000000000000, 1.000000000000000000, 0.000000000000000000 ) ) ;
#17636=ORIENTED_EDGE ( 'NONE', *, *, #14691, .F. ) ;
#17640=CARTESIAN_POINT ( 'NONE',  ( 9.319414158774000256, 2.656512020013999997, -7.884832994446999699 ) ) ;
#17648=CARTESIAN_POINT ( 'NONE',  ( 9.345514158774999913, 5.775964236216999836, -8.174909295649001706 ) ) ;
#17649=ORIENTED_EDGE ( 'NONE', *, *, #6943, .T. ) ;
#17651=CARTESIAN_POINT ( 'NONE',  ( 10.89218604104999955, 2.661903984162000469, -8.236033286991000679 ) ) ;
#17658=CARTESIAN_POINT ( 'NONE',  ( 11.08757144985999865, 2.712428550139000194, 6.571291218949999902 ) ) ;
#17661=ORIENTED_EDGE ( 'NONE', *, *, #55579, .F. ) ;
#17663=CARTESIAN_POINT ( 'NONE',  ( 10.10735778041000010, 4.293584699549000128, -8.994197232567001876 ) ) ;
#17671=EDGE_CURVE ( 'NONE', #28975, #29686, #44671, .T. ) ;
#17673=ORIENTED_EDGE ( 'NONE', *, *, #27146, .T. ) ;
#17674=CARTESIAN_POINT ( 'NONE',  ( 9.286929719595001131, 4.102804347295999854, -5.770625657082999460 ) ) ;
#17678=CARTESIAN_POINT ( 'NONE',  ( 5.000000000000000000, 0.2999999999999999889, -9.776630298829998011 ) ) ;
#17685=CARTESIAN_POINT ( 'NONE',  ( 7.544160676995611325, 5.349767121210510901, -7.146874343389594486 ) ) ;
#17686=DIRECTION ( 'NONE',  ( 1.000000000000000000, 0.000000000000000000, 0.000000000000000000 ) ) ;
#17690=CARTESIAN_POINT ( 'NONE',  ( 4.149992563291999836, 1.599290730647368930, 1.229060429538529675 ) ) ;
#17691=ORIENTED_EDGE ( 'NONE', *, *, #6336, .F. ) ;
#17694=CARTESIAN_POINT ( 'NONE',  ( 9.152520280414000453, 4.102804347295999854, -5.770625657082999460 ) ) ;
#17699=AXIS2_PLACEMENT_3D ( 'NONE', #14512, #47356, #46671 ) ;
#17703=CARTESIAN_POINT ( 'NONE',  ( 2.309200955736999905, -2.649983027386999979, 2.425167579440000054 ) ) ;
#17704=EDGE_LOOP ( 'NONE', ( #64986, #46169, #35936, #17513, #28066, #47590, #35018, #30416, #25068, #22448, #17805, #55550, #42277 ) ) ;
#17708=CARTESIAN_POINT ( 'NONE',  ( 11.09999999999999964, 5.538898460221000519, 7.685179721164000277 ) ) ;
#17709=CARTESIAN_POINT ( 'NONE',  ( 8.630420280412000267, 5.808262417891000062, 7.446016144116000213 ) ) ;
#17710=ORIENTED_EDGE ( 'NONE', *, *, #12794, .T. ) ;
#17712=CARTESIAN_POINT ( 'NONE',  ( 7.341410841227999917, 2.603491674958000157, -7.446887986542999549 ) ) ;
#17714=CARTESIAN_POINT ( 'NONE',  ( 10.81499708368641954, 2.650004840405624673, -7.499999822193707644 ) ) ;
#17717=CARTESIAN_POINT ( 'NONE',  ( 8.200000998245998929, 12.50000000000000000, 0.000000000000000000 ) ) ;
#17726=CARTESIAN_POINT ( 'NONE',  ( 7.491064158769000336, 4.422660346525999486, -6.167928437610999737 ) ) ;
#17739=CARTESIAN_POINT ( 'NONE',  ( 10.93499870985557010, 2.931393928242580937, 4.937945785150366085 ) ) ;
#17741=FACE_OUTER_BOUND ( 'NONE', #6322, .T. ) ;
#17742=CARTESIAN_POINT ( 'NONE',  ( 8.100000113405998903, -12.39999890530000037, 0.000000000000000000 ) ) ;
#17743=VECTOR ( 'NONE', #58096, 1000.000000000000114 ) ;
#17748=ORIENTED_EDGE ( 'NONE', *, *, #44074, .T. ) ;
#17750=CARTESIAN_POINT ( 'NONE',  ( 8.549914158773001205, 2.141799395716999843, -7.895788736628000848 ) ) ;
#17751=CARTESIAN_POINT ( 'NONE',  ( 2.705986907149000142, 2.679358243340999923, -1.776962442616000004 ) ) ;
#17758=ORIENTED_EDGE ( 'NONE', *, *, #30641, .T. ) ;
#17759=CARTESIAN_POINT ( 'NONE',  ( 1.854719994300333408, -2.744941749261882169, -2.197574953528185215 ) ) ;
#17762=CARTESIAN_POINT ( 'NONE',  ( 10.43579914648999996, 2.587602126999999808, 6.390037244031000263 ) ) ;
#17765=DIRECTION ( 'NONE',  ( 1.000000000000000000, 0.000000000000000000, 0.000000000000000000 ) ) ;
#17768=CARTESIAN_POINT ( 'NONE',  ( 7.100000000000397549, 3.326107221750500997, -6.287467994316567221 ) ) ;
#17772=ORIENTED_EDGE ( 'NONE', *, *, #49899, .T. ) ;
#17778=ORIENTED_EDGE ( 'NONE', *, *, #10084, .F. ) ;
#17780=CARTESIAN_POINT ( 'NONE',  ( 7.384454719589999883, 3.346262376537000094, 6.002251090845000192 ) ) ;
#17781=CARTESIAN_POINT ( 'NONE',  ( 8.414360841228999632, 5.461114003844000031, -8.582501063019000398 ) ) ;
#17783=CARTESIAN_POINT ( 'NONE',  ( 10.83487665876999984, 5.800192368099000184, -7.920541111170000370 ) ) ;
#17785=CARTESIAN_POINT ( 'NONE',  ( 10.07770645819999977, 4.622041375574999833, 5.671348593713000596 ) ) ;
#17791=ORIENTED_EDGE ( 'NONE', *, *, #16333, .F. ) ;
#17792=LINE ( 'NONE', #28631, #46690 ) ;
#17794=CARTESIAN_POINT ( 'NONE',  ( 1.323890132541374998, -2.150913519912200478, -2.798833948393631754 ) ) ;
#17803=ADVANCED_FACE ( 'NONE', ( #15742 ), #37070, .F. ) ;
#17805=ORIENTED_EDGE ( 'NONE', *, *, #14134, .T. ) ;
#17807=CARTESIAN_POINT ( 'NONE',  ( 9.972410841228999345, 4.357364160690000432, -9.282962013144999247 ) ) ;
#17814=DIRECTION ( 'NONE',  ( 0.000000000000000000, 1.000000000000000000, 0.000000000000000000 ) ) ;
#17815=ORIENTED_EDGE ( 'NONE', *, *, #21684, .F. ) ;
#17818=ORIENTED_EDGE ( 'NONE', *, *, #40724, .T. ) ;
#17823=CARTESIAN_POINT ( 'NONE',  ( 10.95552360838999917, 4.744046441415999738, -9.198140387677000263 ) ) ;
#17826=CARTESIAN_POINT ( 'NONE',  ( 5.500000000000000000, -11.95749337870000062, 3.642574926947999892 ) ) ;
#17828=CARTESIAN_POINT ( 'NONE',  ( 6.899999691988000450, -12.20988339176000004, 3.111064831549000154 ) ) ;
#17834=CARTESIAN_POINT ( 'NONE',  ( 10.12671450658999994, 3.117528978489000124, 8.613535509676999880 ) ) ;
#17835=CARTESIAN_POINT ( 'NONE',  ( 10.72303311070000120, 3.890114357827999747, -8.859327677199999584 ) ) ;
#17838=CARTESIAN_POINT ( 'NONE',  ( 9.781673028307999118, 5.464749740720999505, 8.817329433105999925 ) ) ;
#17844=ORIENTED_EDGE ( 'NONE', *, *, #22639, .T. ) ;
#17851=CARTESIAN_POINT ( 'NONE',  ( 7.919010841228001141, 5.361039412362000434, 6.973453640356000349 ) ) ;
#17852=CARTESIAN_POINT ( 'NONE',  ( 10.71256887705999894, 5.951815279772000089, 7.233043586354999555 ) ) ;
#17855=CARTESIAN_POINT ( 'NONE',  ( 9.295789158775001226, 5.835196551504000517, -7.008466539623000813 ) ) ;
#17866=CARTESIAN_POINT ( 'NONE',  ( 2.290900752179999778, 2.610776529918000133, -2.002676742402000443 ) ) ;
#17868=DIRECTION ( 'NONE',  ( 0.000000000000000000, 1.000000000000000000, -1.181194934447000133E-14 ) ) ;
#17869=CARTESIAN_POINT ( 'NONE',  ( 6.999999691988000095, -12.49999909016000110, 4.774434232535999529E-10 ) ) ;
#17872=DIRECTION ( 'NONE',  ( -1.000000000000000000, 0.000000000000000000, 0.000000000000000000 ) ) ;
#17884=CARTESIAN_POINT ( 'NONE',  ( 10.12671450658999994, 3.117528978489000124, 8.613535509676999880 ) ) ;
#17895=CARTESIAN_POINT ( 'NONE',  ( 9.243110841233001196, 4.112741311853999271, -5.603466076760000192 ) ) ;
#17896=EDGE_LOOP ( 'NONE', ( #13539, #53047, #23125, #41510 ) ) ;
#17903=CARTESIAN_POINT ( 'NONE',  ( 9.380783851237000093, 2.204242311415999911, 7.545378292079000460 ) ) ;
#17908=CARTESIAN_POINT ( 'NONE',  ( 3.999999999999999112, -1.719326598156197150, -1.321078631445046669 ) ) ;
#17914=B_SPLINE_CURVE_WITH_KNOTS ( 'NONE', 3,
 ( #10046, #68076, #24759, #68417 ),
 .UNSPECIFIED., .F., .F.,
 ( 4, 4 ),
 ( 0.000000000000000000, 1.000000000000000000 ),
 .UNSPECIFIED. ) ;
#17915=CARTESIAN_POINT ( 'NONE',  ( 10.76874784196215629, 3.036568074332222089, -4.838413581444926059 ) ) ;
#17922=CARTESIAN_POINT ( 'NONE',  ( 7.850909765600520451, 2.904933541014710130, -6.663705336267816470 ) ) ;
#17927=DIRECTION ( 'NONE',  ( 1.000000000000000000, 0.000000000000000000, 0.000000000000000000 ) ) ;
#17931=CARTESIAN_POINT ( 'NONE',  ( 9.436104719595000745, 5.619431609641999614, -8.115423117607999615 ) ) ;
#17934=CARTESIAN_POINT ( 'NONE',  ( 10.90000668870999867, -1.199999999999999956, -9.776630298829998011 ) ) ;
#17939=CARTESIAN_POINT ( 'NONE',  ( 1.146806799208750061, -0.9161175952574931447, 3.408904368339100710 ) ) ;
#17941=EDGE_CURVE ( 'NONE', #5127, #24516, #21239, .T. ) ;
#17957=ORIENTED_EDGE ( 'NONE', *, *, #10783, .T. ) ;
#17960=FACE_OUTER_BOUND ( 'NONE', #61017, .T. ) ;
#17968=CARTESIAN_POINT ( 'NONE',  ( 6.999998782146999332, 11.95749337870000062, -3.642574926947999892 ) ) ;
#17970=CARTESIAN_POINT ( 'NONE',  ( 0.000000000000000000, -2.319305672483364056, -1.781768641235244921 ) ) ;
#17975=CARTESIAN_POINT ( 'NONE',  ( 7.000000000000001776, 8.872191283697411279, 4.648286939382654026 ) ) ;
#17977=ORIENTED_EDGE ( 'NONE', *, *, #61009, .F. ) ;
#17983=CARTESIAN_POINT ( 'NONE',  ( 8.456370280410999030, 2.836879604150999601, -8.783908972046001296 ) ) ;
#17989=EDGE_LOOP ( 'NONE', ( #14867, #63456 ) ) ;
#17990=CARTESIAN_POINT ( 'NONE',  ( 8.856851002545001350, 2.832432432432000269, -6.822293592207000934 ) ) ;
#17992=CARTESIAN_POINT ( 'NONE',  ( 6.950000000000000178, 5.221516520829000640, -8.074802043613001246 ) ) ;
#17994=CARTESIAN_POINT ( 'NONE',  ( 10.14584353048000054, 5.370502454907000178, -6.826221644974000746 ) ) ;
#18004=AXIS2_PLACEMENT_3D ( 'NONE', #8224, #3312, #56112 ) ;
#18011=CARTESIAN_POINT ( 'NONE',  ( 10.47111721959000086, 5.170640285885000687, -8.712953516124999354 ) ) ;
#18014=LINE ( 'NONE', #7506, #3570 ) ;
#18020=VERTEX_POINT ( 'NONE', #49967 ) ;
#18022=CARTESIAN_POINT ( 'NONE',  ( 8.649364158774000444, 3.038023536984999939, -5.861661709981000001 ) ) ;
#18036=CARTESIAN_POINT ( 'NONE',  ( 7.881386633191600488, 5.152558727359871860, 6.796436030802987638 ) ) ;
#18037=CARTESIAN_POINT ( 'NONE',  ( 8.470944094208999076, 5.100000000000000533, 6.571291218949999902 ) ) ;
#18038=CARTESIAN_POINT ( 'NONE',  ( 4.149992563291999836, -1.229060429538530563, 1.599290730647368486 ) ) ;
#18039=ORIENTED_EDGE ( 'NONE', *, *, #28287, .T. ) ;
#18041=CARTESIAN_POINT ( 'NONE',  ( 7.931011803055000975, 3.387313518888000363, -6.297038610257000180 ) ) ;
#18042=CARTESIAN_POINT ( 'NONE',  ( 9.211104719594999324, 5.462898983065000102, -8.055936939571999744 ) ) ;
#18045=CARTESIAN_POINT ( 'NONE',  ( 11.09999999999999964, 0.000000000000000000, 0.000000000000000000 ) ) ;
#18047=CARTESIAN_POINT ( 'NONE',  ( 2.118473157973999932, 3.592226503575000507, 0.01333834274854999932 ) ) ;
#18048=EDGE_LOOP ( 'NONE', ( #39421, #50888, #20044, #4609 ) ) ;
#18051=VECTOR ( 'NONE', #67946, 1000.000000000000000 ) ;
#18053=CARTESIAN_POINT ( 'NONE',  ( 8.732392219593000604, 2.806082850903000026, 8.615880516515998622 ) ) ;
#18054=ORIENTED_EDGE ( 'NONE', *, *, #53369, .T. ) ;
#18056=CARTESIAN_POINT ( 'NONE',  ( 10.95126072563318331, 9.104112520226776084, 6.364239214224977736 ) ) ;
#18067=ORIENTED_EDGE ( 'NONE', *, *, #46487, .T. ) ;
#18068=CARTESIAN_POINT ( 'NONE',  ( 10.95996395620064412, 8.913960680409392268, -6.449865299654371498 ) ) ;
#18070=CARTESIAN_POINT ( 'NONE',  ( 7.341889158769000723, 2.602490396417999730, -7.495170534277000307 ) ) ;
#18071=DIRECTION ( 'NONE',  ( 0.000000000000000000, 1.000000000000000000, 0.000000000000000000 ) ) ;
#18074=CARTESIAN_POINT ( 'NONE',  ( 7.999926658772999133, 5.198556077301000222, 8.332552905512999430 ) ) ;
#18078=ORIENTED_EDGE ( 'NONE', *, *, #57966, .T. ) ;
#18082=CARTESIAN_POINT ( 'NONE',  ( 9.118435835444836712, 5.100000000000000533, 6.178531823618069296 ) ) ;
#18089=ADVANCED_FACE ( 'NONE', ( #30040 ), #50245, .T. ) ;
#18092=CARTESIAN_POINT ( 'NONE',  ( 8.400739158770999637, 4.933589693325000525, -9.154576215408999573 ) ) ;
#18096=CARTESIAN_POINT ( 'NONE',  ( 2.712743541013000304, -0.2306114756280000233, -3.371506406067999784 ) ) ;
#18104=CARTESIAN_POINT ( 'NONE',  ( 10.68903608760000168, 2.568976842941999905, 7.728092503410000091 ) ) ;
#18107=CARTESIAN_POINT ( 'NONE',  ( 11.05833333333436741, 2.548905579443693448, 7.980400043919090969 ) ) ;
#18109=EDGE_CURVE ( 'NONE', #62685, #68419, #9629, .T. ) ;
#18110=CARTESIAN_POINT ( 'NONE',  ( 7.100000000000459721, 5.092549871003397399, -6.644539875156245223 ) ) ;
#18113=FACE_OUTER_BOUND ( 'NONE', #39109, .T. ) ;
#18114=CARTESIAN_POINT ( 'NONE',  ( 8.126439348839909371, 4.834870829740609111, -6.246114233407420890 ) ) ;
#18115=CARTESIAN_POINT ( 'NONE',  ( 10.87947334122999976, 2.817426144593000004, -6.828668581221999823 ) ) ;
#18123=CARTESIAN_POINT ( 'NONE',  ( 9.069718325438000051, 4.108964550738000376, 8.851615252874999840 ) ) ;
#18124=CARTESIAN_POINT ( 'NONE',  ( 8.655270280412999284, 4.162493982103000256, -5.775210092227999858 ) ) ;
#18126=CARTESIAN_POINT ( 'NONE',  ( 10.07762665876999897, 2.169012810937000157, -7.244984731085000185 ) ) ;
#18128=CARTESIAN_POINT ( 'NONE',  ( 10.41185190929999926, 2.101586107686999938, 7.856266936613998553 ) ) ;
#18132=CARTESIAN_POINT ( 'NONE',  ( 7.470056312015993960, 3.527048554922000090, 6.623442700707995456 ) ) ;
#18135=CARTESIAN_POINT ( 'NONE',  ( 1.386390132541124309, 0.4581489286485156964, -3.499999999999998668 ) ) ;
#18141=AXIS2_PLACEMENT_3D ( 'NONE', #6832, #54381, #1592 ) ;
#18144=ORIENTED_EDGE ( 'NONE', *, *, #10605, .T. ) ;
#18149=CARTESIAN_POINT ( 'NONE',  ( 8.216604719590000272, 5.331510020787000315, -8.114341808290998159 ) ) ;
#18151=CARTESIAN_POINT ( 'NONE',  ( 8.229424060894674042, 4.864026623416703110, 6.209051899842799926 ) ) ;
#18155=ORIENTED_EDGE ( 'NONE', *, *, #43595, .T. ) ;
#18157=VECTOR ( 'NONE', #20559, 1000.000000000000000 ) ;
#18172=CARTESIAN_POINT ( 'NONE',  ( 7.968176658772001097, 2.280568568659000483, 6.510284508622999233 ) ) ;
#18175=CARTESIAN_POINT ( 'NONE',  ( 8.121343566036543393, 3.646810248691461531, 8.848457998379188894 ) ) ;
#18178=CARTESIAN_POINT ( 'NONE',  ( 10.25165889348999926, 3.418644779562000302, -8.733642166016998942 ) ) ;
#18180=CARTESIAN_POINT ( 'NONE',  ( 10.84920446230533386, 2.899999999999999911, -6.662590550568697090 ) ) ;
#18181=CARTESIAN_POINT ( 'NONE',  ( 9.194604681486000075, 5.157771204918000230, 8.637848577075999401 ) ) ;
#18193=CARTESIAN_POINT ( 'NONE',  ( 7.956795280408998750, 4.524487726177000013, 9.047753146378999745 ) ) ;
#18194=CARTESIAN_POINT ( 'NONE',  ( 11.27110638630999873, 5.469603964121000139, 8.504707115835000053 ) ) ;
#18197=CARTESIAN_POINT ( 'NONE',  ( 9.047164158776000775, 2.156584729807999867, -7.959751745006000689 ) ) ;
#18205=VECTOR ( 'NONE', #18757, 1000.000000000000000 ) ;
#18206=CARTESIAN_POINT ( 'NONE',  ( 1.257791847628999982, 1.635708097465000010, -3.009863393104000195 ) ) ;
#18208=LINE ( 'NONE', #23450, #6204 ) ;
#18211=CARTESIAN_POINT ( 'NONE',  ( 4.900006121741999898, -1.599333684796363508, -1.229093439949825672 ) ) ;
#18215=EDGE_LOOP ( 'NONE', ( #6224, #17673, #45323 ) ) ;
#18216=CARTESIAN_POINT ( 'NONE',  ( 9.933148997456999751, 5.167567567567999731, 6.822293592207000934 ) ) ;
#18219=CARTESIAN_POINT ( 'NONE',  ( -14.79345512259999929, 10.48174933044999868, 5.405686454350000503 ) ) ;
#18221=B_SPLINE_CURVE_WITH_KNOTS ( 'NONE', 3,
 ( #22786, #23485, #38881, #6354 ),
 .UNSPECIFIED., .F., .F.,
 ( 4, 4 ),
 ( 0.000000000000000000, 1.000000000000000000 ),
 .UNSPECIFIED. ) ;
#18223=CARTESIAN_POINT ( 'NONE',  ( 1.886390132539666142, 0.4581489286485156964, -3.499999999999998668 ) ) ;
#18232=EDGE_CURVE ( 'NONE', #10880, #11774, #62509, .T. ) ;
#18237=CARTESIAN_POINT ( 'NONE',  ( 8.056242640631749552, 3.593179318435525182, 5.798412987495025206 ) ) ;
#18238=VERTEX_POINT ( 'NONE', #9029 ) ;
#18247=CARTESIAN_POINT ( 'NONE',  ( 10.56590837162999996, 5.293226105229999590, -7.067087619452999903 ) ) ;
#18248=CARTESIAN_POINT ( 'NONE',  ( 11.10000000008000143, 8.133170861274999552, -6.729066177741999333 ) ) ;
#18258=CARTESIAN_POINT ( 'NONE',  ( 3.500000000000000000, 0.000000000000000000, 0.000000000000000000 ) ) ;
#18270=CARTESIAN_POINT ( 'NONE',  ( 9.405375278053794474, 5.100000000000000533, -6.445686799063087058 ) ) ;
#18272=CARTESIAN_POINT ( 'NONE',  ( 8.483378221910873762, 3.070366253409245072, 6.121136983106237217 ) ) ;
#18273=CARTESIAN_POINT ( 'NONE',  ( 9.278070280414000948, 2.546924812613000189, -6.918870225297999887 ) ) ;
#18274=EDGE_CURVE ( 'NONE', #26681, #25668, #68091, .T. ) ;
#18279=CARTESIAN_POINT ( 'NONE',  ( 9.709999999999999076, 4.496968146123999865, -8.755198255949000696 ) ) ;
#18280=EDGE_CURVE ( 'NONE', #45160, #23923, #63544, .T. ) ;
#18290=ORIENTED_EDGE ( 'NONE', *, *, #19173, .T. ) ;
#18299=ORIENTED_EDGE ( 'NONE', *, *, #38119, .F. ) ;
#18307=DIRECTION ( 'NONE',  ( 0.000000000000000000, 1.000000000000000000, 0.000000000000000000 ) ) ;
#18317=CARTESIAN_POINT ( 'NONE',  ( 3.500000000000000000, -2.946081722130999836, 0.9972449351501998516 ) ) ;
#18318=CARTESIAN_POINT ( 'NONE',  ( 6.999999999999996447, 8.647867546315030296, 4.556671657224676153 ) ) ;
#18326=CARTESIAN_POINT ( 'NONE',  ( 9.889535841229999846, 5.798263352390999437, -8.113145944980999502 ) ) ;
#18336=DIRECTION ( 'NONE',  ( 0.000000000000000000, 0.9916377111174247139, 0.1290528957048031888 ) ) ;
#18340=CARTESIAN_POINT ( 'NONE',  ( 10.06728116094000036, 4.192860729918999496, -5.985054792427000336 ) ) ;
#18341=DIRECTION ( 'NONE',  ( 1.000000000000000000, 0.000000000000000000, 0.000000000000000000 ) ) ;
#18342=ORIENTED_EDGE ( 'NONE', *, *, #57313, .F. ) ;
#18352=CARTESIAN_POINT ( 'NONE',  ( 10.20607971959000082, 2.622352165399999713, -6.528536464360000124 ) ) ;
#18353=VECTOR ( 'NONE', #7146, 1000.000000000000000 ) ;
#18359=CIRCLE ( 'NONE', #41805, 12.50000000000000000 ) ;
#18360=CARTESIAN_POINT ( 'NONE',  ( 10.22180282789683403, 2.874603711584076571, 6.749639981064802008 ) ) ;
#18364=CARTESIAN_POINT ( 'NONE',  ( 9.535554719593998030, 3.927090956378999742, -9.230892435423001530 ) ) ;
#18368=CARTESIAN_POINT ( 'NONE',  ( 10.95319771758351735, 2.911823740494093649, -4.928389130528513462 ) ) ;
#18382=CARTESIAN_POINT ( 'NONE',  ( 8.893723582519571735, 5.100000000000000533, -6.421373690736477791 ) ) ;
#18383=CARTESIAN_POINT ( 'NONE',  ( 8.962479719595000560, 2.546924812613000189, -6.918870225297999887 ) ) ;
#18389=CARTESIAN_POINT ( 'NONE',  ( 9.309825924086673865, 4.346446645907335871, 9.216763236637257606 ) ) ;
#18390=CARTESIAN_POINT ( 'NONE',  ( 2.129593803058000390, 1.784639509494000187, -2.764404103036999683 ) ) ;
#18395=CARTESIAN_POINT ( 'NONE',  ( 7.678989158771000412, 2.599243720295000060, 7.909344432242998657 ) ) ;
#18396=ORIENTED_EDGE ( 'NONE', *, *, #1197, .T. ) ;
#18398=ADVANCED_FACE ( 'NONE', ( #38007 ), #33580, .F. ) ;
#18400=CARTESIAN_POINT ( 'NONE',  ( 7.391135841228000380, 2.898440551356999961, -6.639986657414999272 ) ) ;
#18414=DIRECTION ( 'NONE',  ( 1.000000000000000000, 0.000000000000000000, 0.000000000000000000 ) ) ;
#18419=LINE ( 'NONE', #1642, #24233 ) ;
#18426=DIRECTION ( 'NONE',  ( 0.000000000000000000, 1.000000000000000000, 0.000000000000000000 ) ) ;
#18429=CARTESIAN_POINT ( 'NONE',  ( 8.137522165044002165, 2.460709986978387054, -6.460953617291827378 ) ) ;
#18437=CARTESIAN_POINT ( 'NONE',  ( 0.1499942179680000265, 0.3599680999393979897, 2.749953718116143531 ) ) ;
#18438=CARTESIAN_POINT ( 'NONE',  ( 9.377520280414000098, 4.092867382745001059, -5.937785237406000505 ) ) ;
#18439=CARTESIAN_POINT ( 'NONE',  ( 2.664069943672000118, 1.422849972570999988, -2.883063314296999913 ) ) ;
#18440=B_SPLINE_CURVE_WITH_KNOTS ( 'NONE', 3,
 ( #44693, #40456, #18805, #13564, #2372, #65988, #39432, #60753, #13902, #45029, #7616, #12868, #29654, #34884, #34196, #61102, #28963, #3053 ),
 .UNSPECIFIED., .F., .F.,
 ( 4, 2, 2, 2, 2, 2, 2, 2, 4 ),
 ( 0.000000000000000000, 0.1250000000000000833, 0.2500000000000001110, 0.3750000000000001665, 0.5000000000000002220, 0.6250000000000002220, 0.7500000000000001110, 0.8750000000000001110, 1.000000000000000000 ),
 .UNSPECIFIED. ) ;
#18443=CARTESIAN_POINT ( 'NONE',  ( 7.924470805432005882, 3.443171588504001068, -6.303962341916999890 ) ) ;
#18446=CARTESIAN_POINT ( 'NONE',  ( 10.96580581817999978, 4.930645553951000792, 6.170542400361000546 ) ) ;
#18449=CARTESIAN_POINT ( 'NONE',  ( 10.95833333333431980, 4.952949899269658118, 8.562434272074012753 ) ) ;
#18458=CARTESIAN_POINT ( 'NONE',  ( 10.91620964606000044, 2.818413279081999789, -6.814156272943999504 ) ) ;
#18459=CARTESIAN_POINT ( 'NONE',  ( 10.17270667456000055, 4.650145611776999921, -8.655516756809999990 ) ) ;
#18469=CARTESIAN_POINT ( 'NONE',  ( 11.08729332543999924, 2.258658230726000138, -7.034579402814999938 ) ) ;
#18471=CARTESIAN_POINT ( 'NONE',  ( 9.353724647487000610, 2.823567847429000022, 9.032053040610000139 ) ) ;
#18477=CYLINDRICAL_SURFACE ( 'NONE', #25470, 0.5000000000000002220 ) ;
#18488=B_SPLINE_CURVE_WITH_KNOTS ( 'NONE', 3,
 ( #41798, #15229, #41116, #9628 ),
 .UNSPECIFIED., .F., .F.,
 ( 4, 4 ),
 ( 0.000000000000000000, 1.000000000000000000 ),
 .UNSPECIFIED. ) ;
#18490=ORIENTED_EDGE ( 'NONE', *, *, #6068, .F. ) ;
#18495=CARTESIAN_POINT ( 'NONE',  ( 9.640910841231999484, 2.212639797530000063, -6.855876382544999537 ) ) ;
#18503=AXIS2_PLACEMENT_3D ( 'NONE', #67883, #3904, #47259 ) ;
#18504=ORIENTED_EDGE ( 'NONE', *, *, #35927, .T. ) ;
#18507=ORIENTED_EDGE ( 'NONE', *, *, #28058, .T. ) ;
#18513=CARTESIAN_POINT ( 'NONE',  ( 2.210247277619000084, 2.108360286353999413, -2.286637680308000409 ) ) ;
#18514=CARTESIAN_POINT ( 'NONE',  ( 8.496399244692801389, 5.100022896384949433, -6.666166966519626591 ) ) ;
#18518=DIRECTION ( 'NONE',  ( 1.000000000000000000, 0.000000000000000000, -3.552713678909000227E-14 ) ) ;
#18520=CARTESIAN_POINT ( 'NONE',  ( 8.930989158774000458, 2.019067547072999957, 7.390982789861999969 ) ) ;
#18523=CARTESIAN_POINT ( 'NONE',  ( 7.397586123398784075, 4.761547826166538044, 6.352807996277898717 ) ) ;
#18527=CARTESIAN_POINT ( 'NONE',  ( 10.24961997674000003, 4.184221916050000267, 9.286882020979000174 ) ) ;
#18528=CARTESIAN_POINT ( 'NONE',  ( 8.037016222020598732, 5.285842885613642572, -7.027160484499655801 ) ) ;
#18530=VERTEX_POINT ( 'NONE', #36511 ) ;
#18533=CARTESIAN_POINT ( 'NONE',  ( 10.92717848204000042, 5.023653513500000223, 8.718036113327999104 ) ) ;
#18540=CARTESIAN_POINT ( 'NONE',  ( 8.674239158774001979, 5.983047240001000411, 7.440798119034999658 ) ) ;
#18541=CARTESIAN_POINT ( 'NONE',  ( 11.11845610223999969, 5.767025078915000158, 7.178418469370999588 ) ) ;
#18543=EDGE_LOOP ( 'NONE', ( #67886, #36945, #66121, #12979, #38531, #22944, #25086 ) ) ;
#18544=CARTESIAN_POINT ( 'NONE',  ( 8.400739158770999637, 4.933589693325000525, -9.154576215408999573 ) ) ;
#18546=DIRECTION ( 'NONE',  ( 0.000000000000000000, -1.000000000000000000, 0.000000000000000000 ) ) ;
#18548=CARTESIAN_POINT ( 'NONE',  ( 1.550973465874000201, 3.500000000000000000, 0.000000000000000000 ) ) ;
#18552=CIRCLE ( 'NONE', #68781, 11.35000000000000675 ) ;
#18553=CARTESIAN_POINT ( 'NONE',  ( 1.500974932896000036, -3.258362327980000028, 0.06604197684371000687 ) ) ;
#18555=AXIS2_PLACEMENT_3D ( 'NONE', #57886, #47402, #32020 ) ;
#18561=CARTESIAN_POINT ( 'NONE',  ( 10.61094409420999973, 5.100000000000000533, -6.571291218949999902 ) ) ;
#18565=CARTESIAN_POINT ( 'NONE',  ( 8.753448341231001351, 2.876288091423999660, 6.568897128359000526 ) ) ;
#18570=CARTESIAN_POINT ( 'NONE',  ( 1.933975548942000078, -3.260690222378000325, 1.050103212221999982 ) ) ;
#18571=ORIENTED_EDGE ( 'NONE', *, *, #12794, .F. ) ;
#18572=DIRECTION ( 'NONE',  ( 0.7071182117976623216, 0.000000000000000000, -0.7070953503906501902 ) ) ;
#18574=DIRECTION ( 'NONE',  ( -0.5000000000000169864, 0.000000000000000000, -0.8660254037844288266 ) ) ;
#18575=CARTESIAN_POINT ( 'NONE',  ( 10.61382428715999993, 3.385080336122999967, 5.849521480782000182 ) ) ;
#18582=B_SPLINE_CURVE_WITH_KNOTS ( 'NONE', 3,
 ( #46316, #67617, #30923, #26365 ),
 .UNSPECIFIED., .F., .F.,
 ( 4, 4 ),
 ( 0.000000000000000000, 1.000000000000000000 ),
 .UNSPECIFIED. ) ;
#18583=CARTESIAN_POINT ( 'NONE',  ( 8.215396629533129769, 5.723734980850093912, 7.813254138193835630 ) ) ;
#18591=ADVANCED_FACE ( 'NONE', ( #33674 ), #37523, .F. ) ;
#18594=FACE_OUTER_BOUND ( 'NONE', #40222, .T. ) ;
#18595=CARTESIAN_POINT ( 'NONE',  ( 10.13381533919000077, 5.176445833090999926, -8.189798585019000043 ) ) ;
#18604=CARTESIAN_POINT ( 'NONE',  ( 9.849204462306566654, 2.899999999999999911, -6.662590550605539619 ) ) ;
#18619=CARTESIAN_POINT ( 'NONE',  ( 11.06992513079000062, 8.140394931567000114, -6.682140483390000441 ) ) ;
#18620=EDGE_CURVE ( 'NONE', #14252, #5489, #63698, .T. ) ;
#18622=CARTESIAN_POINT ( 'NONE',  ( 0.5979711358043999780, 3.275095586319999974, -0.8499908244220999443 ) ) ;
#18626=ADVANCED_FACE ( 'NONE', ( #28079 ), #38916, .T. ) ;
#18636=DIRECTION ( 'NONE',  ( 1.000000000000000000, 0.000000000000000000, 0.000000000000000000 ) ) ;
#18647=CARTESIAN_POINT ( 'NONE',  ( 10.38462472191413255, 2.899999999999999911, 6.445686799157043012 ) ) ;
#18650=CARTESIAN_POINT ( 'NONE',  ( 6.899999691988000450, 12.43893545635000031, -2.828937028792000152 ) ) ;
#18654=ORIENTED_EDGE ( 'NONE', *, *, #57285, .F. ) ;
#18655=CARTESIAN_POINT ( 'NONE',  ( 8.383148997457999130, 5.167567567567999731, 6.822293592207000934 ) ) ;
#18660=CARTESIAN_POINT ( 'NONE',  ( 9.410004719593999312, 2.495531372253999791, -7.930944806125000746 ) ) ;
#18666=DIRECTION ( 'NONE',  ( 0.000000000000000000, 0.000000000000000000, -1.000000000000000000 ) ) ;
#18668=ADVANCED_FACE ( 'NONE', ( #1504 ), #10959, .T. ) ;
#18669=CARTESIAN_POINT ( 'NONE',  ( 9.202245280414000916, 5.095038542659000136, -6.157541456184000062 ) ) ;
#18678=CARTESIAN_POINT ( 'NONE',  ( 9.494689158774999527, 2.824732249080000202, -8.992748220058999209 ) ) ;
#18680=CARTESIAN_POINT ( 'NONE',  ( 10.80159548023000049, 2.805082485475999476, -8.157276499959001725 ) ) ;
#18682=ORIENTED_EDGE ( 'NONE', *, *, #46980, .T. ) ;
#18685=STYLED_ITEM ( 'NONE', ( #59513 ), #61967 ) ;
#18694=CARTESIAN_POINT ( 'NONE',  ( 10.01676721958999927, 4.324998751150999965, -9.154078823942999321 ) ) ;
#18696=AXIS2_PLACEMENT_3D ( 'NONE', #58953, #22232, #32394 ) ;
#18701=CARTESIAN_POINT ( 'NONE',  ( 7.867118290853380991, 5.122083207617727396, 6.719810845265266508 ) ) ;
#18703=EDGE_LOOP ( 'NONE', ( #47215, #52694, #1370, #3425, #56592 ) ) ;
#18704=CARTESIAN_POINT ( 'NONE',  ( 8.541054719591000932, 3.807713920470999991, -9.221758713517999695 ) ) ;
#18716=DIRECTION ( 'NONE',  ( -1.000000000000000000, 0.000000000000000000, 0.000000000000000000 ) ) ;
#18722=CARTESIAN_POINT ( 'NONE',  ( 11.09999999999999964, 2.649999999999999911, 7.500000000000000000 ) ) ;
#18724=CARTESIAN_POINT ( 'NONE',  ( 8.406645280410000254, 3.807713920470999991, -9.221758713517999695 ) ) ;
#18728=VECTOR ( 'NONE', #6411, 1000.000000000000000 ) ;
#18733=CARTESIAN_POINT ( 'NONE',  ( 3.219931333175999999, -2.814609116688000068, 2.491254988490000155 ) ) ;
#18734=VERTEX_POINT ( 'NONE', #6047 ) ;
#18735=B_SPLINE_CURVE_WITH_KNOTS ( 'NONE', 3,
 ( #38712, #60031, #27530, #33124, #16683, #11437, #5849, #58651, #268, #49537 ),
 .UNSPECIFIED., .F., .F.,
 ( 4, 2, 2, 2, 4 ),
 ( 0.3720125677995148594, 0.5290094258496361723, 0.6860062838997573742, 0.8430031419498786871, 1.000000000000000000 ),
 .UNSPECIFIED. ) ;
#18742=ORIENTED_EDGE ( 'NONE', *, *, #22639, .F. ) ;
#18744=CARTESIAN_POINT ( 'NONE',  ( 8.683985841228999192, 4.472863460285000592, -8.721137209586000694 ) ) ;
#18757=DIRECTION ( 'NONE',  ( -1.000000000000000000, 0.000000000000000000, 0.000000000000000000 ) ) ;
#18759=CARTESIAN_POINT ( 'NONE',  ( 7.888864158768998713, 2.841678116489999795, -6.718113446527000931 ) ) ;
#18761=CARTESIAN_POINT ( 'NONE',  ( 10.21685100254000034, 2.832432432432000269, 6.822293592207000934 ) ) ;
#18763=ORIENTED_EDGE ( 'NONE', *, *, #5200, .T. ) ;
#18769=ORIENTED_EDGE ( 'NONE', *, *, #25731, .T. ) ;
#18771=DIRECTION ( 'NONE',  ( 1.000000000000000000, 0.000000000000000000, 0.000000000000000000 ) ) ;
#18772=DIRECTION ( 'NONE',  ( -1.000000000000000000, 0.000000000000000000, 0.000000000000000000 ) ) ;
#18773=CARTESIAN_POINT ( 'NONE',  ( 3.500000000000000444, 3.440400109149063024, 0.5815178920906223237 ) ) ;
#18778=ORIENTED_EDGE ( 'NONE', *, *, #29818, .F. ) ;
#18780=ORIENTED_EDGE ( 'NONE', *, *, #67769, .F. ) ;
#18781=CARTESIAN_POINT ( 'NONE',  ( 0.1499942179680000265, -0.7197945678028389027, 2.678379783547566895 ) ) ;
#18782=CARTESIAN_POINT ( 'NONE',  ( 8.780820280412001466, 2.567871051582000241, -6.869011921437000012 ) ) ;
#18783=CARTESIAN_POINT ( 'NONE',  ( 3.041322614968000160, -2.841635719351000233, -1.503882494686000104 ) ) ;
#18785=CONICAL_SURFACE ( 'NONE', #53359, 2.074968475931999734, 0.7853828752794411727 ) ;
#18786=CARTESIAN_POINT ( 'NONE',  ( 10.36503728015293646, 2.650011783304074164, -7.500002219258057323 ) ) ;
#18789=VECTOR ( 'NONE', #61783, 1000.000000000000114 ) ;
#18790=EDGE_CURVE ( 'NONE', #9042, #35521, #21273, .T. ) ;
#18792=CARTESIAN_POINT ( 'NONE',  ( 9.199602729599000384, 2.551394566582000145, 7.536605852160000119 ) ) ;
#18796=CARTESIAN_POINT ( 'NONE',  ( 9.290193290418001126, 2.377818438998999806, 7.540992072119000689 ) ) ;
#18797=CARTESIAN_POINT ( 'NONE',  ( 10.91666666666762886, 5.385217356303825476, 7.523132604489796371 ) ) ;
#18798=VECTOR ( 'NONE', #26472, 1000.000000000000000 ) ;
#18804=AXIS2_PLACEMENT_3D ( 'NONE', #63167, #47810, #16318 ) ;
#18805=CARTESIAN_POINT ( 'NONE',  ( 0.7690682080319749536, -3.431488182670113574, -0.7957590664505270750 ) ) ;
#18806=CARTESIAN_POINT ( 'NONE',  ( 11.10664834123000055, 5.324188120986000250, -7.809342242343999985 ) ) ;
#18812=CARTESIAN_POINT ( 'NONE',  ( 10.38314899745999931, 5.167567567567999731, 6.822293592207000934 ) ) ;
#18814=ADVANCED_FACE ( 'NONE', ( #31439 ), #62214, .F. ) ;
#18815=CARTESIAN_POINT ( 'NONE',  ( 8.128301658772999261, 3.117378429069999957, 8.662179062556001341 ) ) ;
#18816=CARTESIAN_POINT ( 'NONE',  ( 9.491735841231999871, 3.920043641733999884, -9.398198753036000497 ) ) ;
#18817=CARTESIAN_POINT ( 'NONE',  ( 5.500000000000000000, 0.000000000000000000, 0.000000000000000000 ) ) ;
#18824=CARTESIAN_POINT ( 'NONE',  ( 9.725191424783275806, 2.649754699899339538, 7.500009801425228773 ) ) ;
#18825=ORIENTED_EDGE ( 'NONE', *, *, #49899, .F. ) ;
#18839=CARTESIAN_POINT ( 'NONE',  ( 8.994485841233000656, 3.854507394315999758, -9.394302886912999639 ) ) ;
#18847=CARTESIAN_POINT ( 'NONE',  ( 7.524264477127990070, 5.120202152877183721, 8.282468543079009038 ) ) ;
#18849=DIRECTION ( 'NONE',  ( -1.000000000000000000, 0.000000000000000000, 0.000000000000000000 ) ) ;
#18856=CARTESIAN_POINT ( 'NONE',  ( 9.769471092180999960, 5.100000000000000533, -6.152188490330000370 ) ) ;
#18863=EDGE_LOOP ( 'NONE', ( #38348, #46026, #50641, #68291 ) ) ;
#18866=CARTESIAN_POINT ( 'NONE',  ( 8.090129597172534659, 4.176673380087977172, 8.851094058677711374 ) ) ;
#18867=CARTESIAN_POINT ( 'NONE',  ( 10.90634530628000043, 3.089682683751000081, -6.534327427410000055 ) ) ;
#18871=CARTESIAN_POINT ( 'NONE',  ( 9.256664404737000140, 4.025830366070999311, 9.295863330698999505 ) ) ;
#18874=ORIENTED_EDGE ( 'NONE', *, *, #46345, .F. ) ;
#18878=CARTESIAN_POINT ( 'NONE',  ( 9.869051220224999810, 5.575171928796999410, 7.724300137354000562 ) ) ;
#18882=CARTESIAN_POINT ( 'NONE',  ( 9.406704719590001318, 3.705846972803000128, 9.096435887808000942 ) ) ;
#18885=CARTESIAN_POINT ( 'NONE',  ( 9.323722176100000425, 3.947350570199999797, 6.051869652381999920 ) ) ;
#18886=AXIS2_PLACEMENT_3D ( 'NONE', #46306, #19732, #41055 ) ;
#18888=EDGE_LOOP ( 'NONE', ( #24674, #49614, #21068, #55755 ) ) ;
#18889=CARTESIAN_POINT ( 'NONE',  ( 10.03280471959000231, 3.987760651117999711, -9.123263301387000368 ) ) ;
#18897=CARTESIAN_POINT ( 'NONE',  ( 1.777519953414000042, -1.374622313384999961, -3.318774223758000019 ) ) ;
#18902=CARTESIAN_POINT ( 'NONE',  ( 7.726719758561022999, 3.010539354342125051, 6.557630410916043928 ) ) ;
#18904=CARTESIAN_POINT ( 'NONE',  ( 8.474280730212667478, 2.899999999999999911, -6.567100790826333245 ) ) ;
#18908=CARTESIAN_POINT ( 'NONE',  ( 8.277732780410000046, 4.874567052833000069, 6.119507471270999588 ) ) ;
#18909=DIRECTION ( 'NONE',  ( 0.000000000000000000, 0.000000000000000000, -1.000000000000000000 ) ) ;
#18912=CARTESIAN_POINT ( 'NONE',  ( 1.604975240918999901, 3.542864650996000453, -0.5932612529451999350 ) ) ;
#18913=ORIENTED_EDGE ( 'NONE', *, *, #63540, .T. ) ;
#18914=CARTESIAN_POINT ( 'NONE',  ( 10.85460595134761874, 2.649926015913104393, -7.676664732030197058 ) ) ;
#18916=CARTESIAN_POINT ( 'NONE',  ( 10.44675156161000018, 2.885046387990999772, 8.863482298832000339 ) ) ;
#18919=CARTESIAN_POINT ( 'NONE',  ( 11.09999999999999964, -11.35000000000000142, 0.000000000000000000 ) ) ;
#18923=CARTESIAN_POINT ( 'NONE',  ( 8.383086419343017681, 2.825288952757737171, 8.816744424860624818 ) ) ;
#18935=CARTESIAN_POINT ( 'NONE',  ( 10.21237770872999917, 4.072568038926999812, -8.861829932786999819 ) ) ;
#18942=ORIENTED_EDGE ( 'NONE', *, *, #22912, .F. ) ;
#18955=LINE ( 'NONE', #62619, #43807 ) ;
#18956=AXIS2_PLACEMENT_3D ( 'NONE', #66807, #35007, #24507 ) ;
#18960=B_SPLINE_SURFACE_WITH_KNOTS ( 'NONE', 3, 3, ( 
 ( #15435, #52487, #4583, #20676, #42007, #36761, #32890, #17851, #1415, #1765, #27300, #12601, #7005, #17501, #16794, #48624, #54200, #727, #2116, #38824, #12256, #38474, #28337, #60492, #60151, #49656, #38122, #22038, #23083, #65380, #33585, #44430, #43727, #65728, #59449 ),
 ( #39169, #11899, #22390, #49305, #33932, #22732, #7347, #28692, #55251, #18193, #50005, #23433, #44772, #66072, #27648, #54902, #39515, #11212, #32548, #33237, #59796, #5962, #11547, #53861, #27996, #17142, #6301, #43385, #64686, #48967, #1075, #65025, #54557, #6654, #44081 ),
 ( #51037, #24120, #55941, #61186, #34279, #62207, #61864, #13306, #8043, #45455, #35310, #29387, #55599, #67105, #29734, #7700, #40210, #14329, #13641, #50697, #3139, #3475, #34628, #35652, #13984, #29041, #19213, #30075, #19564, #56966, #2794, #40539, #66767, #50351, #18882 ),
 ( #2451, #56285, #60840, #23776, #34968, #8390, #56627, #9067, #30405, #8731, #25149, #51376, #61526, #67442, #46480, #51717, #24467, #3810, #24811, #46136, #45792, #45111, #40887, #18540, #67787, #19909, #12952, #66418, #39866, #32126, #48194, #21277, #31434, #52404, #62882 ) ),
 .UNSPECIFIED., .F., .F., .F.,
 ( 4, 4 ),
 ( 4, 1, 1, 1, 1, 1, 1, 1, 1, 1, 1, 1, 1, 1, 1, 1, 1, 1, 1, 1, 1, 1, 1, 1, 1, 1, 1, 1, 1, 1, 1, 1, 4 ),
 ( -0.1039370721279000015, 1.103937072127999963 ),
 ( -0.02000000000000000042, 0.01250000000000000069, 0.04499999999999999833, 0.07749999999999999944, 0.1100000000000000006, 0.1424999999999999878, 0.1749999999999999889, 0.2074999999999999900, 0.2399999999999999911, 0.2725000000000000200, 0.3049999999999999933, 0.3375000000000000222, 0.3699999999999999956, 0.4025000000000000244, 0.4349999999999999978, 0.4675000000000000266, 0.5000000000000000000, 0.5324999999999999734, 0.5649999999999999467, 0.5975000000000000311, 0.6300000000000000044, 0.6624999999999999778, 0.6949999999999999512, 0.7275000000000000355, 0.7600000000000000089, 0.7924999999999999822, 0.8249999999999999556, 0.8575000000000000400, 0.8900000000000000133, 0.9224999999999999867, 0.9549999999999999600, 0.9875000000000000444, 1.020000000000000018 ),
 .UNSPECIFIED. ) ;
#18962=CARTESIAN_POINT ( 'NONE',  ( -0.06846944822773000372, 1.316872153397000034, -3.459566938009000392 ) ) ;
#18963=CARTESIAN_POINT ( 'NONE',  ( 8.008165174986313417, 4.679062738103456631, 8.679582621499550399 ) ) ;
#18967=FACE_OUTER_BOUND ( 'NONE', #60116, .T. ) ;
#18971=CARTESIAN_POINT ( 'NONE',  ( 27.64127793187000037, -1.199999999999999956, -9.776630298829998011 ) ) ;
#18973=ORIENTED_EDGE ( 'NONE', *, *, #7086, .T. ) ;
#18982=VERTEX_POINT ( 'NONE', #54919 ) ;
#18990=CARTESIAN_POINT ( 'NONE',  ( 10.67905590578999941, 2.899999999999999911, 6.571291218949999902 ) ) ;
#18996=CARTESIAN_POINT ( 'NONE',  ( 2.373822673703999353, -0.09607108383954167385, -3.514941141763996413 ) ) ;
#18998=CARTESIAN_POINT ( 'NONE',  ( 9.360279719594000625, 3.031907308384000022, -8.729608011560001657 ) ) ;
#19006=CARTESIAN_POINT ( 'NONE',  ( 8.655270280412999284, 4.162493982103000256, -5.775210092227999858 ) ) ;
#19015=CARTESIAN_POINT ( 'NONE',  ( 7.894723525210213033, 2.729257430866120604, -7.000779463158162130 ) ) ;
#19017=CARTESIAN_POINT ( 'NONE',  ( 8.748814158775001459, 5.251032986819000214, -6.070151079272999795 ) ) ;
#19019=CARTESIAN_POINT ( 'NONE',  ( 10.26368708477999903, 4.794139572939999816, -8.804452601708000259 ) ) ;
#19020=DIRECTION ( 'NONE',  ( 0.000000000000000000, 0.000000000000000000, 1.000000000000000000 ) ) ;
#19025=DIRECTION ( 'NONE',  ( -0.8660254038577466229, -7.065136648043377324E-14, -0.4999999998730267903 ) ) ;
#19027=ORIENTED_EDGE ( 'NONE', *, *, #6941, .F. ) ;
#19030=DIRECTION ( 'NONE',  ( 0.000000000000000000, 1.000000000000000000, 0.000000000000000000 ) ) ;
#19038=CARTESIAN_POINT ( 'NONE',  ( 9.775320280412000074, 2.527713920559999661, -6.969421869128999525 ) ) ;
#19039=CARTESIAN_POINT ( 'NONE',  ( 11.09999999999999964, 4.000000000000000000, 7.500000000000000000 ) ) ;
#19042=DIRECTION ( 'NONE',  ( 0.000000000000000000, 0.000000000000000000, 1.000000000000000000 ) ) ;
#19046=CARTESIAN_POINT ( 'NONE',  ( 8.962151703908455502, 2.270851035168802490, 7.235830473402728558 ) ) ;
#19048=ORIENTED_EDGE ( 'NONE', *, *, #66539, .T. ) ;
#19050=EDGE_CURVE ( 'NONE', #49079, #46011, #13322, .T. ) ;
#19056=CARTESIAN_POINT ( 'NONE',  ( 4.500000000000000000, 0.000000000000000000, 0.000000000000000000 ) ) ;
#19058=CARTESIAN_POINT ( 'NONE',  ( 10.22514748322308797, 2.649941783575544108, 7.500008211948054893 ) ) ;
#19061=CARTESIAN_POINT ( 'NONE',  ( 0.3276025866252778029, -2.044343127223234191, 2.661567956154585524 ) ) ;
#19062=CARTESIAN_POINT ( 'NONE',  ( 9.898726835366622012, 2.762657331216825884, -6.942781169495302329 ) ) ;
#19066=DIRECTION ( 'NONE',  ( -1.000000000000000000, 0.000000000000000000, 0.000000000000000000 ) ) ;
#19067=CARTESIAN_POINT ( 'NONE',  ( 7.550614158771000284, 4.468366666325000125, 8.882140983065999862 ) ) ;
#19071=CARTESIAN_POINT ( 'NONE',  ( 10.91574126908911069, 9.681045672762477849, 5.885333278431389203 ) ) ;
#19072=CARTESIAN_POINT ( 'NONE',  ( 10.57538794102195290, 5.349775832304656475, -7.676723066621553571 ) ) ;
#19073=CARTESIAN_POINT ( 'NONE',  ( 1.573890132540375131, 2.150913519912194705, 2.798833948393636639 ) ) ;
#19075=ORIENTED_EDGE ( 'NONE', *, *, #21853, .F. ) ;
#19078=ORIENTED_EDGE ( 'NONE', *, *, #6068, .T. ) ;
#19079=VECTOR ( 'NONE', #26862, 999.9999999999998863 ) ;
#19083=EDGE_CURVE ( 'NONE', #59297, #23381, #55617, .T. ) ;
#19085=CARTESIAN_POINT ( 'NONE',  ( 10.98934649328336732, 7.566743496310233574, -6.301340071414541555 ) ) ;
#19087=CARTESIAN_POINT ( 'NONE',  ( 9.225741355579115677, 4.497363567101849036, 9.030598125317942149 ) ) ;
#19103=CARTESIAN_POINT ( 'NONE',  ( 10.67500447327519097, 2.650284540010591439, 7.500001951671590561 ) ) ;
#19111=CARTESIAN_POINT ( 'NONE',  ( 10.48165121391000021, 4.022873529486999722, 9.090897232145000117 ) ) ;
#19113=CARTESIAN_POINT ( 'NONE',  ( 11.09999999999999964, 5.350000000000000533, -7.500000000000000000 ) ) ;
#19114=CARTESIAN_POINT ( 'NONE',  ( 8.938854719593997800, 5.597201461420000967, -8.171008079894999554 ) ) ;
#19115=CARTESIAN_POINT ( 'NONE',  ( 3.096752846175000240, -1.627991971746999944, 3.147629369397000332 ) ) ;
#19117=LINE ( 'NONE', #45699, #22761 ) ;
#19121=CARTESIAN_POINT ( 'NONE',  ( 10.90374609491999891, 3.726846467344000047, 5.900456154266000119 ) ) ;
#19124=CARTESIAN_POINT ( 'NONE',  ( 11.08492721656000057, 3.668390701878999849, 5.558148445539999649 ) ) ;
#19127=CARTESIAN_POINT ( 'NONE',  ( 10.93529823098193710, 2.837224294051361451, -6.734948068539347688 ) ) ;
#19131=B_SPLINE_CURVE_WITH_KNOTS ( 'NONE', 3,
 ( #53527, #47252, #5619, #16115, #63309, #68555, #16795, #37785, #20677, #47939, #26960, #15436, #37440, #58762, #11213, #26272 ),
 .UNSPECIFIED., .F., .F.,
 ( 4, 2, 2, 2, 2, 2, 2, 4 ),
 ( 0.1254233535197428473, 0.2190668680422942494, 0.3127103825648456237, 0.4999974116099478172, 0.5936409261324988584, 0.6872844406550501217, 0.7809279551776012740, 0.8745714697001524263 ),
 .UNSPECIFIED. ) ;
#19133=CARTESIAN_POINT ( 'NONE',  ( 8.119711571783735593, 5.029157459567885624, -6.453063860975558619 ) ) ;
#19138=B_SPLINE_CURVE_WITH_KNOTS ( 'NONE', 3,
 ( #33183, #1025, #49601, #2061, #6250 ),
 .UNSPECIFIED., .F., .F.,
 ( 4, 1, 4 ),
 ( 0.000000000000000000, 0.5000000000000000000, 1.000000000000000000 ),
 .UNSPECIFIED. ) ;
#19149=CARTESIAN_POINT ( 'NONE',  ( 1.384306799207333460, -1.762666431298145930, -3.058252359239904905 ) ) ;
#19155=FACE_OUTER_BOUND ( 'NONE', #4524, .T. ) ;
#19169=CARTESIAN_POINT ( 'NONE',  ( 8.356920280409999791, 4.851303550474000303, -9.008742670124000540 ) ) ;
#19173=EDGE_CURVE ( 'NONE', #718, #2928, #36252, .T. ) ;
#19175=CARTESIAN_POINT ( 'NONE',  ( 9.234510841229999656, 5.964723767581000757, 7.776480083716999836 ) ) ;
#19181=CARTESIAN_POINT ( 'NONE',  ( 10.97499895057999986, -3.730349362740999292E-14, -9.259260025373999922E-14 ) ) ;
#19186=LINE ( 'NONE', #51349, #26560 ) ;
#19192=B_SPLINE_CURVE_WITH_KNOTS ( 'NONE', 3,
 ( #17577, #50083, #12677, #16873 ),
 .UNSPECIFIED., .F., .F.,
 ( 4, 4 ),
 ( 0.8745808026672123869, 1.000000000000000000 ),
 .UNSPECIFIED. ) ;
#19193=FACE_OUTER_BOUND ( 'NONE', #61397, .T. ) ;
#19197=VECTOR ( 'NONE', #373, 1000.000000000000000 ) ;
#19199=CARTESIAN_POINT ( 'NONE',  ( 7.986083034292075666, 5.349307872168524547, 7.676713696079059623 ) ) ;
#19200=CARTESIAN_POINT ( 'NONE',  ( 10.56590837162999996, 5.293226105229999590, -7.067087619452999903 ) ) ;
#19204=CARTESIAN_POINT ( 'NONE',  ( 9.538432183420001209, 5.620896541217999420, 7.423100299691999915 ) ) ;
#19209=CARTESIAN_POINT ( 'NONE',  ( 11.14994211610999919, 2.627136771666999771, 6.696094414592000277 ) ) ;
#19213=CARTESIAN_POINT ( 'NONE',  ( 8.957392219593000249, 2.678331728353000152, 8.735281589464001684 ) ) ;
#19214=CARTESIAN_POINT ( 'NONE',  ( 10.53138775541999905, 5.607751175212000838, 7.280102404048999887 ) ) ;
#19217=ORIENTED_EDGE ( 'NONE', *, *, #24474, .F. ) ;
#19218=CARTESIAN_POINT ( 'NONE',  ( 9.874770280412001000, 4.038835765825999680, -5.935509327774999733 ) ) ;
#19225=ORIENTED_EDGE ( 'NONE', *, *, #20355, .F. ) ;
#19226=VECTOR ( 'NONE', #12826, 1000.000000000000000 ) ;
#19227=CARTESIAN_POINT ( 'NONE',  ( 2.249566109761000465, -3.577811800725999802, 1.152232014823999950 ) ) ;
#19230=CARTESIAN_POINT ( 'NONE',  ( 5.500000000000000000, -12.78667792605000031, -2.345384795463000049 ) ) ;
#19232=CARTESIAN_POINT ( 'NONE',  ( 10.12671450658999994, 3.117528978489000124, 8.613535509676999880 ) ) ;
#19233=CARTESIAN_POINT ( 'NONE',  ( 10.99999999997000089, 4.000000000000000000, -7.500000000000000000 ) ) ;
#19238=CARTESIAN_POINT ( 'NONE',  ( 7.737829719589999655, 5.687206835507000235, 6.847268999608999707 ) ) ;
#19243=CARTESIAN_POINT ( 'NONE',  ( 1.600201902857000036, 0.7023893950988999713, -3.352829814747000370 ) ) ;
#19244=VERTEX_POINT ( 'NONE', #35667 ) ;
#19245=CARTESIAN_POINT ( 'NONE',  ( 1.477094749129042706, -2.689122896592814449, 1.917576298700700566 ) ) ;
#19248=CARTESIAN_POINT ( 'NONE',  ( 10.87148757351999961, 5.567567343464999929, 7.772413227960999649 ) ) ;
#19254=CARTESIAN_POINT ( 'NONE',  ( 10.36180282788866691, 2.874603711589695187, -6.749639981055123528 ) ) ;
#19258=CARTESIAN_POINT ( 'NONE',  ( 8.579017984034141620, 4.083608998234213416, 5.755606773672980125 ) ) ;
#19265=CARTESIAN_POINT ( 'NONE',  ( 4.149992563292000725, 0.5234817089163691373, -1.947893036340042405 ) ) ;
#19266=CARTESIAN_POINT ( 'NONE',  ( 6.899999691988000450, 11.00717859340000082, 1.432487142323000118 ) ) ;
#19267=CARTESIAN_POINT ( 'NONE',  ( 9.538432183420001209, 5.620896541217999420, 7.423100299691999915 ) ) ;
#19273=B_SPLINE_CURVE_WITH_KNOTS ( 'NONE', 3,
 ( #20941, #53096, #10784, #295, #37023, #68469, #42273, #26189, #37358, #53442 ),
 .UNSPECIFIED., .F., .F.,
 ( 4, 2, 2, 2, 4 ),
 ( 0.000000000000000000, 0.2038808316443378454, 0.4077616632886756909, 0.6116424949330134808, 0.8155233265773513818 ),
 .UNSPECIFIED. ) ;
#19276=ORIENTED_EDGE ( 'NONE', *, *, #59925, .F. ) ;
#19294=CARTESIAN_POINT ( 'NONE',  ( 8.489029163847876092, 3.089100507813340446, 6.099830711550906059 ) ) ;
#19295=AXIS2_PLACEMENT_3D ( 'NONE', #28223, #32780, #27531 ) ;
#19296=CARTESIAN_POINT ( 'NONE',  ( 8.865073590557452476, 2.650142864597553327, -7.500004675916596142 ) ) ;
#19305=CARTESIAN_POINT ( 'NONE',  ( 7.766851002543999627, 2.832432432432000269, 6.822293592207000934 ) ) ;
#19307=DIRECTION ( 'NONE',  ( -1.000000000000000000, 0.000000000000000000, 0.000000000000000000 ) ) ;
#19311=EDGE_CURVE ( 'NONE', #29486, #53731, #36002, .T. ) ;
#19318=B_SPLINE_CURVE_WITH_KNOTS ( 'NONE', 3,
 ( #8881, #30216, #63023, #62018 ),
 .UNSPECIFIED., .F., .F.,
 ( 4, 4 ),
 ( 0.000000000000000000, 0.1254192006116268687 ),
 .UNSPECIFIED. ) ;
#19320=AXIS2_PLACEMENT_3D ( 'NONE', #68136, #14335, #69173 ) ;
#19338=CARTESIAN_POINT ( 'NONE',  ( 8.175739158770999992, 4.686731264770999772, -8.717075579553000608 ) ) ;
#19349=CARTESIAN_POINT ( 'NONE',  ( 9.111654719595000174, 4.989193221215000307, -6.287302145481000082 ) ) ;
#19355=EDGE_LOOP ( 'NONE', ( #3907, #26001, #5812, #62593 ) ) ;
#19356=CARTESIAN_POINT ( 'NONE',  ( 7.809591065053155923, 2.953469884859488470, -8.377395465226323168 ) ) ;
#19358=CARTESIAN_POINT ( 'NONE',  ( 9.784179719593000257, 4.042991257420999851, -5.768106221333000327 ) ) ;
#19360=CARTESIAN_POINT ( 'NONE',  ( 10.23643409129999959, 5.517148499152000340, -6.754126239302999934 ) ) ;
#19365=EDGE_CURVE ( 'NONE', #63876, #8401, #30240, .T. ) ;
#19372=CARTESIAN_POINT ( 'NONE',  ( 10.57657334123000048, 5.344886503256999433, -7.298885378918000377 ) ) ;
#19381=ORIENTED_EDGE ( 'NONE', *, *, #59446, .T. ) ;
#19382=CARTESIAN_POINT ( 'NONE',  ( 10.02394528041000044, 5.481267232667000222, -8.005061172455999241 ) ) ;
#19383=CARTESIAN_POINT ( 'NONE',  ( 7.100083736560635295, 0.3076767997638333307, 3.048821334907659608 ) ) ;
#19389=CARTESIAN_POINT ( 'NONE',  ( 9.004177925655991288, 2.621319625803172126, 6.376254879885641103 ) ) ;
#19399=CARTESIAN_POINT ( 'NONE',  ( 7.954101906406737754, 4.935753437653367826, 6.415772546196833126 ) ) ;
#19400=CARTESIAN_POINT ( 'NONE',  ( 5.000030787343000327, 2.099962892530999881, 0.000000000000000000 ) ) ;
#19402=CARTESIAN_POINT ( 'NONE',  ( 8.414360841228999632, 5.461114003844000031, -8.582501063019000398 ) ) ;
#19405=FACE_OUTER_BOUND ( 'NONE', #62405, .T. ) ;
#19406=DIRECTION ( 'NONE',  ( -0.7071074674731144816, -0.7071060948993143080, 1.718725578913035619E-08 ) ) ;
#19407=CARTESIAN_POINT ( 'NONE',  ( 0.2879790830606807628, 0.4312571902316706951, 3.287958384590494276 ) ) ;
#19408=CARTESIAN_POINT ( 'NONE',  ( 2.251972330171000181, 2.697882917481999598, -1.828095362927000034 ) ) ;
#19411=B_SPLINE_CURVE_WITH_KNOTS ( 'NONE', 3,
 ( #25974, #41021, #45923, #67577, #3271, #25285, #31231, #35440, #46619, #51506 ),
 .UNSPECIFIED., .F., .F.,
 ( 4, 1, 1, 1, 1, 1, 1, 4 ),
 ( 0.000000000000000000, 0.06214647846548406601, 0.2363167115191955048, 0.4104869445722291177, 0.5846571776259398279, 0.7588274106789726359, 0.9329976437320062210, 1.000000000000000000 ),
 .UNSPECIFIED. ) ;
#19414=CARTESIAN_POINT ( 'NONE',  ( 7.999926658772999133, 5.198556077301000222, 8.332552905512999430 ) ) ;
#19419=CARTESIAN_POINT ( 'NONE',  ( 10.99020523659462079, 7.555164107387456696, 6.307848186994561956 ) ) ;
#19421=CARTESIAN_POINT ( 'NONE',  ( 1.740556799206375294, -3.500000000000003109, 0.4581489286484972667 ) ) ;
#19425=EDGE_CURVE ( 'NONE', #26212, #36211, #29594, .T. ) ;
#19427=ORIENTED_EDGE ( 'NONE', *, *, #53660, .T. ) ;
#19431=ORIENTED_EDGE ( 'NONE', *, *, #31349, .T. ) ;
#19434=CARTESIAN_POINT ( 'NONE',  ( 8.351820280410001018, 4.901484321470999994, -8.891682961388999829 ) ) ;
#19435=CARTESIAN_POINT ( 'NONE',  ( 9.674960421382234443, 2.650268802166420024, 7.499999178247376719 ) ) ;
#19437=ORIENTED_EDGE ( 'NONE', *, *, #35446, .F. ) ;
#19443=DIRECTION ( 'NONE',  ( 0.000000000000000000, -0.9565994702956990281, -0.2914059941558995726 ) ) ;
#19446=EDGE_CURVE ( 'NONE', #9641, #36464, #64598, .T. ) ;
#19450=CARTESIAN_POINT ( 'NONE',  ( 3.167640132544333742, -1.762666431298160141, 3.058252359239895579 ) ) ;
#19458=CARTESIAN_POINT ( 'NONE',  ( 10.76010575649000067, 4.535386075958999896, 6.001721352166000223 ) ) ;
#19459=DIRECTION ( 'NONE',  ( 0.000000000000000000, -0.9916377111174247139, 0.1290528957048031888 ) ) ;
#19460=CARTESIAN_POINT ( 'NONE',  ( 9.137754719594999742, 2.319062457810000311, -7.919229449146000022 ) ) ;
#19461=CARTESIAN_POINT ( 'NONE',  ( 2.551832320967999834, 0.3084989455321000551, 3.530262701594000241 ) ) ;
#19464=FACE_OUTER_BOUND ( 'NONE', #41866, .T. ) ;
#19471=CARTESIAN_POINT ( 'NONE',  ( 9.352253013669001191, 2.817757427878999632, 6.388459691516000127 ) ) ;
#19483=CARTESIAN_POINT ( 'NONE',  ( 0.2309807866890836170, 0.4165353540672909194, -3.230960454924427072 ) ) ;
#19491=ORIENTED_EDGE ( 'NONE', *, *, #5823, .F. ) ;
#19492=VECTOR ( 'NONE', #20721, 999.9999999999998863 ) ;
#19497=CARTESIAN_POINT ( 'NONE',  ( 10.01676721958999927, 4.324998751150999965, -9.154078823942999321 ) ) ;
#19499=CARTESIAN_POINT ( 'NONE',  ( 1.353056799207333460, -2.798833948393629534, -2.150913519912204031 ) ) ;
#19503=DIRECTION ( 'NONE',  ( 0.000000000000000000, 1.000000000000000000, 0.000000000000000000 ) ) ;
#19510=ORIENTED_EDGE ( 'NONE', *, *, #39965, .F. ) ;
#19522=CARTESIAN_POINT ( 'NONE',  ( 7.667607780408999929, 5.638704226117999596, 8.266404648244000342 ) ) ;
#19524=CARTESIAN_POINT ( 'NONE',  ( 7.487876381280277549, 5.349293767872230099, 7.706633529874828525 ) ) ;
#19539=ADVANCED_FACE ( 'NONE', ( #13915 ), #39166, .T. ) ;
#19549=CARTESIAN_POINT ( 'NONE',  ( 9.949437606643998677, 2.508497579857000392, -7.171862210735000076 ) ) ;
#19554=CARTESIAN_POINT ( 'NONE',  ( 10.90374609491999891, 3.726846467344000047, 5.900456154266000119 ) ) ;
#19556=EDGE_LOOP ( 'NONE', ( #53445, #17636, #52623, #26476, #35881 ) ) ;
#19559=CARTESIAN_POINT ( 'NONE',  ( 11.18484176840999922, 2.599663474744000169, 7.740674686800000259 ) ) ;
#19564=CARTESIAN_POINT ( 'NONE',  ( 9.085767219592000288, 2.821863697211000055, 6.127145479358000024 ) ) ;
#19565=ADVANCED_FACE ( 'NONE', ( #59296 ), #44191, .F. ) ;
#19566=CARTESIAN_POINT ( 'NONE',  ( 10.68403803949000164, 5.436614310638000269, 8.578436083822998270 ) ) ;
#19568=EDGE_LOOP ( 'NONE', ( #21947, #17661, #19027, #18490, #39610, #28117 ) ) ;
#19569=CARTESIAN_POINT ( 'NONE',  ( 9.725595280412999699, 2.495531372253999791, -7.930944806125000746 ) ) ;
#19571=EDGE_CURVE ( 'NONE', #26471, #4832, #48765, .T. ) ;
#19580=CARTESIAN_POINT ( 'NONE',  ( 0.9780474580060999346, 3.010927365844000114, -1.992372462812000089 ) ) ;
#19591=CARTESIAN_POINT ( 'NONE',  ( 7.443295280410000103, 4.698356649019999942, 8.789431186081998248 ) ) ;
#19597=CARTESIAN_POINT ( 'NONE',  ( 1.647883852297000074, 2.470933839010999833, -2.372615558983000472 ) ) ;
#19599=CARTESIAN_POINT ( 'NONE',  ( 1.572458648010261806, -2.764615070225285631, -1.807037445058709224 ) ) ;
#19603=CARTESIAN_POINT ( 'NONE',  ( 11.09425120759000016, 2.431871068503000277, 7.769513029648000391 ) ) ;
#19606=CARTESIAN_POINT ( 'NONE',  ( 10.94076550314999885, 5.140765503144999471, -6.571291218949999902 ) ) ;
#19608=DIRECTION ( 'NONE',  ( 0.8480635683783770418, 0.000000000000000000, -0.5298945026977860406 ) ) ;
#19609=CARTESIAN_POINT ( 'NONE',  ( 7.572196646342158388, 3.914246498630762350, 5.749145437917528412 ) ) ;
#19610=ORIENTED_EDGE ( 'NONE', *, *, #14410, .F. ) ;
#19613=ORIENTED_EDGE ( 'NONE', *, *, #14825, .F. ) ;
#19616=LINE ( 'NONE', #2167, #65084 ) ;
#19618=CARTESIAN_POINT ( 'NONE',  ( 9.075483283097998566, 4.020836891789999257, 8.948690653012000951 ) ) ;
#19619=CARTESIAN_POINT ( 'NONE',  ( 10.89218604104999955, 2.661903984162000469, -8.236033286991000679 ) ) ;
#19627=CARTESIAN_POINT ( 'NONE',  ( 8.111573341229000533, 3.326263523254000098, 8.794511546544999447 ) ) ;
#19632=FACE_OUTER_BOUND ( 'NONE', #5744, .T. ) ;
#19634=CARTESIAN_POINT ( 'NONE',  ( 9.813871383455010644, 10.26951666917000061, 4.796847285345002376 ) ) ;
#19640=CARTESIAN_POINT ( 'NONE',  ( 5.500000000000000000, 6.217248937900999058E-14, -12.99999854704996238 ) ) ;
#19641=VERTEX_POINT ( 'NONE', #27677 ) ;
#19648=VECTOR ( 'NONE', #7672, 1000.000000000000000 ) ;
#19650=CARTESIAN_POINT ( 'NONE',  ( -0.01901103192377000262, -0.5398464557615000325, -3.496157131901000081 ) ) ;
#19651=DIRECTION ( 'NONE',  ( 0.000000000000000000, 0.000000000000000000, -1.000000000000000000 ) ) ;
#19656=EDGE_CURVE ( 'NONE', #11774, #46140, #39246, .T. ) ;
#19658=CARTESIAN_POINT ( 'NONE',  ( 10.45625165877000029, 3.661871102473000406, -9.317475234260999883 ) ) ;
#19665=CARTESIAN_POINT ( 'NONE',  ( 9.350955436992014924, 5.758048718045908565, -7.748523603980665087 ) ) ;
#19671=ORIENTED_EDGE ( 'NONE', *, *, #43970, .F. ) ;
#19672=ADVANCED_FACE ( 'NONE', ( #42456 ), #47361, .F. ) ;
#19689=CARTESIAN_POINT ( 'NONE',  ( 11.10000006013000018, 9.802256759419000431, 6.071885733684999842 ) ) ;
#19690=CARTESIAN_POINT ( 'NONE',  ( 2.350788447235875545, -1.095349359437870262, -3.341294758621923489 ) ) ;
#19691=CARTESIAN_POINT ( 'NONE',  ( 8.672989158774999652, 4.728328492779000136, -8.692725459657999920 ) ) ;
#19693=ORIENTED_EDGE ( 'NONE', *, *, #37469, .F. ) ;
#19699=CARTESIAN_POINT ( 'NONE',  ( 2.780140132544583587, -3.408904368339108260, 0.9161175952574674985 ) ) ;
#19700=CARTESIAN_POINT ( 'NONE',  ( 8.795585841232000490, 5.251032986819000214, -6.070151079272999795 ) ) ;
#19708=CARTESIAN_POINT ( 'NONE',  ( 8.367589158771000513, 5.461114003844000031, -8.582501063019000398 ) ) ;
#19710=CARTESIAN_POINT ( 'NONE',  ( 10.75911768454999873, 4.477564074640000058, -5.708570851020999370 ) ) ;
#19712=ORIENTED_EDGE ( 'NONE', *, *, #54552, .F. ) ;
#19718=CARTESIAN_POINT ( 'NONE',  ( 9.883148997457000817, 5.167567567567999731, 6.822293592207000934 ) ) ;
#19719=VERTEX_POINT ( 'NONE', #22412 ) ;
#19720=CARTESIAN_POINT ( 'NONE',  ( 8.032988339672121114, 4.532664226843759359, -6.238162434079100649 ) ) ;
#19721=CYLINDRICAL_SURFACE ( 'NONE', #15045, 12.50000000000000000 ) ;
#19728=ORIENTED_EDGE ( 'NONE', *, *, #6293, .F. ) ;
#19730=CARTESIAN_POINT ( 'NONE',  ( 10.06481084123000080, 5.336630274082000192, -7.092011739486999922 ) ) ;
#19732=DIRECTION ( 'NONE',  ( -1.000000000000000000, 0.000000000000000000, 0.000000000000000000 ) ) ;
#19737=CARTESIAN_POINT ( 'NONE',  ( 7.890669420221000152, 4.660296061153999858, 6.322498784873999078 ) ) ;
#19742=VERTEX_POINT ( 'NONE', #11928 ) ;
#19754=EDGE_CURVE ( 'NONE', #31394, #34575, #12286, .T. ) ;
#19755=CARTESIAN_POINT ( 'NONE',  ( 9.188234083221754389, 2.648243641808995630, 7.263637137173954983 ) ) ;
#19764=CARTESIAN_POINT ( 'NONE',  ( 7.099999886593999499, -12.39999890530000037, 0.000000000000000000 ) ) ;
#19766=CARTESIAN_POINT ( 'NONE',  ( 0.6780453033732724011, -2.141412704026376623, 2.806277474037436992 ) ) ;
#19773=VERTEX_POINT ( 'NONE', #22762 ) ;
#19777=VERTEX_POINT ( 'NONE', #28368 ) ;
#19778=CARTESIAN_POINT ( 'NONE',  ( 8.267367474942998840, 3.071849710027000135, -6.244583336620999958 ) ) ;
#19779=DIRECTION ( 'NONE',  ( -1.231068759215981725E-07, 1.236409737982979503E-07, -0.9999999999999849010 ) ) ;
#19780=CARTESIAN_POINT ( 'NONE',  ( 7.242439158769000684, 3.554387346680000004, -8.824570035521999145 ) ) ;
#19782=CARTESIAN_POINT ( 'NONE',  ( 10.18823075089156660, 2.651244971521983906, 7.275526744220880637 ) ) ;
#19791=CARTESIAN_POINT ( 'NONE',  ( 7.959096408387808630, 3.398144457071999636, -6.280823960497042613 ) ) ;
#19795=EDGE_CURVE ( 'NONE', #44553, #43316, #40844, .T. ) ;
#19796=CARTESIAN_POINT ( 'NONE',  ( 8.687922088694000067, 3.419384128876999718, -5.860036257779999147 ) ) ;
#19798=EDGE_CURVE ( 'NONE', #49517, #19773, #35894, .T. ) ;
#19803=CARTESIAN_POINT ( 'NONE',  ( 3.427149063888667246, 0.04771112035505382237, -3.543401238238605533 ) ) ;
#19805=CARTESIAN_POINT ( 'NONE',  ( 10.92717848204000042, 5.023653513500000223, 8.718036113327999104 ) ) ;
#19806=DIRECTION ( 'NONE',  ( 0.000000000000000000, 1.000000000000000000, 0.000000000000000000 ) ) ;
#19807=CARTESIAN_POINT ( 'NONE',  ( 8.830545280412000153, 3.207599814920999659, -6.150466394809999571 ) ) ;
#19808=CARTESIAN_POINT ( 'NONE',  ( 3.557839444424999886, 0.04138239269183999897, 3.543466380272000116 ) ) ;
#19814=CARTESIAN_POINT ( 'NONE',  ( 3.103056799211125316, 2.798833948393625981, 2.150913519912208471 ) ) ;
#19817=PLANE ( 'NONE',  #35504 ) ;
#19818=CARTESIAN_POINT ( 'NONE',  ( 9.629022744239000176, 5.794335169544999609, 7.414871903737999759 ) ) ;
#19832=CARTESIAN_POINT ( 'NONE',  ( 3.999985533191000364, -6.914809019160056625E-16, -2.149963194831858715 ) ) ;
#19833=CARTESIAN_POINT ( 'NONE',  ( 5.000030787343000327, -1.834918991542628053, -1.057581170753189692 ) ) ;
#19834=EDGE_LOOP ( 'NONE', ( #1614, #9773, #31573, #17451, #8047 ) ) ;
#19835=AXIS2_PLACEMENT_3D ( 'NONE', #49689, #60873, #39203 ) ;
#19839=CARTESIAN_POINT ( 'NONE',  ( 10.97819528041000048, 5.476824759564999923, -7.128718425160999850 ) ) ;
#19846=CARTESIAN_POINT ( 'NONE',  ( 9.753242276648803610, 2.714773723612766254, 7.027402982326849568 ) ) ;
#19849=FACE_OUTER_BOUND ( 'NONE', #55437, .T. ) ;
#19858=LINE ( 'NONE', #25791, #27512 ) ;
#19859=CARTESIAN_POINT ( 'NONE',  ( 2.550973465877000024, 3.500000000000000000, 0.000000000000000000 ) ) ;
#19863=AXIS2_PLACEMENT_3D ( 'NONE', #8442, #61922, #7753 ) ;
#19865=CARTESIAN_POINT ( 'NONE',  ( 7.330281674562000305, 4.426928431836000044, 9.293321981113999541 ) ) ;
#19875=CARTESIAN_POINT ( 'NONE',  ( 6.684036528646004172, 10.47948907923000306, -4.649236476274002605 ) ) ;
#19885=VERTEX_POINT ( 'NONE', #50380 ) ;
#19886=VERTEX_POINT ( 'NONE', #46167 ) ;
#19891=CARTESIAN_POINT ( 'NONE',  ( 9.819565861057999001, 2.688248842995000221, -7.873038103423000145 ) ) ;
#19892=CARTESIAN_POINT ( 'NONE',  ( 8.623804163831874092, 4.944546604654881605, 6.045403407478842084 ) ) ;
#19895=CARTESIAN_POINT ( 'NONE',  ( 9.137543006348998631, 2.995704926864999784, 8.544754656710999541 ) ) ;
#19899=CARTESIAN_POINT ( 'NONE',  ( 9.471374412057000924, 2.030666183831999927, 7.549764512038000142 ) ) ;
#19901=CARTESIAN_POINT ( 'NONE',  ( 9.778460659405999067, 5.743717947473999885, 7.748300625457000379 ) ) ;
#19905=CARTESIAN_POINT ( 'NONE',  ( 9.383148997457999130, 5.167567567567999731, 6.822293592207000934 ) ) ;
#19909=CARTESIAN_POINT ( 'NONE',  ( 8.802614158774000330, 3.975069902178000270, 9.483774112875002160 ) ) ;
#19910=CARTESIAN_POINT ( 'NONE',  ( 10.24961997674000003, 4.184221916050000267, 9.286882020979000174 ) ) ;
#19913=CARTESIAN_POINT ( 'NONE',  ( 9.088029719595001055, 2.881930053949999682, -8.823338183322999129 ) ) ;
#19915=CARTESIAN_POINT ( 'NONE',  ( 8.945154276125844461, 5.350566776863566965, 7.852883605855088156 ) ) ;
#19917=CARTESIAN_POINT ( 'NONE',  ( 10.93769906950999982, 5.063122007744000008, 4.920829195600999739 ) ) ;
#19920=CARTESIAN_POINT ( 'NONE',  ( 1.438972969266999913, 1.794790469053999971, -3.302590565797000277 ) ) ;
#19924=CARTESIAN_POINT ( 'NONE',  ( 8.822164158776001130, 2.644017913812000131, -7.838184857420000817 ) ) ;
#19928=ADVANCED_FACE ( 'NONE', ( #61897 ), #28718, .T. ) ;
#19932=CARTESIAN_POINT ( 'NONE',  ( 4.074968078372999791, 0.000000000000000000, 0.000000000000000000 ) ) ;
#19934=ORIENTED_EDGE ( 'NONE', *, *, #52979, .F. ) ;
#19935=CARTESIAN_POINT ( 'NONE',  ( 9.475899447075999404, 4.122021000979000149, 9.013569734175000292 ) ) ;
#19941=CARTESIAN_POINT ( 'NONE',  ( 2.172385296145999956, 2.895272466935999933, -1.424404891072999835 ) ) ;
#19943=CARTESIAN_POINT ( 'NONE',  ( 0.8572294063981078516, 1.740182405912205521, 2.807159848119936463 ) ) ;
#19946=CARTESIAN_POINT ( 'NONE',  ( 9.889842476439000052, 4.052276433608000161, 9.260531940735001299 ) ) ;
#19948=CIRCLE ( 'NONE', #12106, 13.10000000000000320 ) ;
#19958=CARTESIAN_POINT ( 'NONE',  ( 5.449999267937000624, 2.451372438371999805E-13, 6.461498003317998333E-14 ) ) ;
#19963=CARTESIAN_POINT ( 'NONE',  ( 10.49785886974000171, 3.776281431161999880, 5.717632172928999168 ) ) ;
#19964=B_SPLINE_CURVE_WITH_KNOTS ( 'NONE', 3,
 ( #7978, #66346, #55526, #49586, #29312, #50625, #50966, #12881, #23012, #3064, #2726, #24049, #34210, #23365, #45384, #66694, #40141, #67035 ),
 .UNSPECIFIED., .F., .F.,
 ( 4, 2, 2, 2, 2, 2, 2, 2, 4 ),
 ( 0.000000000000000000, 0.1250000000000000000, 0.2500000000000000000, 0.3750000000000000000, 0.5000000000000000000, 0.6250000000000000000, 0.7500000000000000000, 0.8750000000000000000, 1.000000000000000000 ),
 .UNSPECIFIED. ) ;
#19965=CARTESIAN_POINT ( 'NONE',  ( 10.86493304757000011, 4.678466548873998931, -9.048467117372998914 ) ) ;
#19968=ADVANCED_FACE ( 'NONE', ( #14356 ), #14011, .T. ) ;
#19972=EDGE_CURVE ( 'NONE', #44831, #28207, #60867, .T. ) ;
#19975=VERTEX_POINT ( 'NONE', #44798 ) ;
#19978=DIRECTION ( 'NONE',  ( 0.8843050097021329936, -0.1786785991674020024, 0.4313682974156600181 ) ) ;
#19995=CARTESIAN_POINT ( 'NONE',  ( 8.039443364739069509, 4.176885327615297960, 8.849067469250631035 ) ) ;
#19999=CARTESIAN_POINT ( 'NONE',  ( 9.785239991807605620, 4.544749735012262093, -8.875846220998239389 ) ) ;
#20000=CARTESIAN_POINT ( 'NONE',  ( 10.50897971959000010, 4.485029564998000318, -9.114435267298000909 ) ) ;
#20002=CARTESIAN_POINT ( 'NONE',  ( 10.10331523854997293, 3.090216591177149752, 8.647999319121542072 ) ) ;
#20004=CARTESIAN_POINT ( 'NONE',  ( 8.780141893066772951, 2.899999999999999911, -6.457321861693552378 ) ) ;
#20012=CARTESIAN_POINT ( 'NONE',  ( 9.332537864288001472, 2.899999999999999911, 6.571291218949999902 ) ) ;
#20015=VERTEX_POINT ( 'NONE', #15724 ) ;
#20026=LINE ( 'NONE', #41352, #22119 ) ;
#20031=CARTESIAN_POINT ( 'NONE',  ( 9.568039158772000619, 5.336630274082000192, -7.092011739486999922 ) ) ;
#20034=CARTESIAN_POINT ( 'NONE',  ( 3.999999999999999112, 2.081773110051107878, 0.5564988119414340240 ) ) ;
#20037=CARTESIAN_POINT ( 'NONE',  ( 8.570375340018618004, 3.646757250303513054, 8.848425586001186005 ) ) ;
#20039=CARTESIAN_POINT ( 'NONE',  ( 4.149992563292000725, -1.007210908820211026, -1.747525841223985132 ) ) ;
#20043=CARTESIAN_POINT ( 'NONE',  ( 8.455992358796999397, 2.899999999999999911, -6.571291218954000257 ) ) ;
#20044=ORIENTED_EDGE ( 'NONE', *, *, #28320, .T. ) ;
#20047=CARTESIAN_POINT ( 'NONE',  ( 9.684729719592999331, 2.370176859044999862, -6.912649125838000508 ) ) ;
#20048=ORIENTED_EDGE ( 'NONE', *, *, #36136, .F. ) ;
#20051=CARTESIAN_POINT ( 'NONE',  ( 10.78637067803999905, 5.666041748529999644, -7.787005432561999285 ) ) ;
#20062=CARTESIAN_POINT ( 'NONE',  ( 11.03092334123000029, 5.020455242919999783, -6.601201971309999195 ) ) ;
#20065=CYLINDRICAL_SURFACE ( 'NONE', #22687, 1.350000000000000533 ) ;
#20072=CARTESIAN_POINT ( 'NONE',  ( 9.675870280412999236, 3.031907308384000022, -8.729608011560001657 ) ) ;
#20079=CARTESIAN_POINT ( 'NONE',  ( 8.625941929927966711, 5.035312777410744900, 6.089150065163800640 ) ) ;
#20082=LINE ( 'NONE', #68651, #43647 ) ;
#20087=ADVANCED_FACE ( 'NONE', ( #62575 ), #42306, .F. ) ;
#20089=CARTESIAN_POINT ( 'NONE',  ( 10.14206215041823000, 3.293869621293751937, 8.705460445251068435 ) ) ;
#20091=VECTOR ( 'NONE', #14291, 1000.000000000000000 ) ;
#20092=CARTESIAN_POINT ( 'NONE',  ( 6.899999691988000450, -12.43893545635000031, 2.828937028792000152 ) ) ;
#20095=CARTESIAN_POINT ( 'NONE',  ( 0.3672260901898748431, -3.367204892844285258, 0.4416305338764572319 ) ) ;
#20097=CARTESIAN_POINT ( 'NONE',  ( 2.442700127934999799, -0.7445022475760999514, 3.172853915553000004 ) ) ;
#20098=ORIENTED_EDGE ( 'NONE', *, *, #64541, .T. ) ;
#20101=LINE ( 'NONE', #56824, #26469 ) ;
#20102=LINE ( 'NONE', #14859, #46853 ) ;
#20103=CARTESIAN_POINT ( 'NONE',  ( 10.11501430098066656, 5.350017391163124358, -7.499999134156894343 ) ) ;
#20104=VERTEX_POINT ( 'NONE', #26565 ) ;
#20113=ORIENTED_EDGE ( 'NONE', *, *, #21000, .T. ) ;
#20116=CARTESIAN_POINT ( 'NONE',  ( 0.000000000000000000, 5.100000000000000533, -7.500000000000000000 ) ) ;
#20118=CARTESIAN_POINT ( 'NONE',  ( -1.222471984994595150E-05, -9.327013418423733093E-16, -2.899969545326207765 ) ) ;
#20119=CARTESIAN_POINT ( 'NONE',  ( 9.150683505092615633, 4.457228368748805458, 8.907085139201905477 ) ) ;
#20120=CARTESIAN_POINT ( 'NONE',  ( 6.695464158771000207, 4.367071440064000498, -8.848478693904000991 ) ) ;
#20123=ORIENTED_EDGE ( 'NONE', *, *, #19571, .F. ) ;
#20124=CARTESIAN_POINT ( 'NONE',  ( 2.042640132539832898, 3.058252359239899132, 1.762666431298154146 ) ) ;
#20129=ORIENTED_EDGE ( 'NONE', *, *, #43929, .F. ) ;
#20132=CARTESIAN_POINT ( 'NONE',  ( 8.296555885771999428, 2.897911263815999838, 6.617317042653000136 ) ) ;
#20134=CARTESIAN_POINT ( 'NONE',  ( 10.95791822924240577, 2.260523080717695699, 7.333870556128064599 ) ) ;
#20136=CARTESIAN_POINT ( 'NONE',  ( 4.600001223043999943, -13.10000000000000142, 0.000000000000000000 ) ) ;
#20137=CARTESIAN_POINT ( 'NONE',  ( 10.93499869900965038, 5.068606067930488734, -4.937945806540904314 ) ) ;
#20141=CARTESIAN_POINT ( 'NONE',  ( 3.351443705081666558, -2.857319464356316896, -2.096114062919034904 ) ) ;
#20142=VERTEX_POINT ( 'NONE', #48916 ) ;
#20143=CARTESIAN_POINT ( 'NONE',  ( 10.14750576281000072, 2.602962605360999770, 6.738577830910999822 ) ) ;
#20144=EDGE_CURVE ( 'NONE', #18982, #57692, #64634, .T. ) ;
#20145=AXIS2_PLACEMENT_3D ( 'NONE', #48358, #64080, #54992 ) ;
#20146=PLANE ( 'NONE',  #2098 ) ;
#20147=DIRECTION ( 'NONE',  ( 0.000000000000000000, 0.8648648648648717963, 0.5020047465136829867 ) ) ;
#20148=CARTESIAN_POINT ( 'NONE',  ( 3.474005517471000282, 3.100289412622999841, 1.716429986814999920 ) ) ;
#20153=ORIENTED_EDGE ( 'NONE', *, *, #16388, .F. ) ;
#20155=CARTESIAN_POINT ( 'NONE',  ( 10.31746213571000048, 5.100000000000000533, 6.571291218949999902 ) ) ;
#20158=CARTESIAN_POINT ( 'NONE',  ( 10.77462860031000069, 5.575476001419000127, 8.682676628339999425 ) ) ;
#20175=CARTESIAN_POINT ( 'NONE',  ( 11.16750778041000025, 3.188704589882000118, -8.788663768996000769 ) ) ;
#20182=CARTESIAN_POINT ( 'NONE',  ( 8.335885841230000537, 4.310355144869000732, 9.459505265942000918 ) ) ;
#20185=B_SPLINE_CURVE_WITH_KNOTS ( 'NONE', 3,
 ( #63808, #54011, #38277, #10674 ),
 .UNSPECIFIED., .F., .F.,
 ( 4, 4 ),
 ( 0.8745766503823925175, 1.000000000000000000 ),
 .UNSPECIFIED. ) ;
#20189=VERTEX_POINT ( 'NONE', #54029 ) ;
#20190=CARTESIAN_POINT ( 'NONE',  ( 2.823890132542957954, -2.150913519912200478, -2.798833948393631754 ) ) ;
#20191=B_SPLINE_CURVE_WITH_KNOTS ( 'NONE', 3,
 ( #34116, #66600, #50190, #2291, #44952, #66256 ),
 .UNSPECIFIED., .F., .F.,
 ( 4, 2, 4 ),
 ( 0.000000000000000000, 0.5000000000000000000, 1.000000000000000000 ),
 .UNSPECIFIED. ) ;
#20202=CARTESIAN_POINT ( 'NONE',  ( 7.924357780410000274, 2.432118421226999949, 6.597517552098000060 ) ) ;
#20210=EDGE_LOOP ( 'NONE', ( #38264, #36028, #61147, #30541 ) ) ;
#20216=CARTESIAN_POINT ( 'NONE',  ( 8.461732853997650849, 5.351516129093011109, 7.263730654262094966 ) ) ;
#20222=CARTESIAN_POINT ( 'NONE',  ( 10.59999999999999964, 3.399999999999999911, 4.756097560976000338 ) ) ;
#20229=CARTESIAN_POINT ( 'NONE',  ( 10.81362367151999848, 3.876947539724999725, -9.022206283674000460 ) ) ;
#20230=ADVANCED_FACE ( 'NONE', ( #48450, #6479 ), #556, .F. ) ;
#20234=CARTESIAN_POINT ( 'NONE',  ( 9.972850246170999355, 5.044468801812000081, 6.258104779495000436 ) ) ;
#20238=ORIENTED_EDGE ( 'NONE', *, *, #34333, .F. ) ;
#20240=CARTESIAN_POINT ( 'NONE',  ( 8.586491082670404396, 5.311483864045265513, -7.867512027660226615 ) ) ;
#20241=CARTESIAN_POINT ( 'NONE',  ( 10.63461554336999981, 5.668731883089999535, 6.527253515312000154 ) ) ;
#20244=CARTESIAN_POINT ( 'NONE',  ( 11.12425657198999929, 7.502475533924000572, -6.531087594010999808 ) ) ;
#20246=DIRECTION ( 'NONE',  ( 1.000000000000000000, 0.000000000000000000, 0.000000000000000000 ) ) ;
#20247=CARTESIAN_POINT ( 'NONE',  ( 10.90724142537947650, 5.175055531252366947, -8.817797332566639668 ) ) ;
#20248=CARTESIAN_POINT ( 'NONE',  ( 7.100000000000000533, 0.000000000000000000, -11.84999999999999964 ) ) ;
#20249=CARTESIAN_POINT ( 'NONE',  ( 10.97807333593999957, 5.235090452703000885, -6.783100406990000053 ) ) ;
#20252=CARTESIAN_POINT ( 'NONE',  ( 8.739954719592999410, 3.122811675949999977, -6.006064052396999919 ) ) ;
#20253=CARTESIAN_POINT ( 'NONE',  ( 0.000000000000000000, 1.460905701137619417, 2.533699434756940594 ) ) ;
#20254=CARTESIAN_POINT ( 'NONE',  ( 9.070134780760145787, 3.647129767632899977, 8.851447081754479029 ) ) ;
#20259=CARTESIAN_POINT ( 'NONE',  ( 2.111293599500000173, -2.202566789350000054, 2.837701071685999832 ) ) ;
#20260=CARTESIAN_POINT ( 'NONE',  ( 7.565635841228000480, 3.206360348473000332, 5.681727837477000165 ) ) ;
#20261=CARTESIAN_POINT ( 'NONE',  ( 5.000000000000000000, -1.199999999999999956, 9.776630298829998011 ) ) ;
#20266=EDGE_CURVE ( 'NONE', #24059, #55227, #55095, .T. ) ;
#20281=CARTESIAN_POINT ( 'NONE',  ( 2.210247277619000084, 2.108360286353999413, -2.286637680308000409 ) ) ;
#20284=CARTESIAN_POINT ( 'NONE',  ( 10.81746213571000048, 5.100000000000000533, 6.571291218949999902 ) ) ;
#20297=VERTEX_POINT ( 'NONE', #58503 ) ;
#20301=CARTESIAN_POINT ( 'NONE',  ( 10.40726830891999910, 3.797905842462999892, 5.889914049998000500 ) ) ;
#20302=CARTESIAN_POINT ( 'NONE',  ( 11.08752642792000032, 2.871528932589999972, -6.302908019754999813 ) ) ;
#20306=CARTESIAN_POINT ( 'NONE',  ( 7.474999999999999645, 5.349999999999999645, 7.500000000000000000 ) ) ;
#20311=FACE_OUTER_BOUND ( 'NONE', #20579, .T. ) ;
#20317=DIRECTION ( 'NONE',  ( 0.000000000000000000, 1.000000000000000000, 0.000000000000000000 ) ) ;
#20334=CARTESIAN_POINT ( 'NONE',  ( 11.05392028041000074, 5.159483628325999938, -8.487146968478000986 ) ) ;
#20344=CARTESIAN_POINT ( 'NONE',  ( 9.628002158527587895, 2.419316678802835963, -6.689506437318967436 ) ) ;
#20347=EDGE_CURVE ( 'NONE', #31922, #44210, #60042, .T. ) ;
#20355=EDGE_CURVE ( 'NONE', #31036, #41936, #3320, .T. ) ;
#20369=CARTESIAN_POINT ( 'NONE',  ( 11.09999999883999955, 8.820692016227001275, 6.691733774959000236 ) ) ;
#20370=CARTESIAN_POINT ( 'NONE',  ( 2.419891126640250523, 1.842658540278711010, -2.994770506591985626 ) ) ;
#20373=CARTESIAN_POINT ( 'NONE',  ( 9.111654719595000174, 4.989193221215000307, -6.287302145481000082 ) ) ;
#20377=CARTESIAN_POINT ( 'NONE',  ( 7.949443559528000414, 4.160078903546944318, -6.143289804786609132 ) ) ;
#20381=CARTESIAN_POINT ( 'NONE',  ( 9.392285841233000809, 5.775964236216999836, -8.174909295649001706 ) ) ;
#20382=CARTESIAN_POINT ( 'NONE',  ( 8.649445371194000032, 5.100000000000000533, -6.459601070175000181 ) ) ;
#20386=VERTEX_POINT ( 'NONE', #9572 ) ;
#20388=CARTESIAN_POINT ( 'NONE',  ( 9.983079719591000156, 5.002683760508999988, -8.912673867568997821 ) ) ;
#20390=AXIS2_PLACEMENT_3D ( 'NONE', #24583, #45906, #24235 ) ;
#20391=CARTESIAN_POINT ( 'NONE',  ( 11.02205778663999958, 2.309481324353999554, -7.515673747780000191 ) ) ;
#20403=CARTESIAN_POINT ( 'NONE',  ( 11.06878584122999953, 5.318802051720999735, -7.168446171767000052 ) ) ;
#20409=ORIENTED_EDGE ( 'NONE', *, *, #58785, .T. ) ;
#20410=ORIENTED_EDGE ( 'NONE', *, *, #47968, .T. ) ;
#20412=CARTESIAN_POINT ( 'NONE',  ( 10.21398584123000042, 3.990126737362999609, -8.809457313313998839 ) ) ;
#20419=CARTESIAN_POINT ( 'NONE',  ( 8.616995677562000466, 4.876077402042000131, 5.996974966532000018 ) ) ;
#20421=ORIENTED_EDGE ( 'NONE', *, *, #28495, .F. ) ;
#20426=CARTESIAN_POINT ( 'NONE',  ( 7.956227822045499387, 4.972404917557740944, 6.449457438518853891 ) ) ;
#20430=EDGE_CURVE ( 'NONE', #45133, #28965, #848, .T. ) ;
#20433=CARTESIAN_POINT ( 'NONE',  ( 7.968428156063966483, 2.973737269781533410, -6.513357571637738097 ) ) ;
#20436=LINE ( 'NONE', #51228, #51034 ) ;
#20438=CARTESIAN_POINT ( 'NONE',  ( 3.162702707610999919, 2.867491953926999848, -1.874115396504999920 ) ) ;
#20442=CARTESIAN_POINT ( 'NONE',  ( 10.90000000000000036, 0.2999999999999999889, -4.902439024389999567 ) ) ;
#20444=CARTESIAN_POINT ( 'NONE',  ( 10.12544718489628437, 5.350147103445117125, -7.676667778836200995 ) ) ;
#20445=EDGE_LOOP ( 'NONE', ( #29591, #56874 ) ) ;
#20446=DIRECTION ( 'NONE',  ( 0.000000000000000000, -1.000000000000000000, 0.000000000000000000 ) ) ;
#20447=CARTESIAN_POINT ( 'NONE',  ( 0.6989630074183774688, -2.794206512036536250, 2.158557316518020741 ) ) ;
#20448=ADVANCED_FACE ( 'NONE', ( #45941 ), #9557, .T. ) ;
#20459=CARTESIAN_POINT ( 'NONE',  ( 8.460086291669814074, 4.111641193682548767, -9.252673147083232408 ) ) ;
#20460=DIRECTION ( 'NONE',  ( 0.000000000000000000, -1.000000000000000000, 0.000000000000000000 ) ) ;
#20461=CARTESIAN_POINT ( 'NONE',  ( 8.261229719591000276, 4.814347755891000169, -8.757164289523000633 ) ) ;
#20464=ORIENTED_EDGE ( 'NONE', *, *, #49273, .T. ) ;
#20468=DIRECTION ( 'NONE',  ( 0.000000000000000000, 1.000000000000000000, 0.000000000000000000 ) ) ;
#20479=CARTESIAN_POINT ( 'NONE',  ( 3.084306799210666750, 1.762666431298138825, 3.058252359239908014 ) ) ;
#20480=B_SPLINE_CURVE_WITH_KNOTS ( 'NONE', 3,
 ( #10625, #141, #37202, #55277, #28364, #32313, #42792, #49680, #58870, #66098, #49327 ),
 .UNSPECIFIED., .F., .F.,
 ( 4, 1, 1, 1, 1, 1, 1, 1, 4 ),
 ( 0.000000000000000000, 0.1099981905781512725, 0.2399987910428944826, 0.3699993915076381090, 0.4999999919727210473, 0.6300005924374643129, 0.7600011929022079116, 0.8900017933672909054, 1.000000000000000000 ),
 .UNSPECIFIED. ) ;
#20485=CARTESIAN_POINT ( 'NONE',  ( 3.389296384485166236, -1.580232515686062822, -3.171881757336630248 ) ) ;
#20487=CARTESIAN_POINT ( 'NONE',  ( 10.50244247011999832, 2.268911387573000038, 7.824865741583000300 ) ) ;
#20490=CARTESIAN_POINT ( 'NONE',  ( 9.219485841232998524, 3.892978337449999771, -8.893414073324001023 ) ) ;
#20491=CARTESIAN_POINT ( 'NONE',  ( 2.642422881787000133, 0.3228049546832999495, 3.693971431390000060 ) ) ;
#20499=CARTESIAN_POINT ( 'NONE',  ( 10.28579080656071199, 5.375703358358307149, -6.377628306183688700 ) ) ;
#20502=CARTESIAN_POINT ( 'NONE',  ( 10.62697636434999993, 3.142921793056999924, 8.668445734229999644 ) ) ;
#20503=DIRECTION ( 'NONE',  ( -1.000000000000000000, 0.000000000000000000, 0.000000000000000000 ) ) ;
#20510=CARTESIAN_POINT ( 'NONE',  ( 0.2066231058121046349, -2.618168328974044765E-06, -3.206444164765644977 ) ) ;
#20514=EDGE_CURVE ( 'NONE', #56588, #59750, #61674, .T. ) ;
#20515=CARTESIAN_POINT ( 'NONE',  ( 4.500000000000000000, 0.000000000000000000, 0.000000000000000000 ) ) ;
#20521=CARTESIAN_POINT ( 'NONE',  ( 11.09178278040999999, 4.578541652803000517, -8.908598806528001290 ) ) ;
#20522=EDGE_LOOP ( 'NONE', ( #13186, #10632, #51903, #58698 ) ) ;
#20527=CARTESIAN_POINT ( 'NONE',  ( 8.207510841230000409, 5.944584532500000407, 7.106843289410999631 ) ) ;
#20530=CARTESIAN_POINT ( 'NONE',  ( 7.069639158769000176, 2.101490574575000103, -7.427795877530000368 ) ) ;
#20541=FACE_OUTER_BOUND ( 'NONE', #65677, .T. ) ;
#20542=ORIENTED_EDGE ( 'NONE', *, *, #24966, .F. ) ;
#20545=CARTESIAN_POINT ( 'NONE',  ( 2.446806799209917394, 0.9161175952574844850, -3.408904368339102930 ) ) ;
#20559=DIRECTION ( 'NONE',  ( 1.000000000000000000, 1.776356839339000149E-14, 1.776356839339000149E-14 ) ) ;
#20571=CARTESIAN_POINT ( 'NONE',  ( 9.741003491525001223, 3.588532719919999892, -8.800216240366001585 ) ) ;
#20576=CARTESIAN_POINT ( 'NONE',  ( 10.49785886974000171, 3.776281431161999880, 5.717632172928999168 ) ) ;
#20579=EDGE_LOOP ( 'NONE', ( #24181, #24070, #32797, #46210 ) ) ;
#20582=B_SPLINE_CURVE_WITH_KNOTS ( 'NONE', 3,
 ( #38595, #59918, #7467, #23899, #50132, #18317 ),
 .UNSPECIFIED., .F., .F.,
 ( 4, 2, 4 ),
 ( 0.000000000000000000, 0.5000000000000000000, 1.000000000000000000 ),
 .UNSPECIFIED. ) ;
#20583=CARTESIAN_POINT ( 'NONE',  ( 10.22398792753999963, 5.507894434963000130, 6.589802269404000157 ) ) ;
#20586=VECTOR ( 'NONE', #11349, 1000.000000000000000 ) ;
#20592=CARTESIAN_POINT ( 'NONE',  ( 8.169376727357384738, 5.058218492709852576, -8.358305702195062636 ) ) ;
#20595=CARTESIAN_POINT ( 'NONE',  ( 9.576420280414000175, 4.861259245430999520, -8.806664389576001284 ) ) ;
#20596=CARTESIAN_POINT ( 'NONE',  ( -0.000000000000000000, -2.319407620233877587, 1.781870588985297932 ) ) ;
#20603=ORIENTED_EDGE ( 'NONE', *, *, #54123, .F. ) ;
#20606=CARTESIAN_POINT ( 'NONE',  ( 8.271698341229999585, 5.629399530851999955, 8.631829656822000985 ) ) ;
#20607=PRODUCT_DEFINITION_CONTEXT ( 'detailed design', #23077, 'design' ) ;
#20608=CARTESIAN_POINT ( 'NONE',  ( 8.971339158776000744, 4.082930418187999955, -6.104944817728999773 ) ) ;
#20613=CARTESIAN_POINT ( 'NONE',  ( 9.792569055495000896, 3.463432304708999876, 6.184396499233999478 ) ) ;
#20619=CARTESIAN_POINT ( 'NONE',  ( 8.738426658774001154, 5.414918126383000185, 8.890678916765999418 ) ) ;
#20624=CARTESIAN_POINT ( 'NONE',  ( 1.976884160321000339, -1.998287707672000035, 2.574515877127999897 ) ) ;
#20626=CARTESIAN_POINT ( 'NONE',  ( 1.381730850247262055, 0.8076383959196232754, 3.202530411377747743 ) ) ;
#20629=CARTESIAN_POINT ( 'NONE',  ( 10.15403136780999915, 5.267988602993999514, 5.992335067371000079 ) ) ;
#20630=CARTESIAN_POINT ( 'NONE',  ( 10.18908827523999960, 5.907871695079999874, 7.801541097952000570 ) ) ;
#20635=CARTESIAN_POINT ( 'NONE',  ( 5.000000000000000000, 0.2999999999999999889, 3.149999999999999911 ) ) ;
#20641=DIRECTION ( 'NONE',  ( 1.000000000000000000, 0.000000000000000000, 0.000000000000000000 ) ) ;
#20644=CARTESIAN_POINT ( 'NONE',  ( 8.444541443210569653, 4.172527014369068254, 6.000552138965343119 ) ) ;
#20647=CARTESIAN_POINT ( 'NONE',  ( 10.44079719460000000, 5.435719122931000236, 7.303631812894000319 ) ) ;
#20648=CARTESIAN_POINT ( 'NONE',  ( 10.94349541711000029, 3.081616890687000065, -8.919380927961000793 ) ) ;
#20654=CARTESIAN_POINT ( 'NONE',  ( 7.464691113743000095, 4.351669901925999895, 8.977196921526999773 ) ) ;
#20660=CARTESIAN_POINT ( 'NONE',  ( 6.365856561449002804, 10.53291268342000464, 4.483160362205999228 ) ) ;
#20663=ADVANCED_FACE ( 'NONE', ( #58147 ), #27029, .T. ) ;
#20665=CARTESIAN_POINT ( 'NONE',  ( 10.59999999999999964, 3.399999999999999911, -4.756097560976000338 ) ) ;
#20673=B_SPLINE_SURFACE_WITH_KNOTS ( 'NONE', 3, 3, ( 
 ( #38811, #55238, #7334, #1749, #60136, #55931, #22719, #29371, #8034, #17838, #12245, #54891, #23423, #34264, #61172, #55586, #23764, #28323, #49994, #12589, #61516, #44758, #27983, #6991, #45099, #39158, #23069, #49292, #28677, #50686, #1404, #50339, #34618, #44417, #45442 ),
 ( #18181, #66756, #18871, #33223, #60481, #54545, #65717, #33918, #29030, #13294, #2105, #2437, #66408, #66062, #39503, #60827, #39853, #12939, #18527, #57283, #46123, #8720, #20576, #36314, #67429, #41901, #41560, #62869, #51702, #14653, #62196, #56954, #30063, #34957, #24458 ),
 ( #67092, #41222, #13971, #68453, #46810, #51026, #13631, #51366, #19204, #40527, #56271, #25823, #35299, #8380, #35970, #20234, #14316, #4483, #29723, #45781, #35642, #9387, #47154, #24798, #3125, #61853, #67770, #52389, #56614, #3460, #19554, #40873, #9055, #30393, #30732 ),
 ( #3799, #25136, #46468, #19895, #52039, #14987, #62533, #4142, #57631, #25479, #68116, #9734, #31083, #21600, #42938, #68803, #53770, #64246, #59354, #11456, #286, #27548, #16360, #15678, #637, #37689, #47499, #59019, #20924, #32454, #42261, #31420, #15337, #11121, #52737 ) ),
 .UNSPECIFIED., .F., .F., .F.,
 ( 4, 4 ),
 ( 4, 1, 1, 1, 1, 1, 1, 1, 1, 1, 1, 1, 1, 1, 1, 1, 1, 1, 1, 1, 1, 1, 1, 1, 1, 1, 1, 1, 1, 1, 1, 1, 4 ),
 ( -0.1039370721279000015, 1.103937072127999963 ),
 ( -0.01933701211302999920, 0.01208563257065999909, 0.04350827725433999843, 0.07493092193802000645, 0.1063535666217000075, 0.1377762113054000204, 0.1691988559891000055, 0.2006215006727000150, 0.2320441453564000001, 0.2634667900400999851, 0.2948894347238000258, 0.3263120794074999553, 0.3577347240911999959, 0.3891573687748000054, 0.4205800134584999905, 0.4520026581421999756, 0.4834253028259000162, 0.5148479475096000568, 0.5462705921932000663, 0.5776932368768999959, 0.6091158815606000365, 0.6405385262443000771, 0.6719611709280000067, 0.7033838156117000473, 0.7348064602953000568, 0.7662291049789999864, 0.7976517496627000270, 0.8290743943464000676, 0.8604970390300999972, 0.8919196837138000378, 0.9233423283974000473, 0.9547649730810999769, 0.9861876177648000175 ),
 .UNSPECIFIED. ) ;
#20676=CARTESIAN_POINT ( 'NONE',  ( 7.662260841227999997, 2.688365364125000045, 8.140015608605001063 ) ) ;
#20677=CARTESIAN_POINT ( 'NONE',  ( 9.668957801871640001, 4.353212854359610695, -8.814514396735029678 ) ) ;
#20682=EDGE_CURVE ( 'NONE', #44911, #14252, #4651, .T. ) ;
#20683=CARTESIAN_POINT ( 'NONE',  ( 10.82674528040999995, 3.167160000746000126, -6.225151413000000744 ) ) ;
#20686=DIRECTION ( 'NONE',  ( 1.000000000000000000, -1.157371756819000075E-14, 2.893429392047000287E-14 ) ) ;
#20688=B_SPLINE_CURVE_WITH_KNOTS ( 'NONE', 3,
 ( #23541, #8156, #2902, #45570, #66875, #46251 ),
 .UNSPECIFIED., .F., .F.,
 ( 4, 1, 1, 4 ),
 ( 0.000000000000000000, 0.3333333333333000081, 0.6666666666667000474, 1.000000000000000000 ),
 .UNSPECIFIED. ) ;
#20689=EDGE_CURVE ( 'NONE', #28596, #27423, #50279, .T. ) ;
#20698=CARTESIAN_POINT ( 'NONE',  ( 8.154398449966548057, 3.068578756614712688, 6.310691935350006609 ) ) ;
#20706=CARTESIAN_POINT ( 'NONE',  ( 6.899999691988000450, 12.20988339176000004, -3.111064831549000154 ) ) ;
#20708=CARTESIAN_POINT ( 'NONE',  ( 7.432076984665996200, 3.524670056070998037, 6.650527748631001046 ) ) ;
#20712=VECTOR ( 'NONE', #5008, 1000.000000000000000 ) ;
#20718=CARTESIAN_POINT ( 'NONE',  ( 9.898395280408998076, 3.987760651117999711, -9.123263301387000368 ) ) ;
#20721=DIRECTION ( 'NONE',  ( -0.7071067783004970631, -0.7071067840725973053, 3.040673411905991405E-08 ) ) ;
#20723=ORIENTED_EDGE ( 'NONE', *, *, #16868, .T. ) ;
#20725=CARTESIAN_POINT ( 'NONE',  ( 9.690635841230999858, 2.927176851028000293, -5.932007155957999878 ) ) ;
#20731=CARTESIAN_POINT ( 'NONE',  ( 11.09999999999999964, 5.449702574547000467, 5.124965750789000296 ) ) ;
#20734=CARTESIAN_POINT ( 'NONE',  ( 9.775320280412000074, 2.527713920559999661, -6.969421869128999525 ) ) ;
#20735=EDGE_LOOP ( 'NONE', ( #40591, #18742, #55112 ) ) ;
#20737=CARTESIAN_POINT ( 'NONE',  ( 10.62924593896999959, 3.609487840896999700, -5.855139066690000504 ) ) ;
#20743=EDGE_CURVE ( 'NONE', #5981, #50591, #30821, .T. ) ;
#20745=CARTESIAN_POINT ( 'NONE',  ( 4.600000365992000795, 13.09999963393000044, 1.605909783351000005E-09 ) ) ;
#20748=ORIENTED_EDGE ( 'NONE', *, *, #26635, .F. ) ;
#20753=CARTESIAN_POINT ( 'NONE',  ( 8.351014158771000950, 5.616457598545999907, -8.245813000738998255 ) ) ;
#20758=CARTESIAN_POINT ( 'NONE',  ( 10.96083988518000041, 5.155325283248000545, -5.100114892965000202 ) ) ;
#20760=CARTESIAN_POINT ( 'NONE',  ( 1.290556799207375205, -3.500000000000002220, 0.4581489286484968781 ) ) ;
#20765=CARTESIAN_POINT ( 'NONE',  ( 8.436397631282501308, 5.097046128306766732, -6.518116409473913464 ) ) ;
#20772=CARTESIAN_POINT ( 'NONE',  ( 6.916496230701000059, -12.19459988848999998, -3.104235478652000335 ) ) ;
#20775=CARTESIAN_POINT ( 'NONE',  ( 4.550000802215999229, 1.829647544581999737E-13, 0.000000000000000000 ) ) ;
#20780=EDGE_CURVE ( 'NONE', #12815, #866, #58297, .T. ) ;
#20781=CARTESIAN_POINT ( 'NONE',  ( 1.050973465875000068, 3.500000000000000000, 0.000000000000000000 ) ) ;
#20790=CARTESIAN_POINT ( 'NONE',  ( 10.25047016403597766, 3.823336794438951802, -8.849920973561742343 ) ) ;
#20795=CARTESIAN_POINT ( 'NONE',  ( 10.87668353155578238, 2.650012393098275520, -7.302148410131429124 ) ) ;
#20799=ORIENTED_EDGE ( 'NONE', *, *, #14631, .F. ) ;
#20806=CARTESIAN_POINT ( 'NONE',  ( 0.000000000000000000, 1.781768641235091266, -2.319305672483670921 ) ) ;
#20807=CARTESIAN_POINT ( 'NONE',  ( 8.119770280407001550, 3.402419637676000086, -5.873899751133000002 ) ) ;
#20809=CARTESIAN_POINT ( 'NONE',  ( 9.517711781556004169, 4.527670937829623377, 8.747760000556041859 ) ) ;
#20813=PLANE ( 'NONE',  #67363 ) ;
#20821=AXIS2_PLACEMENT_3D ( 'NONE', #16004, #15667, #36996 ) ;
#20825=EDGE_CURVE ( 'NONE', #7065, #23338, #66592, .T. ) ;
#20828=EDGE_CURVE ( 'NONE', #15877, #66683, #11619, .T. ) ;
#20831=ORIENTED_EDGE ( 'NONE', *, *, #5387, .F. ) ;
#20832=CARTESIAN_POINT ( 'NONE',  ( 10.16829701902000060, 4.567214950372999738, 5.832525041908999341 ) ) ;
#20839=CARTESIAN_POINT ( 'NONE',  ( 8.327313733649477356, 2.900678655379088866, 6.583019346906352709 ) ) ;
#20841=DIRECTION ( 'NONE',  ( 0.000000000000000000, 0.000000000000000000, -1.000000000000000000 ) ) ;
#20845=CARTESIAN_POINT ( 'NONE',  ( 10.44872595140593674, 4.356130030004455200, -9.239985720784517298 ) ) ;
#20847=EDGE_CURVE ( 'NONE', #8436, #56231, #51612, .T. ) ;
#20849=CARTESIAN_POINT ( 'NONE',  ( 9.944319408602000365, 5.443001719280999851, 7.367350382395000175 ) ) ;
#20863=VECTOR ( 'NONE', #23884, 999.9999999999998863 ) ;
#20866=CARTESIAN_POINT ( 'NONE',  ( 10.16821721959000158, 2.330395133894000548, -7.267461653224000173 ) ) ;
#20874=CARTESIAN_POINT ( 'NONE',  ( 7.373073341229000377, 3.394842219570000097, 9.388954446285000088 ) ) ;
#20877=CARTESIAN_POINT ( 'NONE',  ( 9.883148997457000817, 5.167567567567999731, 6.822293592207000934 ) ) ;
#20881=ORIENTED_EDGE ( 'NONE', *, *, #51190, .T. ) ;
#20883=CARTESIAN_POINT ( 'NONE',  ( 0.5060514795710333580, 2.965189113800866139, -1.878291422148264500 ) ) ;
#20896=CARTESIAN_POINT ( 'NONE',  ( 8.887170280412000523, 2.193665972875999959, 7.400591513898000073 ) ) ;
#20904=CARTESIAN_POINT ( 'NONE',  ( 11.05639837197999853, 7.348631596275997602, -6.145103702012999491 ) ) ;
#20913=ORIENTED_EDGE ( 'NONE', *, *, #43797, .F. ) ;
#20918=CARTESIAN_POINT ( 'NONE',  ( 10.99999648468999958, -1.199999999999999956, -11.37663418768599932 ) ) ;
#20919=CARTESIAN_POINT ( 'NONE',  ( 0.07497316781761000082, 0.000000000000000000, 0.000000000000000000 ) ) ;
#20920=CARTESIAN_POINT ( 'NONE',  ( 9.843622243630001378, 5.021682716044000294, -8.761466596873999535 ) ) ;
#20923=CARTESIAN_POINT ( 'NONE',  ( 8.347004975328005116, 2.870635057193001050, -6.340345019934002124 ) ) ;
#20924=CARTESIAN_POINT ( 'NONE',  ( 10.68903608760000168, 2.568976842941999905, 7.728092503410000091 ) ) ;
#20927=CARTESIAN_POINT ( 'NONE',  ( 8.847812662421663532, 5.766884700386136764, -7.677413152681796582 ) ) ;
#20928=ORIENTED_EDGE ( 'NONE', *, *, #9941, .F. ) ;
#20929=CARTESIAN_POINT ( 'NONE',  ( 9.595493858556999101, 3.928424745541000185, 5.531312048131000303 ) ) ;
#20931=CARTESIAN_POINT ( 'NONE',  ( 10.33536974457000035, 5.153692264686000613, 8.830864265869999841 ) ) ;
#20934=CARTESIAN_POINT ( 'NONE',  ( 8.970860841232001448, 4.131080973160000447, -6.108642999115999395 ) ) ;
#20935=AXIS2_PLACEMENT_3D ( 'NONE', #62056, #30589, #24314 ) ;
#20936=CARTESIAN_POINT ( 'NONE',  ( 11.04766418734000055, 10.00030158377000156, -5.674024927225000070 ) ) ;
#20937=EDGE_CURVE ( 'NONE', #12035, #28207, #47088, .T. ) ;
#20939=CARTESIAN_POINT ( 'NONE',  ( 10.79704720403517548, 5.515590898206272463, -6.594712059625336131 ) ) ;
#20941=CARTESIAN_POINT ( 'NONE',  ( 8.179999999999999716, 4.924138593003999809, -8.484107647018999998 ) ) ;
#20942=CARTESIAN_POINT ( 'NONE',  ( 8.158534024102223725, 5.166158726348323071, -8.205174899589399828 ) ) ;
#20945=CARTESIAN_POINT ( 'NONE',  ( 9.816185841232000442, 2.656512020013999997, -7.884832994446999699 ) ) ;
#20949=CARTESIAN_POINT ( 'NONE',  ( 10.62716797202100949, 4.757662754245695957, 4.769350230254125300 ) ) ;
#20953=CARTESIAN_POINT ( 'NONE',  ( 8.656823341231000057, 5.329437560656000272, 6.027391099688998999 ) ) ;
#20954=CARTESIAN_POINT ( 'NONE',  ( 8.474089158773999486, 4.131080973160000447, -6.108642999115999395 ) ) ;
#20958=CARTESIAN_POINT ( 'NONE',  ( 10.42596030538999941, 5.042177533603999784, 8.702224267793999601 ) ) ;
#20964=CARTESIAN_POINT ( 'NONE',  ( 8.610051658774001027, 5.329437560656000272, 6.027391099688998999 ) ) ;
#20965=VECTOR ( 'NONE', #67156, 1000.000000000000000 ) ;
#20966=DIRECTION ( 'NONE',  ( -1.000000000000000000, 0.000000000000000000, 0.000000000000000000 ) ) ;
#20975=CARTESIAN_POINT ( 'NONE',  ( 10.63461554336999981, 5.668731883089999535, 6.527253515312000154 ) ) ;
#20987=VERTEX_POINT ( 'NONE', #63983 ) ;
#20989=DIRECTION ( 'NONE',  ( 0.000000000000000000, -0.7158784314710769925, 0.6982249432342777506 ) ) ;
#20993=CARTESIAN_POINT ( 'NONE',  ( 10.10656234570999956, 4.887646627408000377, -6.257286147482000516 ) ) ;
#20994=CARTESIAN_POINT ( 'NONE',  ( 8.064674013518999374, 4.643178316509001036, 6.221316387655001279 ) ) ;
#21000=EDGE_CURVE ( 'NONE', #14597, #66034, #36752, .T. ) ;
#21001=CARTESIAN_POINT ( 'NONE',  ( 9.368920280410000245, 5.618384167307999277, 7.727742442702000503 ) ) ;
#21003=VERTEX_POINT ( 'NONE', #15425 ) ;
#21004=CARTESIAN_POINT ( 'NONE',  ( 11.10000000000000320, 2.593029302020504190, -6.574394117172995600 ) ) ;
#21007=CARTESIAN_POINT ( 'NONE',  ( 6.032675742706998356, 9.323387372329005274, 4.734447514572996951 ) ) ;
#21008=CARTESIAN_POINT ( 'NONE',  ( 11.01654511052000096, 6.705990105703999227, 5.523018908835999774 ) ) ;
#21009=CARTESIAN_POINT ( 'NONE',  ( 11.06173598926000068, 9.149873930312999448, 6.515098905781000482 ) ) ;
#21019=EDGE_CURVE ( 'NONE', #56837, #30029, #9474, .T. ) ;
#21021=CARTESIAN_POINT ( 'NONE',  ( 0.2361081069562999957, 3.176450105220999909, 1.136354878726999917 ) ) ;
#21028=CARTESIAN_POINT ( 'NONE',  ( 9.900934992105000276, 4.883852641422000040, -9.070888919673000927 ) ) ;
#21033=EDGE_LOOP ( 'NONE', ( #50233, #4644, #36832 ) ) ;
#21036=CARTESIAN_POINT ( 'NONE',  ( 9.133199450400381281, 5.099761357576720222, 6.159710572180461696 ) ) ;
#21050=CARTESIAN_POINT ( 'NONE',  ( 8.597024389729941873, 4.990110225107529551, 6.127963972499145484 ) ) ;
#21054=CARTESIAN_POINT ( 'NONE',  ( 8.500493705215999896, 2.902642539927001941, 6.605602875546000341 ) ) ;
#21063=CARTESIAN_POINT ( 'NONE',  ( 9.500595280412998278, 2.334550724494000029, -7.977056617806000283 ) ) ;
#21068=ORIENTED_EDGE ( 'NONE', *, *, #5680, .F. ) ;
#21070=CARTESIAN_POINT ( 'NONE',  ( 9.143660841233000269, 2.235961884443999459, -6.794506518623999902 ) ) ;
#21075=DIRECTION ( 'NONE',  ( 0.5298945043518727971, -2.050974249430894312E-08, 0.8480635673448556622 ) ) ;
#21079=CARTESIAN_POINT ( 'NONE',  ( 9.766460841231999979, 3.135494838036999798, -8.598037907310999373 ) ) ;
#21090=B_SPLINE_SURFACE_WITH_KNOTS ( 'NONE', 3, 3, ( 
 ( #45202, #66507, #29823, #61961, #51128, #61275, #13393, #34715, #50788, #3231, #14073, #56723, #24897, #8819, #30162, #51465, #46227, #67534, #19658, #40977, #62301, #41663, #47945, #45, #31189, #53533, #47604, #68911, #37447, #57387, #48281, #62967, #68216, #21028, #15442 ),
 ( #15094, #5625, #31521, #52145, #52843, #63314, #21365, #26278, #4249, #4940, #57732, #36418, #58768, #42362, #63663, #42697, #37109, #26966, #58424, #20000, #15780, #31869, #10875, #10529, #5285, #46913, #41324, #10191, #26627, #53187, #58089, #64003, #68561, #36767, #62630 ),
 ( #32220, #16121, #14755, #36073, #9492, #30835, #25586, #20334, #9843, #52494, #4591, #25927, #47257, #20683, #42013, #66335, #16459, #13224, #32555, #48630, #44694, #12869, #733, #21702, #23352, #24040, #38128, #54209, #23696, #7618, #8309, #56201, #60754, #37791, #55861 ),
 ( #65989, #2034, #11218, #61447, #34197, #34551, #28964, #50269, #18806, #59113, #29655, #43392, #22046, #2373, #18115, #2716, #5968, #39433, #64692, #64342, #53867, #16801, #59455, #39782, #11553, #32896, #6308, #27307, #55516, #28609, #29303, #45030, #49923, #18459, #61104 ) ),
 .UNSPECIFIED., .F., .F., .F.,
 ( 4, 4 ),
 ( 4, 1, 1, 1, 1, 1, 1, 1, 1, 1, 1, 1, 1, 1, 1, 1, 1, 1, 1, 1, 1, 1, 1, 1, 1, 1, 1, 1, 1, 1, 1, 1, 4 ),
 ( -0.1039370721279000015, 1.103937072127999963 ),
 ( 0.2233333333344000027, 0.2480800653604999795, 0.2728267973865999840, 0.2975735294126999886, 0.3223202614387999931, 0.3470669934649999733, 0.3718137254910999778, 0.3965604575171999824, 0.4213071895433000424, 0.4460539215694000470, 0.4708006535954999960, 0.4955473856216000006, 0.5202941176476999496, 0.5450408496738000652, 0.5697875816999000698, 0.5945343137260000743, 0.6192810457521999989, 0.6440277777783000035, 0.6687745098044000081, 0.6935212418305000126, 0.7182679738566000172, 0.7430147058827000217, 0.7677614379088000263, 0.7925081699349000308, 0.8172549019609999243, 0.8420016339870999289, 0.8667483660132000445, 0.8914950980394000801, 0.9162418300655000847, 0.9409885620915999782, 0.9657352941176999828, 0.9904820261437999873, 1.015228758169999912 ),
 .UNSPECIFIED. ) ;
#21099=CARTESIAN_POINT ( 'NONE',  ( 8.947714158774999760, 3.854507394315999758, -9.394302886912999639 ) ) ;
#21104=CARTESIAN_POINT ( 'NONE',  ( 10.90728307559000143, 5.030511622218999612, -4.935980611296999498 ) ) ;
#21111=CARTESIAN_POINT ( 'NONE',  ( 8.422931970811326607, 5.091594506052739000, -6.480649903393177702 ) ) ;
#21114=B_SPLINE_CURVE_WITH_KNOTS ( 'NONE', 3,
 ( #944, #58630, #22257, #53732, #43596, #10732, #596, #64894, #59666, #11763 ),
 .UNSPECIFIED., .F., .F.,
 ( 4, 2, 2, 2, 4 ),
 ( 0.000000000000000000, 0.2500000000000000000, 0.5000000000000000000, 0.7500000000000000000, 1.000000000000000000 ),
 .UNSPECIFIED. ) ;
#21119=AXIS2_PLACEMENT_3D ( 'NONE', #25175, #60259, #12363 ) ;
#21124=DIRECTION ( 'NONE',  ( 1.000000000000000000, 0.000000000000000000, 0.000000000000000000 ) ) ;
#21137=CARTESIAN_POINT ( 'NONE',  ( 1.748890132541458753, -2.798833948393641080, 2.150913519912190708 ) ) ;
#21139=DIRECTION ( 'NONE',  ( 1.000000000000000000, 0.000000000000000000, 0.000000000000000000 ) ) ;
#21146=ORIENTED_EDGE ( 'NONE', *, *, #62724, .T. ) ;
#21152=PLANE ( 'NONE',  #12100 ) ;
#21155=CARTESIAN_POINT ( 'NONE',  ( 7.274445280404999714, 5.732054911314000023, -7.535918460973999977 ) ) ;
#21157=CARTESIAN_POINT ( 'NONE',  ( 7.260912495782270604, 3.646496072872962735, -8.815167414925308975 ) ) ;
#21158=ORIENTED_EDGE ( 'NONE', *, *, #30641, .F. ) ;
#21168=CARTESIAN_POINT ( 'NONE',  ( 8.093993643936004290, 4.563399802036997244, -6.204632025667001116 ) ) ;
#21171=ORIENTED_EDGE ( 'NONE', *, *, #23066, .F. ) ;
#21174=CARTESIAN_POINT ( 'NONE',  ( 9.409415556003999370, 2.113395950889999764, 7.914199712930999553 ) ) ;
#21175=CARTESIAN_POINT ( 'NONE',  ( 10.56983915876999980, 2.152856944368999770, -7.425100664021000441 ) ) ;
#21189=CARTESIAN_POINT ( 'NONE',  ( 10.03490996941999924, 5.615906393494999982, 7.351455918368999143 ) ) ;
#21190=CARTESIAN_POINT ( 'NONE',  ( 9.674960421382234443, 2.650268802166420024, 7.499999178247376719 ) ) ;
#21192=B_SPLINE_CURVE_WITH_KNOTS ( 'NONE', 3,
 ( #5779, #47762, #11368, #43195 ),
 .UNSPECIFIED., .F., .F.,
 ( 4, 4 ),
 ( 0.000000000000000000, 1.000000000000000000 ),
 .UNSPECIFIED. ) ;
#21201=CARTESIAN_POINT ( 'NONE',  ( 5.500000000000000000, 0.000000000000000000, 0.000000000000000000 ) ) ;
#21203=ORIENTED_EDGE ( 'NONE', *, *, #48616, .T. ) ;
#21206=CARTESIAN_POINT ( 'NONE',  ( 2.790793788209000148, -3.707132657157000022, -0.6209224904536000400 ) ) ;
#21207=ORIENTED_EDGE ( 'NONE', *, *, #66523, .F. ) ;
#21209=ADVANCED_FACE ( 'NONE', ( #60828 ), #56616, .T. ) ;
#21219=EDGE_CURVE ( 'NONE', #19719, #12749, #35770, .T. ) ;
#21220=CARTESIAN_POINT ( 'NONE',  ( 7.707204719585000419, 2.598436872309000112, -6.481704782070000448 ) ) ;
#21224=CARTESIAN_POINT ( 'NONE',  ( 2.917640132543333209, 1.762666431298152370, -3.058252359239900464 ) ) ;
#21229=CARTESIAN_POINT ( 'NONE',  ( 9.161916987464291395, 2.900038627299713401, -6.155438822667427701 ) ) ;
#21231=DIRECTION ( 'NONE',  ( 0.000000000000000000, 0.000000000000000000, -1.000000000000000000 ) ) ;
#21236=CARTESIAN_POINT ( 'NONE',  ( 7.191892219589999691, 3.501518846194999757, 9.055971388486000251 ) ) ;
#21239=CIRCLE ( 'NONE', #8965, 11.55000444562000439 ) ;
#21247=CARTESIAN_POINT ( 'NONE',  ( 9.020081723712005228, 10.01659799728000522, -5.797890173437007633 ) ) ;
#21256=ORIENTED_EDGE ( 'NONE', *, *, #50671, .F. ) ;
#21259=CARTESIAN_POINT ( 'NONE',  ( 4.900006121741999898, -0.5234957687185584074, 1.947945353336631991 ) ) ;
#21260=CARTESIAN_POINT ( 'NONE',  ( 10.23643409129999959, 5.517148499152000340, -6.754126239302999934 ) ) ;
#21267=EDGE_CURVE ( 'NONE', #62089, #53586, #7407, .T. ) ;
#21269=CARTESIAN_POINT ( 'NONE',  ( 9.533434135307000901, 2.564753581125000181, 6.150586364588000343 ) ) ;
#21273=B_SPLINE_CURVE_WITH_KNOTS ( 'NONE', 3,
 ( #30081, #57304, #61871, #56633, #35987, #9407, #20253, #58005, #10104, #68135, #26194, #41579, #14334, #20596, #68824, #41921, #9072, #41239 ),
 .UNSPECIFIED., .F., .F.,
 ( 4, 2, 2, 2, 2, 2, 2, 2, 4 ),
 ( 0.000000000000000000, 0.1250000000000000000, 0.2500000000000000000, 0.3750000000000000000, 0.5000000000000000000, 0.6250000000000000000, 0.7500000000000000000, 0.8750000000000000000, 1.000000000000000000 ),
 .UNSPECIFIED. ) ;
#21277=CARTESIAN_POINT ( 'NONE',  ( 9.187739158772000536, 5.964723767581000757, 7.776480083716999836 ) ) ;
#21281=CARTESIAN_POINT ( 'NONE',  ( 9.468110841233000841, 4.082930418187999955, -6.104944817728999773 ) ) ;
#21284=CARTESIAN_POINT ( 'NONE',  ( 3.489623894411582938, 3.494155582390569670, -0.4991450110755751290 ) ) ;
#21289=CARTESIAN_POINT ( 'NONE',  ( 2.487975856965999988, 3.176854988377000311, -1.562936765141999862 ) ) ;
#21291=CARTESIAN_POINT ( 'NONE',  ( 8.216604719590000272, 5.331510020787000315, -8.114341808290998159 ) ) ;
#21294=CARTESIAN_POINT ( 'NONE',  ( 2.436201009244109983, -1.386434525806842011, 2.948195033656590081 ) ) ;
#21296=CARTESIAN_POINT ( 'NONE',  ( 11.27765994926999937, 3.273804980682999854, 6.368305648407000419 ) ) ;
#21301=ORIENTED_EDGE ( 'NONE', *, *, #20689, .F. ) ;
#21302=CARTESIAN_POINT ( 'NONE',  ( 7.839801658770999992, 3.084076314893000159, 9.259847992573000397 ) ) ;
#21314=ORIENTED_EDGE ( 'NONE', *, *, #12938, .F. ) ;
#21315=CARTESIAN_POINT ( 'NONE',  ( 9.791229719590001324, 4.294368353031000396, -8.968663198664000191 ) ) ;
#21330=CARTESIAN_POINT ( 'NONE',  ( 10.58996475420000039, 2.876740601533999797, -6.236530348556999392 ) ) ;
#21335=CARTESIAN_POINT ( 'NONE',  ( 9.028524608540857699, 5.063478752693338691, 8.333910756878536219 ) ) ;
#21337=CARTESIAN_POINT ( 'NONE',  ( 7.635857780409000206, 2.466388272391000225, 6.935562100014999842 ) ) ;
#21339=CARTESIAN_POINT ( 'NONE',  ( 11.09999999999999787, 2.396165420595747442, -6.907370999140288959 ) ) ;
#21344=CARTESIAN_POINT ( 'NONE',  ( 11.07206066007000089, 6.377621165504000267, 5.347654869262000510 ) ) ;
#21345=B_SPLINE_CURVE_WITH_KNOTS ( 'NONE', 3,
 ( #21190, #63829, #6136, #38301 ),
 .UNSPECIFIED., .F., .F.,
 ( 4, 4 ),
 ( 0.7819104999562735969, 1.000000000000000000 ),
 .UNSPECIFIED. ) ;
#21346=CARTESIAN_POINT ( 'NONE',  ( 10.85407964676000070, 9.831998789269000838, 5.581261321082999771 ) ) ;
#21358=CARTESIAN_POINT ( 'NONE',  ( 0.03044738438019000196, -2.003871238023999801, -2.529037764236000019 ) ) ;
#21362=CARTESIAN_POINT ( 'NONE',  ( 8.111573341229000533, 3.326263523254000098, 8.794511546544999447 ) ) ;
#21364=CARTESIAN_POINT ( 'NONE',  ( 8.347004975328005116, 2.870635057193001050, -6.340345019934002124 ) ) ;
#21365=CARTESIAN_POINT ( 'NONE',  ( 11.00119221959000093, 4.640446572790000168, -9.059321223816999336 ) ) ;
#21368=DIRECTION ( 'NONE',  ( 0.000000000000000000, 1.000000000000000000, 0.000000000000000000 ) ) ;
#21369=CARTESIAN_POINT ( 'NONE',  ( 8.968535790263077345, 5.344945407621378486, 7.382749812548996537 ) ) ;
#21379=EDGE_LOOP ( 'NONE', ( #47091, #33451, #30768, #2374 ) ) ;
#21381=EDGE_CURVE ( 'NONE', #25126, #37419, #4050, .T. ) ;
#21385=CARTESIAN_POINT ( 'NONE',  ( 10.94532229106000010, 5.075441716071999565, -4.924547694085999794 ) ) ;
#21397=CARTESIAN_POINT ( 'NONE',  ( 9.881820280408998514, 4.325866256860000369, -9.125812605905000652 ) ) ;
#21399=EDGE_LOOP ( 'NONE', ( #49888, #21203, #5755, #41860 ) ) ;
#21412=CARTESIAN_POINT ( 'NONE',  ( 10.21398584123000042, 3.990126737362999609, -8.809457313313998839 ) ) ;
#21415=B_SPLINE_CURVE_WITH_KNOTS ( 'NONE', 3,
 ( #68089, #30367, #42236, #10402, #57605, #9711 ),
 .UNSPECIFIED., .F., .F.,
 ( 4, 2, 4 ),
 ( 0.000000000000000000, 0.5000000000000000000, 1.000000000000000000 ),
 .UNSPECIFIED. ) ;
#21419=CARTESIAN_POINT ( 'NONE',  ( 4.500000125099000492, 1.829647544581999737E-13, 0.000000000000000000 ) ) ;
#21427=CARTESIAN_POINT ( 'NONE',  ( 9.784179719593000257, 4.042991257420999851, -5.768106221333000327 ) ) ;
#21428=CARTESIAN_POINT ( 'NONE',  ( 10.56498513754044311, 5.349957030113837497, -7.500000808964303545 ) ) ;
#21432=EDGE_CURVE ( 'NONE', #21901, #38721, #27550, .T. ) ;
#21435=CARTESIAN_POINT ( 'NONE',  ( 8.622785841227999626, 5.189036231907000030, -8.048606212067999977 ) ) ;
#21444=CARTESIAN_POINT ( 'NONE',  ( 1.996201642328499837, 2.726743374470193437, -2.246552915429937070 ) ) ;
#21456=CARTESIAN_POINT ( 'NONE',  ( 7.932045741440900244, 5.134137158643878429, 6.756605230894701997 ) ) ;
#21469=CARTESIAN_POINT ( 'NONE',  ( 10.18795867446423387, 4.829522773136188718, -8.579479308274169824 ) ) ;
#21482=EDGE_CURVE ( 'NONE', #66219, #8436, #9879, .T. ) ;
#21483=DIRECTION ( 'NONE',  ( 0.7071067537449087226, -0.5063799918121058008, -0.4935375798262057745 ) ) ;
#21486=CARTESIAN_POINT ( 'NONE',  ( 9.568039158772000619, 5.336630274082000192, -7.092011739486999922 ) ) ;
#21487=ORIENTED_EDGE ( 'NONE', *, *, #36440, .T. ) ;
#21489=CARTESIAN_POINT ( 'NONE',  ( 8.260085841226999293, 4.511685119297999869, -5.670317910541000650 ) ) ;
#21491=CARTESIAN_POINT ( 'NONE',  ( 7.281729984065945516, 3.320395505273955994, -8.679445286782913271 ) ) ;
#21492=VERTEX_POINT ( 'NONE', #36146 ) ;
#21499=B_SPLINE_CURVE_WITH_KNOTS ( 'NONE', 3,
 ( #19917, #52061, #48549, #42957, #26886, #53104, #64612, #64950, #6580, #58688, #53450, #653, #47868, #37367, #20949, #22313, #15702, #1001 ),
 .UNSPECIFIED., .F., .F.,
 ( 4, 1, 2, 2, 1, 2, 2, 2, 2, 4 ),
 ( 0.000000000000000000, 0.1250000000000013323, 0.1874999999999983902, 0.2499999999999954481, 0.3749999999999931721, 0.4374999999999959477, 0.4999999999999987232, 0.6249999999999994449, 0.7500000000000002220, 1.000000000000000000 ),
 .UNSPECIFIED. ) ;
#21501=CARTESIAN_POINT ( 'NONE',  ( 1.985247277619000217, 2.372532593102000043, -2.573147701680999599 ) ) ;
#21506=CARTESIAN_POINT ( 'NONE',  ( 10.45187178376759185, 5.320780938513880898, 7.955756249381567002 ) ) ;
#21512=CARTESIAN_POINT ( 'NONE',  ( 9.854942824136999846, 2.800308224477999985, 9.013816726157999781 ) ) ;
#21516=CARTESIAN_POINT ( 'NONE',  ( 8.622785841227999626, 5.189036231907000030, -8.048606212067999977 ) ) ;
#21517=AXIS2_PLACEMENT_3D ( 'NONE', #21201, #21541, #11061 ) ;
#21529=CARTESIAN_POINT ( 'NONE',  ( 9.323722176100000425, 3.947350570199999797, 6.051869652381999920 ) ) ;
#21538=ORIENTED_EDGE ( 'NONE', *, *, #56121, .T. ) ;
#21541=DIRECTION ( 'NONE',  ( 1.000000000000000000, 0.000000000000000000, 0.000000000000000000 ) ) ;
#21542=LINE ( 'NONE', #42199, #31171 ) ;
#21544=ADVANCED_FACE ( 'NONE', ( #45951 ), #39422, .T. ) ;
#21547=CARTESIAN_POINT ( 'NONE',  ( 2.361656243241000208, -1.849229342384999919, -3.272419312099999811 ) ) ;
#21549=CARTESIAN_POINT ( 'NONE',  ( 7.000002934099999408, 1.243449787579999883E-13, -1.714942011622999690E-13 ) ) ;
#21553=CARTESIAN_POINT ( 'NONE',  ( 8.014948341228999240, 2.280568568659000483, 6.510284508622999233 ) ) ;
#21556=CARTESIAN_POINT ( 'NONE',  ( 7.897245280407999779, 4.473304741848999733, -6.008315738301999609 ) ) ;
#21567=EDGE_LOOP ( 'NONE', ( #52365, #18290, #22890, #35381 ) ) ;
#21573=ORIENTED_EDGE ( 'NONE', *, *, #64240, .F. ) ;
#21574=CARTESIAN_POINT ( 'NONE',  ( 9.208107780409999776, 5.057081813675999626, 8.967637988488998957 ) ) ;
#21583=CARTESIAN_POINT ( 'NONE',  ( 11.09999999999999964, 2.899999999999999911, -4.467422426380999845 ) ) ;
#21590=ORIENTED_EDGE ( 'NONE', *, *, #45620, .F. ) ;
#21595=CARTESIAN_POINT ( 'NONE',  ( 10.09133754351999990, 2.216715295763999727, -8.007133643737999407 ) ) ;
#21598=CARTESIAN_POINT ( 'NONE',  ( 8.500392882431995645, 2.902640497153002652, -6.605631719337000440 ) ) ;
#21600=CARTESIAN_POINT ( 'NONE',  ( 9.758140238852000437, 2.901378080241999946, 6.555076849497999625 ) ) ;
#21602=B_SPLINE_CURVE_WITH_KNOTS ( 'NONE', 3,
 ( #22570, #27839, #32728, #18037 ),
 .UNSPECIFIED., .F., .F.,
 ( 4, 4 ),
 ( 0.000000000000000000, 1.000000000000000000 ),
 .UNSPECIFIED. ) ;
#21606=EDGE_CURVE ( 'NONE', #26681, #43316, #39861, .T. ) ;
#21608=CARTESIAN_POINT ( 'NONE',  ( 10.18756025349000005, 5.387489739490000318, 8.640945789268998922 ) ) ;
#21609=CARTESIAN_POINT ( 'NONE',  ( 0.5000220334827000235, 0.000000000000000000, 0.000000000000000000 ) ) ;
#21616=CARTESIAN_POINT ( 'NONE',  ( 9.696080515601000371, 2.554416243104999928, 7.600685069647000525 ) ) ;
#21627=CARTESIAN_POINT ( 'NONE',  ( 8.951357780412001475, 2.821863697211000055, 6.127145479358000024 ) ) ;
#21629=CARTESIAN_POINT ( 'NONE',  ( 8.953620280414000376, 2.881930053949999682, -8.823338183322999129 ) ) ;
#21630=CARTESIAN_POINT ( 'NONE',  ( 10.58079553770030046, 5.100000000000000533, -6.662590550610039131 ) ) ;
#21633=CARTESIAN_POINT ( 'NONE',  ( 10.92717848204000042, 5.023653513500000223, 8.718036113327999104 ) ) ;
#21639=CARTESIAN_POINT ( 'NONE',  ( 9.278329719590999503, 5.791553967443999973, 7.752111263209999770 ) ) ;
#21652=CARTESIAN_POINT ( 'NONE',  ( 8.523814158775000038, 4.920236664407999783, -6.448229650796999834 ) ) ;
#21656=DIRECTION ( 'NONE',  ( 0.7071067811865475727, -0.7071067811865475727, 0.000000000000000000 ) ) ;
#21658=ORIENTED_EDGE ( 'NONE', *, *, #35139, .F. ) ;
#21664=CARTESIAN_POINT ( 'NONE',  ( 10.22452454188789517, 3.422561976923200078, -8.739574331469023960 ) ) ;
#21665=CARTESIAN_POINT ( 'NONE',  ( 10.98168093019000047, 2.885380650160000116, -4.904815280032999603 ) ) ;
#21671=CARTESIAN_POINT ( 'NONE',  ( 8.753448341231001351, 2.876288091423999660, 6.568897128359000526 ) ) ;
#21675=CARTESIAN_POINT ( 'NONE',  ( 11.09999999999999964, 2.274006712557999688, -7.281956340829000673 ) ) ;
#21680=CARTESIAN_POINT ( 'NONE',  ( 10.09999999999999964, 0.000000000000000000, 0.000000000000000000 ) ) ;
#21681=CARTESIAN_POINT ( 'NONE',  ( 11.12718332839000013, 8.468770115145998645, 6.787300010133001216 ) ) ;
#21682=ADVANCED_FACE ( 'NONE', ( #17583 ), #38909, .T. ) ;
#21684=EDGE_CURVE ( 'NONE', #11316, #52043, #24004, .T. ) ;
#21687=ORIENTED_EDGE ( 'NONE', *, *, #50048, .T. ) ;
#21695=CARTESIAN_POINT ( 'NONE',  ( 0.2855665232602999648, 3.161455490150999914, -0.5535149012972000460 ) ) ;
#21696=CARTESIAN_POINT ( 'NONE',  ( 8.769549439917666334, 5.100000000000000533, 6.459823844766666490 ) ) ;
#21699=CARTESIAN_POINT ( 'NONE',  ( 10.16000000000000014, 4.496968146123999865, -8.755198255949000696 ) ) ;
#21701=CARTESIAN_POINT ( 'NONE',  ( 8.181902110542997875, 2.891006945229997793, -6.386045997152003828 ) ) ;
#21702=CARTESIAN_POINT ( 'NONE',  ( 10.44812028041000040, 5.235600787608000850, -6.609970743661000903 ) ) ;
#21705=CARTESIAN_POINT ( 'NONE',  ( 7.729292060080003246, 5.085123327752999245, 6.553315682963002153 ) ) ;
#21711=CARTESIAN_POINT ( 'NONE',  ( 10.84999882987999875, 0.000000000000000000, 0.000000000000000000 ) ) ;
#21715=CYLINDRICAL_SURFACE ( 'NONE', #40900, 1.350000000000000533 ) ;
#21717=ORIENTED_EDGE ( 'NONE', *, *, #43344, .F. ) ;
#21724=CARTESIAN_POINT ( 'NONE',  ( 10.26947109217999810, 5.100000000000000533, -6.152188490330000370 ) ) ;
#21728=ADVANCED_FACE ( 'NONE', ( #13034 ), #65807, .F. ) ;
#21731=FACE_OUTER_BOUND ( 'NONE', #14727, .T. ) ;
#21737=CARTESIAN_POINT ( 'NONE',  ( 8.365779719592000063, 2.949305648881000330, -8.659807625323999503 ) ) ;
#21745=DIRECTION ( 'NONE',  ( 1.000000000000000000, 0.000000000000000000, 0.000000000000000000 ) ) ;
#21755=CARTESIAN_POINT ( 'NONE',  ( 0.5091598036225351009, -3.178301708211344945, 0.6894924743205468332 ) ) ;
#21781=CARTESIAN_POINT ( 'NONE',  ( 0.000000000000000000, 0.000000000000000000, 0.000000000000000000 ) ) ;
#21788=CARTESIAN_POINT ( 'NONE',  ( 1.985247277619000217, 2.372532593102000043, -2.573147701680999599 ) ) ;
#21800=AXIS2_PLACEMENT_3D ( 'NONE', #53933, #64756, #49042 ) ;
#21811=FACE_OUTER_BOUND ( 'NONE', #41812, .T. ) ;
#21825=CARTESIAN_POINT ( 'NONE',  ( 7.100083736560635295, 0.3076767997638333307, -3.048821334907659608 ) ) ;
#21826=LINE ( 'NONE', #38253, #63652 ) ;
#21828=CARTESIAN_POINT ( 'NONE',  ( 8.722714158775000115, 3.892978337449999771, -8.893414073324001023 ) ) ;
#21830=VERTEX_POINT ( 'NONE', #54281 ) ;
#21832=CARTESIAN_POINT ( 'NONE',  ( 7.713110841224000147, 3.406663518590999917, -5.695144508491999602 ) ) ;
#21846=CARTESIAN_POINT ( 'NONE',  ( 7.917797682304002826, 5.086214043998999124, -6.452211737291995597 ) ) ;
#21853=EDGE_CURVE ( 'NONE', #23533, #35290, #55705, .T. ) ;
#21855=CARTESIAN_POINT ( 'NONE',  ( 10.98286939055999945, 3.998514186275999638, 9.091062412789998604 ) ) ;
#21867=DIRECTION ( 'NONE',  ( -1.000000000000000000, 0.000000000000000000, 0.000000000000000000 ) ) ;
#21868=CARTESIAN_POINT ( 'NONE',  ( 10.57314899745999881, 5.167567567567999731, -6.822293592207000934 ) ) ;
#21870=CARTESIAN_POINT ( 'NONE',  ( 10.13049857835000012, 3.092060693447000297, 8.629378633793999498 ) ) ;
#21877=CARTESIAN_POINT ( 'NONE',  ( 10.34271159708237242, 5.100000000000000533, -6.305985890001590377 ) ) ;
#21887=CARTESIAN_POINT ( 'NONE',  ( 0.4199759624411000258, 3.484641797009000008, -0.6100991035018999975 ) ) ;
#21888=DIRECTION ( 'NONE',  ( 1.000000000000000000, 0.000000000000000000, 0.000000000000000000 ) ) ;
#21889=CARTESIAN_POINT ( 'NONE',  ( 2.075564546595999982, 3.096074255452000212, 2.131331154000000172 ) ) ;
#21895=CARTESIAN_POINT ( 'NONE',  ( 8.437857780412000963, 2.606995215518000286, 6.345762205468999717 ) ) ;
#21898=CARTESIAN_POINT ( 'NONE',  ( 8.394495280407999971, 4.421485762723999180, -5.992852494763999616 ) ) ;
#21901=VERTEX_POINT ( 'NONE', #56367 ) ;
#21915=CARTESIAN_POINT ( 'NONE',  ( 9.911640687502833558, 2.873222873817937284, -6.752018918866299124 ) ) ;
#21918=CARTESIAN_POINT ( 'NONE',  ( 7.384454719589999883, 3.346262376537000094, 6.002251090845000192 ) ) ;
#21919=B_SPLINE_CURVE_WITH_KNOTS ( 'NONE', 3,
 ( #43165, #33028, #64471, #54340, #32346, #37920, #64820, #16595, #32683, #52973, #16930, #15571, #5070, #68695, #58905, #27096, #5419, #174, #47388, #26059, #48759, #48411, #59239, #27437, #20809, #38263 ),
 .UNSPECIFIED., .F., .F.,
 ( 4, 2, 2, 2, 2, 2, 2, 2, 2, 2, 2, 2, 4 ),
 ( 0.2965955339900564480, 0.4724466504925387000, 0.4944280400553493493, 0.5164094296181600541, 0.5603722087437794652, 0.6482977669950162891, 0.7362233252462531130, 0.7472140200276574662, 0.7582047148090619304, 0.7801861043718725242, 0.8241488834974980415, 0.9120744417487489653, 1.000000000000000000 ),
 .UNSPECIFIED. ) ;
#21920=ORIENTED_EDGE ( 'NONE', *, *, #60053, .T. ) ;
#21921=CARTESIAN_POINT ( 'NONE',  ( 4.600000365992000795, -13.09999963393000044, -1.605909432238000048E-09 ) ) ;
#21924=CARTESIAN_POINT ( 'NONE',  ( 11.01817350255000072, 5.556623262518999518, -4.991714128839999987 ) ) ;
#21928=CARTESIAN_POINT ( 'NONE',  ( 7.908904767662867208, 2.849922932654429975, -6.792160572118948636 ) ) ;
#21929=CARTESIAN_POINT ( 'NONE',  ( 5.000030787343000327, -2.099962892530999881, 0.000000000000000000 ) ) ;
#21939=CARTESIAN_POINT ( 'NONE',  ( 9.942214158770999788, 3.986577607995999806, -9.280166295424001177 ) ) ;
#21940=EDGE_CURVE ( 'NONE', #42555, #958, #11475, .T. ) ;
#21941=CARTESIAN_POINT ( 'NONE',  ( 11.07336716268999943, 2.375546981533999791, -8.393546861057000541 ) ) ;
#21947=ORIENTED_EDGE ( 'NONE', *, *, #27306, .T. ) ;
#21949=CARTESIAN_POINT ( 'NONE',  ( 9.442843574488000158, 2.691255504502000129, 6.269523028052000235 ) ) ;
#21953=CARTESIAN_POINT ( 'NONE',  ( 11.14004124368000070, 9.840151972678000902, -6.095223425601000500 ) ) ;
#21956=CARTESIAN_POINT ( 'NONE',  ( 10.76947109217999810, 5.100000000000000533, -6.152188490330000370 ) ) ;
#21963=PLANE ( 'NONE',  #26430 ) ;
#21968=VERTEX_POINT ( 'NONE', #67184 ) ;
#21970=DIRECTION ( 'NONE',  ( -1.000000000000000000, 0.000000000000000000, 0.000000000000000000 ) ) ;
#21971=CARTESIAN_POINT ( 'NONE',  ( 8.090517219592001652, 5.342170561818999630, 8.432311822615000452 ) ) ;
#21972=CARTESIAN_POINT ( 'NONE',  ( 9.758079719591000512, 4.905765359186999852, -8.776126235875999271 ) ) ;
#21974=DIRECTION ( 'NONE',  ( 0.000000000000000000, 0.7158784314710769925, 0.6982249432342778617 ) ) ;
#21975=ORIENTED_EDGE ( 'NONE', *, *, #54835, .F. ) ;
#21976=CARTESIAN_POINT ( 'NONE',  ( 9.667078842372998082, 4.541623431405000133, 5.824038024834000460 ) ) ;
#21989=VERTEX_POINT ( 'NONE', #62622 ) ;
#21996=CARTESIAN_POINT ( 'NONE',  ( 9.708354719591000048, 5.481267232667000222, -8.005061172455999241 ) ) ;
#22000=CARTESIAN_POINT ( 'NONE',  ( 7.959567355576805170, 4.656486088299985227, -6.280552176398384923 ) ) ;
#22010=CARTESIAN_POINT ( 'NONE',  ( 10.86068541027999856, 2.936800615939000103, -5.173500112890999425 ) ) ;
#22011=CARTESIAN_POINT ( 'NONE',  ( 7.875072778631000858, 5.143389081112999861, 6.784077933858997156 ) ) ;
#22018=CARTESIAN_POINT ( 'NONE',  ( 9.497295280408998508, 3.734279507827999556, 8.942126004519000304 ) ) ;
#22020=AXIS2_PLACEMENT_3D ( 'NONE', #58519, #63412, #5032 ) ;
#22025=FACE_OUTER_BOUND ( 'NONE', #64459, .T. ) ;
#22030=ORIENTED_EDGE ( 'NONE', *, *, #5200, .F. ) ;
#22033=CARTESIAN_POINT ( 'NONE',  ( 11.09999999999999964, 2.700000001389000204, 5.148506132424000015 ) ) ;
#22038=CARTESIAN_POINT ( 'NONE',  ( 9.202760841230999134, 2.542862824481000317, 7.419808961972999661 ) ) ;
#22042=LINE ( 'NONE', #58421, #51083 ) ;
#22046=CARTESIAN_POINT ( 'NONE',  ( 10.95519834123000003, 3.860336562672999960, -6.147350406894000585 ) ) ;
#22048=CARTESIAN_POINT ( 'NONE',  ( 8.244330716364007827, 4.955554988691996954, 6.175165069893004954 ) ) ;
#22060=CARTESIAN_POINT ( 'NONE',  ( 11.00000000000000000, 2.799999999999999822, 5.865766984179000332 ) ) ;
#22061=ORIENTED_EDGE ( 'NONE', *, *, #40787, .T. ) ;
#22064=CONICAL_SURFACE ( 'NONE', #11999, 1.599998535647999987, 0.7853971506429492377 ) ;
#22070=EDGE_CURVE ( 'NONE', #15028, #19773, #63234, .T. ) ;
#22077=EDGE_CURVE ( 'NONE', #4993, #56617, #53217, .T. ) ;
#22079=ADVANCED_FACE ( 'NONE', ( #11131 ), #38736, .T. ) ;
#22083=CARTESIAN_POINT ( 'NONE',  ( 9.640910841231999484, 2.212639797530000063, -6.855876382544999537 ) ) ;
#22088=ORIENTED_EDGE ( 'NONE', *, *, #67079, .T. ) ;
#22098=ORIENTED_EDGE ( 'NONE', *, *, #23580, .T. ) ;
#22100=CARTESIAN_POINT ( 'NONE',  ( 9.517835841233001304, 4.883347899767999323, -6.417062834774999835 ) ) ;
#22101=ORIENTED_EDGE ( 'NONE', *, *, #65898, .F. ) ;
#22113=CARTESIAN_POINT ( 'NONE',  ( 7.849701421142106561, 2.923599143255341204, -6.630674260272470200 ) ) ;
#22116=CARTESIAN_POINT ( 'NONE',  ( 6.594228317542000006, 5.278582711742999756, -7.933273873238999130 ) ) ;
#22119=VECTOR ( 'NONE', #62663, 1000.000000000000000 ) ;
#22122=EDGE_CURVE ( 'NONE', #8436, #67604, #5655, .T. ) ;
#22125=EDGE_LOOP ( 'NONE', ( #21207, #42051, #10952, #22101, #16515, #38165, #38887, #33702, #61648, #43611, #15392, #17145, #56795, #29806, #194, #59180, #2577, #8867, #47030, #58383, #877, #41778, #50921, #53295, #67403 ) ) ;
#22137=CARTESIAN_POINT ( 'NONE',  ( 8.413394984202977156, 5.085467435940341119, -6.452616802181529110 ) ) ;
#22147=FACE_BOUND ( 'NONE', #49823, .T. ) ;
#22160=EDGE_CURVE ( 'NONE', #65620, #47736, #46547, .T. ) ;
#22162=EDGE_CURVE ( 'NONE', #51068, #55845, #54120, .T. ) ;
#22166=CARTESIAN_POINT ( 'NONE',  ( 7.000000000000000000, 10.69544759345840745, 3.757555162259658132 ) ) ;
#22173=CARTESIAN_POINT ( 'NONE',  ( 8.200000998245998929, 0.000000000000000000, 0.000000000000000000 ) ) ;
#22175=CARTESIAN_POINT ( 'NONE',  ( 9.559179719593000613, 4.038835765825999680, -5.935509327774999733 ) ) ;
#22179=CARTESIAN_POINT ( 'NONE',  ( 7.672245280404999868, 4.523949137149999800, -5.848703038986000635 ) ) ;
#22181=CARTESIAN_POINT ( 'NONE',  ( 7.188051286789615801, 4.829459561370207155, -8.579151395879588193 ) ) ;
#22182=ORIENTED_EDGE ( 'NONE', *, *, #9966, .F. ) ;
#22185=B_SPLINE_CURVE_WITH_KNOTS ( 'NONE', 3,
 ( #56051, #23547, #45908, #23894, #17970, #67220, #12373, #49776, #13755, #50464 ),
 .UNSPECIFIED., .F., .F.,
 ( 4, 2, 2, 2, 4 ),
 ( 0.000000000000000000, 0.1250000000000000000, 0.2500000000000000000, 0.3750000000000000000, 0.5000000000000000000 ),
 .UNSPECIFIED. ) ;
#22197=CARTESIAN_POINT ( 'NONE',  ( 8.024543455198998032, 4.549053763738999834, -6.246376295157002545 ) ) ;
#22199=CARTESIAN_POINT ( 'NONE',  ( 10.54885180107587495, 4.021057955977791920, 8.964620661115885625 ) ) ;
#22203=CARTESIAN_POINT ( 'NONE',  ( 10.45625165877000029, 3.661871102473000406, -9.317475234260999883 ) ) ;
#22213=CARTESIAN_POINT ( 'NONE',  ( 10.85737917744000036, 2.754548910086000113, 8.976376585747001258 ) ) ;
#22222=DIRECTION ( 'NONE',  ( 0.000000000000000000, 1.000000000000000000, 0.000000000000000000 ) ) ;
#22225=CARTESIAN_POINT ( 'NONE',  ( 7.900104261408000816, 3.351183067932000270, -6.316134894229000096 ) ) ;
#22227=B_SPLINE_SURFACE_WITH_KNOTS ( 'NONE', 3, 3, ( 
 ( #64339, #5965, #32893, #27652, #1421, #22736, #48973, #33241, #5622, #44085, #21362, #42692, #54562, #64000, #16118, #37444, #58765, #48277, #61212, #50722, #18565, #35676, #8758, #13665, #24147, #30099, #40233, #46508, #29758, #45477, #40912, #45134, #3164, #7724, #2475 ),
 ( #19591, #45817, #51403, #56309, #51063, #29065, #41256, #30431, #56989, #62234, #66445, #66794, #29414, #2816, #18908, #61549, #51741, #55964, #39892, #24835, #13329, #23801, #62571, #14351, #34994, #34653, #46162, #25173, #36009, #8070, #67811, #67466, #3499, #19935, #8415 ),
 ( #14008, #14690, #50376, #67128, #9092, #24494, #3835, #19238, #35337, #40565, #61892, #56651, #4525, #5562, #32153, #52777, #15718, #10127, #41599, #53121, #41943, #26904, #42302, #36353, #323, #9426, #64281, #53469, #26213, #63600, #63251, #21639, #15376, #57668, #10463 ),
 ( #31805, #62908, #15029, #47194, #63942, #9774, #48216, #58025, #68495, #47541, #21302, #5223, #42974, #16398, #58361, #57325, #30769, #36705, #31459, #58706, #52079, #4183, #20964, #68846, #20619, #69190, #4872, #31125, #52428, #10809, #26559, #25861, #37046, #47886, #16053 ) ),
 .UNSPECIFIED., .F., .F., .F.,
 ( 4, 4 ),
 ( 4, 1, 1, 1, 1, 1, 1, 1, 1, 1, 1, 1, 1, 1, 1, 1, 1, 1, 1, 1, 1, 1, 1, 1, 1, 1, 1, 1, 1, 1, 1, 1, 4 ),
 ( -0.1039370721279000015, 1.103937072127999963 ),
 ( -0.02000000000000000042, 0.01250000000000000069, 0.04499999999999999833, 0.07749999999999999944, 0.1100000000000000006, 0.1424999999999999878, 0.1749999999999999889, 0.2074999999999999900, 0.2399999999999999911, 0.2725000000000000200, 0.3049999999999999933, 0.3375000000000000222, 0.3699999999999999956, 0.4025000000000000244, 0.4349999999999999978, 0.4675000000000000266, 0.5000000000000000000, 0.5324999999999999734, 0.5649999999999999467, 0.5975000000000000311, 0.6300000000000000044, 0.6624999999999999778, 0.6949999999999999512, 0.7275000000000000355, 0.7600000000000000089, 0.7924999999999999822, 0.8249999999999999556, 0.8575000000000000400, 0.8900000000000000133, 0.9224999999999999867, 0.9549999999999999600, 0.9875000000000000444, 1.020000000000000018 ),
 .UNSPECIFIED. ) ;
#22232=DIRECTION ( 'NONE',  ( 1.000000000000000000, 0.000000000000000000, 0.000000000000000000 ) ) ;
#22238=CARTESIAN_POINT ( 'NONE',  ( 2.886157687091000401, -0.7705521370824999217, -3.678943691011999917 ) ) ;
#22239=ORIENTED_EDGE ( 'NONE', *, *, #42496, .F. ) ;
#22244=CARTESIAN_POINT ( 'NONE',  ( 7.058509992104999853, 4.314040636970999820, 8.819134391732999845 ) ) ;
#22247=ADVANCED_FACE ( 'NONE', ( #51630 ), #56538, .T. ) ;
#22248=EDGE_CURVE ( 'NONE', #47790, #38520, #44075, .T. ) ;
#22249=CARTESIAN_POINT ( 'NONE',  ( 8.154729719586999437, 2.268410489563000176, -7.553872882963998947 ) ) ;
#22257=CARTESIAN_POINT ( 'NONE',  ( 11.09999999999999787, 3.168181714683488970, -8.858103688129558506 ) ) ;
#22260=VERTEX_POINT ( 'NONE', #14240 ) ;
#22262=DIRECTION ( 'NONE',  ( 0.000000000000000000, 0.000000000000000000, -1.000000000000000000 ) ) ;
#22264=CARTESIAN_POINT ( 'NONE',  ( 9.972537864286000087, 2.899999999999999911, -6.571291218949999902 ) ) ;
#22267=CARTESIAN_POINT ( 'NONE',  ( 7.962142219590999659, 4.874567052833000069, 6.119507471270999588 ) ) ;
#22269=VERTEX_POINT ( 'NONE', #24034 ) ;
#22273=CARTESIAN_POINT ( 'NONE',  ( 11.07071174448999962, 6.643989958501999915, -5.583274979969999663 ) ) ;
#22278=CARTESIAN_POINT ( 'NONE',  ( 7.839172165042807450, 5.856979424599929374, -7.474329324089589832 ) ) ;
#22290=CARTESIAN_POINT ( 'NONE',  ( 8.798539158775000146, 5.851083642416999631, -7.072167224702999633 ) ) ;
#22291=CARTESIAN_POINT ( 'NONE',  ( 10.24846228258000025, 4.234133568259999869, -5.660851473941000300 ) ) ;
#22296=EDGE_LOOP ( 'NONE', ( #63001, #41296, #9127, #63383, #47567 ) ) ;
#22298=CARTESIAN_POINT ( 'NONE',  ( 10.55991859298999991, 5.094266430778000121, 6.075406703384000018 ) ) ;
#22301=CARTESIAN_POINT ( 'NONE',  ( 5.407309682996999989, 12.95251760905999916, -1.915207572621000054 ) ) ;
#22302=CARTESIAN_POINT ( 'NONE',  ( 11.14287956900000154, 10.00655548732999911, -5.859452652895000391 ) ) ;
#22303=CARTESIAN_POINT ( 'NONE',  ( 10.14579102373339481, 5.375586255833037619, 6.376694730363436925 ) ) ;
#22309=CARTESIAN_POINT ( 'NONE',  ( 9.716735841232001292, 3.941185585667000169, -8.896279800194999865 ) ) ;
#22311=B_SPLINE_CURVE_WITH_KNOTS ( 'NONE', 3,
 ( #43731, #47942, #26963, #53530 ),
 .UNSPECIFIED., .F., .F.,
 ( 4, 4 ),
 ( 0.000000000000000000, 0.1254285313929423273 ),
 .UNSPECIFIED. ) ;
#22313=CARTESIAN_POINT ( 'NONE',  ( 10.60679199300537867, 4.691919759246326649, 4.759410728295280002 ) ) ;
#22317=CARTESIAN_POINT ( 'NONE',  ( 9.298698341228998743, 5.159258275969999197, 9.109498396691998678 ) ) ;
#22318=CARTESIAN_POINT ( 'NONE',  ( 8.465229719592999302, 2.567871051582000241, -6.869011921437000012 ) ) ;
#22320=CARTESIAN_POINT ( 'NONE',  ( 2.729619753586109976, 2.715085506907106705, -1.800656924566107486 ) ) ;
#22322=CARTESIAN_POINT ( 'NONE',  ( 9.889842476439000052, 4.052276433608000161, 9.260531940735001299 ) ) ;
#22327=ORIENTED_EDGE ( 'NONE', *, *, #32070, .F. ) ;
#22328=CARTESIAN_POINT ( 'NONE',  ( 8.434258806866999691, 2.899999996372999433, -6.577564833295999946 ) ) ;
#22344=B_SPLINE_CURVE_WITH_KNOTS ( 'NONE', 3,
 ( #55843, #8292, #61085, #7946 ),
 .UNSPECIFIED., .F., .F.,
 ( 4, 4 ),
 ( 0.000000000000000000, 1.000000000000000000 ),
 .UNSPECIFIED. ) ;
#22345=B_SPLINE_CURVE_WITH_KNOTS ( 'NONE', 3,
 ( #710, #64316, #37765, #59090, #11192, #32531, #10505, #31844, #53845, #10169, #53161, #31498, #4913, #25903 ),
 .UNSPECIFIED., .F., .F.,
 ( 4, 2, 2, 2, 1, 1, 2, 4 ),
 ( 0.000000000000000000, 0.09969170620282293005, 0.1246146327535289089, 0.1277299985723673315, 0.1308453643912057540, 0.1370760960288826269, 0.1495375593042358453, 0.1993834124056478585 ),
 .UNSPECIFIED. ) ;
#22346=CARTESIAN_POINT ( 'NONE',  ( 9.369139158774000720, 2.685250982074999904, -7.026194612421999608 ) ) ;
#22351=CARTESIAN_POINT ( 'NONE',  ( 9.075186946668578614, 5.349648441228561424, -7.676810942292243034 ) ) ;
#22356=EDGE_LOOP ( 'NONE', ( #63330, #37485, #63615, #4855 ) ) ;
#22361=CARTESIAN_POINT ( 'NONE',  ( 10.91194337838000017, 2.977644878599000400, -4.912228107105999442 ) ) ;
#22364=CARTESIAN_POINT ( 'NONE',  ( 7.966901574931999797, 4.609574279519000228, -6.276317554486000816 ) ) ;
#22368=CARTESIAN_POINT ( 'NONE',  ( 8.957392219593000249, 2.678331728353000152, 8.735281589464001684 ) ) ;
#22369=ORIENTED_EDGE ( 'NONE', *, *, #59783, .T. ) ;
#22376=CARTESIAN_POINT ( 'NONE',  ( 11.01438209788000044, 8.148461013471999692, 6.594582989364000447 ) ) ;
#22390=CARTESIAN_POINT ( 'NONE',  ( 7.507482780409000078, 3.501518846194999757, 9.055971388486000251 ) ) ;
#22398=CARTESIAN_POINT ( 'NONE',  ( 7.591358119366002022, 4.587777998512997613, 6.499953102827994655 ) ) ;
#22401=ORIENTED_EDGE ( 'NONE', *, *, #35079, .T. ) ;
#22402=CARTESIAN_POINT ( 'NONE',  ( 0.7968663363676999900, 2.744051942617999895, -1.815777288092999875 ) ) ;
#22407=CARTESIAN_POINT ( 'NONE',  ( 11.13729092314000013, 2.663668339045000000, 5.186744572171000378 ) ) ;
#22412=CARTESIAN_POINT ( 'NONE',  ( 8.064958992852089281, 5.350069970865218849, -7.500002487662858819 ) ) ;
#22413=CARTESIAN_POINT ( 'NONE',  ( 0.9851098981878999572, -0.3635854775007999473, -3.573745162754999871 ) ) ;
#22417=AXIS2_PLACEMENT_3D ( 'NONE', #53844, #6637, #5942 ) ;
#22428=ORIENTED_EDGE ( 'NONE', *, *, #41572, .T. ) ;
#22429=CARTESIAN_POINT ( 'NONE',  ( 7.392787521145388396, 2.688866882091175192, 8.641971157071431264 ) ) ;
#22439=DIRECTION ( 'NONE',  ( 1.000000000000000000, 0.000000000000000000, 0.000000000000000000 ) ) ;
#22441=CARTESIAN_POINT ( 'NONE',  ( 8.100000113405998903, -3.446132268436000216E-13, -3.324929372075999932E-14 ) ) ;
#22444=ORIENTED_EDGE ( 'NONE', *, *, #11430, .T. ) ;
#22445=CARTESIAN_POINT ( 'NONE',  ( 9.865910841232000905, 2.685250982074999904, -7.026194612421999608 ) ) ;
#22446=ORIENTED_EDGE ( 'NONE', *, *, #38346, .F. ) ;
#22447=CARTESIAN_POINT ( 'NONE',  ( 9.947306532704999427, 4.892812229297999416, -9.067756197920999739 ) ) ;
#22448=ORIENTED_EDGE ( 'NONE', *, *, #29229, .T. ) ;
#22458=CARTESIAN_POINT ( 'NONE',  ( 7.307590560818999492, 4.037115771921000018, -6.023232697733999608 ) ) ;
#22462=CARTESIAN_POINT ( 'NONE',  ( 9.286929719595001131, 4.102804347295999854, -5.770625657082999460 ) ) ;
#22463=CARTESIAN_POINT ( 'NONE',  ( 3.999971066382000284, -2.149963194831999935, 0.000000000000000000 ) ) ;
#22469=B_SPLINE_CURVE_WITH_KNOTS ( 'NONE', 3,
 ( #25914, #60145, #22033, #27989 ),
 .UNSPECIFIED., .F., .F.,
 ( 4, 4 ),
 ( 0.000000000000000000, 1.000000000000000000 ),
 .UNSPECIFIED. ) ;
#22476=FACE_BOUND ( 'NONE', #16268, .T. ) ;
#22482=ORIENTED_EDGE ( 'NONE', *, *, #29769, .T. ) ;
#22496=CARTESIAN_POINT ( 'NONE',  ( 9.433536308085933797, 2.899999999999999911, -6.665341197419093255 ) ) ;
#22499=PLANE ( 'NONE',  #35679 ) ;
#22507=CARTESIAN_POINT ( 'NONE',  ( 10.51720455737510562, 5.205742106671379155, 8.206130011351980613 ) ) ;
#22509=ORIENTED_EDGE ( 'NONE', *, *, #56907, .F. ) ;
#22520=CARTESIAN_POINT ( 'NONE',  ( 8.409260841228999084, 5.592690705327999723, -8.535639167491000379 ) ) ;
#22524=ORIENTED_EDGE ( 'NONE', *, *, #33542, .F. ) ;
#22526=B_SPLINE_CURVE_WITH_KNOTS ( 'NONE', 3,
 ( #52069, #13999, #46153, #40903, #46498, #58015, #56642, #62898, #46839, #30090, #41589, #62560, #36343, #42290, #4860, #15018, #35665, #57659, #25164, #56980, #63241, #67802, #31114, #14342 ),
 .UNSPECIFIED., .F., .F.,
 ( 4, 2, 2, 1, 2, 2, 2, 2, 2, 2, 1, 2, 4 ),
 ( 0.000000000000000000, 0.1249999999999996669, 0.1874999999999996947, 0.2499999999999997224, 0.3124999999999997224, 0.3749999999999997780, 0.4999999999999997780, 0.6249999999999995559, 0.7499999999999993339, 0.8124999999999994449, 0.8749999999999996669, 0.9374999999999997780, 1.000000000000000000 ),
 .UNSPECIFIED. ) ;
#22531=DIRECTION ( 'NONE',  ( 0.5000000000000169864, 0.000000000000000000, -0.8660254037844288266 ) ) ;
#22537=CARTESIAN_POINT ( 'NONE',  ( 8.367699215443000327, 5.101426577346004798, -6.644016792819001260 ) ) ;
#22539=FACE_OUTER_BOUND ( 'NONE', #27014, .T. ) ;
#22543=CARTESIAN_POINT ( 'NONE',  ( 10.57892463485000079, 4.649960478797999563, 5.681084732956000138 ) ) ;
#22544=CARTESIAN_POINT ( 'NONE',  ( 11.12964528040999923, 3.869081149487999749, -9.017143166339000260 ) ) ;
#22554=FACE_OUTER_BOUND ( 'NONE', #65911, .T. ) ;
#22568=CARTESIAN_POINT ( 'NONE',  ( 8.677306202554058601, 2.980089076194122999, -6.115478653393680908 ) ) ;
#22570=CARTESIAN_POINT ( 'NONE',  ( 8.474485200571999499, 5.100000000000000533, 6.560614371780999043 ) ) ;
#22574=CARTESIAN_POINT ( 'NONE',  ( 9.198551576885758863, 4.680098380207501130, -8.679821298980339606 ) ) ;
#22575=CARTESIAN_POINT ( 'NONE',  ( 9.251970280414001380, 5.673443217382001080, -7.051790060464000476 ) ) ;
#22583=CARTESIAN_POINT ( 'NONE',  ( 2.695429889327000339, -1.927268832017999811, 3.227074855961999944 ) ) ;
#22589=CARTESIAN_POINT ( 'NONE',  ( 7.988545280410000338, 3.566637212418000136, 5.743604853744000316 ) ) ;
#22590=ORIENTED_EDGE ( 'NONE', *, *, #47917, .T. ) ;
#22592=CARTESIAN_POINT ( 'NONE',  ( 7.151370280410000113, 3.450042761745999886, -8.965148246193999526 ) ) ;
#22594=CARTESIAN_POINT ( 'NONE',  ( 9.632179190069999564, 5.638172764974000550, 6.476627236431999890 ) ) ;
#22599=ORIENTED_EDGE ( 'NONE', *, *, #35079, .F. ) ;
#22603=EDGE_LOOP ( 'NONE', ( #61844, #30167, #48560, #55070 ) ) ;
#22606=EDGE_CURVE ( 'NONE', #22744, #18238, #61910, .T. ) ;
#22611=CARTESIAN_POINT ( 'NONE',  ( 8.128301658772999261, 3.117378429069999957, 8.662179062556001341 ) ) ;
#22613=LINE ( 'NONE', #63877, #32929 ) ;
#22619=CARTESIAN_POINT ( 'NONE',  ( 7.988347165043021114, 3.468997027298886149, -9.279625640052284297 ) ) ;
#22625=ORIENTED_EDGE ( 'NONE', *, *, #20430, .T. ) ;
#22628=VECTOR ( 'NONE', #14705, 1000.000000000000114 ) ;
#22630=CARTESIAN_POINT ( 'NONE',  ( 8.599639158772999892, 2.261390688294000029, -6.733978371730000134 ) ) ;
#22631=CARTESIAN_POINT ( 'NONE',  ( 2.335490869717000262, 3.363656811547999670, -0.3259338917754999732 ) ) ;
#22632=B_SPLINE_CURVE_WITH_KNOTS ( 'NONE', 3,
 ( #37525, #10268, #41744, #15856 ),
 .UNSPECIFIED., .F., .F.,
 ( 4, 4 ),
 ( 0.000000000000000000, 1.000000000000000000 ),
 .UNSPECIFIED. ) ;
#22637=ORIENTED_EDGE ( 'NONE', *, *, #3466, .F. ) ;
#22639=EDGE_CURVE ( 'NONE', #39722, #10018, #59256, .T. ) ;
#22640=CARTESIAN_POINT ( 'NONE',  ( 9.380783851237000093, 2.204242311415999911, 7.545378292079000460 ) ) ;
#22642=CARTESIAN_POINT ( 'NONE',  ( 2.061390132542666898, 3.499999999999999112, 0.4581489286485193602 ) ) ;
#22646=CARTESIAN_POINT ( 'NONE',  ( 10.26817165544659893, 5.148139224407167980, 8.818277135132042588 ) ) ;
#22649=SURFACE_SIDE_STYLE ('',( #11816 ) ) ;
#22650=VERTEX_POINT ( 'NONE', #24298 ) ;
#22655=CARTESIAN_POINT ( 'NONE',  ( 8.073148997456000231, 5.167567567567999731, -6.822293592207000934 ) ) ;
#22657=ORIENTED_EDGE ( 'NONE', *, *, #33621, .F. ) ;
#22661=CARTESIAN_POINT ( 'NONE',  ( 7.603420280409000753, 5.687206835507000235, 6.847268999608999707 ) ) ;
#22662=CARTESIAN_POINT ( 'NONE',  ( 9.211104719594999324, 5.462898983065000102, -8.055936939571999744 ) ) ;
#22665=CARTESIAN_POINT ( 'NONE',  ( 2.981121534451109945, -2.748581895732221003, 1.749100406568057986 ) ) ;
#22667=CARTESIAN_POINT ( 'NONE',  ( 10.69030645188999884, 5.903031974240000146, 7.830710565751001440 ) ) ;
#22671=CARTESIAN_POINT ( 'NONE',  ( 8.328793652375997780, 2.897388771918001371, 6.655272502545993341 ) ) ;
#22672=ORIENTED_EDGE ( 'NONE', *, *, #11389, .T. ) ;
#22674=CARTESIAN_POINT ( 'NONE',  ( 0.1499942179679999987, -2.750000000000000000, 0.000000000000000000 ) ) ;
#22685=CARTESIAN_POINT ( 'NONE',  ( 7.640464943433003420, 3.216280862983999622, 6.362631827276998386 ) ) ;
#22687=AXIS2_PLACEMENT_3D ( 'NONE', #58494, #58153, #10256 ) ;
#22688=VERTEX_POINT ( 'NONE', #23608 ) ;
#22689=CARTESIAN_POINT ( 'NONE',  ( 9.111654719595000174, 4.989193221215000307, -6.287302145481000082 ) ) ;
#22696=ORIENTED_EDGE ( 'NONE', *, *, #14055, .T. ) ;
#22703=CARTESIAN_POINT ( 'NONE',  ( 10.16989991304999918, 2.594216849811000092, -6.291257009166999481 ) ) ;
#22705=DIRECTION ( 'NONE',  ( 0.9999999999999987788, 4.835300621521984030E-08, 1.472962709867996247E-08 ) ) ;
#22710=CARTESIAN_POINT ( 'NONE',  ( 7.262114158771001193, 4.847807297114000491, 9.065373753110998578 ) ) ;
#22712=VECTOR ( 'NONE', #48586, 1000.000000000000114 ) ;
#22715=CARTESIAN_POINT ( 'NONE',  ( 7.444482658958142984, 5.271178084961285926, 6.970094358920671418 ) ) ;
#22719=CARTESIAN_POINT ( 'NONE',  ( 9.595493858556999101, 3.928424745541000185, 5.531312048131000303 ) ) ;
#22732=CARTESIAN_POINT ( 'NONE',  ( 7.700045280408999382, 3.346262376537000094, 6.002251090845000192 ) ) ;
#22736=CARTESIAN_POINT ( 'NONE',  ( 7.790635841228000125, 3.416213390569000197, 6.162512717529000206 ) ) ;
#22743=CARTESIAN_POINT ( 'NONE',  ( 8.933148997457999840, 5.167567567567999731, 6.822293592207000934 ) ) ;
#22744=VERTEX_POINT ( 'NONE', #34113 ) ;
#22745=CARTESIAN_POINT ( 'NONE',  ( 1.787066629541000040, 2.957881470139000157, 1.368292308076999975 ) ) ;
#22761=VECTOR ( 'NONE', #56526, 1000.000000000000114 ) ;
#22762=CARTESIAN_POINT ( 'NONE',  ( 10.76947109217999810, 5.100000000000000533, -6.152188490330000370 ) ) ;
#22763=CARTESIAN_POINT ( 'NONE',  ( 1.562066629540999951, 3.411444769430000079, 1.578107062294999974 ) ) ;
#22764=CARTESIAN_POINT ( 'NONE',  ( 1.771806799206333327, -3.408904368339104263, -0.9161175952574814874 ) ) ;
#22766=CARTESIAN_POINT ( 'NONE',  ( 10.29378723213999969, 3.483632952461999999, 6.176337842045999338 ) ) ;
#22774=CARTESIAN_POINT ( 'NONE',  ( 8.944760841233000193, 4.990139824845000405, -9.121472988377998803 ) ) ;
#22776=ORIENTED_EDGE ( 'NONE', *, *, #16412, .F. ) ;
#22782=LINE ( 'NONE', #32595, #35565 ) ;
#22783=EDGE_CURVE ( 'NONE', #25073, #54494, #61517, .T. ) ;
#22784=CARTESIAN_POINT ( 'NONE',  ( 11.08492721656000057, 3.668390701878999849, 5.558148445539999649 ) ) ;
#22785=EDGE_CURVE ( 'NONE', #59750, #58906, #5701, .T. ) ;
#22786=CARTESIAN_POINT ( 'NONE',  ( 8.610944094208999644, 5.100000000000000533, -6.571291218949999902 ) ) ;
#22787=CARTESIAN_POINT ( 'NONE',  ( 27.64127793187000037, -13.87069231928999891, 4.225386915259999654 ) ) ;
#22794=EDGE_LOOP ( 'NONE', ( #3449, #50289, #27944, #61218 ) ) ;
#22795=CARTESIAN_POINT ( 'NONE',  ( 0.6325562371681370255, -0.7533924460659336964, -3.163756291279751220 ) ) ;
#22802=B_SPLINE_SURFACE_WITH_KNOTS ( 'NONE', 3, 3, ( 
 ( #28360, #12621, #44102, #49676 ),
 ( #32908, #65401, #44452, #33950 ),
 ( #43051, #59126, #17520, #55273 ),
 ( #12279, #38850, #398, #60173 ),
 ( #746, #32567, #59816, #53879 ),
 ( #22407, #1785, #33605, #5979 ) ),
 .UNSPECIFIED., .F., .F., .F.,
 ( 4, 1, 1, 4 ),
 ( 4, 4 ),
 ( 0.8990818836185000551, 0.9285714285714000704, 1.000000000000000000, 1.007603470889000041 ),
 ( -0.1835655572433000093, 1.183565557057000062 ),
 .UNSPECIFIED. ) ;
#22807=FACE_OUTER_BOUND ( 'NONE', #50030, .T. ) ;
#22809=CARTESIAN_POINT ( 'NONE',  ( 9.269471092183000138, 5.100000000000000533, -6.152188490330000370 ) ) ;
#22813=EDGE_CURVE ( 'NONE', #3577, #44210, #20082, .T. ) ;
#22814=B_SPLINE_SURFACE_WITH_KNOTS ( 'NONE', 3, 3, ( 
 ( #64158, #26428, #4737, #58577, #53683, #15926, #37258, #10680, #47759, #69069, #36920, #37595, #58236, #32028, #64495, #21175, #47410, #42506, #22203, #48782, #27119, #63814, #53341, #5443, #16615, #37940, #26780, #48093, #48434, #59262, #27456, #32703, #68714, #889, #64840 ),
 ( #16952, #59610, #11708, #26081, #15591, #1926, #60306, #6813, #12761, #60994, #33398, #29193, #55410, #55757, #34443, #2268, #38987, #50166, #23586, #44927, #18011, #27813, #28149, #66231, #66575, #28502, #43886, #18352, #23247, #39675, #13114, #49461, #18694, #1233, #55061 ),
 ( #7502, #2605, #1574, #28857, #44590, #22544, #39327, #54363, #7859, #50504, #23934, #22892, #49119, #45269, #65883, #60648, #44243, #40028, #65188, #49815, #6467, #17308, #7162, #34090, #61340, #13458, #38633, #59955, #12066, #33746, #54713, #65539, #17663, #12413, #57115 ),
 ( #67947, #34781, #51198, #14483, #62364, #62698, #3626, #40693, #50850, #20403, #20062, #24625, #25650, #56090, #46979, #8200, #35801, #14818, #24962, #46294, #56439, #63031, #19372, #9216, #45946, #67256, #62023, #51868, #14137, #30554, #3966, #25303, #67596, #29550, #8540 ) ),
 .UNSPECIFIED., .F., .F., .F.,
 ( 4, 4 ),
 ( 4, 1, 1, 1, 1, 1, 1, 1, 1, 1, 1, 1, 1, 1, 1, 1, 1, 1, 1, 1, 1, 1, 1, 1, 1, 1, 1, 1, 1, 1, 1, 1, 4 ),
 ( -0.1039370721279000015, 1.103937072127999963 ),
 ( 0.2233333333344000027, 0.2480800653604999795, 0.2728267973865999840, 0.2975735294126999886, 0.3223202614387999931, 0.3470669934649999733, 0.3718137254910999778, 0.3965604575171999824, 0.4213071895433000424, 0.4460539215694000470, 0.4708006535954999960, 0.4955473856216000006, 0.5202941176476999496, 0.5450408496738000652, 0.5697875816999000698, 0.5945343137260000743, 0.6192810457521999989, 0.6440277777783000035, 0.6687745098044000081, 0.6935212418305000126, 0.7182679738566000172, 0.7430147058827000217, 0.7677614379088000263, 0.7925081699349000308, 0.8172549019609999243, 0.8420016339870999289, 0.8667483660132000445, 0.8914950980394000801, 0.9162418300655000847, 0.9409885620915999782, 0.9657352941176999828, 0.9904820261437999873, 1.015228758169999912 ),
 .UNSPECIFIED. ) ;
#22815=CARTESIAN_POINT ( 'NONE',  ( 9.137754719594999742, 2.319062457810000311, -7.919229449146000022 ) ) ;
#22818=CARTESIAN_POINT ( 'NONE',  ( 8.314979508587148516, 2.649972834346558059, -7.499998738096613771 ) ) ;
#22821=CARTESIAN_POINT ( 'NONE',  ( 4.500000484264000455, -12.99999951562999989, -2.124868964128000431E-09 ) ) ;
#22829=ORIENTED_EDGE ( 'NONE', *, *, #67775, .F. ) ;
#22832=AXIS2_PLACEMENT_3D ( 'NONE', #27452, #65183, #6458 ) ;
#22849=CARTESIAN_POINT ( 'NONE',  ( 2.210247277619000084, 2.108360286353999413, -2.286637680308000409 ) ) ;
#22857=CARTESIAN_POINT ( 'NONE',  ( 9.856851002545999663, 2.832432432432000269, -6.822293592207000934 ) ) ;
#22858=CARTESIAN_POINT ( 'NONE',  ( 10.23921655905618699, 2.650856495401566093, 7.263814070341827467 ) ) ;
#22867=EDGE_CURVE ( 'NONE', #39380, #19742, #18582, .T. ) ;
#22876=CARTESIAN_POINT ( 'NONE',  ( 8.819055905797000605, 2.899999999999999911, -6.571291218949999902 ) ) ;
#22878=CARTESIAN_POINT ( 'NONE',  ( 9.444964158775000840, 3.920043641733999884, -9.398198753036000497 ) ) ;
#22880=CARTESIAN_POINT ( 'NONE',  ( 10.99693586709999948, 2.980605808171000071, -6.418617723582000778 ) ) ;
#22890=ORIENTED_EDGE ( 'NONE', *, *, #32833, .T. ) ;
#22892=CARTESIAN_POINT ( 'NONE',  ( 10.90247028041000021, 4.554785930130000438, -6.081876607904999510 ) ) ;
#22901=CARTESIAN_POINT ( 'NONE',  ( 8.549914158773001205, 2.141799395716999843, -7.895788736628000848 ) ) ;
#22905=DIRECTION ( 'NONE',  ( -0.000000000000000000, 1.000000000000000000, 0.000000000000000000 ) ) ;
#22908=CARTESIAN_POINT ( 'NONE',  ( 8.753601108638063621, 2.714205948350784325, 7.027810827039986386 ) ) ;
#22912=EDGE_CURVE ( 'NONE', #38413, #57550, #41117, .T. ) ;
#22916=CARTESIAN_POINT ( 'NONE',  ( 6.988896813636456429, -12.37529600717038214, -2.766866756147773998 ) ) ;
#22917=EDGE_CURVE ( 'NONE', #62021, #15326, #14502, .T. ) ;
#22918=CARTESIAN_POINT ( 'NONE',  ( 4.149992563291999836, -0.5234817089163712467, 1.947893036340041961 ) ) ;
#22922=CARTESIAN_POINT ( 'NONE',  ( 8.763579719593998618, 4.815598936798999752, -8.835641302565999666 ) ) ;
#22923=B_SPLINE_CURVE_WITH_KNOTS ( 'NONE', 3,
 ( #19859, #68771, #62837, #30695, #41190, #56920, #14955, #20545, #62160, #57953, #36280, #57596, #35938, #14619, #46434, #63176, #15304, #10052 ),
 .UNSPECIFIED., .F., .F.,
 ( 4, 2, 2, 2, 2, 2, 2, 2, 4 ),
 ( 0.000000000000000000, 0.1250000000000000000, 0.2500000000000000000, 0.3750000000000000000, 0.5000000000000000000, 0.6250000000000000000, 0.7500000000000000000, 0.8750000000000000000, 1.000000000000000000 ),
 .UNSPECIFIED. ) ;
#22925=DIRECTION ( 'NONE',  ( 1.000000000000000000, 0.000000000000000000, 0.000000000000000000 ) ) ;
#22926=CARTESIAN_POINT ( 'NONE',  ( 0.3597486600377999832, -1.720643726402999896, -3.153834707638000001 ) ) ;
#22929=CARTESIAN_POINT ( 'NONE',  ( 2.542837364878999917, -1.685321747336000264, -2.982366387278999831 ) ) ;
#22934=CARTESIAN_POINT ( 'NONE',  ( 7.897954719591000483, 3.608525622520999843, 5.913376237674000002 ) ) ;
#22937=CARTESIAN_POINT ( 'NONE',  ( 7.540310841227999994, 5.150153908582999485, -6.706147112165000479 ) ) ;
#22939=DIRECTION ( 'NONE',  ( 0.000000000000000000, 0.000000000000000000, -1.000000000000000000 ) ) ;
#22944=ORIENTED_EDGE ( 'NONE', *, *, #27728, .T. ) ;
#22945=CARTESIAN_POINT ( 'NONE',  ( -2.444943969992999916E-05, 2.899969545325999931, 0.000000000000000000 ) ) ;
#22948=ORIENTED_EDGE ( 'NONE', *, *, #20743, .T. ) ;
#22956=ORIENTED_EDGE ( 'NONE', *, *, #49188, .F. ) ;
#22962=FACE_OUTER_BOUND ( 'NONE', #67394, .T. ) ;
#22969=CARTESIAN_POINT ( 'NONE',  ( 5.000030787343000327, 1.057581170753191913, 1.834918991542626943 ) ) ;
#22971=LINE ( 'NONE', #2002, #6285 ) ;
#22979=CARTESIAN_POINT ( 'NONE',  ( 9.246064158776000852, 5.200883864107000321, -6.027780766890000308 ) ) ;
#22980=CARTESIAN_POINT ( 'NONE',  ( 2.754660504490999973, 1.495576858855999891, -3.030426860594000349 ) ) ;
#22983=LINE ( 'NONE', #44331, #55159 ) ;
#22989=CARTESIAN_POINT ( 'NONE',  ( 10.96080777006000062, 2.054568739078000306, 7.810084630238000258 ) ) ;
#22992=CARTESIAN_POINT ( 'NONE',  ( 11.09999999999999964, 2.646159083949000124, 6.745271721726000536 ) ) ;
#22994=CARTESIAN_POINT ( 'NONE',  ( 10.35791745203637326, 3.287858841512209640, 9.125997197693916263 ) ) ;
#23009=CARTESIAN_POINT ( 'NONE',  ( 8.116920280410999666, 5.773189794777000117, 7.141495931231999883 ) ) ;
#23010=CONICAL_SURFACE ( 'NONE', #62091, 2.074968475931999734, 0.7853828752794411727 ) ;
#23011=CARTESIAN_POINT ( 'NONE',  ( 9.292835841232999883, 5.200883864107000321, -6.027780766890000308 ) ) ;
#23012=CARTESIAN_POINT ( 'NONE',  ( 0.6472501130994691154, 1.225110017767339077, 3.318548330844829142 ) ) ;
#23020=CARTESIAN_POINT ( 'NONE',  ( 8.212416242268998801, 3.104180772687998857, 6.104177153569003700 ) ) ;
#23024=CARTESIAN_POINT ( 'NONE',  ( 1.261390132541624576, -3.499999999999999556, -0.4581489286485119772 ) ) ;
#23033=VERTEX_POINT ( 'NONE', #66690 ) ;
#23035=ORIENTED_EDGE ( 'NONE', *, *, #55487, .T. ) ;
#23036=CARTESIAN_POINT ( 'NONE',  ( 9.690635841230999858, 2.927176851028000293, -5.932007155957999878 ) ) ;
#23050=FACE_OUTER_BOUND ( 'NONE', #19834, .T. ) ;
#23051=CARTESIAN_POINT ( 'NONE',  ( 7.591358119366002022, 4.587777998512997613, 6.499953102827994655 ) ) ;
#23055=CARTESIAN_POINT ( 'NONE',  ( 6.966665954281333839, -12.09896498756869576, 3.276379939815991627 ) ) ;
#23057=CARTESIAN_POINT ( 'NONE',  ( 8.187142219590999304, 4.968147183437999992, 5.971792472497999604 ) ) ;
#23058=VERTEX_POINT ( 'NONE', #13229 ) ;
#23059=B_SPLINE_CURVE_WITH_KNOTS ( 'NONE', 3,
 ( #27586, #17081, #44714, #60434 ),
 .UNSPECIFIED., .F., .F.,
 ( 4, 4 ),
 ( 0.000000000000000000, 1.000000000000000000 ),
 .UNSPECIFIED. ) ;
#23063=CARTESIAN_POINT ( 'NONE',  ( 9.705773468360421319, 5.100000000000000533, -6.304440313841762844 ) ) ;
#23066=EDGE_CURVE ( 'NONE', #31174, #66219, #30222, .T. ) ;
#23068=CARTESIAN_POINT ( 'NONE',  ( 10.96499058814000094, 5.558059231066999395, 4.905737858409000118 ) ) ;
#23069=CARTESIAN_POINT ( 'NONE',  ( 10.83668832355999889, 4.288537082977999404, 9.448742031664000507 ) ) ;
#23077=APPLICATION_CONTEXT ( 'automotive_design' ) ;
#23083=CARTESIAN_POINT ( 'NONE',  ( 9.266948341230998309, 3.049618631524000367, 6.392542946894000266 ) ) ;
#23084=CARTESIAN_POINT ( 'NONE',  ( 9.843732751558000871, 4.115124343450999866, 9.466620196856998959 ) ) ;
#23086=VERTEX_POINT ( 'NONE', #35236 ) ;
#23087=CARTESIAN_POINT ( 'NONE',  ( 9.925639158771000226, 4.357364160690000432, -9.282962013144999247 ) ) ;
#23095=CARTESIAN_POINT ( 'NONE',  ( 1.973021089241999704, -0.2083462584559999942, 3.419270530009000275 ) ) ;
#23097=CARTESIAN_POINT ( 'NONE',  ( 5.000000000000000000, 0.6769230769231000533, 2.665384615385000266 ) ) ;
#23102=DIRECTION ( 'NONE',  ( 1.000000000000000000, 0.000000000000000000, 0.000000000000000000 ) ) ;
#23105=CARTESIAN_POINT ( 'NONE',  ( 7.385833333331250472, 2.685136886497773379, -7.146640356114973613 ) ) ;
#23112=CARTESIAN_POINT ( 'NONE',  ( 10.84419170916004660, 2.685373094371836356, -7.853312882625375302 ) ) ;
#23113=B_SPLINE_CURVE_WITH_KNOTS ( 'NONE', 3,
 ( #42877, #54051, #26110, #4768 ),
 .UNSPECIFIED., .F., .F.,
 ( 4, 4 ),
 ( 0.000000000000000000, 1.000000000000000000 ),
 .UNSPECIFIED. ) ;
#23115=CARTESIAN_POINT ( 'NONE',  ( 10.68362359175999998, 2.603561947343000060, 7.762063351517999976 ) ) ;
#23117=CARTESIAN_POINT ( 'NONE',  ( 7.105195101234886401, 5.342010355555824930, -7.330391889570061714 ) ) ;
#23125=ORIENTED_EDGE ( 'NONE', *, *, #21432, .F. ) ;
#23127=ORIENTED_EDGE ( 'NONE', *, *, #64083, .T. ) ;
#23128=CONICAL_SURFACE ( 'NONE', #45450, 12.44999944941000081, 0.7853981146832407223 ) ;
#23135=CARTESIAN_POINT ( 'NONE',  ( 11.14698693981000055, 5.129806801114000336, 5.886034047559999927 ) ) ;
#23139=CIRCLE ( 'NONE', #16442, 0.5000000000000000000 ) ;
#23141=CARTESIAN_POINT ( 'NONE',  ( 4.000000000000000000, -2.081773110051108322, -0.5564988119414342460 ) ) ;
#23145=EDGE_LOOP ( 'NONE', ( #38822, #40056, #31659, #57576 ) ) ;
#23146=CARTESIAN_POINT ( 'NONE',  ( 10.69798710243586548, 3.113013961156086751, -4.803896147529662208 ) ) ;
#23153=VERTEX_POINT ( 'NONE', #27363 ) ;
#23154=CARTESIAN_POINT ( 'NONE',  ( 10.26685100253999927, 2.832432432432000269, 6.822293592207000934 ) ) ;
#23156=( BOUNDED_SURFACE ( )  B_SPLINE_SURFACE ( 3, 3, ( 
 ( #40316, #61635, #56397, #8500, #29847, #8843, #3584, #46252, #11500, #43680, #21054 ),
 ( #62993, #6956, #65333, #27947, #68586, #47284, #4969, #38423, #28288, #32844, #64977 ),
 ( #16747, #15121, #49607, #17452, #22685, #6605, #31214, #10215, #63341, #38778, #57758 ),
 ( #54156, #20708, #52519, #59748, #4618, #68939, #17091, #38074, #43335, #12208, #59401 ) ),
 .UNSPECIFIED., .F., .F., .T. ) 
 B_SPLINE_SURFACE_WITH_KNOTS ( ( 4, 4 ),
 ( 4, 1, 1, 1, 1, 1, 1, 1, 4 ),
 ( 0.000000000000000000, 1.000000000000000000 ),
 ( 0.8312902889582000077, 0.8338388411866000105, 0.8555869174461000481, 0.8794646334507000285, 0.9056938526918999477, 0.9344431701381999966, 0.9658387281735000274, 1.000000000000000000, 1.004668145018999814 ),
 .UNSPECIFIED. ) 
 GEOMETRIC_REPRESENTATION_ITEM ( )  RATIONAL_B_SPLINE_SURFACE ( (
 ( 1.221026506593000160, 1.221026506593000160, 1.221026506593000160, 1.221026506593000160, 1.221026506593000160, 1.221026506593000160, 1.221026506593000160, 1.221026506593000160, 1.221026506593000160, 1.221026506593000160, 1.221026506593000160),
 ( 0.9263244978021999421, 0.9263244978021999421, 0.9263244978021999421, 0.9263244978021999421, 0.9263244978021999421, 0.9263244978021999421, 0.9263244978021999421, 0.9263244978021999421, 0.9263244978021999421, 0.9263244978021999421, 0.9263244978021999421),
 ( 0.9263244978021999421, 0.9263244978021999421, 0.9263244978021999421, 0.9263244978021999421, 0.9263244978021999421, 0.9263244978021999421, 0.9263244978021999421, 0.9263244978021999421, 0.9263244978021999421, 0.9263244978021999421, 0.9263244978021999421),
 ( 1.221026506593000160, 1.221026506593000160, 1.221026506593000160, 1.221026506593000160, 1.221026506593000160, 1.221026506593000160, 1.221026506593000160, 1.221026506593000160, 1.221026506593000160, 1.221026506593000160, 1.221026506593000160) ) ) 
 REPRESENTATION_ITEM ( '' )  SURFACE ( )  );
#23158=CARTESIAN_POINT ( 'NONE',  ( 7.073590560819000395, 3.668692617901999853, -8.939602259005999585 ) ) ;
#23161=CARTESIAN_POINT ( 'NONE',  ( 8.461669748674118807, 3.016807879086336630, 6.195864493290629049 ) ) ;
#23163=CARTESIAN_POINT ( 'NONE',  ( 9.038304719595000591, 3.867331042029999999, -9.227339949050001877 ) ) ;
#23168=AXIS2_PLACEMENT_3D ( 'NONE', #64499, #9997, #15252 ) ;
#23189=CARTESIAN_POINT ( 'NONE',  ( 5.399998535875000449, -12.98068687585000092, -1.765643277146000001 ) ) ;
#23203=CARTESIAN_POINT ( 'NONE',  ( 7.856851002541000106, 2.832432432432000269, -6.822293592207000934 ) ) ;
#23211=CARTESIAN_POINT ( 'NONE',  ( 7.000000000000000000, 10.80467225524999897, 3.475853594956999970 ) ) ;
#23215=DIRECTION ( 'NONE',  ( -1.000000000000000000, 0.000000000000000000, 0.000000000000000000 ) ) ;
#23221=CARTESIAN_POINT ( 'NONE',  ( 9.401145280412999128, 3.927090956378999742, -9.230892435423001530 ) ) ;
#23225=AXIS2_PLACEMENT_3D ( 'NONE', #58258, #59638, #64180 ) ;
#23230=CARTESIAN_POINT ( 'NONE',  ( 9.246064158776000852, 5.200883864107000321, -6.027780766890000308 ) ) ;
#23231=ORIENTED_EDGE ( 'NONE', *, *, #68553, .T. ) ;
#23233=CARTESIAN_POINT ( 'NONE',  ( 9.937409415358999354, 3.510662261693000108, -6.227052446266999830 ) ) ;
#23240=LINE ( 'NONE', #13103, #13769 ) ;
#23242=AXIS2_PLACEMENT_3D ( 'NONE', #30438, #62578, #40919 ) ;
#23247=CARTESIAN_POINT ( 'NONE',  ( 10.16821721959000158, 2.330395133894000548, -7.267461653224000173 ) ) ;
#23248=LINE ( 'NONE', #40357, #36335 ) ;
#23257=CARTESIAN_POINT ( 'NONE',  ( 8.938854719593997800, 5.597201461420000967, -8.171008079894999554 ) ) ;
#23265=DIRECTION ( 'NONE',  ( -1.000000000000000000, 0.000000000000000000, 0.000000000000000000 ) ) ;
#23267=DIRECTION ( 'NONE',  ( 1.239633395933026350E-11, -1.000000000000000000, 7.155734338404329264E-12 ) ) ;
#23268=CARTESIAN_POINT ( 'NONE',  ( 8.693164714044028685, 2.945149437845938856, -6.183674439331818817 ) ) ;
#23270=EDGE_CURVE ( 'NONE', #19975, #27999, #443, .T. ) ;
#23275=EDGE_LOOP ( 'NONE', ( #2454, #51947, #10676, #57262 ) ) ;
#23278=CARTESIAN_POINT ( 'NONE',  ( 9.600045280412000892, 3.021734963141999852, -6.070209284876999511 ) ) ;
#23286=CARTESIAN_POINT ( 'NONE',  ( 3.267613282616999903, -3.729289631816000039, 0.4698937791177000278 ) ) ;
#23287=ORIENTED_EDGE ( 'NONE', *, *, #36389, .F. ) ;
#23288=CONICAL_SURFACE ( 'NONE', #2088, 0.3796172482170003804, 0.7853981633972997312 ) ;
#23292=CARTESIAN_POINT ( 'NONE',  ( 9.015545280411000562, 4.175915362023999933, 5.699506188181000077 ) ) ;
#23293=VERTEX_POINT ( 'NONE', #44148 ) ;
#23295=CARTESIAN_POINT ( 'NONE',  ( 10.94048160847601991, 9.309402769125675547, 6.237066211927379200 ) ) ;
#23297=CARTESIAN_POINT ( 'NONE',  ( 10.70039988502543871, 3.823246508712561109, -8.849946088921042175 ) ) ;
#23301=EDGE_CURVE ( 'NONE', #40281, #14597, #9395, .T. ) ;
#23303=VERTEX_POINT ( 'NONE', #66481 ) ;
#23305=FACE_OUTER_BOUND ( 'NONE', #19556, .T. ) ;
#23308=CARTESIAN_POINT ( 'NONE',  ( 10.97312085988376928, 8.562142776844346770, -6.539677800798914475 ) ) ;
#23310=DIRECTION ( 'NONE',  ( 0.000000000000000000, -0.1218274111675001353, -0.9925512993736016476 ) ) ;
#23311=CARTESIAN_POINT ( 'NONE',  ( 8.188938565157510396, 2.652235273545433092, 7.263344527950063245 ) ) ;
#23319=CARTESIAN_POINT ( 'NONE',  ( 7.100000000000000533, 4.000000000000000000, 8.849999999999999645 ) ) ;
#23321=CARTESIAN_POINT ( 'NONE',  ( 4.900006121741999898, -6.122517096885939548E-17, -1.999970730383187734 ) ) ;
#23322=DIRECTION ( 'NONE',  ( 1.000000000000000000, 0.000000000000000000, 0.000000000000000000 ) ) ;
#23323=DIRECTION ( 'NONE',  ( 1.000000000000000000, 0.000000000000000000, 0.000000000000000000 ) ) ;
#23325=VECTOR ( 'NONE', #42111, 1000.000000000000000 ) ;
#23328=ORIENTED_EDGE ( 'NONE', *, *, #17460, .T. ) ;
#23332=CARTESIAN_POINT ( 'NONE',  ( 8.997439158776000312, 2.773858540272000184, -8.951250717848999727 ) ) ;
#23333=CARTESIAN_POINT ( 'NONE',  ( 3.292824395831999595, 2.812750220982000116, 1.557238109803000148 ) ) ;
#23338=VERTEX_POINT ( 'NONE', #23841 ) ;
#23341=CARTESIAN_POINT ( 'NONE',  ( 10.28314886242000092, 2.387776420306999992, 7.684265965147999644 ) ) ;
#23344=CARTESIAN_POINT ( 'NONE',  ( 9.215336765710809175, 2.659996753869333208, 7.664888201578709648 ) ) ;
#23346=CARTESIAN_POINT ( 'NONE',  ( 7.100000000000000533, 5.221516520829000640, -8.074802043613001246 ) ) ;
#23348=EDGE_CURVE ( 'NONE', #67676, #33524, #29364, .T. ) ;
#23351=CARTESIAN_POINT ( 'NONE',  ( 8.104887188112282814, 4.724403967564894558, -6.210088579440072643 ) ) ;
#23352=CARTESIAN_POINT ( 'NONE',  ( 10.41025778040999938, 4.690688562647999937, -6.142866736126999960 ) ) ;
#23356=ADVANCED_FACE ( 'NONE', ( #19632 ), #45177, .T. ) ;
#23359=LINE ( 'NONE', #22655, #67972 ) ;
#23361=ORIENTED_EDGE ( 'NONE', *, *, #28344, .F. ) ;
#23363=CARTESIAN_POINT ( 'NONE',  ( 8.320864158774000430, 3.894644548817000285, 6.044465307984999924 ) ) ;
#23365=CARTESIAN_POINT ( 'NONE',  ( 0.7415127311769281748, -2.608895429637665853, 2.390477409079596161 ) ) ;
#23366=CARTESIAN_POINT ( 'NONE',  ( 11.06205165877000063, 2.154392227069000132, -7.605898171884000192 ) ) ;
#23367=VERTEX_POINT ( 'NONE', #7410 ) ;
#23368=CARTESIAN_POINT ( 'NONE',  ( 10.18908827523999960, 5.907871695079999874, 7.801541097952000570 ) ) ;
#23372=FACE_OUTER_BOUND ( 'NONE', #54947, .T. ) ;
#23374=LINE ( 'NONE', #54146, #53325 ) ;
#23379=LINE ( 'NONE', #6601, #6428 ) ;
#23381=VERTEX_POINT ( 'NONE', #55312 ) ;
#23387=B_SPLINE_SURFACE_WITH_KNOTS ( 'NONE', 3, 3, ( 
 ( #58037, #47204, #25870, #52787, #46860, #41611, #41266, #62580, #68506, #31136, #9786, #36364, #15038, #15388, #52438, #20629, #52090, #14701, #41953, #36716, #36019, #68163, #3385, #67694, #30318, #20158, #4065, #35563, #25401, #51964, #19124, #40448, #35895, #34540, #68043 ),
 ( #61774, #41485, #7955, #55853, #46737, #13894, #67016, #2706, #19818, #24721, #29293, #35222, #24377, #62117, #8638, #62794, #41148, #56192, #62458, #14578, #45707, #50605, #14235, #56880, #24031, #45365, #66673, #8300, #13557, #8978, #29988, #57210, #40125, #51288, #29645 ),
 ( #46045, #67352, #9313, #40794, #18796, #19471, #61437, #51626, #34874, #50948, #3722, #30653, #25059, #3044, #46390, #56534, #21189, #26794, #53697, #5458, #209, #41827, #43207, #36238, #48453, #37610, #64171, #48109, #4413, #52659, #36584, #57910, #10009, #4755, #58941 ),
 ( #25751, #42862, #32384, #5791, #10693, #31005, #21529, #47080, #63135, #58249, #26097, #27133, #68730, #63485, #11048, #47422, #20849, #37271, #42519, #21870, #561, #5107, #52319, #16285, #15605, #68381, #63828, #20502, #15261, #42182, #31346, #14916, #57555, #10353, #15942 ) ),
 .UNSPECIFIED., .F., .F., .F.,
 ( 4, 4 ),
 ( 4, 1, 1, 1, 1, 1, 1, 1, 1, 1, 1, 1, 1, 1, 1, 1, 1, 1, 1, 1, 1, 1, 1, 1, 1, 1, 1, 1, 1, 1, 1, 1, 4 ),
 ( -0.1039370721279000015, 1.103937072127999963 ),
 ( -0.01933701211302999920, 0.01208563257065999909, 0.04350827725433999843, 0.07493092193802000645, 0.1063535666217000075, 0.1377762113054000204, 0.1691988559891000055, 0.2006215006727000150, 0.2320441453564000001, 0.2634667900400999851, 0.2948894347238000258, 0.3263120794074999553, 0.3577347240911999959, 0.3891573687748000054, 0.4205800134584999905, 0.4520026581421999756, 0.4834253028259000162, 0.5148479475096000568, 0.5462705921932000663, 0.5776932368768999959, 0.6091158815606000365, 0.6405385262443000771, 0.6719611709280000067, 0.7033838156117000473, 0.7348064602953000568, 0.7662291049789999864, 0.7976517496627000270, 0.8290743943464000676, 0.8604970390300999972, 0.8919196837138000378, 0.9233423283974000473, 0.9547649730810999769, 0.9861876177648000175 ),
 .UNSPECIFIED. ) ;
#23388=CARTESIAN_POINT ( 'NONE',  ( 8.804445280412998898, 5.597201461420000967, -8.171008079894999554 ) ) ;
#23394=ORIENTED_EDGE ( 'NONE', *, *, #11866, .T. ) ;
#23396=CARTESIAN_POINT ( 'NONE',  ( 9.174642513462172744, 2.649442673323004538, 7.499981897072118819 ) ) ;
#23411=EDGE_CURVE ( 'NONE', #5657, #21830, #62277, .T. ) ;
#23415=CARTESIAN_POINT ( 'NONE',  ( 9.278329719590999503, 5.791553967443999973, 7.752111263209999770 ) ) ;
#23418=CARTESIAN_POINT ( 'NONE',  ( 8.183771503764571520, 2.796787595787193492, 8.203896902613271536 ) ) ;
#23419=CARTESIAN_POINT ( 'NONE',  ( 10.76231429546999863, 3.259156861436999897, -8.644989069184999764 ) ) ;
#23422=CARTESIAN_POINT ( 'NONE',  ( 11.07202612390000063, 5.767975602871000085, 5.098339902409000146 ) ) ;
#23423=CARTESIAN_POINT ( 'NONE',  ( 9.967852198058999136, 2.034774058634999605, 7.636878205663998997 ) ) ;
#23429=CARTESIAN_POINT ( 'NONE',  ( 9.625496329943999285, 3.134638325776999856, 8.626949804392001653 ) ) ;
#23433=CARTESIAN_POINT ( 'NONE',  ( 8.085170280410000743, 2.431401017850999935, 7.958393275880999873 ) ) ;
#23434=CARTESIAN_POINT ( 'NONE',  ( 11.14698693981000055, 5.129806801114000336, 5.886034047559999927 ) ) ;
#23436=ORIENTED_EDGE ( 'NONE', *, *, #8691, .T. ) ;
#23437=CARTESIAN_POINT ( 'NONE',  ( 9.096889158776001238, 2.235961884443999459, -6.794506518623999902 ) ) ;
#23439=EDGE_CURVE ( 'NONE', #227, #46731, #32521, .T. ) ;
#23441=CARTESIAN_POINT ( 'NONE',  ( 11.09999999999999964, 2.685305999535000154, 6.664030027596000494 ) ) ;
#23447=ORIENTED_EDGE ( 'NONE', *, *, #41348, .F. ) ;
#23448=CARTESIAN_POINT ( 'NONE',  ( 1.167201286810000127, 1.556166911672999920, -2.863499806755999799 ) ) ;
#23450=CARTESIAN_POINT ( 'NONE',  ( 11.09999999999999964, 5.299316147296000423, -5.124965750789000296 ) ) ;
#23458=CARTESIAN_POINT ( 'NONE',  ( 7.364999999998000035, 2.649999999999999911, -7.500000000000000000 ) ) ;
#23460=CARTESIAN_POINT ( 'NONE',  ( 11.13508722347999935, 5.337982475388999504, 5.085688468496000425 ) ) ;
#23463=CARTESIAN_POINT ( 'NONE',  ( 1.943522225067000120, 1.849469983415999996, -3.272124421528999960 ) ) ;
#23465=DIRECTION ( 'NONE',  ( 0.000000000000000000, 0.000000000000000000, -1.000000000000000000 ) ) ;
#23475=CARTESIAN_POINT ( 'NONE',  ( 7.993786007972365049, 2.489810687196663430, 6.574732386051532096 ) ) ;
#23479=EDGE_LOOP ( 'NONE', ( #9204, #58123, #17818, #29413, #22444, #11974, #15447 ) ) ;
#23482=CARTESIAN_POINT ( 'NONE',  ( 4.149992563292000725, 1.007210908820210360, -1.747525841223985132 ) ) ;
#23484=CARTESIAN_POINT ( 'NONE',  ( 9.285195242305000818, 5.269680202247999823, 8.747831873285999649 ) ) ;
#23485=CARTESIAN_POINT ( 'NONE',  ( 8.559672690406999962, 5.100000000000000533, -6.571331466262537724 ) ) ;
#23486=CARTESIAN_POINT ( 'NONE',  ( 6.899999691988000450, 13.87069231928999891, 4.225386915259999654 ) ) ;
#23503=CARTESIAN_POINT ( 'NONE',  ( 6.775409439180998916, 5.278582711742999756, -7.933273873238999130 ) ) ;
#23504=CARTESIAN_POINT ( 'NONE',  ( 10.90000000000000036, 5.599999999999999645, 6.571291218949999902 ) ) ;
#23507=B_SPLINE_CURVE_WITH_KNOTS ( 'NONE', 3,
 ( #462, #58163, #5703, #63741 ),
 .UNSPECIFIED., .F., .F.,
 ( 4, 4 ),
 ( 0.000000000000000000, 0.1254918003289636208 ),
 .UNSPECIFIED. ) ;
#23508=CARTESIAN_POINT ( 'NONE',  ( 8.789679719592999874, 4.162493982103000256, -5.775210092227999858 ) ) ;
#23516=CARTESIAN_POINT ( 'NONE',  ( 1.115556799208874850, 0.4581489286485002088, 3.500000000000001776 ) ) ;
#23518=EDGE_CURVE ( 'NONE', #34596, #7076, #47670, .T. ) ;
#23523=CARTESIAN_POINT ( 'NONE',  ( 7.717206997734000318, 2.839603336731772565, 6.809939399899146650 ) ) ;
#23533=VERTEX_POINT ( 'NONE', #25563 ) ;
#23541=CARTESIAN_POINT ( 'NONE',  ( 5.500000000000000000, 12.78667792605000031, 2.345384795462000405 ) ) ;
#23545=CARTESIAN_POINT ( 'NONE',  ( 10.58422653167975902, 2.899999999999999911, 6.304440313954331465 ) ) ;
#23547=CARTESIAN_POINT ( 'NONE',  ( 0.000000000000000000, -2.899969545326000375, -0.3804588500739426449 ) ) ;
#23551=CARTESIAN_POINT ( 'NONE',  ( 4.900006121741999898, 1.999999999999999112, -0.2617993877991531826 ) ) ;
#23552=CARTESIAN_POINT ( 'NONE',  ( 7.000000000000001776, 10.07825177844479647, 4.450660970158813790 ) ) ;
#23559=CARTESIAN_POINT ( 'NONE',  ( 2.717640132544332676, -1.762666431298159475, 3.058252359239895135 ) ) ;
#23560=CARTESIAN_POINT ( 'NONE',  ( 9.053070280414001303, 2.391443348526999912, -6.856688371964000162 ) ) ;
#23567=CARTESIAN_POINT ( 'NONE',  ( 11.09999999999999964, 5.350000000000000533, -7.500000000000000000 ) ) ;
#23571=CARTESIAN_POINT ( 'NONE',  ( 9.988718791410999387, 2.842026940133999702, -6.504333051298999635 ) ) ;
#23577=CARTESIAN_POINT ( 'NONE',  ( 10.98768472569999943, 6.720753179915999631, -5.471698458723999181 ) ) ;
#23580=EDGE_CURVE ( 'NONE', #1011, #56588, #10145, .T. ) ;
#23586=CARTESIAN_POINT ( 'NONE',  ( 10.54684221959000112, 3.691673619534999951, -9.157283848447001162 ) ) ;
#23594=VERTEX_POINT ( 'NONE', #36048 ) ;
#23595=CARTESIAN_POINT ( 'NONE',  ( 9.047164158776000775, 2.156584729807999867, -7.959751745006000689 ) ) ;
#23608=CARTESIAN_POINT ( 'NONE',  ( 11.09999999999999964, 6.593648131501000265, 5.598803515845999890 ) ) ;
#23612=CARTESIAN_POINT ( 'NONE',  ( 4.149992563291998948, -1.007210908820212358, 1.747525841223983800 ) ) ;
#23613=ORIENTED_EDGE ( 'NONE', *, *, #63736, .F. ) ;
#23615=CARTESIAN_POINT ( 'NONE',  ( 9.883148997457000817, 5.167567567567999731, 6.822293592207000934 ) ) ;
#23616=CARTESIAN_POINT ( 'NONE',  ( 8.564679719593000229, 4.146787477634999775, -5.941926545671999627 ) ) ;
#23619=B_SPLINE_CURVE_WITH_KNOTS ( 'NONE', 3,
 ( #57533, #46717, #40427, #51602, #25038, #13871, #20479, #67331, #68019, #35202, #62095, #19450, #56512, #8618, #30634, #59254, #53677, #5771 ),
 .UNSPECIFIED., .F., .F.,
 ( 4, 2, 2, 2, 2, 2, 2, 2, 4 ),
 ( 0.000000000000000000, 0.1250000000000000000, 0.2500000000000000000, 0.3750000000000000000, 0.5000000000000000000, 0.6250000000000000000, 0.7500000000000000000, 0.8750000000000000000, 1.000000000000000000 ),
 .UNSPECIFIED. ) ;
#23624=CARTESIAN_POINT ( 'NONE',  ( 3.310521893996000387, -2.689871800245000610, 2.380848019370000124 ) ) ;
#23628=DIRECTION ( 'NONE',  ( -1.000000000000000000, 0.000000000000000000, 0.000000000000000000 ) ) ;
#23634=CARTESIAN_POINT ( 'NONE',  ( 7.639760841226999943, 5.116254232901999544, -8.340852485897000790 ) ) ;
#23641=CARTESIAN_POINT ( 'NONE',  ( 9.766851002543001314, 2.832432432432000269, 6.822293592207000934 ) ) ;
#23646=CARTESIAN_POINT ( 'NONE',  ( 10.94168356394703601, 9.287995240817338072, -6.252185766115418097 ) ) ;
#23647=CARTESIAN_POINT ( 'NONE',  ( 8.331682176603999679, 5.101289360622999425, 6.607176324693000424 ) ) ;
#23648=CARTESIAN_POINT ( 'NONE',  ( 7.540789158769000800, 5.122039080790999677, -6.666882531104000087 ) ) ;
#23649=CARTESIAN_POINT ( 'NONE',  ( 10.17500046684965120, 2.650307855385062972, 7.500001770945063484 ) ) ;
#23651=ORIENTED_EDGE ( 'NONE', *, *, #47045, .F. ) ;
#23652=CARTESIAN_POINT ( 'NONE',  ( 9.660528907822998335, 2.899999999999999911, -6.152188490330000370 ) ) ;
#23654=CARTESIAN_POINT ( 'NONE',  ( 10.97843137008999825, 5.235400103863000254, 6.782920672145000829 ) ) ;
#23656=VERTEX_POINT ( 'NONE', #1061 ) ;
#23663=EDGE_CURVE ( 'NONE', #16917, #7065, #53484, .T. ) ;
#23666=ORIENTED_EDGE ( 'NONE', *, *, #50052, .T. ) ;
#23671=CARTESIAN_POINT ( 'NONE',  ( 0.1499942179680000265, 0.7197945678028339067, 2.678379783547567339 ) ) ;
#23672=CARTESIAN_POINT ( 'NONE',  ( 8.541054719591000932, 3.807713920470999991, -9.221758713517999695 ) ) ;
#23674=CARTESIAN_POINT ( 'NONE',  ( 3.334741359309999709, 1.648620317156999970, 2.760184582139999954 ) ) ;
#23682=CARTESIAN_POINT ( 'NONE',  ( 10.66052890781999984, 2.899999999999999911, -6.152188490330000370 ) ) ;
#23686=CARTESIAN_POINT ( 'NONE',  ( 9.169143502787418853, 2.970327438714448931, 8.373611167771709773 ) ) ;
#23689=EDGE_CURVE ( 'NONE', #56100, #38774, #38106, .T. ) ;
#23692=B_SPLINE_CURVE_WITH_KNOTS ( 'NONE', 3,
 ( #2652, #24325, #45658, #7213, #28194, #19071, #39724, #61042, #49860, #40399, #44291, #50211, #33443, #60350, #13163, #7904, #23980, #61721, #55107, #28550, #23295, #44636, #65928, #18056, #60694, #12809, #34138, #35510, #47026, #13841, #30267, #62742, #8930, #63079, #4699, #25348, #29937, #68677, #68329, #3668, #19419, #62067 ),
 .UNSPECIFIED., .F., .F.,
 ( 4, 2, 2, 1, 2, 2, 2, 2, 1, 1, 1, 2, 2, 2, 2, 2, 2, 2, 2, 2, 2, 2, 4 ),
 ( 0.000000000000000000, 0.06250000000000227596, 0.09375000000000296985, 0.1093750000000033168, 0.1171875000000036221, 0.1250000000000039413, 0.1875000000000053013, 0.2187500000000060230, 0.2343750000000058564, 0.2421875000000067724, 0.2460937500000072164, 0.2480468750000070222, 0.2500000000000068279, 0.3125000000000048295, 0.3437500000000036082, 0.3593750000000036082, 0.3750000000000035527, 0.4374999999999996669, 0.4687499999999985012, 0.4999999999999973910, 0.6249999999999982236, 0.7499999999999990008, 1.000000000000000000 ),
 .UNSPECIFIED. ) ;
#23696=CARTESIAN_POINT ( 'NONE',  ( 10.25880778041000063, 2.491777456852000139, -7.289938575364999451 ) ) ;
#23703=CARTESIAN_POINT ( 'NONE',  ( 8.989142219592000771, 5.284130523641000110, 6.489275570566000795 ) ) ;
#23708=ORIENTED_EDGE ( 'NONE', *, *, #67689, .T. ) ;
#23709=CARTESIAN_POINT ( 'NONE',  ( 10.61382428715999993, 3.385080336122999967, 5.849521480782000182 ) ) ;
#23713=CARTESIAN_POINT ( 'NONE',  ( 7.581295643773000137, 2.929975047062999050, 6.543750339501001712 ) ) ;
#23715=DIRECTION ( 'NONE',  ( 0.000000000000000000, -0.7158784314710769925, 0.6982249432342778617 ) ) ;
#23716=CARTESIAN_POINT ( 'NONE',  ( 1.490556799207374716, 3.500000000000001776, -0.4581489286485044832 ) ) ;
#23723=CARTESIAN_POINT ( 'NONE',  ( 7.975339216757242333, 5.350090185752605976, 7.499980949462685231 ) ) ;
#23727=ORIENTED_EDGE ( 'NONE', *, *, #42056, .F. ) ;
#23729=CARTESIAN_POINT ( 'NONE',  ( 8.233179719589999834, 5.203550244299999683, -8.391678825488000371 ) ) ;
#23736=CARTESIAN_POINT ( 'NONE',  ( 7.645558129953747617, 3.263515245515704155, 8.650331983164434746 ) ) ;
#23740=CARTESIAN_POINT ( 'NONE',  ( 7.950512946206999665, 3.409920107335999706, -6.285779624696999690 ) ) ;
#23741=ORIENTED_EDGE ( 'NONE', *, *, #37638, .T. ) ;
#23747=ADVANCED_FACE ( 'NONE', ( #11531 ), #45761, .F. ) ;
#23754=EDGE_CURVE ( 'NONE', #26667, #63941, #44341, .T. ) ;
#23756=CARTESIAN_POINT ( 'NONE',  ( 7.583051658771000625, 4.763536573491999881, 5.668879554882000349 ) ) ;
#23764=CARTESIAN_POINT ( 'NONE',  ( 10.21609109105999913, 5.961715741921000067, 7.319666990313999477 ) ) ;
#23770=CARTESIAN_POINT ( 'NONE',  ( 11.24053267693000002, 2.774035422596999645, 6.782113650547000105 ) ) ;
#23776=CARTESIAN_POINT ( 'NONE',  ( 7.390489158771000433, 2.216873702600000051, 8.370081218683999680 ) ) ;
#23777=CARTESIAN_POINT ( 'NONE',  ( 9.504903297738000134, 3.934733353759999552, 5.704831249548000471 ) ) ;
#23780=CARTESIAN_POINT ( 'NONE',  ( 9.436104719595000745, 5.619431609641999614, -8.115423117607999615 ) ) ;
#23789=CARTESIAN_POINT ( 'NONE',  ( 1.877657190359999895, 3.109069236570999539, 1.438230559479999782 ) ) ;
#23800=ORIENTED_EDGE ( 'NONE', *, *, #11337, .T. ) ;
#23801=CARTESIAN_POINT ( 'NONE',  ( 8.727045280411999784, 3.882020551409000042, 5.870058896428999695 ) ) ;
#23806=CARTESIAN_POINT ( 'NONE',  ( 0.7943821004246000017, -2.155162080922000012, 2.873869168568000010 ) ) ;
#23807=VERTEX_POINT ( 'NONE', #28856 ) ;
#23808=CARTESIAN_POINT ( 'NONE',  ( 1.990556799206333105, 3.500000000000001776, -0.4581489286485044832 ) ) ;
#23810=CARTESIAN_POINT ( 'NONE',  ( 9.388624299788999039, 4.079402096444999515, 9.259357173634999327 ) ) ;
#23817=CARTESIAN_POINT ( 'NONE',  ( 8.314631905207910734, 4.229903678034249381, 9.254809312259414611 ) ) ;
#23818=ORIENTED_EDGE ( 'NONE', *, *, #6773, .F. ) ;
#23826=DIRECTION ( 'NONE',  ( -1.000000000000000000, 0.000000000000000000, 4.629487027166999918E-14 ) ) ;
#23827=DIRECTION ( 'NONE',  ( 0.000000000000000000, 1.000000000000000000, 0.000000000000000000 ) ) ;
#23828=CARTESIAN_POINT ( 'NONE',  ( 10.64447074117000014, 5.073827170570999634, -8.340679549192000053 ) ) ;
#23829=CARTESIAN_POINT ( 'NONE',  ( 7.100000000000000533, 0.000000000000000000, 11.84999999999999964 ) ) ;
#23830=CARTESIAN_POINT ( 'NONE',  ( 11.09999999999999964, 7.357009467662000368, -6.362164853100000350 ) ) ;
#23831=B_SPLINE_CURVE_WITH_KNOTS ( 'NONE', 3,
 ( #23615, #44273, #50880, #61369 ),
 .UNSPECIFIED., .F., .F.,
 ( 4, 4 ),
 ( 0.000000000000000000, 0.1253704142480318307 ),
 .UNSPECIFIED. ) ;
#23835=CARTESIAN_POINT ( 'NONE',  ( 3.999985533191000364, -6.914809019160056625E-16, -2.149963194831858715 ) ) ;
#23841=CARTESIAN_POINT ( 'NONE',  ( 7.900104261408000816, 3.351183067932000270, -6.316134894229000096 ) ) ;
#23843=CARTESIAN_POINT ( 'NONE',  ( 11.05626362482999880, 7.348667259608998137, 6.145046404742999790 ) ) ;
#23851=PLANE ( 'NONE',  #25353 ) ;
#23858=CARTESIAN_POINT ( 'NONE',  ( 9.378359312500634815, 5.126777126186428113, 6.752018918873821107 ) ) ;
#23859=CARTESIAN_POINT ( 'NONE',  ( 0.02212111259145000189, 1.258511261458999941, -3.306246502378999974 ) ) ;
#23861=CARTESIAN_POINT ( 'NONE',  ( 8.314979508587148516, 2.649972834346558059, -7.499998738096613771 ) ) ;
#23877=ADVANCED_FACE ( 'NONE', ( #44242 ), #55756, .F. ) ;
#23878=CARTESIAN_POINT ( 'NONE',  ( 11.09999999999999964, 4.000000000000000000, -7.500000000000000000 ) ) ;
#23884=DIRECTION ( 'NONE',  ( -0.7071067811865952013, 0.7071067811864951702, -8.251256364954943451E-08 ) ) ;
#23894=CARTESIAN_POINT ( 'NONE',  ( -0.000000000000000000, -2.533832635911827502, -1.460960874862264225 ) ) ;
#23899=CARTESIAN_POINT ( 'NONE',  ( 3.499999999999999556, -2.703350975099395814, 1.634640570342158705 ) ) ;
#23900=CARTESIAN_POINT ( 'NONE',  ( 8.126014158770999529, 5.189036231907000030, -8.048606212067999977 ) ) ;
#23903=CARTESIAN_POINT ( 'NONE',  ( 4.000000000000000000, 1.719326598156197372, 1.321078631445046669 ) ) ;
#23905=ORIENTED_EDGE ( 'NONE', *, *, #27386, .F. ) ;
#23908=CARTESIAN_POINT ( 'NONE',  ( 8.813304719595000947, 3.880154689736000417, -9.060377011187000562 ) ) ;
#23914=CARTESIAN_POINT ( 'NONE',  ( 7.639326144738664226, 5.301174781770192190, -7.912266426404620745 ) ) ;
#23916=EDGE_CURVE ( 'NONE', #34596, #19886, #50849, .T. ) ;
#23918=CARTESIAN_POINT ( 'NONE',  ( 9.295789158775001226, 5.835196551504000517, -7.008466539623000813 ) ) ;
#23920=CONICAL_SURFACE ( 'NONE', #455, 2.049966935984999683, 0.7853819979415218588 ) ;
#23921=CARTESIAN_POINT ( 'NONE',  ( 10.52662718686000076, 4.933722097448000277, -6.506013113666999637 ) ) ;
#23923=VERTEX_POINT ( 'NONE', #41043 ) ;
#23927=CARTESIAN_POINT ( 'NONE',  ( -14.79345512259999929, 10.48174933044999868, -5.405686454350000503 ) ) ;
#23934=CARTESIAN_POINT ( 'NONE',  ( 10.94033278040999946, 5.142729166069000435, -6.493505370358000128 ) ) ;
#23940=EDGE_CURVE ( 'NONE', #4878, #69017, #63500, .T. ) ;
#23947=CARTESIAN_POINT ( 'NONE',  ( 9.743314158772999889, 5.149303692842000402, -5.987168472229000393 ) ) ;
#23948=CARTESIAN_POINT ( 'NONE',  ( 6.433333127195900225, 12.43895222601385697, 2.828919834970925251 ) ) ;
#23965=CARTESIAN_POINT ( 'NONE',  ( 8.754720280412998434, 5.687930027805999877, -7.109876198051000351 ) ) ;
#23966=CARTESIAN_POINT ( 'NONE',  ( 8.610944094208999644, 5.100000000000000533, -6.571291218949999902 ) ) ;
#23969=DIRECTION ( 'NONE',  ( 1.000000000000000000, 0.000000000000000000, 0.000000000000000000 ) ) ;
#23972=CARTESIAN_POINT ( 'NONE',  ( 2.738338500705999934, 0.2183327149865000039, 3.585551516645999914 ) ) ;
#23977=CARTESIAN_POINT ( 'NONE',  ( 8.192489158772998437, 2.550241116032999855, 7.666973618349000041 ) ) ;
#23980=CARTESIAN_POINT ( 'NONE',  ( 10.93980696525934171, 9.321087494126425455, 6.228652191884624045 ) ) ;
#23983=CIRCLE ( 'NONE', #12813, 2.000000000000000000 ) ;
#23985=CARTESIAN_POINT ( 'NONE',  ( 11.09999999999999964, 3.512324525112999751, -8.971282648301999174 ) ) ;
#23989=CYLINDRICAL_SURFACE ( 'NONE', #44005, 3.500000000000000000 ) ;
#23993=CARTESIAN_POINT ( 'NONE',  ( 10.91202604904536777, 9.732768313057503562, -5.831340146199694985 ) ) ;
#23995=CARTESIAN_POINT ( 'NONE',  ( 7.988314158770000617, 4.376386084436000523, -6.154119786874999498 ) ) ;
#23996=CARTESIAN_POINT ( 'NONE',  ( 10.21612608405689038, 2.826342078250798195, 6.832754235737262150 ) ) ;
#23998=VERTEX_POINT ( 'NONE', #67255 ) ;
#24004=B_SPLINE_CURVE_WITH_KNOTS ( 'NONE', 3,
 ( #22463, #60232, #1847, #43809 ),
 .UNSPECIFIED., .F., .F.,
 ( 4, 4 ),
 ( 0.000000000000000000, 1.000000000000000000 ),
 .UNSPECIFIED. ) ;
#24008=DIRECTION ( 'NONE',  ( 0.000000000000000000, -1.000000000000000000, 0.000000000000000000 ) ) ;
#24009=CARTESIAN_POINT ( 'NONE',  ( 0.04997405931212996200, -2.849971983161023292, -1.472631476147704172E-09 ) ) ;
#24010=CARTESIAN_POINT ( 'NONE',  ( 3.499999999999999556, 1.045906356845314189, 3.160857899937222992 ) ) ;
#24019=CARTESIAN_POINT ( 'NONE',  ( 9.038304719595000591, 3.867331042029999999, -9.227339949050001877 ) ) ;
#24020=CARTESIAN_POINT ( 'NONE',  ( 2.838494431446000110, 3.373532321960999614, -0.1987882563307999950 ) ) ;
#24028=CARTESIAN_POINT ( 'NONE',  ( 9.261662452849000360, 2.944259351255000379, 6.507396354981000108 ) ) ;
#24031=CARTESIAN_POINT ( 'NONE',  ( 10.62197831623999988, 5.779783227492000464, 7.256572995198999898 ) ) ;
#24032=CARTESIAN_POINT ( 'NONE',  ( 11.06666666666770382, 2.480181672120659986, 7.732127511715679802 ) ) ;
#24034=CARTESIAN_POINT ( 'NONE',  ( 8.610875063856999745, 4.757997781751000410, 5.934102420827000124 ) ) ;
#24039=CARTESIAN_POINT ( 'NONE',  ( 10.90000000011000125, 2.899999999889000257, -6.571291220762999430 ) ) ;
#24040=CARTESIAN_POINT ( 'NONE',  ( 10.37239528041000014, 3.992345698584000235, -5.977238432995000572 ) ) ;
#24047=CARTESIAN_POINT ( 'NONE',  ( 7.614801658771000348, 3.326263523254000098, 8.794511546544999447 ) ) ;
#24048=CARTESIAN_POINT ( 'NONE',  ( 8.456370280410999030, 2.836879604150999601, -8.783908972046001296 ) ) ;
#24049=CARTESIAN_POINT ( 'NONE',  ( 0.7061642493978850244, -1.328001061679412009, 3.278594772182098271 ) ) ;
#24050=CARTESIAN_POINT ( 'NONE',  ( 10.68342665876999931, 3.810131921595000026, -5.661115150006999386 ) ) ;
#24053=EDGE_CURVE ( 'NONE', #21968, #10113, #40124, .T. ) ;
#24059=VERTEX_POINT ( 'NONE', #13457 ) ;
#24063=VECTOR ( 'NONE', #39144, 1000.000000000000114 ) ;
#24070=ORIENTED_EDGE ( 'NONE', *, *, #44371, .F. ) ;
#24074=CARTESIAN_POINT ( 'NONE',  ( 9.044210841233001119, 2.773858540272000184, -8.951250717848999727 ) ) ;
#24076=CARTESIAN_POINT ( 'NONE',  ( 8.288053023084509974, 5.073577879423888604, 6.476688461073075054 ) ) ;
#24094=CARTESIAN_POINT ( 'NONE',  ( 2.500973465876000112, 3.500000000000000000, 0.000000000000000000 ) ) ;
#24098=B_SPLINE_CURVE_WITH_KNOTS ( 'NONE', 3,
 ( #33997, #34348, #29107, #50413, #44836, #60560, #29456, #61251, #40608, #29801 ),
 .UNSPECIFIED., .F., .F.,
 ( 4, 2, 2, 2, 4 ),
 ( 0.5000000000000005551, 0.6250000000000004441, 0.7500000000000002220, 0.8750000000000001110, 1.000000000000000000 ),
 .UNSPECIFIED. ) ;
#24100=FACE_OUTER_BOUND ( 'NONE', #11457, .T. ) ;
#24101=DIRECTION ( 'NONE',  ( -1.000000000000000000, 0.000000000000000000, 0.000000000000000000 ) ) ;
#24111=ORIENTED_EDGE ( 'NONE', *, *, #34269, .T. ) ;
#24114=CARTESIAN_POINT ( 'NONE',  ( 9.500006116823001889, 2.279680316922000127, 7.877692351087999256 ) ) ;
#24120=CARTESIAN_POINT ( 'NONE',  ( 7.374100552923999352, 4.389299166881000858, 9.135259451319999613 ) ) ;
#24121=CARTESIAN_POINT ( 'NONE',  ( 10.31167969999000000, 2.874476822401000220, 8.900029516786000627 ) ) ;
#24124=CARTESIAN_POINT ( 'NONE',  ( 8.599639158772999892, 2.261390688294000029, -6.733978371730000134 ) ) ;
#24132=AXIS2_PLACEMENT_3D ( 'NONE', #54936, #33963, #55285 ) ;
#24133=CARTESIAN_POINT ( 'NONE',  ( 1.825201902854999947, 0.7365451747729999665, -3.515871166463000019 ) ) ;
#24143=CARTESIAN_POINT ( 'NONE',  ( 9.584226531641581559, 2.899999999999999911, 6.304440313841761068 ) ) ;
#24145=ORIENTED_EDGE ( 'NONE', *, *, #64064, .T. ) ;
#24146=ADVANCED_FACE ( 'NONE', ( #22807 ), #34007, .T. ) ;
#24147=CARTESIAN_POINT ( 'NONE',  ( 9.010198341230998054, 5.040787533781999841, 8.522957620707000359 ) ) ;
#24151=CARTESIAN_POINT ( 'NONE',  ( 1.652657190360000028, 3.260257002997999809, 1.508168810892000167 ) ) ;
#24153=CARTESIAN_POINT ( 'NONE',  ( 1.865556799206333549, -0.4581489286485082579, -3.500000000000000888 ) ) ;
#24155=CARTESIAN_POINT ( 'NONE',  ( 10.05691520198999989, 2.453477278391000382, 6.657104391228999773 ) ) ;
#24162=CARTESIAN_POINT ( 'NONE',  ( 7.682133832350131364, 5.705319479758692580, 7.108996016928172956 ) ) ;
#24170=CARTESIAN_POINT ( 'NONE',  ( 4.149992563291999836, 4.286198015044692593E-16, -1.999973142472143861 ) ) ;
#24172=CARTESIAN_POINT ( 'NONE',  ( 10.40227026081000083, 2.765684886876999649, 9.035354958280999327 ) ) ;
#24174=CARTESIAN_POINT ( 'NONE',  ( 9.780284676292000157, 3.021596928575999819, -8.450035627617001666 ) ) ;
#24175=CARTESIAN_POINT ( 'NONE',  ( 8.784042939651088844, 2.728506136107232471, -8.022165079612438632 ) ) ;
#24181=ORIENTED_EDGE ( 'NONE', *, *, #68504, .F. ) ;
#24184=CARTESIAN_POINT ( 'NONE',  ( 10.60679199295805475, 3.308080241071473360, -4.759410728272197133 ) ) ;
#24185=ADVANCED_FACE ( 'NONE', ( #49730 ), #2763, .T. ) ;
#24186=CARTESIAN_POINT ( 'NONE',  ( 9.991825906548994496, 7.624304478282991404, 5.686370327077997722 ) ) ;
#24191=EDGE_CURVE ( 'NONE', #36211, #53667, #45206, .T. ) ;
#24195=DIRECTION ( 'NONE',  ( 0.000000000000000000, 0.000000000000000000, 1.000000000000000000 ) ) ;
#24196=CARTESIAN_POINT ( 'NONE',  ( 6.899999691988000450, 12.43893545635000031, 2.828937028792000152 ) ) ;
#24200=FACE_OUTER_BOUND ( 'NONE', #39963, .T. ) ;
#24210=CARTESIAN_POINT ( 'NONE',  ( 10.98768472567999943, 6.720753181080999283, 5.471698459870999898 ) ) ;
#24211=ORIENTED_EDGE ( 'NONE', *, *, #38767, .T. ) ;
#24218=CARTESIAN_POINT ( 'NONE',  ( 9.110944094209999733, 5.100000000000000533, -6.571291218949999902 ) ) ;
#24223=ORIENTED_EDGE ( 'NONE', *, *, #19173, .F. ) ;
#24228=DIRECTION ( 'NONE',  ( 0.000000000000000000, 0.000000000000000000, -1.000000000000000000 ) ) ;
#24231=CARTESIAN_POINT ( 'NONE',  ( 10.97843137008999825, 5.235400103863000254, 6.782920672145000829 ) ) ;
#24233=VECTOR ( 'NONE', #61063, 999.9999999999998863 ) ;
#24235=DIRECTION ( 'NONE',  ( 0.000000000000000000, -1.000000000000000000, 0.000000000000000000 ) ) ;
#24241=CARTESIAN_POINT ( 'NONE',  ( 2.358466522725250147, -0.7663246491380458769, -3.431732421873642469 ) ) ;
#24243=CARTESIAN_POINT ( 'NONE',  ( 9.459729719592999686, 2.527713920559999661, -6.969421869128999525 ) ) ;
#24245=ORIENTED_EDGE ( 'NONE', *, *, #38112, .T. ) ;
#24246=CARTESIAN_POINT ( 'NONE',  ( 4.000000000000000000, -0.2816038378556620092, 2.150035234257813954 ) ) ;
#24250=DIRECTION ( 'NONE',  ( 0.7071090068939822615, 0.000000000000000000, -0.7071045554721071547 ) ) ;
#24251=CARTESIAN_POINT ( 'NONE',  ( 8.804445280412998898, 5.597201461420000967, -8.171008079894999554 ) ) ;
#24257=CARTESIAN_POINT ( 'NONE',  ( 7.846076405120456343, 2.673882995022637932, -7.823504703768565882 ) ) ;
#24263=CARTESIAN_POINT ( 'NONE',  ( 10.77434248675000106, 4.612886656332999991, -8.898793847069001117 ) ) ;
#24268=ADVANCED_FACE ( 'NONE', ( #34702 ), #61096, .T. ) ;
#24270=CARTESIAN_POINT ( 'NONE',  ( 7.100000000000000533, 0.000000000000000000, 0.000000000000000000 ) ) ;
#24277=CARTESIAN_POINT ( 'NONE',  ( 8.061933748689000367, 4.603465626214999773, -6.221450782568999749 ) ) ;
#24278=CARTESIAN_POINT ( 'NONE',  ( 8.732935610179060504, 4.384544241869580361, -5.799574763991691917 ) ) ;
#24280=AXIS2_PLACEMENT_3D ( 'NONE', #58199, #10301, #502 ) ;
#24288=CARTESIAN_POINT ( 'NONE',  ( 8.400739158770999637, 4.933589693325000525, -9.154576215408999573 ) ) ;
#24289=CARTESIAN_POINT ( 'NONE',  ( 4.900006121741999010, -2.000000000000000000, 0.000000000000000000 ) ) ;
#24295=LINE ( 'NONE', #44609, #2708 ) ;
#24296=CARTESIAN_POINT ( 'NONE',  ( 10.44773515093974403, 5.286251723462902952, 7.027580072218848173 ) ) ;
#24298=CARTESIAN_POINT ( 'NONE',  ( 0.1359928592618749876, 2.324556273228959184E-06, -3.136013406113613122 ) ) ;
#24304=ORIENTED_EDGE ( 'NONE', *, *, #44335, .T. ) ;
#24305=CARTESIAN_POINT ( 'NONE',  ( 8.587349144951568647, 5.286378939600184346, -7.027172277035280246 ) ) ;
#24307=CIRCLE ( 'NONE', #63367, 13.10000000000000142 ) ;
#24314=DIRECTION ( 'NONE',  ( 0.000000000000000000, 1.000000000000000000, 0.000000000000000000 ) ) ;
#24315=CARTESIAN_POINT ( 'NONE',  ( 2.786020450147000282, -1.841856495097000002, 3.084057960614999594 ) ) ;
#24316=ORIENTED_EDGE ( 'NONE', *, *, #2564, .F. ) ;
#24323=ORIENTED_EDGE ( 'NONE', *, *, #1822, .T. ) ;
#24325=CARTESIAN_POINT ( 'NONE',  ( 10.90258158703495006, 9.831149648873696023, 5.672179247097546728 ) ) ;
#24326=ADVANCED_FACE ( 'NONE', ( #24884 ), #46214, .T. ) ;
#24327=CARTESIAN_POINT ( 'NONE',  ( 7.000000000000000000, 6.255435840762999966, -3.000000000000000000 ) ) ;
#24328=CARTESIAN_POINT ( 'NONE',  ( 1.500973465873999935, 3.500000000000000000, 0.000000000000000000 ) ) ;
#24331=ORIENTED_EDGE ( 'NONE', *, *, #2275, .F. ) ;
#24338=CARTESIAN_POINT ( 'NONE',  ( 10.96923347446639774, 8.678024018201968559, -6.520394081641061490 ) ) ;
#24339=FACE_OUTER_BOUND ( 'NONE', #45915, .T. ) ;
#24345=CARTESIAN_POINT ( 'NONE',  ( 2.073890132539958131, 2.150913519912194705, 2.798833948393636639 ) ) ;
#24348=FACE_OUTER_BOUND ( 'NONE', #59414, .T. ) ;
#24353=CARTESIAN_POINT ( 'NONE',  ( 6.875000000000000000, 5.574137966889000317, -8.240733100917999820 ) ) ;
#24362=CARTESIAN_POINT ( 'NONE',  ( 9.534905769125000319, 3.030948166328000237, 8.761984216465000586 ) ) ;
#24363=B_SPLINE_CURVE_WITH_KNOTS ( 'NONE', 3,
 ( #41770, #30943, #46682, #31291, #5396, #4355, #26385, #58530, #47020, #10636 ),
 .UNSPECIFIED., .F., .F.,
 ( 4, 2, 2, 2, 4 ),
 ( 0.000000000000000000, 0.2500000000000000000, 0.5000000000000000000, 0.7500000000000000000, 1.000000000000000000 ),
 .UNSPECIFIED. ) ;
#24365=CARTESIAN_POINT ( 'NONE',  ( 10.06481084123000080, 5.336630274082000192, -7.092011739486999922 ) ) ;
#24366=CARTESIAN_POINT ( 'NONE',  ( 3.019675553083999819, 3.701628467739999984, -0.2181216002955000122 ) ) ;
#24372=( GEOMETRIC_REPRESENTATION_CONTEXT ( 3 ) GLOBAL_UNCERTAINTY_ASSIGNED_CONTEXT ( ( #49759 ) ) GLOBAL_UNIT_ASSIGNED_CONTEXT ( ( #64260, #58682, #32130 ) ) REPRESENTATION_CONTEXT ( 'NONE', 'WORKASPACE' ) );
#24374=CARTESIAN_POINT ( 'NONE',  ( 10.87521525736000072, 4.831064930369000088, 6.312796576761000367 ) ) ;
#24375=DIRECTION ( 'NONE',  ( 0.000000000000000000, 0.9999285272608851027, -0.01195576722244981981 ) ) ;
#24377=CARTESIAN_POINT ( 'NONE',  ( 9.877261637240000169, 2.207988120125000009, 7.624813826992999921 ) ) ;
#24378=CARTESIAN_POINT ( 'NONE',  ( 9.160383927730638476, 3.070077541678596589, 8.479412441495636443 ) ) ;
#24389=ADVANCED_FACE ( 'NONE', ( #2525 ), #23851, .T. ) ;
#24395=CARTESIAN_POINT ( 'NONE',  ( 8.962739158771999115, 5.445214367171999470, 7.703373622193999459 ) ) ;
#24398=CARTESIAN_POINT ( 'NONE',  ( 11.11477971959000044, 2.548217283716999848, -8.356742414746999970 ) ) ;
#24407=CARTESIAN_POINT ( 'NONE',  ( 1.396806799207750194, 0.9161175952574848180, -3.408904368339103819 ) ) ;
#24416=B_SPLINE_CURVE_WITH_KNOTS ( 'NONE', 3,
 ( #44521, #27742, #49055, #43818, #33328, #28431, #49745, #1854, #23516, #65814, #17939, #39258, #34025, #55338, #39603, #7434, #35735, #29822 ),
 .UNSPECIFIED., .F., .F.,
 ( 4, 2, 2, 2, 2, 2, 2, 2, 4 ),
 ( 0.000000000000000000, 0.1250000000000000000, 0.2500000000000000000, 0.3750000000000000000, 0.5000000000000000000, 0.6250000000000000000, 0.7500000000000000000, 0.8750000000000000000, 1.000000000000000000 ),
 .UNSPECIFIED. ) ;
#24418=EDGE_LOOP ( 'NONE', ( #3266, #11607, #58063, #18342, #25867 ) ) ;
#24424=CARTESIAN_POINT ( 'NONE',  ( 9.881820280408998514, 4.325866256860000369, -9.125812605905000652 ) ) ;
#24430=CARTESIAN_POINT ( 'NONE',  ( 7.860170280410000210, 2.263558315407000254, 8.007442119518000112 ) ) ;
#24441=CARTESIAN_POINT ( 'NONE',  ( 9.797119508974258650, 5.515971184441423425, -6.595903550150567618 ) ) ;
#24449=AXIS2_PLACEMENT_3D ( 'NONE', #41814, #14566, #35883 ) ;
#24450=CARTESIAN_POINT ( 'NONE',  ( 10.32891357011167166, 2.649873868442942371, -7.263327745080984776 ) ) ;
#24451=CARTESIAN_POINT ( 'NONE',  ( 7.975339216757242333, 5.350090185752605976, 7.499980949462685231 ) ) ;
#24457=ADVANCED_FACE ( 'NONE', ( #47851 ), #51900, .F. ) ;
#24458=CARTESIAN_POINT ( 'NONE',  ( 11.18051582549000145, 5.340073783367000892, 8.416152717850000187 ) ) ;
#24463=CARTESIAN_POINT ( 'NONE',  ( 11.01776904286000125, 4.914120883409999863, 8.587704221454000475 ) ) ;
#24467=CARTESIAN_POINT ( 'NONE',  ( 8.224926658773000554, 5.629399530851999955, 8.631829656822000985 ) ) ;
#24468=CARTESIAN_POINT ( 'NONE',  ( 10.09696969267000100, 5.253376380222999131, 8.530663119653999260 ) ) ;
#24469=CIRCLE ( 'NONE', #18886, 0.5000000000000000000 ) ;
#24471=VERTEX_POINT ( 'NONE', #39424 ) ;
#24472=CARTESIAN_POINT ( 'NONE',  ( 8.699089158774000907, 4.178200486578000472, -5.608493638783999202 ) ) ;
#24474=EDGE_CURVE ( 'NONE', #8000, #44629, #28446, .T. ) ;
#24475=EDGE_CURVE ( 'NONE', #62424, #44629, #35861, .T. ) ;
#24482=EDGE_CURVE ( 'NONE', #14271, #60041, #45896, .T. ) ;
#24483=CARTESIAN_POINT ( 'NONE',  ( 1.343609070385000104, -2.423129934138000152, -2.873468012158999940 ) ) ;
#24484=CARTESIAN_POINT ( 'NONE',  ( 10.98768472639999949, 2.860903110339000133, 4.945212061661000469 ) ) ;
#24488=CARTESIAN_POINT ( 'NONE',  ( 10.01533268956000100, 4.946987614118000032, 8.559212393557999121 ) ) ;
#24494=CARTESIAN_POINT ( 'NONE',  ( 7.609454719589999527, 3.276311362504999991, 5.841989464160999290 ) ) ;
#24499=CARTESIAN_POINT ( 'NONE',  ( 1.986430836446000159, -0.3042438094541999871, -3.579344195347000213 ) ) ;
#24501=FACE_BOUND ( 'NONE', #64142, .T. ) ;
#24505=CARTESIAN_POINT ( 'NONE',  ( 11.14994211610999919, 2.627136771666999771, 6.696094414592000277 ) ) ;
#24507=DIRECTION ( 'NONE',  ( 0.000000000000000000, -1.000000000000000000, 0.000000000000000000 ) ) ;
#24512=CARTESIAN_POINT ( 'NONE',  ( 7.836291913262656728, 3.773376814137977320, 9.261296850680157178 ) ) ;
#24516=VERTEX_POINT ( 'NONE', #41823 ) ;
#24517=VERTEX_POINT ( 'NONE', #46733 ) ;
#24521=CARTESIAN_POINT ( 'NONE',  ( 9.034110134264999203, 4.695345051283999815, 8.660667941667000491 ) ) ;
#24522=CARTESIAN_POINT ( 'NONE',  ( 10.81905590578999998, 2.899999999999999911, -6.571291218949999902 ) ) ;
#24535=EDGE_CURVE ( 'NONE', #66219, #20189, #68039, .T. ) ;
#24542=ORIENTED_EDGE ( 'NONE', *, *, #30702, .T. ) ;
#24546=PLANE ( 'NONE',  #59786 ) ;
#24550=CARTESIAN_POINT ( 'NONE',  ( 8.813083809908729194, 2.920641027582035143, -8.329586155797288782 ) ) ;
#24552=CARTESIAN_POINT ( 'NONE',  ( 0.3511782687132000147, -3.457229061792999936, 0.7500022461462000356 ) ) ;
#24553=CARTESIAN_POINT ( 'NONE',  ( 11.07766112459999874, 2.724913093130999719, 5.089213754333000495 ) ) ;
#24557=CARTESIAN_POINT ( 'NONE',  ( 6.999998782146999332, -11.95749337870000062, -3.642574926947999892 ) ) ;
#24577=ADVANCED_FACE ( 'NONE', ( #4408 ), #3718, .F. ) ;
#24583=CARTESIAN_POINT ( 'NONE',  ( 10.20000099824999928, 0.000000000000000000, 0.000000000000000000 ) ) ;
#24584=ORIENTED_EDGE ( 'NONE', *, *, #60890, .T. ) ;
#24592=CARTESIAN_POINT ( 'NONE',  ( 8.374639158773000247, 2.721111233225000259, -6.936528696292000085 ) ) ;
#24596=CARTESIAN_POINT ( 'NONE',  ( 4.000000000000000000, 0.2816038378556620092, 2.149891155406186805 ) ) ;
#24600=CARTESIAN_POINT ( 'NONE',  ( 0.2500098862125000321, 0.000000000000000000, -3.249989426617000188 ) ) ;
#24601=CARTESIAN_POINT ( 'NONE',  ( 9.003345280414000840, 2.319062457810000311, -7.919229449146000022 ) ) ;
#24604=LINE ( 'NONE', #25977, #13654 ) ;
#24605=DIRECTION ( 'NONE',  ( -1.000000000000000000, 0.000000000000000000, 0.000000000000000000 ) ) ;
#24606=VERTEX_POINT ( 'NONE', #12683 ) ;
#24607=DIRECTION ( 'NONE',  ( 1.000000000000000000, 0.000000000000000000, 0.000000000000000000 ) ) ;
#24609=CARTESIAN_POINT ( 'NONE',  ( 10.01622971959000097, 4.325866256860000369, -9.125812605905000652 ) ) ;
#24610=ORIENTED_EDGE ( 'NONE', *, *, #61702, .F. ) ;
#24611=CARTESIAN_POINT ( 'NONE',  ( 10.11859053700000111, 3.393394511985999618, -5.921995869926000466 ) ) ;
#24618=EDGE_CURVE ( 'NONE', #30029, #23303, #5241, .T. ) ;
#24625=CARTESIAN_POINT ( 'NONE',  ( 10.99306084123000105, 4.495422912016000083, -6.233618171705999522 ) ) ;
#24633=CARTESIAN_POINT ( 'NONE',  ( 7.836395553874887732, 4.967689597840368343, 6.498195682940909101 ) ) ;
#24635=EDGE_LOOP ( 'NONE', ( #19712, #5518, #10120 ) ) ;
#24636=CARTESIAN_POINT ( 'NONE',  ( 9.526695280414001488, 5.462898983065000102, -8.055936939571999744 ) ) ;
#24644=CARTESIAN_POINT ( 'NONE',  ( 8.987367436956978040, 2.413693647671283138, 6.702895723592559030 ) ) ;
#24645=CARTESIAN_POINT ( 'NONE',  ( 10.43314899746000002, 5.167567567567999731, 6.822293592207000934 ) ) ;
#24650=DIRECTION ( 'NONE',  ( -1.000000000000000000, 0.000000000000000000, 0.000000000000000000 ) ) ;
#24651=DIRECTION ( 'NONE',  ( 1.083438471561000184E-09, -7.356835621337999415E-11, -1.000000000000000000 ) ) ;
#24653=CARTESIAN_POINT ( 'NONE',  ( 8.895035841232999729, 5.751585344281000545, -8.235867044345999588 ) ) ;
#24657=CARTESIAN_POINT ( 'NONE',  ( 0.2219399104530190292, 3.221919627416792054, 0.4208838488400382660 ) ) ;
#24658=CARTESIAN_POINT ( 'NONE',  ( 3.253293268430000218, 2.728051603523000246, -1.782980944594999784 ) ) ;
#24664=CARTESIAN_POINT ( 'NONE',  ( 7.743176658771999676, 2.735218126362000124, 6.771983639047999937 ) ) ;
#24668=VECTOR ( 'NONE', #27397, 1000.000000000000227 ) ;
#24672=CARTESIAN_POINT ( 'NONE',  ( 1.646806799206750105, -0.9161175952574931447, 3.408904368339100710 ) ) ;
#24674=ORIENTED_EDGE ( 'NONE', *, *, #10275, .T. ) ;
#24678=AXIS2_PLACEMENT_3D ( 'NONE', #24270, #45605, #34435 ) ;
#24684=CARTESIAN_POINT ( 'NONE',  ( 7.998183527237331170, 4.138725758259847787, -6.144309761568537809 ) ) ;
#24690=CARTESIAN_POINT ( 'NONE',  ( 2.209306799207166883, -3.058252359239909790, 1.762666431298136382 ) ) ;
#24699=CARTESIAN_POINT ( 'NONE',  ( 10.90000000296000060, 5.100000000009000445, -5.160242730682999657 ) ) ;
#24702=EDGE_CURVE ( 'NONE', #41793, #59855, #39895, .T. ) ;
#24708=CARTESIAN_POINT ( 'NONE',  ( 10.23809632363000155, 2.752447932331000047, 6.820051270595000048 ) ) ;
#24710=CARTESIAN_POINT ( 'NONE',  ( 9.626145280412998773, 3.934138271021000222, -9.063586117809000697 ) ) ;
#24711=CARTESIAN_POINT ( 'NONE',  ( 3.396928224380999950, -0.1132628685336000002, -3.706319183960999908 ) ) ;
#24717=CARTESIAN_POINT ( 'NONE',  ( 9.509901345851000443, 5.077442745148000647, 8.469003100811999474 ) ) ;
#24721=CARTESIAN_POINT ( 'NONE',  ( 9.691082467489000152, 5.335647408863999352, 8.701220655673999715 ) ) ;
#24728=VECTOR ( 'NONE', #34692, 1000.000000000000000 ) ;
#24731=ORIENTED_EDGE ( 'NONE', *, *, #25485, .T. ) ;
#24737=CARTESIAN_POINT ( 'NONE',  ( 8.577614158774000686, 3.981661882377999895, 8.959227447876999761 ) ) ;
#24740=VECTOR ( 'NONE', #62432, 1000.000000000000114 ) ;
#24741=CARTESIAN_POINT ( 'NONE',  ( 10.56170778040999991, 5.057487376164999660, -8.595710652231000282 ) ) ;
#24751=CARTESIAN_POINT ( 'NONE',  ( 7.517164158767000615, 2.455281733534999677, -8.606072783617999988 ) ) ;
#24755=ORIENTED_EDGE ( 'NONE', *, *, #3297, .T. ) ;
#24759=CARTESIAN_POINT ( 'NONE',  ( 9.518359312502500558, 5.126777126186113698, -6.752018918873279318 ) ) ;
#24768=CARTESIAN_POINT ( 'NONE',  ( 7.218295280410000458, 4.773081973066999772, 8.927402469597002010 ) ) ;
#24770=CARTESIAN_POINT ( 'NONE',  ( 7.681946225801584482, 2.830976189063534321, 8.204262802077490591 ) ) ;
#24774=ORIENTED_EDGE ( 'NONE', *, *, #43256, .F. ) ;
#24785=CARTESIAN_POINT ( 'NONE',  ( 11.02038275177999971, 5.599999999999999645, -6.571291218949999902 ) ) ;
#24786=EDGE_CURVE ( 'NONE', #52595, #19719, #8382, .T. ) ;
#24788=VERTEX_POINT ( 'NONE', #6734 ) ;
#24793=CARTESIAN_POINT ( 'NONE',  ( 10.65649893244999902, 5.448184228579000532, -7.015214795518000201 ) ) ;
#24798=CARTESIAN_POINT ( 'NONE',  ( 10.46932803217000085, 4.988495740890000363, 6.213106455073000411 ) ) ;
#24803=B_SPLINE_CURVE_WITH_KNOTS ( 'NONE', 3,
 ( #17271, #13076, #34057, #2237, #34407, #55723, #12377, #45235, #23551, #38955 ),
 .UNSPECIFIED., .F., .F.,
 ( 4, 2, 2, 2, 4 ),
 ( 0.5000000000000011102, 0.6250000000000008882, 0.7500000000000005551, 0.8750000000000002220, 1.000000000000000000 ),
 .UNSPECIFIED. ) ;
#24804=CARTESIAN_POINT ( 'NONE',  ( 10.68362359175999998, 2.603561947343000060, 7.762063351517999976 ) ) ;
#24807=CARTESIAN_POINT ( 'NONE',  ( 8.548770280408998445, 5.203550244299999683, -8.391678825488000371 ) ) ;
#24811=CARTESIAN_POINT ( 'NONE',  ( 8.353301658773000682, 2.800103557244999930, 9.079946116129001155 ) ) ;
#24812=CARTESIAN_POINT ( 'NONE',  ( 10.55991859298999991, 5.094266430778000121, 6.075406703384000018 ) ) ;
#24815=CARTESIAN_POINT ( 'NONE',  ( 9.526695280414001488, 5.462898983065000102, -8.055936939571999744 ) ) ;
#24820=CARTESIAN_POINT ( 'NONE',  ( 7.099999886593999499, 1.243449787579999883E-13, -12.39999890530017446 ) ) ;
#24822=EDGE_LOOP ( 'NONE', ( #38420, #48950, #55211, #16404 ) ) ;
#24824=CARTESIAN_POINT ( 'NONE',  ( 1.868110514233000119, -1.438367618452000007, -3.472675606904999768 ) ) ;
#24826=CARTESIAN_POINT ( 'NONE',  ( 9.617764158771999305, 5.322769172805999816, -7.951018786192998178 ) ) ;
#24828=CARTESIAN_POINT ( 'NONE',  ( 10.77164068750943393, 2.873222873819646583, 6.752018918863353925 ) ) ;
#24829=DIRECTION ( 'NONE',  ( 0.000000000000000000, 1.000000000000000000, 0.000000000000000000 ) ) ;
#24835=CARTESIAN_POINT ( 'NONE',  ( 8.598670280411999656, 2.376526778640999815, 7.686980884243000745 ) ) ;
#24839=AXIS2_PLACEMENT_3D ( 'NONE', #44808, #8771, #61563 ) ;
#24840=DIRECTION ( 'NONE',  ( 0.8231338744408063235, 0.000000000000000000, -0.5678473604306591982 ) ) ;
#24841=CARTESIAN_POINT ( 'NONE',  ( 2.065900752180000133, 2.737733327009000295, -2.100062873276000275 ) ) ;
#24843=CARTESIAN_POINT ( 'NONE',  ( 10.99999999997000089, 4.000000000000000000, -7.500000000000000000 ) ) ;
#24846=CARTESIAN_POINT ( 'NONE',  ( 10.33536974457000035, 5.153692264686000613, 8.830864265869999841 ) ) ;
#24853=CARTESIAN_POINT ( 'NONE',  ( 8.495025031241056013, 2.494743783266746284, 6.576609861288141623 ) ) ;
#24862=CARTESIAN_POINT ( 'NONE',  ( 10.22108913916999917, 2.983268757921999637, 8.764704075288999974 ) ) ;
#24863=CARTESIAN_POINT ( 'NONE',  ( 9.662441121991999893, 4.824173073626999653, -8.517602418144999632 ) ) ;
#24876=CARTESIAN_POINT ( 'NONE',  ( 6.950330780312001799, 10.43291458946000461, 4.786367813216996225 ) ) ;
#24884=FACE_OUTER_BOUND ( 'NONE', #9249, .T. ) ;
#24897=CARTESIAN_POINT ( 'NONE',  ( 10.68342665876999931, 3.810131921595000026, -5.661115150006999386 ) ) ;
#24902=VERTEX_POINT ( 'NONE', #8812 ) ;
#24904=CARTESIAN_POINT ( 'NONE',  ( 9.383549168937532770, 5.519605098629036810, -8.419222652796641171 ) ) ;
#24912=VECTOR ( 'NONE', #66420, 1000.000000000000000 ) ;
#24917=CARTESIAN_POINT ( 'NONE',  ( 2.500973465876000112, 3.500000000000000000, 0.000000000000000000 ) ) ;
#24920=ADVANCED_FACE ( 'NONE', ( #24200 ), #49621, .F. ) ;
#24924=DIRECTION ( 'NONE',  ( 0.7071149608238868067, -0.7070986014545870280, -9.105180035418829085E-10 ) ) ;
#24926=CARTESIAN_POINT ( 'NONE',  ( 10.72510394928502286, 2.650147065043140238, 7.500007457243191844 ) ) ;
#24931=AXIS2_PLACEMENT_3D ( 'NONE', #40864, #62187, #14307 ) ;
#24933=CARTESIAN_POINT ( 'NONE',  ( 4.000000000000000000, -1.321078631445433471, 1.719326598155805463 ) ) ;
#24935=EDGE_LOOP ( 'NONE', ( #17649, #45693, #19510, #65028, #8622, #68649, #32048 ) ) ;
#24940=CARTESIAN_POINT ( 'NONE',  ( 9.764472292182821533, 3.575760007354200187, -8.840577379916510381 ) ) ;
#24947=CARTESIAN_POINT ( 'NONE',  ( 9.825045280412000537, 3.116293075258000478, -6.208411413796000033 ) ) ;
#24950=CARTESIAN_POINT ( 'NONE',  ( 10.83768005408999890, 5.758100475276000552, -6.911469147650000977 ) ) ;
#24960=ORIENTED_EDGE ( 'NONE', *, *, #20355, .T. ) ;
#24962=CARTESIAN_POINT ( 'NONE',  ( 10.72802334123000101, 3.751278653658999929, -8.836901076820000256 ) ) ;
#24965=VECTOR ( 'NONE', #53768, 1000.000000000000227 ) ;
#24966=EDGE_CURVE ( 'NONE', #7034, #129, #52836, .T. ) ;
#24972=CARTESIAN_POINT ( 'NONE',  ( 8.458179719589999479, 5.332332124071999857, -8.487089944253000340 ) ) ;
#24975=LINE ( 'NONE', #25661, #43983 ) ;
#24987=CARTESIAN_POINT ( 'NONE',  ( 10.98768472639999949, 5.139096889661000311, -4.945212061661000469 ) ) ;
#24988=DIRECTION ( 'NONE',  ( 0.000000000000000000, -1.000000000000000000, 0.000000000000000000 ) ) ;
#24990=CARTESIAN_POINT ( 'NONE',  ( 9.790085841230000696, 5.149303692842000402, -5.987168472229000393 ) ) ;
#24991=( BOUNDED_SURFACE ( )  B_SPLINE_SURFACE ( 3, 3, ( 
 ( #23843, #39580, #35377, #24186, #56698, #7412, #28761, #45523, #60904, #66832 ),
 ( #62945, #4918, #25905, #15422, #41641, #4569, #52123, #46891, #47236, #21007 ),
 ( #68539, #36747, #41987, #10508, #63294, #9132, #40955, #24876, #52822, #20660 ),
 ( #51785, #42343, #63642, #58068, #19634, #10171, #35715, #3882, #68195, #36396 ) ),
 .UNSPECIFIED., .F., .F., .T. ) 
 B_SPLINE_SURFACE_WITH_KNOTS ( ( 4, 4 ),
 ( 4, 1, 1, 1, 1, 1, 1, 4 ),
 ( 0.000000000000000000, 1.000000000000000000 ),
 ( 0.2001824097869999985, 0.2006924593532999901, 0.2158499230326000051, 0.2291387176639999856, 0.2408062938197000069, 0.2510851730549999994, 0.2605211562811999837, 0.2678345471516999643 ),
 .UNSPECIFIED. ) 
 GEOMETRIC_REPRESENTATION_ITEM ( )  RATIONAL_B_SPLINE_SURFACE ( (
 ( 1.325324361584000021, 1.325324361584000021, 1.325324361584000021, 1.325324361584000021, 1.325324361584000021, 1.325324361584000021, 1.325324361584000021, 1.325324361584000021, 1.325324361584000021, 1.325324361584000021),
 ( 0.8915585461385999722, 0.8915585461385999722, 0.8915585461385999722, 0.8915585461385999722, 0.8915585461385999722, 0.8915585461385999722, 0.8915585461385999722, 0.8915585461385999722, 0.8915585461385999722, 0.8915585461385999722),
 ( 0.8915585461385999722, 0.8915585461385999722, 0.8915585461385999722, 0.8915585461385999722, 0.8915585461385999722, 0.8915585461385999722, 0.8915585461385999722, 0.8915585461385999722, 0.8915585461385999722, 0.8915585461385999722),
 ( 1.325324361584000021, 1.325324361584000021, 1.325324361584000021, 1.325324361584000021, 1.325324361584000021, 1.325324361584000021, 1.325324361584000021, 1.325324361584000021, 1.325324361584000021, 1.325324361584000021) ) ) 
 REPRESENTATION_ITEM ( '' )  SURFACE ( )  );
#24995=CARTESIAN_POINT ( 'NONE',  ( 0.1823164064783775740, 2.544165622319755293, -1.956281073432186712 ) ) ;
#24996=CARTESIAN_POINT ( 'NONE',  ( 3.014883521226000340, -2.957936814457999830, 1.368172651669000039 ) ) ;
#24999=EDGE_CURVE ( 'NONE', #23153, #20104, #36740, .T. ) ;
#25006=CARTESIAN_POINT ( 'NONE',  ( 9.716851002543000604, 2.832432432432000269, 6.822293592207000934 ) ) ;
#25007=ADVANCED_FACE ( 'NONE', ( #31182 ), #18960, .F. ) ;
#25009=CARTESIAN_POINT ( 'NONE',  ( 10.86501009699162701, 2.649983380500041008, -7.500000587580665901 ) ) ;
#25011=CARTESIAN_POINT ( 'NONE',  ( 7.812760732415217291, 3.078855207953160367, 6.461200734285722724 ) ) ;
#25016=VERTEX_POINT ( 'NONE', #20248 ) ;
#25020=B_SPLINE_CURVE_WITH_KNOTS ( 'NONE', 3,
 ( #57332, #8421, #62242, #40572, #19943, #47202, #9099, #51749, #67478, #35343, #41264, #56659, #68503, #46858, #51069, #20626, #30106, #19245, #51409, #19599, #3505, #35684, #52088, #46170, #14359, #3172, #56997, #9784, #3843, #4192, #62915, #25181, #15036, #14698, #20281 ),
 .UNSPECIFIED., .F., .F.,
 ( 4, 1, 1, 1, 1, 1, 1, 1, 1, 1, 1, 1, 1, 1, 1, 1, 1, 1, 1, 1, 1, 1, 1, 1, 1, 1, 1, 1, 1, 1, 1, 1, 4 ),
 ( 0.000000000000000000, 0.01250527213657373973, 0.04500493301836113597, 0.07750459390014853567, 0.1100042547819059385, 0.1425039156636933313, 0.1750035765454807379, 0.2075032374272681168, 0.2400028983090555235, 0.2725025591908429856, 0.3050022200726303367, 0.3375018809544177989, 0.3700015418362051500, 0.4025012027179926122, 0.4350008635997799633, 0.4675005244815674255, 0.5000001853633546656, 0.5324998462451421277, 0.5649995071269294789, 0.5974991680087169410, 0.6299988288905042921, 0.6624984897722917543, 0.6949981506540791054, 0.7274978115358665676, 0.7599974724176539187, 0.7924971332994412698, 0.8249967941812287320, 0.8574964550630161941, 0.8899961159448035453, 0.9224957768265908964, 0.9549954377083782475, 0.9874950985901658207, 1.000000000000000000 ),
 .UNSPECIFIED. ) ;
#25021=ORIENTED_EDGE ( 'NONE', *, *, #51778, .T. ) ;
#25023=CARTESIAN_POINT ( 'NONE',  ( 7.716851002542999716, 2.832432432432000269, 6.822293592207000934 ) ) ;
#25024=CARTESIAN_POINT ( 'NONE',  ( 7.681104719587999341, 5.564823112884000444, -7.478368060284999785 ) ) ;
#25025=DIRECTION ( 'NONE',  ( 0.000000000000000000, -1.000000000000000000, 0.000000000000000000 ) ) ;
#25035=AXIS2_PLACEMENT_3D ( 'NONE', #55730, #34754, #34413 ) ;
#25038=CARTESIAN_POINT ( 'NONE',  ( 3.053056799210541072, 2.798833948393625537, 2.150913519912209360 ) ) ;
#25045=CARTESIAN_POINT ( 'NONE',  ( 10.85069631730999973, 4.478098874537000285, 6.162039661770999821 ) ) ;
#25047=CARTESIAN_POINT ( 'NONE',  ( 10.02394528041000044, 5.481267232667000222, -8.005061172455999241 ) ) ;
#25048=CARTESIAN_POINT ( 'NONE',  ( 2.474755027877999947, 3.010559775858999920, -2.164644249678000509 ) ) ;
#25050=EDGE_CURVE ( 'NONE', #34762, #62430, #19273, .T. ) ;
#25056=CARTESIAN_POINT ( 'NONE',  ( 10.64424812522415920, 2.623953476961054410, -6.377174817668581852 ) ) ;
#25059=CARTESIAN_POINT ( 'NONE',  ( 9.786671076420999427, 2.381202181614999525, 7.612749448318000489 ) ) ;
#25066=CARTESIAN_POINT ( 'NONE',  ( 9.523148997461001741, 5.167567567567999731, -6.822293592207000934 ) ) ;
#25068=ORIENTED_EDGE ( 'NONE', *, *, #62365, .F. ) ;
#25070=DIRECTION ( 'NONE',  ( 0.000000000000000000, 0.7158784314710769925, 0.6982249432342777506 ) ) ;
#25073=VERTEX_POINT ( 'NONE', #14667 ) ;
#25078=CARTESIAN_POINT ( 'NONE',  ( 10.24394221959000184, 3.220342255699999878, -6.005413528376000620 ) ) ;
#25081=CARTESIAN_POINT ( 'NONE',  ( 1.446806799207333905, 0.9161175952574844850, -3.408904368339102930 ) ) ;
#25085=CARTESIAN_POINT ( 'NONE',  ( 10.02052890782000105, 2.899999999999999911, 6.152188490330000370 ) ) ;
#25086=ORIENTED_EDGE ( 'NONE', *, *, #6551, .F. ) ;
#25104=CARTESIAN_POINT ( 'NONE',  ( 8.817462135714999150, 5.100000000000000533, 6.571291218949999902 ) ) ;
#25107=CARTESIAN_POINT ( 'NONE',  ( 7.410857780409000561, 2.302289264429000504, 6.875166305059000393 ) ) ;
#25119=CARTESIAN_POINT ( 'NONE',  ( 7.016658217992999269, 10.82163639346000394, -3.419280833082998683 ) ) ;
#25125=DIRECTION ( 'NONE',  ( 1.000000000000000000, 0.000000000000000000, 0.000000000000000000 ) ) ;
#25126=VERTEX_POINT ( 'NONE', #21501 ) ;
#25127=ORIENTED_EDGE ( 'NONE', *, *, #59446, .F. ) ;
#25131=CARTESIAN_POINT ( 'NONE',  ( 10.86493304757000011, 4.678466548873998931, -9.048467117372998914 ) ) ;
#25132=CARTESIAN_POINT ( 'NONE',  ( 8.745593092018999926, 5.100000000000000533, 6.404090157675000228 ) ) ;
#25136=CARTESIAN_POINT ( 'NONE',  ( 9.034110134264999203, 4.695345051283999815, 8.660667941667000491 ) ) ;
#25139=ORIENTED_EDGE ( 'NONE', *, *, #47453, .F. ) ;
#25142=CARTESIAN_POINT ( 'NONE',  ( 10.37026939687000038, 5.571553923009999743, 7.748385725654999945 ) ) ;
#25145=CARTESIAN_POINT ( 'NONE',  ( 11.01863125001000121, 7.596591408283000391, -6.386077099867999429 ) ) ;
#25149=CARTESIAN_POINT ( 'NONE',  ( 7.839801658770999992, 3.084076314893000159, 9.259847992573000397 ) ) ;
#25150=CARTESIAN_POINT ( 'NONE',  ( 10.06344080699000010, 5.156228702401000952, 6.125219923432000613 ) ) ;
#25153=CARTESIAN_POINT ( 'NONE',  ( 9.038304719595000591, 3.867331042029999999, -9.227339949050001877 ) ) ;
#25162=CARTESIAN_POINT ( 'NONE',  ( 1.152881272621999909, -0.1662993809364999853, 3.755095982464999871 ) ) ;
#25164=CARTESIAN_POINT ( 'NONE',  ( 9.955712514275658620, 2.254889933401060809, 7.383222385005002053 ) ) ;
#25165=CARTESIAN_POINT ( 'NONE',  ( 7.716851002542999716, 2.832432432432000269, 6.822293592207000934 ) ) ;
#25166=DIRECTION ( 'NONE',  ( 0.7071082394066938726, -0.7071053229633939008, 3.720439694272969466E-11 ) ) ;
#25172=ORIENTED_EDGE ( 'NONE', *, *, #51392, .F. ) ;
#25173=CARTESIAN_POINT ( 'NONE',  ( 9.112170280412000167, 2.368264398678999516, 7.410200237937000445 ) ) ;
#25175=CARTESIAN_POINT ( 'NONE',  ( 6.899999691988000450, -13.87069231928999891, 4.225386915259999654 ) ) ;
#25179=CARTESIAN_POINT ( 'NONE',  ( 2.156491312998999987, 2.610776529918000133, -2.002676742402000443 ) ) ;
#25180=EDGE_LOOP ( 'NONE', ( #23905, #39796, #16600, #8529 ) ) ;
#25181=CARTESIAN_POINT ( 'NONE',  ( 2.144642041300283353, -0.2797333540616577241, -3.290985472785137755 ) ) ;
#25183=FACE_OUTER_BOUND ( 'NONE', #26506, .T. ) ;
#25184=CARTESIAN_POINT ( 'NONE',  ( 9.351497027444999333, 4.821940693094999730, 8.950154065657999425 ) ) ;
#25201=CARTESIAN_POINT ( 'NONE',  ( 10.80815748598999981, 2.937526572573000205, 8.948458885032000154 ) ) ;
#25202=CARTESIAN_POINT ( 'NONE',  ( 10.76231429546999863, 3.259156861436999897, -8.644989069184999764 ) ) ;
#25208=CARTESIAN_POINT ( 'NONE',  ( 8.368323341230000878, 4.780986922229000236, 6.267222470044999660 ) ) ;
#25210=CIRCLE ( 'NONE', #7344, 12.99999854704999969 ) ;
#25212=CARTESIAN_POINT ( 'NONE',  ( 11.09999999999999964, 4.000000000000000000, -7.500000000000000000 ) ) ;
#25215=LINE ( 'NONE', #62611, #17167 ) ;
#25230=CARTESIAN_POINT ( 'NONE',  ( -0.1507337372581999957, -2.198759671591000053, -2.775001775783000113 ) ) ;
#25231=B_SPLINE_CURVE_WITH_KNOTS ( 'NONE', 3,
 ( #41709, #30201, #3604, #24940, #46273, #30536, #9537, #51848 ),
 .UNSPECIFIED., .F., .F.,
 ( 4, 1, 1, 1, 1, 4 ),
 ( 0.000000000000000000, 0.07676470621494888014, 0.2763109384346265074, 0.4758571706543032187, 0.6754034028747566420, 0.7874025540483345909 ),
 .UNSPECIFIED. ) ;
#25239=CARTESIAN_POINT ( 'NONE',  ( 10.04762433003745414, 4.043475630241087693, 8.964144173642713653 ) ) ;
#25241=CARTESIAN_POINT ( 'NONE',  ( 10.07314899745999881, 5.167567567567999731, -6.822293592207000934 ) ) ;
#25249=DIRECTION ( 'NONE',  ( 1.000000000000000000, 0.000000000000000000, 0.000000000000000000 ) ) ;
#25251=VERTEX_POINT ( 'NONE', #57881 ) ;
#25256=ADVANCED_FACE ( 'NONE', ( #58564 ), #25720, .T. ) ;
#25257=CARTESIAN_POINT ( 'NONE',  ( 4.074968078372999791, 0.000000000000000000, 0.000000000000000000 ) ) ;
#25264=LINE ( 'NONE', #31549, #42410 ) ;
#25272=CARTESIAN_POINT ( 'NONE',  ( 2.936390132544666187, 0.4581489286485155299, -3.499999999999999556 ) ) ;
#25274=CARTESIAN_POINT ( 'NONE',  ( 9.559179719593000613, 4.038835765825999680, -5.935509327774999733 ) ) ;
#25275=CARTESIAN_POINT ( 'NONE',  ( 8.716851002545999094, 2.832432432432000269, 6.822293592207000934 ) ) ;
#25280=VERTEX_POINT ( 'NONE', #31663 ) ;
#25284=CARTESIAN_POINT ( 'NONE',  ( 4.149992563292000725, -1.999946284944287722, -0.2617923565148043141 ) ) ;
#25285=CARTESIAN_POINT ( 'NONE',  ( 10.02877429409719667, 2.700021399671855615, -8.762287518837057476 ) ) ;
#25289=ORIENTED_EDGE ( 'NONE', *, *, #45588, .T. ) ;
#25290=PLANE ( 'NONE',  #26485 ) ;
#25291=CARTESIAN_POINT ( 'NONE',  ( 9.734454719592999794, 3.021734963141999852, -6.070209284876999511 ) ) ;
#25293=CARTESIAN_POINT ( 'NONE',  ( 10.40558702164999971, 5.599341344818000721, -8.437759619346000051 ) ) ;
#25303=CARTESIAN_POINT ( 'NONE',  ( 10.23581084123000018, 3.621841509808999771, -8.806208131805998818 ) ) ;
#25307=DIRECTION ( 'NONE',  ( -1.000000000000000000, 0.000000000000000000, 0.000000000000000000 ) ) ;
#25309=EDGE_CURVE ( 'NONE', #13611, #15150, #7454, .T. ) ;
#25312=ORIENTED_EDGE ( 'NONE', *, *, #16388, .T. ) ;
#25313=CARTESIAN_POINT ( 'NONE',  ( 9.278070280414000948, 2.546924812613000189, -6.918870225297999887 ) ) ;
#25318=DIRECTION ( 'NONE',  ( -1.000000000000000000, 0.000000000000000000, 0.000000000000000000 ) ) ;
#25321=CARTESIAN_POINT ( 'NONE',  ( 8.920125482160894848, 2.358211129006373863, 8.150900180138641815 ) ) ;
#25327=CARTESIAN_POINT ( 'NONE',  ( 7.936333771302000351, 5.123034328734999754, 6.721303713258000023 ) ) ;
#25330=CARTESIAN_POINT ( 'NONE',  ( 8.546960841229999772, 2.724453559418999582, -8.908010318766001134 ) ) ;
#25334=PLANE ( 'NONE',  #17699 ) ;
#25335=ADVANCED_FACE ( 'NONE', ( #17960 ), #55707, .T. ) ;
#25337=CARTESIAN_POINT ( 'NONE',  ( 0.3077908348429792551, -0.8650031602613956760, 3.222008420499449688 ) ) ;
#25339=ORIENTED_EDGE ( 'NONE', *, *, #4803, .F. ) ;
#25344=CARTESIAN_POINT ( 'NONE',  ( 3.500000000000000888, -0.4453636064423555641, 3.246405014819000900 ) ) ;
#25348=CARTESIAN_POINT ( 'NONE',  ( 10.97540928332104215, 8.495318605243999954, 6.551665373225851852 ) ) ;
#25350=CARTESIAN_POINT ( 'NONE',  ( 1.667640132540000097, -1.762666431298160141, 3.058252359239895579 ) ) ;
#25353=AXIS2_PLACEMENT_3D ( 'NONE', #45186, #66493, #39942 ) ;
#25355=VERTEX_POINT ( 'NONE', #45220 ) ;
#25360=ORIENTED_EDGE ( 'NONE', *, *, #32656, .T. ) ;
#25361=CARTESIAN_POINT ( 'NONE',  ( 0.000000000000000000, 2.533699434757234137, -1.460905701136922197 ) ) ;
#25363=CARTESIAN_POINT ( 'NONE',  ( 6.786054719591000151, 4.411055010497999973, -9.010057343561001630 ) ) ;
#25366=DIRECTION ( 'NONE',  ( 1.000000000000000000, 0.000000000000000000, 0.000000000000000000 ) ) ;
#25367=ORIENTED_EDGE ( 'NONE', *, *, #6525, .F. ) ;
#25373=AXIS2_PLACEMENT_3D ( 'NONE', #4515, #36001, #63591 ) ;
#25376=CARTESIAN_POINT ( 'NONE',  ( 10.80572075886704653, 4.425289333137247816, 9.224018707921255000 ) ) ;
#25380=VECTOR ( 'NONE', #7841, 1000.000000000000000 ) ;
#25386=CARTESIAN_POINT ( 'NONE',  ( 9.479214860607999782, 4.071727169861000029, 9.089299483126000112 ) ) ;
#25387=DIRECTION ( 'NONE',  ( 0.000000000000000000, -0.9916377111174248249, 0.1290528957048032721 ) ) ;
#25388=CARTESIAN_POINT ( 'NONE',  ( 8.722235841230000730, 3.844886277615000125, -8.888911790991000927 ) ) ;
#25389=CARTESIAN_POINT ( 'NONE',  ( 2.803334101832999803, -0.2418256465843999781, -3.535455962752999781 ) ) ;
#25391=CARTESIAN_POINT ( 'NONE',  ( -15.86200481174999943, 2.399999999999999911, -6.571291218949999902 ) ) ;
#25394=EDGE_CURVE ( 'NONE', #37746, #39911, #6759, .T. ) ;
#25401=CARTESIAN_POINT ( 'NONE',  ( 10.96080777006000062, 2.054568739078000306, 7.810084630238000258 ) ) ;
#25405=B_SPLINE_CURVE_WITH_KNOTS ( 'NONE', 3,
 ( #38534, #7761, #18604, #39930 ),
 .UNSPECIFIED., .F., .F.,
 ( 4, 4 ),
 ( 0.000000000000000000, 1.000000000000000000 ),
 .UNSPECIFIED. ) ;
#25407=B_SPLINE_CURVE_WITH_KNOTS ( 'NONE', 3,
 ( #68009, #34845, #41454, #20124, #51259, #24345, #29613, #56850, #46359, #4029, #67660, #57181, #40417, #62084, #24690, #9276, #62762, #40762 ),
 .UNSPECIFIED., .F., .F.,
 ( 4, 2, 2, 2, 2, 2, 2, 2, 4 ),
 ( 0.000000000000000000, 0.1250000000000000000, 0.2500000000000000000, 0.3750000000000000000, 0.5000000000000000000, 0.6250000000000000000, 0.7500000000000000000, 0.8750000000000000000, 1.000000000000000000 ),
 .UNSPECIFIED. ) ;
#25417=CARTESIAN_POINT ( 'NONE',  ( 8.523148997455999520, 5.167567567567999731, -6.822293592207000934 ) ) ;
#25421=CARTESIAN_POINT ( 'NONE',  ( 10.71685100253999856, 2.832432432432000269, 6.822293592207000934 ) ) ;
#25423=CARTESIAN_POINT ( 'NONE',  ( 10.29667028040999988, 2.755514216060999999, -6.622437150225000124 ) ) ;
#25424=ORIENTED_EDGE ( 'NONE', *, *, #45280, .F. ) ;
#25425=CARTESIAN_POINT ( 'NONE',  ( 1.342640132540666720, -3.058252359239902685, -1.762666431298148595 ) ) ;
#25433=CARTESIAN_POINT ( 'NONE',  ( 8.312764158770001188, 5.897697057214000615, -7.408103789850999377 ) ) ;
#25440=EDGE_CURVE ( 'NONE', #42736, #65371, #65134, .T. ) ;
#25442=ORIENTED_EDGE ( 'NONE', *, *, #54920, .F. ) ;
#25444=CARTESIAN_POINT ( 'NONE',  ( 8.745860841232000027, 4.178200486578000472, -5.608493638783999202 ) ) ;
#25450=FACE_OUTER_BOUND ( 'NONE', #24935, .T. ) ;
#25454=CARTESIAN_POINT ( 'NONE',  ( 8.819055905797000605, 2.899999999999999911, -6.571291218949999902 ) ) ;
#25459=CARTESIAN_POINT ( 'NONE',  ( 6.068038739436002693, 9.317488949900994299, -4.752944535109002722 ) ) ;
#25461=LINE ( 'NONE', #47831, #3999 ) ;
#25467=ORIENTED_EDGE ( 'NONE', *, *, #55027, .T. ) ;
#25470=AXIS2_PLACEMENT_3D ( 'NONE', #7636, #35250, #28983 ) ;
#25474=CARTESIAN_POINT ( 'NONE',  ( 9.937409415358999354, 3.510662261693000108, -6.227052446266999830 ) ) ;
#25478=EDGE_CURVE ( 'NONE', #48780, #38871, #38579, .T. ) ;
#25479=CARTESIAN_POINT ( 'NONE',  ( 9.509901345851000443, 5.077442745148000647, 8.469003100811999474 ) ) ;
#25480=EDGE_CURVE ( 'NONE', #53586, #53307, #15794, .T. ) ;
#25481=AXIS2_PLACEMENT_3D ( 'NONE', #38421, #49255, #64975 ) ;
#25482=ORIENTED_EDGE ( 'NONE', *, *, #61587, .F. ) ;
#25483=CARTESIAN_POINT ( 'NONE',  ( 9.078327844090949839, 2.243031650800266341, -7.767462267625812267 ) ) ;
#25485=EDGE_CURVE ( 'NONE', #28596, #31943, #68236, .T. ) ;
#25489=CARTESIAN_POINT ( 'NONE',  ( 9.892489158770999325, 5.099602161831000124, -9.049221499261999924 ) ) ;
#25492=CARTESIAN_POINT ( 'NONE',  ( 10.96421577872000164, 7.493628354714999773, -6.190747039866000279 ) ) ;
#25496=CARTESIAN_POINT ( 'NONE',  ( 9.476372460169001144, 5.098395626600999542, 6.305536056092000408 ) ) ;
#25498=ORIENTED_EDGE ( 'NONE', *, *, #4605, .T. ) ;
#25499=CARTESIAN_POINT ( 'NONE',  ( 8.441604719589999917, 5.473983809665999622, -8.180077404516000072 ) ) ;
#25501=EDGE_CURVE ( 'NONE', #37337, #35262, #38327, .T. ) ;
#25502=CARTESIAN_POINT ( 'NONE',  ( 9.028474612548713196, 4.352782978232004218, 8.850949115404432632 ) ) ;
#25506=EDGE_LOOP ( 'NONE', ( #28253, #61165, #7290, #11279, #50728 ) ) ;
#25507=CARTESIAN_POINT ( 'NONE',  ( 1.348382408447000191, 1.715249283262000102, -3.156226979448999881 ) ) ;
#25508=CARTESIAN_POINT ( 'NONE',  ( 7.437260841228000352, 2.216873702600000051, 8.370081218683999680 ) ) ;
#25511=CARTESIAN_POINT ( 'NONE',  ( 9.219964158774999419, 3.941185585667000169, -8.896279800194999865 ) ) ;
#25516=AXIS2_PLACEMENT_3D ( 'NONE', #40300, #62638, #14080 ) ;
#25519=CARTESIAN_POINT ( 'NONE',  ( 9.637068864299580540, 2.899999999999999911, 6.444141223381761208 ) ) ;
#25527=CARTESIAN_POINT ( 'NONE',  ( 1.175837695950999739, 2.689776413290000168, 2.380956047316999946 ) ) ;
#25528=ORIENTED_EDGE ( 'NONE', *, *, #44117, .F. ) ;
#25537=ADVANCED_FACE ( 'NONE', ( #51482 ), #45536, .F. ) ;
#25547=ORIENTED_EDGE ( 'NONE', *, *, #63373, .T. ) ;
#25550=CARTESIAN_POINT ( 'NONE',  ( 10.12550053024000007, 5.788811067708000024, 7.335561454339999621 ) ) ;
#25551=CARTESIAN_POINT ( 'NONE',  ( 9.910156421876999744, 2.531070993918000056, -7.917736616860999277 ) ) ;
#25557=CARTESIAN_POINT ( 'NONE',  ( 10.88314899746000108, 5.167567567567999731, 6.822293592207000934 ) ) ;
#25558=ORIENTED_EDGE ( 'NONE', *, *, #6608, .F. ) ;
#25563=CARTESIAN_POINT ( 'NONE',  ( 9.332537864288001472, 2.899999999999999911, 6.571291218949999902 ) ) ;
#25567=ORIENTED_EDGE ( 'NONE', *, *, #68635, .T. ) ;
#25575=CYLINDRICAL_SURFACE ( 'NONE', #14761, 3.500000000000000000 ) ;
#25580=CARTESIAN_POINT ( 'NONE',  ( 0.6146236793818999899, -2.189299194929000159, -2.346944523683000217 ) ) ;
#25583=CARTESIAN_POINT ( 'NONE',  ( 10.66052890781999984, 2.899999999999999911, -6.152188490330000370 ) ) ;
#25586=CARTESIAN_POINT ( 'NONE',  ( 11.09178278040999999, 4.578541652803000517, -8.908598806528001290 ) ) ;
#25591=DIRECTION ( 'NONE',  ( 0.5298945027589778700, -0.5996715052832758408, 0.5996714948178758497 ) ) ;
#25595=CARTESIAN_POINT ( 'NONE',  ( 9.140753410162000492, 5.100000000000000533, 6.175944241622000064 ) ) ;
#25598=FACE_OUTER_BOUND ( 'NONE', #53221, .T. ) ;
#25603=ORIENTED_EDGE ( 'NONE', *, *, #35618, .T. ) ;
#25616=DIRECTION ( 'NONE',  ( 1.000000000000000000, 0.000000000000000000, 0.000000000000000000 ) ) ;
#25618=CARTESIAN_POINT ( 'NONE',  ( 11.09999987043000047, 9.962291482759999539, 5.845852616619999331 ) ) ;
#25619=CARTESIAN_POINT ( 'NONE',  ( 2.905140132544666631, -0.9161175952574773795, -3.408904368339105595 ) ) ;
#25621=CARTESIAN_POINT ( 'NONE',  ( 8.514954719592999766, 3.207599814920999659, -6.150466394809999571 ) ) ;
#25626=ORIENTED_EDGE ( 'NONE', *, *, #60890, .F. ) ;
#25629=CARTESIAN_POINT ( 'NONE',  ( 4.149992563292001613, -1.229060429538525900, -1.599290730647372927 ) ) ;
#25635=DIRECTION ( 'NONE',  ( 0.000000000000000000, -1.000000000000000000, 0.000000000000000000 ) ) ;
#25636=CARTESIAN_POINT ( 'NONE',  ( 9.088029719595001055, 2.881930053949999682, -8.823338183322999129 ) ) ;
#25639=CARTESIAN_POINT ( 'NONE',  ( 10.66852712374000056, 4.435471808682999395, -5.866466547508000673 ) ) ;
#25640=ORIENTED_EDGE ( 'NONE', *, *, #50938, .T. ) ;
#25643=DIRECTION ( 'NONE',  ( -1.000000000000000000, 0.000000000000000000, 0.000000000000000000 ) ) ;
#25646=CARTESIAN_POINT ( 'NONE',  ( 9.878359312496433731, 5.126777126183345246, 6.752018918868509800 ) ) ;
#25647=EDGE_CURVE ( 'NONE', #52595, #62430, #8838, .T. ) ;
#25650=CARTESIAN_POINT ( 'NONE',  ( 10.95519834123000003, 3.860336562672999960, -6.147350406894000585 ) ) ;
#25656=VERTEX_POINT ( 'NONE', #62320 ) ;
#25657=ORIENTED_EDGE ( 'NONE', *, *, #62271, .T. ) ;
#25658=CARTESIAN_POINT ( 'NONE',  ( 9.029445280412998542, 5.442817578555000146, -8.106149115450000053 ) ) ;
#25661=CARTESIAN_POINT ( 'NONE',  ( 4.500000484264000455, 12.99999951562999989, 2.124870431850000170E-09 ) ) ;
#25666=FACE_OUTER_BOUND ( 'NONE', #28472, .T. ) ;
#25668=VERTEX_POINT ( 'NONE', #43415 ) ;
#25669=EDGE_CURVE ( 'NONE', #47578, #3072, #47963, .T. ) ;
#25674=CARTESIAN_POINT ( 'NONE',  ( 10.90000000011000125, 5.100000000110999743, 6.571291220762999430 ) ) ;
#25676=CARTESIAN_POINT ( 'NONE',  ( 9.392285841233000809, 5.775964236216999836, -8.174909295649001706 ) ) ;
#25678=CARTESIAN_POINT ( 'NONE',  ( 7.993094057962528254, 3.103801558224323465, -6.363363910445399618 ) ) ;
#25679=CARTESIAN_POINT ( 'NONE',  ( 0.07497316781761000082, 0.000000000000000000, 0.000000000000000000 ) ) ;
#25680=CARTESIAN_POINT ( 'NONE',  ( 0.2615634140176161249, 2.004981734223959755, 2.607536443111408087 ) ) ;
#25682=CARTESIAN_POINT ( 'NONE',  ( 2.871837672902999739, 1.998183433799000319, 2.574596971963000414 ) ) ;
#25690=ORIENTED_EDGE ( 'NONE', *, *, #58784, .F. ) ;
#25694=CARTESIAN_POINT ( 'NONE',  ( 0.5420802270800906264, 3.075918330867753792, 1.732122671253175650 ) ) ;
#25695=CARTESIAN_POINT ( 'NONE',  ( 11.09806944063140399, 2.697063473146602330, 6.634103937412520580 ) ) ;
#25696=CARTESIAN_POINT ( 'NONE',  ( 6.999999691988000095, 12.11716380430000051, 3.069905306952999791 ) ) ;
#25700=ORIENTED_EDGE ( 'NONE', *, *, #2538, .F. ) ;
#25705=ORIENTED_EDGE ( 'NONE', *, *, #59990, .F. ) ;
#25706=CARTESIAN_POINT ( 'NONE',  ( 8.416230770385023874, 5.016073627869618079, -8.932544507081987106 ) ) ;
#25707=CARTESIAN_POINT ( 'NONE',  ( 8.009154640314669393, 4.326009048175516902, -6.176799728275869761 ) ) ;
#25708=CARTESIAN_POINT ( 'NONE',  ( 7.730829719587998916, 5.281793838578000333, -8.397855149904000172 ) ) ;
#25715=ORIENTED_EDGE ( 'NONE', *, *, #59783, .F. ) ;
#25717=CARTESIAN_POINT ( 'NONE',  ( 5.000000000000000000, -1.382741116750999977, -11.26545724788999969 ) ) ;
#25718=B_SPLINE_CURVE_WITH_KNOTS ( 'NONE', 3,
 ( #47027, #63080, #25695, #35511 ),
 .UNSPECIFIED., .F., .F.,
 ( 4, 4 ),
 ( 0.000000000000000000, 1.000000000000000000 ),
 .UNSPECIFIED. ) ;
#25720=CYLINDRICAL_SURFACE ( 'NONE', #51018, 12.50000000000000000 ) ;
#25721=CARTESIAN_POINT ( 'NONE',  ( 10.99797019513065699, 2.534916329350139552, 6.496562598600510441 ) ) ;
#25731=EDGE_CURVE ( 'NONE', #5681, #4832, #16142, .T. ) ;
#25733=CARTESIAN_POINT ( 'NONE',  ( 9.514114512910998300, 4.887632373702999189, 8.462748516415999234 ) ) ;
#25738=CARTESIAN_POINT ( 'NONE',  ( 9.169760841232999837, 4.728328492779000136, -8.692725459657999920 ) ) ;
#25740=CARTESIAN_POINT ( 'NONE',  ( 2.677583211399999996, -3.533016733676999976, 0.2751748379743000350 ) ) ;
#25741=CARTESIAN_POINT ( 'NONE',  ( 7.000000000000000000, 6.495643345158865323, -2.999999999999999556 ) ) ;
#25742=DIRECTION ( 'NONE',  ( 1.000000000000000000, 0.000000000000000000, 0.000000000000000000 ) ) ;
#25747=CARTESIAN_POINT ( 'NONE',  ( 10.39984540795353318, 5.293498025891123504, -8.716172560647471812 ) ) ;
#25751=CARTESIAN_POINT ( 'NONE',  ( 9.013423559847998590, 4.933953210258000155, 8.417881984655998906 ) ) ;
#25763=DIRECTION ( 'NONE',  ( -1.000000000000000000, 0.000000000000000000, 0.000000000000000000 ) ) ;
#25769=CARTESIAN_POINT ( 'NONE',  ( 11.28109528040999976, 2.660125405577999924, -6.904121770750999865 ) ) ;
#25771=DIRECTION ( 'NONE',  ( 1.000000000000000000, 0.000000000000000000, 0.000000000000000000 ) ) ;
#25776=CARTESIAN_POINT ( 'NONE',  ( 7.758198341228000672, 5.797099724369999763, 8.340484548805999765 ) ) ;
#25787=CARTESIAN_POINT ( 'NONE',  ( 7.196266048625999723, 10.76669857437999944, -3.593894311215999782 ) ) ;
#25789=ADVANCED_FACE ( 'NONE', ( #68934 ), #58790, .F. ) ;
#25791=CARTESIAN_POINT ( 'NONE',  ( 11.09999999999999964, 2.649999999999999911, 7.500000000000000000 ) ) ;
#25792=CARTESIAN_POINT ( 'NONE',  ( 8.795585841232000490, 5.251032986819000214, -6.070151079272999795 ) ) ;
#25804=CARTESIAN_POINT ( 'NONE',  ( 7.146208818154000220, 8.240697770480998940, -4.339685437942002899 ) ) ;
#25805=CARTESIAN_POINT ( 'NONE',  ( 7.000000000000000000, 0.3230303992915000144, -3.000000000000000000 ) ) ;
#25819=CARTESIAN_POINT ( 'NONE',  ( 10.82565186280000091, 5.331165376905000031, -8.542144899688000947 ) ) ;
#25823=CARTESIAN_POINT ( 'NONE',  ( 9.724611353170001138, 2.928305163963000446, 8.718478150869000132 ) ) ;
#25825=ORIENTED_EDGE ( 'NONE', *, *, #54535, .F. ) ;
#25827=ORIENTED_EDGE ( 'NONE', *, *, #1197, .F. ) ;
#25830=CARTESIAN_POINT ( 'NONE',  ( 10.94796973825000030, 2.864322365205000054, 8.846249469408000721 ) ) ;
#25832=CARTESIAN_POINT ( 'NONE',  ( 9.667010841233000917, 4.769103072373000352, -8.666849124598000387 ) ) ;
#25836=CARTESIAN_POINT ( 'NONE',  ( 10.86591859237855395, 5.674200084745228523, -8.061124942614856792 ) ) ;
#25839=CARTESIAN_POINT ( 'NONE',  ( 9.944319408602000365, 5.443001719280999851, 7.367350382395000175 ) ) ;
#25842=CARTESIAN_POINT ( 'NONE',  ( 8.690229719593000723, 2.414630869937000046, -6.801495146585999407 ) ) ;
#25850=CARTESIAN_POINT ( 'NONE',  ( 8.079135841228998416, 3.524748802314000340, 5.573833469815000718 ) ) ;
#25851=DIRECTION ( 'NONE',  ( 1.000000000000000000, 0.000000000000000000, 0.000000000000000000 ) ) ;
#25855=CARTESIAN_POINT ( 'NONE',  ( 9.681187238460999822, 2.612249048987000055, 7.804677627401999551 ) ) ;
#25861=CARTESIAN_POINT ( 'NONE',  ( 9.187739158772000536, 5.964723767581000757, 7.776480083716999836 ) ) ;
#25867=ORIENTED_EDGE ( 'NONE', *, *, #25959, .T. ) ;
#25870=CARTESIAN_POINT ( 'NONE',  ( 9.347254965556000883, 4.028327103212000715, 9.469449669541999626 ) ) ;
#25871=CARTESIAN_POINT ( 'NONE',  ( 9.854942824136999846, 2.800308224477999985, 9.013816726157999781 ) ) ;
#25875=ADVANCED_FACE ( 'NONE', ( #59473 ), #46328, .F. ) ;
#25876=AXIS2_PLACEMENT_3D ( 'NONE', #18219, #62239, #45820 ) ;
#25880=PLANE ( 'NONE',  #54372 ) ;
#25882=CARTESIAN_POINT ( 'NONE',  ( 10.98768472639999949, 2.860900986606000007, -4.945212061661000469 ) ) ;
#25886=CYLINDRICAL_SURFACE ( 'NONE', #58175, 1.350000000000000533 ) ;
#25889=CARTESIAN_POINT ( 'NONE',  ( 8.426541430992324777, 3.894762663531519564, 6.010944450864965205 ) ) ;
#25891=AXIS2_PLACEMENT_3D ( 'NONE', #3694, #35536, #19443 ) ;
#25893=CARTESIAN_POINT ( 'NONE',  ( 10.90374609491999891, 3.726846467344000047, 5.900456154266000119 ) ) ;
#25894=CARTESIAN_POINT ( 'NONE',  ( 11.17811698873999937, 2.762452057009999962, -6.187198315927000536 ) ) ;
#25901=ORIENTED_EDGE ( 'NONE', *, *, #60247, .F. ) ;
#25903=CARTESIAN_POINT ( 'NONE',  ( 9.225036466121004253, 2.649952287134117235, 7.500002258928285315 ) ) ;
#25904=CARTESIAN_POINT ( 'NONE',  ( 8.659024459946206065, 3.018043227519824345, -6.080012726073716678 ) ) ;
#25905=CARTESIAN_POINT ( 'NONE',  ( 10.52696718958000055, 8.359475522667993985, 6.870968795365002713 ) ) ;
#25911=EDGE_LOOP ( 'NONE', ( #15899, #22182, #60023, #2256, #56489, #51610, #53762, #27882 ) ) ;
#25914=CARTESIAN_POINT ( 'NONE',  ( 11.09999999999999964, 2.700683852703999577, 5.124965750789000296 ) ) ;
#25920=CARTESIAN_POINT ( 'NONE',  ( 0.1127116734105999968, 1.200150369511000070, -3.152926066752000267 ) ) ;
#25924=CARTESIAN_POINT ( 'NONE',  ( 8.365056901398830291, 2.650139792115765669, -7.500003826568613086 ) ) ;
#25927=CARTESIAN_POINT ( 'NONE',  ( 10.90247028041000021, 4.554785930130000438, -6.081876607904999510 ) ) ;
#25932=VERTEX_POINT ( 'NONE', #38070 ) ;
#25939=DIRECTION ( 'NONE',  ( 0.000000000000000000, -0.9916377111174248249, -0.1290528957048032721 ) ) ;
#25949=CARTESIAN_POINT ( 'NONE',  ( 8.737804660583998739, 4.491756428607999396, -5.831236541471000123 ) ) ;
#25951=ADVANCED_FACE ( 'NONE', ( #12202 ), #59396, .T. ) ;
#25956=B_SPLINE_CURVE_WITH_KNOTS ( 'NONE', 3,
 ( #40425, #13534, #18773, #8275, #61751, #45344, #29621, #50581, #50924, #55830, #2683, #24010, #66653, #34853, #42156, #42462, #67986, #25344, #15200, #47021, #58880, #51910 ),
 .UNSPECIFIED., .F., .F.,
 ( 4, 2, 2, 2, 2, 2, 2, 2, 2, 2, 4 ),
 ( 0.000000000000000000, 0.1250000000000000278, 0.2500000000000000555, 0.3750000000000001110, 0.5000000000000001110, 0.5625000000000001110, 0.6250000000000001110, 0.6875000000000001110, 0.7500000000000002220, 0.8750000000000001110, 1.000000000000000000 ),
 .UNSPECIFIED. ) ;
#25959=EDGE_CURVE ( 'NONE', #39911, #48489, #19138, .T. ) ;
#25960=DIRECTION ( 'NONE',  ( 0.000000000000000000, -0.7158784314710769925, 0.6982249432342777506 ) ) ;
#25964=ORIENTED_EDGE ( 'NONE', *, *, #18109, .T. ) ;
#25965=CARTESIAN_POINT ( 'NONE',  ( 8.953620280414000376, 2.881930053949999682, -8.823338183322999129 ) ) ;
#25968=AXIS2_PLACEMENT_3D ( 'NONE', #34459, #45286, #40711 ) ;
#25973=CARTESIAN_POINT ( 'NONE',  ( 8.745860841232000027, 4.178200486578000472, -5.608493638783999202 ) ) ;
#25974=CARTESIAN_POINT ( 'NONE',  ( 10.16052890781999984, 2.899999999999999911, -6.152188490330000370 ) ) ;
#25977=CARTESIAN_POINT ( 'NONE',  ( 1.250973465874999802, -3.500000000000000000, 0.000000000000000000 ) ) ;
#25979=ORIENTED_EDGE ( 'NONE', *, *, #5436, .T. ) ;
#25980=CARTESIAN_POINT ( 'NONE',  ( 4.500000000000000000, 0.000000000000000000, 0.000000000000000000 ) ) ;
#25981=CARTESIAN_POINT ( 'NONE',  ( 8.690229719593000723, 2.414630869937000046, -6.801495146585999407 ) ) ;
#25983=EDGE_CURVE ( 'NONE', #38001, #12182, #23379, .T. ) ;
#25985=CARTESIAN_POINT ( 'NONE',  ( 10.90421423234000109, 3.863780721621000058, -9.185084890147001246 ) ) ;
#25990=DIRECTION ( 'NONE',  ( -0.7071063750895308919, -0.7071071872833308847, 1.205024241302051880E-09 ) ) ;
#25992=CARTESIAN_POINT ( 'NONE',  ( 8.550850940329604910, 3.105567053290974044, 6.047889655643520435 ) ) ;
#25993=ORIENTED_EDGE ( 'NONE', *, *, #7003, .F. ) ;
#25998=CARTESIAN_POINT ( 'NONE',  ( 9.295789158775001226, 5.835196551504000517, -7.008466539623000813 ) ) ;
#26001=ORIENTED_EDGE ( 'NONE', *, *, #44809, .F. ) ;
#26003=CARTESIAN_POINT ( 'NONE',  ( 9.816185841232000442, 2.656512020013999997, -7.884832994446999699 ) ) ;
#26019=CARTESIAN_POINT ( 'NONE',  ( 6.983163067140000457, -12.13278666557000030, -3.076795749344999997 ) ) ;
#26032=EDGE_LOOP ( 'NONE', ( #47757, #44084 ) ) ;
#26038=CARTESIAN_POINT ( 'NONE',  ( 1.780140132541583320, -3.408904368339108260, 0.9161175952574674985 ) ) ;
#26039=ORIENTED_EDGE ( 'NONE', *, *, #42138, .F. ) ;
#26056=CARTESIAN_POINT ( 'NONE',  ( 8.668369459057998938, 3.037916315484999963, -6.050520490110999461 ) ) ;
#26057=CARTESIAN_POINT ( 'NONE',  ( 8.318670280409000028, 5.452311718892000059, -8.444358433472999081 ) ) ;
#26059=CARTESIAN_POINT ( 'NONE',  ( 9.492233239867587713, 4.893451691336926146, 8.512174158741519392 ) ) ;
#26066=EDGE_CURVE ( 'NONE', #62430, #20015, #12458, .T. ) ;
#26071=CARTESIAN_POINT ( 'NONE',  ( 11.01356641589999974, 2.786433584103999994, 6.253463831328000211 ) ) ;
#26074=CARTESIAN_POINT ( 'NONE',  ( 8.002383708823000319, 5.117451078405999887, -6.702236199791999915 ) ) ;
#26080=CARTESIAN_POINT ( 'NONE',  ( 9.444315208305999576, 2.927258006877999641, 8.897018628538001295 ) ) ;
#26081=CARTESIAN_POINT ( 'NONE',  ( 11.11477971959000044, 2.548217283716999848, -8.356742414746999970 ) ) ;
#26082=AXIS2_PLACEMENT_3D ( 'NONE', #40423, #18771, #18426 ) ;
#26088=CIRCLE ( 'NONE', #36162, 11.84999999999999964 ) ;
#26094=CARTESIAN_POINT ( 'NONE',  ( 10.53019352383165952, 2.722060504686575122, -8.693776886016852501 ) ) ;
#26097=CARTESIAN_POINT ( 'NONE',  ( 9.571961069101000419, 4.084683332033999470, 8.946609345378000455 ) ) ;
#26110=CARTESIAN_POINT ( 'NONE',  ( 0.9900191011665666618, 3.500000000000000888, -0.4817981237445647102 ) ) ;
#26115=CARTESIAN_POINT ( 'NONE',  ( 10.96332971959000169, 5.283550306828000309, -8.592773337476000250 ) ) ;
#26116=VERTEX_POINT ( 'NONE', #55721 ) ;
#26123=LINE ( 'NONE', #47451, #18798 ) ;
#26124=EDGE_CURVE ( 'NONE', #61390, #5573, #5752, .T. ) ;
#26126=CARTESIAN_POINT ( 'NONE',  ( 8.163589158768997933, 3.344658122371999998, -5.716722540613000447 ) ) ;
#26128=AXIS2_PLACEMENT_3D ( 'NONE', #16650, #25771, #37976 ) ;
#26130=ORIENTED_EDGE ( 'NONE', *, *, #61179, .F. ) ;
#26133=ORIENTED_EDGE ( 'NONE', *, *, #38112, .F. ) ;
#26135=DIRECTION ( 'NONE',  ( 0.000000000000000000, 0.8648648648648717963, 0.5020047465136829867 ) ) ;
#26137=ORIENTED_EDGE ( 'NONE', *, *, #64091, .F. ) ;
#26142=AXIS2_PLACEMENT_3D ( 'NONE', #34395, #8499, #61984 ) ;
#26147=CARTESIAN_POINT ( 'NONE',  ( 7.897954719591000483, 3.608525622520999843, 5.913376237674000002 ) ) ;
#26152=ORIENTED_EDGE ( 'NONE', *, *, #30312, .T. ) ;
#26156=B_SPLINE_CURVE_WITH_KNOTS ( 'NONE', 3,
 ( #21675, #31497, #47579, #18, #21339, #68885, #21004, #42339 ),
 .UNSPECIFIED., .F., .F.,
 ( 4, 2, 2, 4 ),
 ( 0.000000000000000000, 0.2499999999999993894, 0.4999999999999987788, 1.000000000000000000 ),
 .UNSPECIFIED. ) ;
#26165=CIRCLE ( 'NONE', #67474, 13.10000000000000320 ) ;
#26169=CARTESIAN_POINT ( 'NONE',  ( 10.34224945431000009, 3.348985101650000296, -8.881460768006000706 ) ) ;
#26172=CARTESIAN_POINT ( 'NONE',  ( 8.181902110542997875, 2.891006945229997793, -6.386045997152003828 ) ) ;
#26179=CARTESIAN_POINT ( 'NONE',  ( 10.89227882974000039, 3.998355201738000630, 9.261308739708001170 ) ) ;
#26181=CARTESIAN_POINT ( 'NONE',  ( 9.567560841232999991, 5.349936549139000519, -7.138437102151999447 ) ) ;
#26189=CARTESIAN_POINT ( 'NONE',  ( 8.334295743503886911, 2.728512518251676511, -8.022178723330675609 ) ) ;
#26190=CARTESIAN_POINT ( 'NONE',  ( 10.97864812944000157, 5.273131703456000352, 7.958028903907000462 ) ) ;
#26193=CARTESIAN_POINT ( 'NONE',  ( 8.631645280409999899, 3.826300099041999747, -9.055335252254000267 ) ) ;
#26194=CARTESIAN_POINT ( 'NONE',  ( 0.000000000000000000, -0.7585797238574915058, 2.824612379753441260 ) ) ;
#26195=CARTESIAN_POINT ( 'NONE',  ( 9.090964864865862083, 3.294502121218171098, 8.704449896995647862 ) ) ;
#26203=CARTESIAN_POINT ( 'NONE',  ( 8.523814158775000038, 4.920236664407999783, -6.448229650796999834 ) ) ;
#26207=CARTESIAN_POINT ( 'NONE',  ( 10.73931450027999901, 2.763002390638999994, 6.801034082888999244 ) ) ;
#26212=VERTEX_POINT ( 'NONE', #13423 ) ;
#26213=CARTESIAN_POINT ( 'NONE',  ( 9.085767219592000288, 2.821863697211000055, 6.127145479358000024 ) ) ;
#26215=CYLINDRICAL_SURFACE ( 'NONE', #9936, 0.5000000000000002220 ) ;
#26216=CARTESIAN_POINT ( 'NONE',  ( 10.98168094034000042, 5.114619317328000569, 4.904815184644999881 ) ) ;
#26224=CARTESIAN_POINT ( 'NONE',  ( 10.41185190929999926, 2.101586107686999938, 7.856266936613998553 ) ) ;
#26227=ORIENTED_EDGE ( 'NONE', *, *, #14752, .T. ) ;
#26228=CARTESIAN_POINT ( 'NONE',  ( 10.90000000000000036, 5.100000000000000533, -6.436740704805999691 ) ) ;
#26232=CARTESIAN_POINT ( 'NONE',  ( 11.09999999999999964, 4.000000000000000000, 7.500000000000000000 ) ) ;
#26234=ORIENTED_EDGE ( 'NONE', *, *, #12901, .F. ) ;
#26243=CARTESIAN_POINT ( 'NONE',  ( 10.53865537815000053, 3.647234352455999584, -6.014129666051999834 ) ) ;
#26250=CARTESIAN_POINT ( 'NONE',  ( 9.047982780412000992, 2.806082850903000026, 8.615880516515998622 ) ) ;
#26255=DIRECTION ( 'NONE',  ( 0.000000000000000000, -0.7071067811865474617, 0.7071067811865474617 ) ) ;
#26263=CARTESIAN_POINT ( 'NONE',  ( 8.856851002545001350, 2.832432432432000269, -6.822293592207000934 ) ) ;
#26269=EDGE_CURVE ( 'NONE', #57358, #44634, #65576, .T. ) ;
#26272=CARTESIAN_POINT ( 'NONE',  ( 9.564884880418375701, 5.349923162331274185, -7.500006638304977713 ) ) ;
#26274=CARTESIAN_POINT ( 'NONE',  ( -15.86200481174999943, 5.599999999999999645, 6.571291218949999902 ) ) ;
#26278=CARTESIAN_POINT ( 'NONE',  ( 10.96332971959000169, 5.283550306828000309, -8.592773337476000250 ) ) ;
#26285=CARTESIAN_POINT ( 'NONE',  ( 8.642077642326000841, 2.899999999999999911, 6.463854830420999953 ) ) ;
#26292=CARTESIAN_POINT ( 'NONE',  ( 8.170084835020603009, 3.293757737277087205, 6.167713512348048432 ) ) ;
#26293=VERTEX_POINT ( 'NONE', #3931 ) ;
#26296=DIRECTION ( 'NONE',  ( -0.7071067811865074937, -0.7011937492414073159, -0.09125418360182094291 ) ) ;
#26297=CARTESIAN_POINT ( 'NONE',  ( 3.250973465878000290, -3.500000000000000000, 0.000000000000000000 ) ) ;
#26299=CARTESIAN_POINT ( 'NONE',  ( 8.616995677562000466, 4.876077402042000131, 5.996974966532000018 ) ) ;
#26311=CARTESIAN_POINT ( 'NONE',  ( 9.649770280412001355, 4.042991257420999851, -5.768106221333000327 ) ) ;
#26323=DIRECTION ( 'NONE',  ( 0.000000000000000000, 0.000000000000000000, -1.000000000000000000 ) ) ;
#26328=CARTESIAN_POINT ( 'NONE',  ( 8.642358819840294970, 3.294576102360962988, 8.704493534904408136 ) ) ;
#26330=AXIS2_PLACEMENT_3D ( 'NONE', #66509, #7790, #14076 ) ;
#26331=CARTESIAN_POINT ( 'NONE',  ( 10.93769853197999886, 5.063116524846000388, -4.920828787216999345 ) ) ;
#26338=DIRECTION ( 'NONE',  ( 0.000000000000000000, 1.000000000000000000, 0.000000000000000000 ) ) ;
#26340=CARTESIAN_POINT ( 'NONE',  ( 8.550260823830997836, 3.169363294249995633, 6.002781648002655679 ) ) ;
#26353=DIRECTION ( 'NONE',  ( 1.000000000000000000, 0.000000000000000000, 0.000000000000000000 ) ) ;
#26356=EDGE_CURVE ( 'NONE', #718, #54751, #39954, .T. ) ;
#26363=CARTESIAN_POINT ( 'NONE',  ( 10.89999913120000130, 0.3000008665460999757, -9.776630266016001158 ) ) ;
#26365=CARTESIAN_POINT ( 'NONE',  ( 10.17905590578999941, 2.899999999999999911, 6.571291218949999902 ) ) ;
#26368=CARTESIAN_POINT ( 'NONE',  ( 11.09999999999999964, 6.593648130222000248, -5.598803514566000672 ) ) ;
#26374=FACE_OUTER_BOUND ( 'NONE', #35014, .T. ) ;
#26376=VECTOR ( 'NONE', #54924, 1000.000000000000227 ) ;
#26379=DIRECTION ( 'NONE',  ( 1.000000000000000000, 0.000000000000000000, 0.000000000000000000 ) ) ;
#26385=CARTESIAN_POINT ( 'NONE',  ( 3.499658142331559585, -2.179804560773650479, -2.476966527028495957 ) ) ;
#26393=CARTESIAN_POINT ( 'NONE',  ( 7.961495038489999843, 3.389986099490999827, -6.279439026173999849 ) ) ;
#26397=CARTESIAN_POINT ( 'NONE',  ( -2.444943969992999916E-05, 2.899969545325999931, 0.000000000000000000 ) ) ;
#26402=FACE_OUTER_BOUND ( 'NONE', #46712, .T. ) ;
#26404=CARTESIAN_POINT ( 'NONE',  ( 8.299720885770000223, 3.399999999999999911, -6.084164326786999588 ) ) ;
#26408=DIRECTION ( 'NONE',  ( 1.000000000000000000, -2.684047399077999465E-14, 2.619093452019999937E-10 ) ) ;
#26413=ORIENTED_EDGE ( 'NONE', *, *, #32524, .F. ) ;
#26421=CARTESIAN_POINT ( 'NONE',  ( 10.90000154029999990, -1.382741116750999977, -11.26545724788999969 ) ) ;
#26422=CARTESIAN_POINT ( 'NONE',  ( 8.020642159885767342, 5.146218562000625774, -6.785513053889468793 ) ) ;
#26427=CARTESIAN_POINT ( 'NONE',  ( 9.611387933856001098, 3.334846092635999959, 5.869117602953000556 ) ) ;
#26428=CARTESIAN_POINT ( 'NONE',  ( 11.08729332543999924, 2.258658230726000138, -7.034579402814999938 ) ) ;
#26430=AXIS2_PLACEMENT_3D ( 'NONE', #43302, #16377, #59371 ) ;
#26431=CARTESIAN_POINT ( 'NONE',  ( 9.070310841232000598, 5.361622798585000460, -7.185294144754000634 ) ) ;
#26432=CARTESIAN_POINT ( 'NONE',  ( 3.774180895676000347, -3.540496567027000108, 0.007937750490802000097 ) ) ;
#26433=FACE_OUTER_BOUND ( 'NONE', #1464, .T. ) ;
#26435=DIRECTION ( 'NONE',  ( -1.000000000000000000, 0.000000000000000000, 0.000000000000000000 ) ) ;
#26444=CARTESIAN_POINT ( 'NONE',  ( 6.875000000000000000, 5.574137966889000317, -8.240733100917999820 ) ) ;
#26452=VERTEX_POINT ( 'NONE', #59833 ) ;
#26454=CARTESIAN_POINT ( 'NONE',  ( 9.568039158772000619, 5.336630274082000192, -7.092011739486999922 ) ) ;
#26456=EDGE_CURVE ( 'NONE', #2243, #37337, #60535, .T. ) ;
#26457=CARTESIAN_POINT ( 'NONE',  ( 10.99143984058640378, 5.686599839966610226, 4.947043824675725787 ) ) ;
#26461=AXIS2_PLACEMENT_3D ( 'NONE', #63360, #47303, #67234 ) ;
#26463=CARTESIAN_POINT ( 'NONE',  ( 2.027882597155000521, 3.758808678259999869, 0.01395688117858999953 ) ) ;
#26469=VECTOR ( 'NONE', #9253, 1000.000000000000114 ) ;
#26470=CARTESIAN_POINT ( 'NONE',  ( 8.656823341231000057, 5.329437560656000272, 6.027391099688998999 ) ) ;
#26471=VERTEX_POINT ( 'NONE', #11939 ) ;
#26472=DIRECTION ( 'NONE',  ( 1.000000000000000000, 0.000000000000000000, -7.847361993451999840E-14 ) ) ;
#26473=CARTESIAN_POINT ( 'NONE',  ( 6.928179719591000207, 5.602143124542999786, -7.927308852422999763 ) ) ;
#26476=ORIENTED_EDGE ( 'NONE', *, *, #58578, .F. ) ;
#26485=AXIS2_PLACEMENT_3D ( 'NONE', #67239, #67582, #24607 ) ;
#26487=EDGE_CURVE ( 'NONE', #15849, #44476, #57384, .T. ) ;
#26491=ORIENTED_EDGE ( 'NONE', *, *, #12810, .F. ) ;
#26492=CARTESIAN_POINT ( 'NONE',  ( 9.053329719590999858, 5.618384167307999277, 7.727742442702000503 ) ) ;
#26496=CARTESIAN_POINT ( 'NONE',  ( 11.12484647810999938, 6.576551162614999946, -5.637922378081000829 ) ) ;
#26506=EDGE_LOOP ( 'NONE', ( #17572, #59269, #6950, #9990 ) ) ;
#26509=VECTOR ( 'NONE', #26296, 1000.000000000000114 ) ;
#26513=CARTESIAN_POINT ( 'NONE',  ( 10.00074698269999907, 2.373893144840999891, -7.962435130300000274 ) ) ;
#26521=CARTESIAN_POINT ( 'NONE',  ( 8.880743402660417729, 5.552835561677609277, -8.364321471810635344 ) ) ;
#26526=CARTESIAN_POINT ( 'NONE',  ( 10.57892463485000079, 4.649960478797999563, 5.681084732956000138 ) ) ;
#26533=CARTESIAN_POINT ( 'NONE',  ( 8.126005914336607461, 5.349985204051306731, -7.683689342979575621 ) ) ;
#26535=CARTESIAN_POINT ( 'NONE',  ( 0.9681103717476999826, 3.205765437135000173, -1.404659375816999844 ) ) ;
#26543=LINE ( 'NONE', #32138, #12191 ) ;
#26545=VERTEX_POINT ( 'NONE', #28732 ) ;
#26548=CARTESIAN_POINT ( 'NONE',  ( 7.099999886593999499, 12.39999890530000037, 0.000000000000000000 ) ) ;
#26549=CARTESIAN_POINT ( 'NONE',  ( 8.564679719593000229, 4.146787477634999775, -5.941926545671999627 ) ) ;
#26550=CARTESIAN_POINT ( 'NONE',  ( 9.073148997461000675, 5.167567567567999731, -6.822293592207000934 ) ) ;
#26551=CARTESIAN_POINT ( 'NONE',  ( 3.358374205747110430, 1.670603451639867121, 2.796989605246705590 ) ) ;
#26552=VERTEX_POINT ( 'NONE', #29080 ) ;
#26553=CARTESIAN_POINT ( 'NONE',  ( 11.18484176840999922, 2.599663474744000169, 7.740674686800000259 ) ) ;
#26559=CARTESIAN_POINT ( 'NONE',  ( 9.123551658772999673, 5.558938731259999599, 6.272977177425000050 ) ) ;
#26560=VECTOR ( 'NONE', #45083, 1000.000000000000114 ) ;
#26565=CARTESIAN_POINT ( 'NONE',  ( 8.970944094206998898, 5.100000000000000533, 6.571291218949999902 ) ) ;
#26566=CARTESIAN_POINT ( 'NONE',  ( 1.357018817589999982, 2.440310627160000134, 2.160132089918000098 ) ) ;
#26570=CARTESIAN_POINT ( 'NONE',  ( 10.24477918374999952, 5.265206995764999398, 8.959504263949002123 ) ) ;
#26575=CARTESIAN_POINT ( 'NONE',  ( 9.269689158774999882, 3.135494838036999798, -8.598037907310999373 ) ) ;
#26576=AXIS2_PLACEMENT_3D ( 'NONE', #34372, #29480, #13728 ) ;
#26580=CARTESIAN_POINT ( 'NONE',  ( 11.03613257345000065, 2.777644159685000336, -5.022749861804999938 ) ) ;
#26584=CARTESIAN_POINT ( 'NONE',  ( 11.09999999999999964, 4.000000000000000000, -7.500000000000000000 ) ) ;
#26588=CARTESIAN_POINT ( 'NONE',  ( 9.137543006348998631, 2.995704926864999784, 8.544754656710999541 ) ) ;
#26590=CARTESIAN_POINT ( 'NONE',  ( 9.766125411066999717, 4.735428155407000794, -8.791393655830999521 ) ) ;
#26595=CARTESIAN_POINT ( 'NONE',  ( 9.001480659271445361, 5.278232124331313280, 7.933979055097461597 ) ) ;
#26597=CARTESIAN_POINT ( 'NONE',  ( 8.946010841230998878, 5.458692773671000253, 7.456452194274000078 ) ) ;
#26599=FACE_OUTER_BOUND ( 'NONE', #32035, .T. ) ;
#26602=B_SPLINE_CURVE_WITH_KNOTS ( 'NONE', 3,
 ( #13807, #56799, #19383, #35136 ),
 .UNSPECIFIED., .F., .F.,
 ( 4, 4 ),
 ( 0.000000000000000000, 1.000000000000000000 ),
 .UNSPECIFIED. ) ;
#26605=CARTESIAN_POINT ( 'NONE',  ( 11.06523650270000125, 8.808136091477001273, 6.643946570999999857 ) ) ;
#26607=CARTESIAN_POINT ( 'NONE',  ( 2.000973465872999846, 3.500000000000000000, 0.000000000000000000 ) ) ;
#26611=EDGE_CURVE ( 'NONE', #21492, #59329, #63195, .T. ) ;
#26613=DIRECTION ( 'NONE',  ( -1.000000000000000000, 0.000000000000000000, 0.000000000000000000 ) ) ;
#26618=CARTESIAN_POINT ( 'NONE',  ( 0.1210379451993999905, -1.906427021235999941, -2.406055758466000061 ) ) ;
#26625=CARTESIAN_POINT ( 'NONE',  ( 7.681993940831000067, 3.468925063633002903, -6.455929610676999886 ) ) ;
#26627=CARTESIAN_POINT ( 'NONE',  ( 10.16821721959000158, 2.330395133894000548, -7.267461653224000173 ) ) ;
#26634=CARTESIAN_POINT ( 'NONE',  ( 0.8811095901647999495, -0.1441893070566999946, 3.255843074068999865 ) ) ;
#26635=EDGE_CURVE ( 'NONE', #27999, #34076, #32395, .T. ) ;
#26637=CARTESIAN_POINT ( 'NONE',  ( 3.467799898000360592, 1.131362752643461977, -3.282759086874214027 ) ) ;
#26642=CARTESIAN_POINT ( 'NONE',  ( 8.194126132207950164, 2.898246542105644696, 6.620179831079268773 ) ) ;
#26650=CARTESIAN_POINT ( 'NONE',  ( 8.647266668088249730, 4.120490794148916613, -5.883508675810684707 ) ) ;
#26652=B_SPLINE_CURVE_WITH_KNOTS ( 'NONE', 3,
 ( #64946, #6577, #32471, #55518 ),
 .UNSPECIFIED., .F., .F.,
 ( 4, 4 ),
 ( 0.000000000000000000, 1.000000000000000000 ),
 .UNSPECIFIED. ) ;
#26658=CARTESIAN_POINT ( 'NONE',  ( 9.417722590937366078, 5.345104022944846989, 7.384957899024609418 ) ) ;
#26662=CARTESIAN_POINT ( 'NONE',  ( 8.415504719592000527, 2.469361196073999842, -7.826019481986000059 ) ) ;
#26667=VERTEX_POINT ( 'NONE', #14025 ) ;
#26678=LINE ( 'NONE', #53233, #55233 ) ;
#26680=CARTESIAN_POINT ( 'NONE',  ( 8.475341021510232054, 5.350570349241480450, 7.499981640446101494 ) ) ;
#26681=VERTEX_POINT ( 'NONE', #66810 ) ;
#26696=CARTESIAN_POINT ( 'NONE',  ( 8.500189158773000742, 2.724453559418999582, -8.908010318766001134 ) ) ;
#26701=CARTESIAN_POINT ( 'NONE',  ( 8.639360841228999277, 5.074768364528000397, -8.296267706722000312 ) ) ;
#26705=CARTESIAN_POINT ( 'NONE',  ( 1.228056799207625227, -2.150913519912213800, 2.798833948393621540 ) ) ;
#26706=CYLINDRICAL_SURFACE ( 'NONE', #32190, 3.500000000000000000 ) ;
#26710=CARTESIAN_POINT ( 'NONE',  ( 2.007156007037999679, 3.012404793772358147, -1.845954168039164678 ) ) ;
#26711=DIRECTION ( 'NONE',  ( -0.9999999999999893419, -1.468722421713984115E-07, -5.561711760123941642E-09 ) ) ;
#26723=CARTESIAN_POINT ( 'NONE',  ( 7.417083333331121686, 2.920449762762455492, -6.670361928033868182 ) ) ;
#26727=CARTESIAN_POINT ( 'NONE',  ( 0.1499942179679999987, 5.893556041935713383E-16, -2.749976859058071543 ) ) ;
#26733=CARTESIAN_POINT ( 'NONE',  ( 10.15670292967811150, 5.179682183662283279, -8.179940953558951122 ) ) ;
#26734=ORIENTED_EDGE ( 'NONE', *, *, #23754, .F. ) ;
#26752=DIRECTION ( 'NONE',  ( 0.000000000000000000, 0.7158784314711267305, 0.6982249432342270135 ) ) ;
#26754=CARTESIAN_POINT ( 'NONE',  ( 8.442410841228998208, 4.988620887051999908, -9.026201633254999024 ) ) ;
#26758=EDGE_LOOP ( 'NONE', ( #54561, #12383, #40365, #37287, #49444, #9296, #474, #26778, #5116, #64463 ) ) ;
#26762=B_SPLINE_CURVE_WITH_KNOTS ( 'NONE', 3,
 ( #38306, #48804, #54738, #64862 ),
 .UNSPECIFIED., .F., .F.,
 ( 4, 4 ),
 ( 0.000000000000000000, 1.000000000000000000 ),
 .UNSPECIFIED. ) ;
#26763=CARTESIAN_POINT ( 'NONE',  ( 10.76947109217999810, 5.100000000000000533, -6.152188490330000370 ) ) ;
#26774=CARTESIAN_POINT ( 'NONE',  ( 10.64659450977357658, 2.685850423140129895, 7.981710561160634931 ) ) ;
#26778=ORIENTED_EDGE ( 'NONE', *, *, #3932, .F. ) ;
#26779=CARTESIAN_POINT ( 'NONE',  ( 9.242342830452999536, 5.206708472530999998, 8.808826521083998884 ) ) ;
#26780=CARTESIAN_POINT ( 'NONE',  ( 10.15335165876999923, 3.144981324235999853, -5.860948306964999688 ) ) ;
#26782=DIRECTION ( 'NONE',  ( -1.000000000000000000, 0.000000000000000000, 0.000000000000000000 ) ) ;
#26793=VECTOR ( 'NONE', #30370, 1000.000000000000000 ) ;
#26794=CARTESIAN_POINT ( 'NONE',  ( 10.09696969267000100, 5.253376380222999131, 8.530663119653999260 ) ) ;
#26798=EDGE_CURVE ( 'NONE', #4475, #21968, #51572, .T. ) ;
#26806=CARTESIAN_POINT ( 'NONE',  ( 9.667489158770999680, 4.808846957865000604, -8.639578604182998944 ) ) ;
#26809=VERTEX_POINT ( 'NONE', #29429 ) ;
#26810=CARTESIAN_POINT ( 'NONE',  ( 0.6750951013211000662, -1.176389486124999939, 3.509795687408999942 ) ) ;
#26812=CARTESIAN_POINT ( 'NONE',  ( 11.10664834123000055, 5.324188120986000250, -7.809342242343999985 ) ) ;
#26813=ORIENTED_EDGE ( 'NONE', *, *, #4247, .T. ) ;
#26818=CARTESIAN_POINT ( 'NONE',  ( 9.298698341228998743, 5.159258275969999197, 9.109498396691998678 ) ) ;
#26821=CARTESIAN_POINT ( 'NONE',  ( 7.458579719585999968, 5.383759907926999766, -8.542359279933998906 ) ) ;
#26825=CARTESIAN_POINT ( 'NONE',  ( 4.900006121741999010, 2.000000000000000000, 0.000000000000000000 ) ) ;
#26826=CARTESIAN_POINT ( 'NONE',  ( 0.5000220334827000235, 2.806761118207999672, -2.090954811877999919 ) ) ;
#26840=CARTESIAN_POINT ( 'NONE',  ( 7.037114158771000660, 4.623631324973000112, 8.651459902566999816 ) ) ;
#26841=EDGE_CURVE ( 'NONE', #10178, #6658, #51417, .T. ) ;
#26843=ORIENTED_EDGE ( 'NONE', *, *, #21381, .T. ) ;
#26847=CARTESIAN_POINT ( 'NONE',  ( 11.07074944260999949, 6.638253589849999692, -5.577401735838000363 ) ) ;
#26851=CARTESIAN_POINT ( 'NONE',  ( 0.1103081484368000076, -1.521127753326000143, -2.712944034833999929 ) ) ;
#26853=CARTESIAN_POINT ( 'NONE',  ( 8.447783767286768608, 5.285582108569087723, 7.027722483016013655 ) ) ;
#26858=VERTEX_POINT ( 'NONE', #11169 ) ;
#26860=ORIENTED_EDGE ( 'NONE', *, *, #31530, .T. ) ;
#26862=DIRECTION ( 'NONE',  ( 0.7071051450805292404, 0.000000000000000000, -0.7071084172887802666 ) ) ;
#26863=CARTESIAN_POINT ( 'NONE',  ( 4.900006121741999898, -1.947945353336631102, 0.5234957687185606279 ) ) ;
#26864=CARTESIAN_POINT ( 'NONE',  ( 10.32702465212000043, 5.663794543395000325, -6.682030833630000721 ) ) ;
#26865=CARTESIAN_POINT ( 'NONE',  ( 8.100000113405998903, 3.037570195374000164E-13, -3.946654265865999873E-14 ) ) ;
#26866=PLANE ( 'NONE',  #33911 ) ;
#26869=EDGE_LOOP ( 'NONE', ( #25547, #6280, #58500, #50382 ) ) ;
#26871=CARTESIAN_POINT ( 'NONE',  ( 10.74609776273999984, 4.263105564403999459, 9.276980853981999786 ) ) ;
#26877=CARTESIAN_POINT ( 'NONE',  ( 11.00366136905836889, 3.174009385455987431, -9.060794845599636105 ) ) ;
#26879=DIRECTION ( 'NONE',  ( 1.000000000000000000, 0.000000000000000000, 0.000000000000000000 ) ) ;
#26880=FILL_AREA_STYLE ('',( #5541 ) ) ;
#26886=CARTESIAN_POINT ( 'NONE',  ( 10.81218444446805016, 4.996894876589563772, 4.859602168033166691 ) ) ;
#26888=ORIENTED_EDGE ( 'NONE', *, *, #14239, .F. ) ;
#26890=DIRECTION ( 'NONE',  ( 0.000000000000000000, -1.000000000000000000, -1.110693484091000068E-14 ) ) ;
#26891=CARTESIAN_POINT ( 'NONE',  ( 8.502045280412000139, 3.869396554003000421, 5.695652484872999466 ) ) ;
#26893=CARTESIAN_POINT ( 'NONE',  ( 8.863029719594999634, 2.990001567622999623, -8.695425648791999862 ) ) ;
#26894=CARTESIAN_POINT ( 'NONE',  ( 3.500000000000000000, -3.033011252059000018, -1.020217008720000207 ) ) ;
#26897=ORIENTED_EDGE ( 'NONE', *, *, #32912, .F. ) ;
#26898=CARTESIAN_POINT ( 'NONE',  ( 10.09181485429000169, 2.440912084162000006, 7.817367409531000177 ) ) ;
#26904=CARTESIAN_POINT ( 'NONE',  ( 8.636454719592999041, 3.869396554003000421, 5.695652484872999466 ) ) ;
#26909=CARTESIAN_POINT ( 'NONE',  ( 2.215293907524999995, 1.603576596796000064, -2.837084241009999896 ) ) ;
#26915=CARTESIAN_POINT ( 'NONE',  ( 9.219964158774999419, 3.941185585667000169, -8.896279800194999865 ) ) ;
#26920=CARTESIAN_POINT ( 'NONE',  ( 7.947862523144673119, 4.896691652056699873, -6.386472708437699985 ) ) ;
#26929=CARTESIAN_POINT ( 'NONE',  ( 9.634020792350998619, 3.042978295541999945, 8.588098960242001922 ) ) ;
#26930=CARTESIAN_POINT ( 'NONE',  ( 10.48414939117999900, 4.098653981087000631, -9.351365234892998757 ) ) ;
#26937=CARTESIAN_POINT ( 'NONE',  ( 8.791232780412000736, 5.095085596809999728, 6.286981168432999922 ) ) ;
#26941=B_SPLINE_CURVE_WITH_KNOTS ( 'NONE', 3,
 ( #68336, #14536, #35853, #30608 ),
 .UNSPECIFIED., .F., .F.,
 ( 4, 4 ),
 ( 0.000000000000000000, 1.000000000000000000 ),
 .UNSPECIFIED. ) ;
#26948=CARTESIAN_POINT ( 'NONE',  ( 10.92020230602999931, 9.067058286522998500, 6.347630032935000166 ) ) ;
#26959=CARTESIAN_POINT ( 'NONE',  ( 0.2444343787449999583, 2.474918916286999782, -2.043501580946999852 ) ) ;
#26960=CARTESIAN_POINT ( 'NONE',  ( 9.637701392160892055, 4.829637745207382871, -8.579854099904720144 ) ) ;
#26963=CARTESIAN_POINT ( 'NONE',  ( 9.101287939753134992, 5.350063131615271139, -7.263153235713748046 ) ) ;
#26966=CARTESIAN_POINT ( 'NONE',  ( 10.58470471959000037, 2.966809777448999874, -8.831980808885999679 ) ) ;
#26968=CARTESIAN_POINT ( 'NONE',  ( 8.436984272513997851, 5.098716299041000433, 6.624027315230001101 ) ) ;
#26970=CARTESIAN_POINT ( 'NONE',  ( 8.949580915942656034, 5.282157812751564485, 7.064122796597747111 ) ) ;
#26987=CARTESIAN_POINT ( 'NONE',  ( 8.611421496779771090, 4.936505472987223975, 6.052097162928508745 ) ) ;
#26990=DIRECTION ( 'NONE',  ( -1.000000000000000000, 0.000000000000000000, 0.000000000000000000 ) ) ;
#26999=CARTESIAN_POINT ( 'NONE',  ( 8.763579719593998618, 4.815598936798999752, -8.835641302565999666 ) ) ;
#27014=EDGE_LOOP ( 'NONE', ( #20153, #49936, #32881, #29399 ) ) ;
#27018=DIRECTION ( 'NONE',  ( 6.273181768770000388E-11, 6.273307657911000434E-11, -1.000000000000000000 ) ) ;
#27023=B_SPLINE_CURVE_WITH_KNOTS ( 'NONE', 3,
 ( #10774, #5872, #42600, #27210, #43290, #38732, #42942, #64936, #64595, #32120, #16021, #27907, #38382, #59023, #16364, #290, #22642, #63911 ),
 .UNSPECIFIED., .F., .F.,
 ( 4, 2, 2, 2, 2, 2, 2, 2, 4 ),
 ( 0.000000000000000000, 0.1250000000000000278, 0.2500000000000000000, 0.3749999999999999445, 0.4999999999999999445, 0.6249999999999998890, 0.7499999999999998890, 0.8750000000000000000, 1.000000000000000000 ),
 .UNSPECIFIED. ) ;
#27025=EDGE_CURVE ( 'NONE', #12675, #44325, #65604, .T. ) ;
#27029=CYLINDRICAL_SURFACE ( 'NONE', #58110, 1.999999999999999556 ) ;
#27037=CARTESIAN_POINT ( 'NONE',  ( 9.693589158772999426, 4.047146749018000200, -5.600703114891000034 ) ) ;
#27039=AXIS2_PLACEMENT_3D ( 'NONE', #21609, #33841, #24375 ) ;
#27047=CARTESIAN_POINT ( 'NONE',  ( 0.1499942179679999987, 1.689975037551097792, -2.199046806507070517 ) ) ;
#27066=CARTESIAN_POINT ( 'NONE',  ( 6.999999999999999112, 8.540090292376646630, -4.496300658368356906 ) ) ;
#27078=EDGE_CURVE ( 'NONE', #61078, #37966, #66948, .T. ) ;
#27094=CARTESIAN_POINT ( 'NONE',  ( 7.265585841225999708, 4.636818559850000909, -5.710024136463999866 ) ) ;
#27096=CARTESIAN_POINT ( 'NONE',  ( 9.489403898701906925, 4.927997357771009668, 8.480306757541997698 ) ) ;
#27106=CARTESIAN_POINT ( 'NONE',  ( 5.500000000000000000, 0.000000000000000000, 0.000000000000000000 ) ) ;
#27114=B_SPLINE_SURFACE_WITH_KNOTS ( 'NONE', 3, 3, ( 
 ( #14681, #52418, #4514, #24826, #47182, #36000, #62224, #68485, #41933, #9083, #68836, #25511, #67457, #68145, #57316, #15366, #20608, #30422, #36693, #19924, #51732, #51395, #30759, #10117, #31448, #26203, #20954, #35326, #8745, #3490, #3825, #4173, #11480, #53794, #5552 ),
 ( #1345, #6234, #21972, #59726, #11828, #661, #37036, #58351, #43312, #33168, #16725, #27575, #32820, #22662, #27925, #63590, #48901, #49235, #15708, #1006, #26893, #10453, #5212, #43660, #31793, #53111, #26549, #64957, #22318, #47875, #5891, #42622, #69180, #16385, #21291 ),
 ( #38403, #63931, #17070, #64617, #32480, #37715, #54485, #16043, #37374, #48556, #38055, #58694, #10798, #48206, #6585, #64271, #313, #27232, #32143, #53458, #21629, #42964, #59043, #11146, #59379, #54136, #18124, #65312, #8320, #66693, #24048, #7977, #33515, #12530, #65659 ),
 ( #29311, #29663, #44006, #50624, #7281, #17427, #54831, #45383, #60081, #50965, #38755, #18816, #2725, #12186, #55525, #23011, #6930, #66000, #3063, #28265, #61456, #49585, #50280, #1692, #44359, #34209, #7626, #55176, #13573, #28972, #56211, #2381, #39444, #17781, #60424 ) ),
 .UNSPECIFIED., .F., .F., .F.,
 ( 4, 4 ),
 ( 4, 1, 1, 1, 1, 1, 1, 1, 1, 1, 1, 1, 1, 1, 1, 1, 1, 1, 1, 1, 1, 1, 1, 1, 1, 1, 1, 1, 1, 1, 1, 1, 4 ),
 ( -0.1039370721279000015, 1.103937072127999963 ),
 ( -0.02000000000000000042, 0.01250000000000000069, 0.04499999999999999833, 0.07749999999999999944, 0.1100000000000000006, 0.1424999999999999878, 0.1749999999999999889, 0.2074999999999999900, 0.2399999999999999911, 0.2725000000000000200, 0.3049999999999999933, 0.3375000000000000222, 0.3699999999999999956, 0.4025000000000000244, 0.4349999999999999978, 0.4675000000000000266, 0.5000000000000000000, 0.5324999999999999734, 0.5649999999999999467, 0.5975000000000000311, 0.6300000000000000044, 0.6624999999999999778, 0.6949999999999999512, 0.7275000000000000355, 0.7600000000000000089, 0.7924999999999999822, 0.8249999999999999556, 0.8575000000000000400, 0.8900000000000000133, 0.9224999999999999867, 0.9549999999999999600, 0.9875000000000000444, 1.020000000000000018 ),
 .UNSPECIFIED. ) ;
#27118=CARTESIAN_POINT ( 'NONE',  ( 10.41185190929999926, 2.101586107686999938, 7.856266936613998553 ) ) ;
#27119=CARTESIAN_POINT ( 'NONE',  ( 10.38052665877000003, 5.283793195606000026, -8.830196380017000024 ) ) ;
#27133=CARTESIAN_POINT ( 'NONE',  ( 9.634020792350998619, 3.042978295541999945, 8.588098960242001922 ) ) ;
#27139=EDGE_CURVE ( 'NONE', #8792, #4832, #47768, .T. ) ;
#27145=CARTESIAN_POINT ( 'NONE',  ( 9.070789158774999805, 5.349936549139000519, -7.138437102151999447 ) ) ;
#27146=EDGE_CURVE ( 'NONE', #6055, #41535, #14140, .T. ) ;
#27150=CARTESIAN_POINT ( 'NONE',  ( 0.8998509817850999237, 3.128647331775999962, -1.414269894618000123 ) ) ;
#27151=CARTESIAN_POINT ( 'NONE',  ( 8.150000662387999029, -3.446132268436000216E-13, -3.324010876891999568E-14 ) ) ;
#27152=CARTESIAN_POINT ( 'NONE',  ( 11.06878584122999953, 5.318802051720999735, -7.168446171767000052 ) ) ;
#27155=DIRECTION ( 'NONE',  ( 1.000000000000000000, 0.000000000000000000, 0.000000000000000000 ) ) ;
#27158=CARTESIAN_POINT ( 'NONE',  ( 8.566232780412001091, 5.212261578733999201, 6.157186134061999994 ) ) ;
#27159=ORIENTED_EDGE ( 'NONE', *, *, #15560, .F. ) ;
#27161=CARTESIAN_POINT ( 'NONE',  ( 8.303904719589001004, 4.466585441010000324, -5.831585202652000532 ) ) ;
#27169=CYLINDRICAL_SURFACE ( 'NONE', #45163, 1.350000000000000533 ) ;
#27179=CARTESIAN_POINT ( 'NONE',  ( 8.796579719592999780, 2.368264398678999516, 7.410200237937000445 ) ) ;
#27184=CARTESIAN_POINT ( 'NONE',  ( 11.02038863743000086, 5.796704460786999746, -5.015990784938999525 ) ) ;
#27188=AXIS2_PLACEMENT_3D ( 'NONE', #58401, #68886, #5597 ) ;
#27197=ORIENTED_EDGE ( 'NONE', *, *, #43457, .F. ) ;
#27202=CARTESIAN_POINT ( 'NONE',  ( 10.35427764559999986, 4.879113829302000660, -8.944031201701999834 ) ) ;
#27205=CARTESIAN_POINT ( 'NONE',  ( 8.283628111110997949, 2.878995628920999916, -6.357604486408997779 ) ) ;
#27209=CARTESIAN_POINT ( 'NONE',  ( 9.290193290418001126, 2.377818438998999806, 7.540992072119000689 ) ) ;
#27210=CARTESIAN_POINT ( 'NONE',  ( 2.259306799209333416, -3.058252359239909346, 1.762666431298136605 ) ) ;
#27214=CARTESIAN_POINT ( 'NONE',  ( 10.87850165404999991, 9.620987454954001095, -5.906477034301000018 ) ) ;
#27215=CARTESIAN_POINT ( 'NONE',  ( 7.100000000000317613, 2.856882225463113656, -6.715485463213433093 ) ) ;
#27218=CARTESIAN_POINT ( 'NONE',  ( 8.115081613917173087, 5.350113345104855256, -7.499995474391613293 ) ) ;
#27223=EDGE_CURVE ( 'NONE', #67676, #33656, #58789, .T. ) ;
#27224=EDGE_CURVE ( 'NONE', #27749, #25016, #46525, .T. ) ;
#27230=CARTESIAN_POINT ( 'NONE',  ( 7.897954719591000483, 3.608525622520999843, 5.913376237674000002 ) ) ;
#27232=CARTESIAN_POINT ( 'NONE',  ( 9.102795280413999990, 3.071719032003000116, -6.037263251225000182 ) ) ;
#27236=CARTESIAN_POINT ( 'NONE',  ( 10.03612394578000000, 3.011788727150999989, 8.746962581836999817 ) ) ;
#27237=B_SPLINE_CURVE_WITH_KNOTS ( 'NONE', 3,
 ( #46660, #13479, #29909, #50870 ),
 .UNSPECIFIED., .F., .F.,
 ( 4, 4 ),
 ( 0.000000000000000000, 1.000000000000000000 ),
 .UNSPECIFIED. ) ;
#27250=B_SPLINE_CURVE_WITH_KNOTS ( 'NONE', 3,
 ( #67832, #57340, #57685, #5040 ),
 .UNSPECIFIED., .F., .F.,
 ( 4, 4 ),
 ( 0.000000000000000000, 1.000000000000000000 ),
 .UNSPECIFIED. ) ;
#27251=VERTEX_POINT ( 'NONE', #19435 ) ;
#27256=B_SPLINE_SURFACE_WITH_KNOTS ( 'NONE', 3, 3, ( 
 ( #56152, #61058, #39387, #55470, #60708, #23995, #7569, #18759, #28920, #13178, #2328, #65603, #8601, #34506, #23648, #17726, #39049, #60367, #18070, #44987, #19780, #68343, #9272, #15569, #68005, #62421, #9972, #14199, #41450, #46007, #40758, #20120, #62758, #4373, #42142 ),
 ( #14877, #20461, #63447, #62080, #35525, #31308, #56846, #14542, #67656, #52620, #67316, #35860, #25708, #25024, #8944, #63094, #30284, #51588, #31649, #4713, #57176, #3683, #15219, #36897, #5068, #46355, #58212, #36544, #41789, #10316, #30616, #25363, #52971, #68692, #47040 ),
 ( #57871, #19434, #26057, #47386, #36200, #57514, #20807, #9620, #51929, #41108, #4025, #30965, #46701, #52279, #10656, #22179, #49098, #58902, #37917, #63792, #16928, #27789, #5417, #21155, #48068, #11006, #5751, #59585, #59237, #47732, #32681, #48757, #1210, #32344, #53315 ),
 ( #33026, #26754, #22520, #27435, #43519, #21489, #53994, #43861, #64817, #38260, #11686, #11342, #12042, #65164, #53658, #515, #21832, #15901, #54338, #43163, #6440, #17284, #172, #59931, #42482, #27094, #6096, #37233, #48409, #38611, #33375, #37568, #42823, #58550, #64131 ) ),
 .UNSPECIFIED., .F., .F., .F.,
 ( 4, 4 ),
 ( 4, 1, 1, 1, 1, 1, 1, 1, 1, 1, 1, 1, 1, 1, 1, 1, 1, 1, 1, 1, 1, 1, 1, 1, 1, 1, 1, 1, 1, 1, 1, 1, 4 ),
 ( -0.1039370721279000015, 1.103937072127999963 ),
 ( -0.01999999999998999800, 0.01250000000001000137, 0.04499999999999999833, 0.07749999999999999944, 0.1100000000000000006, 0.1424999999999999878, 0.1749999999999999889, 0.2074999999999999900, 0.2399999999999999911, 0.2725000000000000200, 0.3049999999999999933, 0.3375000000000000222, 0.3699999999999999956, 0.4025000000000000244, 0.4349999999999999978, 0.4675000000000000266, 0.5000000000000000000, 0.5324999999999999734, 0.5649999999999999467, 0.5975000000000000311, 0.6300000000000000044, 0.6624999999999999778, 0.6949999999999999512, 0.7275000000000000355, 0.7600000000000000089, 0.7924999999999999822, 0.8249999999999999556, 0.8575000000000000400, 0.8900000000000000133, 0.9224999999999999867, 0.9549999999999999600, 0.9875000000000000444, 1.020000000000000018 ),
 .UNSPECIFIED. ) ;
#27257=CARTESIAN_POINT ( 'NONE',  ( 9.070789158774999805, 5.349936549139000519, -7.138437102151999447 ) ) ;
#27271=CARTESIAN_POINT ( 'NONE',  ( 10.87521525736000072, 4.831064930369000088, 6.312796576761000367 ) ) ;
#27272=CARTESIAN_POINT ( 'NONE',  ( 11.04467482811000067, 2.754798779176999890, -5.185341710892000577 ) ) ;
#27273=CARTESIAN_POINT ( 'NONE',  ( 7.826132327310000747, 5.086383815897999483, 6.522343373212003748 ) ) ;
#27277=ADVANCED_FACE ( 'NONE', ( #45331 ), #8603, .F. ) ;
#27280=CARTESIAN_POINT ( 'NONE',  ( 8.470295280410999439, 4.255646040929000229, 9.114085578076998928 ) ) ;
#27290=CARTESIAN_POINT ( 'NONE',  ( 11.12453464744999998, 7.791996397176999878, 6.679342906043000738 ) ) ;
#27293=EDGE_LOOP ( 'NONE', ( #17492, #42960, #822 ) ) ;
#27300=CARTESIAN_POINT ( 'NONE',  ( 8.111573341229000533, 3.326263523254000098, 8.794511546544999447 ) ) ;
#27306=EDGE_CURVE ( 'NONE', #27904, #57225, #3010, .T. ) ;
#27307=CARTESIAN_POINT ( 'NONE',  ( 10.38726084123000071, 2.888676266723000374, -6.716337836090000124 ) ) ;
#27309=CARTESIAN_POINT ( 'NONE',  ( 7.903774407030003779, 5.139635483293002238, 6.776036904885998524 ) ) ;
#27311=CARTESIAN_POINT ( 'NONE',  ( 10.98768472638000127, 7.408460564924999936, -6.159405844198999169 ) ) ;
#27312=ORIENTED_EDGE ( 'NONE', *, *, #1431, .T. ) ;
#27315=DIRECTION ( 'NONE',  ( 0.5298945044129969029, -0.5996714842328959572, 0.5996715144066958603 ) ) ;
#27319=LINE ( 'NONE', #48645, #26376 ) ;
#27320=DIRECTION ( 'NONE',  ( -1.000000000000000000, -1.776356839465000168E-14, 0.000000000000000000 ) ) ;
#27329=CARTESIAN_POINT ( 'NONE',  ( 8.615570209625364129, 4.906878460622427163, 6.021351945580431853 ) ) ;
#27330=AXIS2_PLACEMENT_3D ( 'NONE', #52609, #11329, #10303 ) ;
#27337=DIRECTION ( 'NONE',  ( 0.000000000000000000, -1.000000000000000000, 0.000000000000000000 ) ) ;
#27340=EDGE_LOOP ( 'NONE', ( #29005, #42833, #52709, #67981 ) ) ;
#27341=CARTESIAN_POINT ( 'NONE',  ( 7.387702836194001144, 2.764883607873137361, 8.723309566181695729 ) ) ;
#27343=ORIENTED_EDGE ( 'NONE', *, *, #13506, .F. ) ;
#27346=ORIENTED_EDGE ( 'NONE', *, *, #55359, .F. ) ;
#27349=DIRECTION ( 'NONE',  ( 0.8660254003319995952, -4.365146055948999335E-12, -0.5000000059797998775 ) ) ;
#27358=CARTESIAN_POINT ( 'NONE',  ( 8.532195280408998883, 5.331510020787000315, -8.114341808290998159 ) ) ;
#27360=CARTESIAN_POINT ( 'NONE',  ( 7.100000000000000533, 4.000000000000000000, -7.500000000000000000 ) ) ;
#27361=FILL_AREA_STYLE ('',( #31925 ) ) ;
#27363=CARTESIAN_POINT ( 'NONE',  ( 9.112942518363999156, 5.100000000000000533, 6.192000867487999827 ) ) ;
#27372=CARTESIAN_POINT ( 'NONE',  ( 7.249090560818999940, 3.037137096735000430, -6.379793420563999895 ) ) ;
#27376=CARTESIAN_POINT ( 'NONE',  ( 8.748814158775001459, 5.251032986819000214, -6.070151079272999795 ) ) ;
#27381=CARTESIAN_POINT ( 'NONE',  ( 3.186390132544124842, -0.4581489286485234680, 3.499999999999998668 ) ) ;
#27386=EDGE_CURVE ( 'NONE', #51068, #12021, #205, .T. ) ;
#27391=CARTESIAN_POINT ( 'NONE',  ( 8.447041273813589157, 5.099348809280254358, -6.546252130241257738 ) ) ;
#27397=DIRECTION ( 'NONE',  ( -0.7071060865236062920, 0.7071074758488062884, 8.142048014830070602E-10 ) ) ;
#27423=VERTEX_POINT ( 'NONE', #50911 ) ;
#27435=CARTESIAN_POINT ( 'NONE',  ( 8.359535841228000308, 5.897697057214000615, -7.408103789850999377 ) ) ;
#27437=CARTESIAN_POINT ( 'NONE',  ( 9.511909210317325503, 4.618071422035288087, 8.703327943634770136 ) ) ;
#27445=ORIENTED_EDGE ( 'NONE', *, *, #28685, .F. ) ;
#27452=CARTESIAN_POINT ( 'NONE',  ( 6.950034089120999958, 13.87069231928999891, -4.225386915259999654 ) ) ;
#27456=CARTESIAN_POINT ( 'NONE',  ( 10.00190165877000048, 2.729646201450000031, -8.843033333815998986 ) ) ;
#27477=AXIS2_PLACEMENT_3D ( 'NONE', #40524, #62866, #56951 ) ;
#27484=VERTEX_POINT ( 'NONE', #63793 ) ;
#27493=CARTESIAN_POINT ( 'NONE',  ( 11.03092334123000029, 5.020455242919999783, -6.601201971309999195 ) ) ;
#27496=CARTESIAN_POINT ( 'NONE',  ( 6.949466529116000046, 12.16404197558000000, -3.090625629547000042 ) ) ;
#27499=CARTESIAN_POINT ( 'NONE',  ( 7.037114158771000660, 4.623631324973000112, 8.651459902566999816 ) ) ;
#27500=ORIENTED_EDGE ( 'NONE', *, *, #20689, .T. ) ;
#27502=CARTESIAN_POINT ( 'NONE',  ( 8.195595280407001582, 2.759821810153000321, -8.454514188070000102 ) ) ;
#27512=VECTOR ( 'NONE', #15983, 1000.000000000000000 ) ;
#27521=CARTESIAN_POINT ( 'NONE',  ( 7.127704719590999716, 4.698356649019999942, 8.789431186081998248 ) ) ;
#27527=CARTESIAN_POINT ( 'NONE',  ( 11.02029022880999953, 6.435658501792000052, -5.283992956780000583 ) ) ;
#27528=ORIENTED_EDGE ( 'NONE', *, *, #17294, .F. ) ;
#27530=CARTESIAN_POINT ( 'NONE',  ( 0.4398691794437870617, -0.9011714948220468369, -3.349986680846007037 ) ) ;
#27531=DIRECTION ( 'NONE',  ( 0.000000000000000000, 1.000000000000000000, 0.000000000000000000 ) ) ;
#27543=CARTESIAN_POINT ( 'NONE',  ( 9.842764158772000727, 5.798263352390999437, -8.113145944980999502 ) ) ;
#27544=CARTESIAN_POINT ( 'NONE',  ( 10.39355883036999906, 4.089958667033000594, -9.188186800857998549 ) ) ;
#27548=CARTESIAN_POINT ( 'NONE',  ( 10.25461802485000007, 2.860644035673999941, 6.604613005744999654 ) ) ;
#27550=LINE ( 'NONE', #17047, #16824 ) ;
#27551=CARTESIAN_POINT ( 'NONE',  ( 11.14698693981000055, 5.129806801114000336, 5.886034047559999927 ) ) ;
#27552=CARTESIAN_POINT ( 'NONE',  ( 10.42819717210663555, 5.125396288445606352, 6.749639981115941545 ) ) ;
#27558=CARTESIAN_POINT ( 'NONE',  ( 10.48845679253054897, 2.446973213462996455, 6.696139198371997558 ) ) ;
#27571=AXIS2_PLACEMENT_3D ( 'NONE', #20775, #9939, #10973 ) ;
#27573=CARTESIAN_POINT ( 'NONE',  ( 9.341490007895000502, 4.148133901461999784, 9.337478696773001019 ) ) ;
#27575=CARTESIAN_POINT ( 'NONE',  ( 9.310554719594000161, 3.934138271021000222, -9.063586117809000697 ) ) ;
#27577=CARTESIAN_POINT ( 'NONE',  ( 10.93769855012999948, 2.936883479403999964, 4.920828759365000415 ) ) ;
#27579=CARTESIAN_POINT ( 'NONE',  ( 10.62793268324000096, 3.100586971929999880, 8.599896650316999569 ) ) ;
#27584=CARTESIAN_POINT ( 'NONE',  ( 8.266390833065004884, 2.877128322603998534, 6.332041950470006064 ) ) ;
#27585=EDGE_LOOP ( 'NONE', ( #34425, #41386, #22446, #47920 ) ) ;
#27586=CARTESIAN_POINT ( 'NONE',  ( 11.09999999999999964, 5.299999999999999822, 5.160242730440000258 ) ) ;
#27598=CARTESIAN_POINT ( 'NONE',  ( 9.061929719594999710, 4.092867382745001059, -5.937785237406000505 ) ) ;
#27601=ORIENTED_EDGE ( 'NONE', *, *, #60188, .F. ) ;
#27603=CARTESIAN_POINT ( 'NONE',  ( 8.002383708823000319, 5.117451078405999887, -6.702236199791999915 ) ) ;
#27606=EDGE_LOOP ( 'NONE', ( #22482, #54203, #39732, #10794 ) ) ;
#27612=CARTESIAN_POINT ( 'NONE',  ( 9.882259685352000389, 4.932708901218999742, 6.390989635557000170 ) ) ;
#27613=CARTESIAN_POINT ( 'NONE',  ( 10.99480479316000014, 3.850613903518000036, -9.347963496621000345 ) ) ;
#27614=CARTESIAN_POINT ( 'NONE',  ( 7.712330476186004979, 4.866816057961001363, 6.392636141994996635 ) ) ;
#27621=CARTESIAN_POINT ( 'NONE',  ( 8.571413182547999554, 4.599999999999999645, 5.927302706106000407 ) ) ;
#27626=CARTESIAN_POINT ( 'NONE',  ( 8.496698341230001006, 5.198556077301000222, 8.332552905512999430 ) ) ;
#27627=ORIENTED_EDGE ( 'NONE', *, *, #12013, .T. ) ;
#27631=CARTESIAN_POINT ( 'NONE',  ( 7.116206910042869538, 3.734875113800864455, 8.831328650134384617 ) ) ;
#27635=CARTESIAN_POINT ( 'NONE',  ( 10.85467514323000060, 9.827446706043000191, 5.589517099280000068 ) ) ;
#27639=ORIENTED_EDGE ( 'NONE', *, *, #31710, .T. ) ;
#27648=CARTESIAN_POINT ( 'NONE',  ( 8.277732780410000046, 4.874567052833000069, 6.119507471270999588 ) ) ;
#27649=CARTESIAN_POINT ( 'NONE',  ( 9.815201913989998417, 2.813632032385000148, 8.848857341496000117 ) ) ;
#27652=CARTESIAN_POINT ( 'NONE',  ( 7.662260841227999997, 2.688365364125000045, 8.140015608605001063 ) ) ;
#27657=CARTESIAN_POINT ( 'NONE',  ( 9.660528907822998335, 2.899999999999999911, -6.152188490330000370 ) ) ;
#27661=AXIS2_PLACEMENT_3D ( 'NONE', #1709, #54152, #65675 ) ;
#27673=ORIENTED_EDGE ( 'NONE', *, *, #28344, .T. ) ;
#27677=CARTESIAN_POINT ( 'NONE',  ( 8.457129882803000598, 5.100036551512999949, -6.571411952062999440 ) ) ;
#27678=CARTESIAN_POINT ( 'NONE',  ( 1.371338831777000111, -1.438367618452000007, -3.472675606904999768 ) ) ;
#27694=ORIENTED_EDGE ( 'NONE', *, *, #14239, .T. ) ;
#27697=VERTEX_POINT ( 'NONE', #42144 ) ;
#27703=DIRECTION ( 'NONE',  ( 0.000000000000000000, -0.8304044637637929549, -0.5571610418551961041 ) ) ;
#27707=ORIENTED_EDGE ( 'NONE', *, *, #48490, .T. ) ;
#27710=CARTESIAN_POINT ( 'NONE',  ( 8.581920280410001212, 4.769017407621999993, -8.862909124839001507 ) ) ;
#27715=ORIENTED_EDGE ( 'NONE', *, *, #54531, .T. ) ;
#27726=CARTESIAN_POINT ( 'NONE',  ( 7.547271682458000619, 5.017953588770000195, -6.429833855306000601 ) ) ;
#27728=EDGE_CURVE ( 'NONE', #17232, #16376, #64450, .T. ) ;
#27730=CIRCLE ( 'NONE', #14308, 12.50000000000000000 ) ;
#27732=B_SPLINE_CURVE_WITH_KNOTS ( 'NONE', 3,
 ( #12789, #50532, #29220, #65567, #17690, #13140, #11734, #45295, #44616, #49842, #22918, #23612, #18038, #44270, #33424, #61023, #2634, #39015 ),
 .UNSPECIFIED., .F., .F.,
 ( 4, 2, 2, 2, 2, 2, 2, 2, 4 ),
 ( 0.000000000000000000, 0.1250000000000000000, 0.2500000000000000000, 0.3750000000000000000, 0.5000000000000000000, 0.6250000000000000000, 0.7500000000000000000, 0.8750000000000000000, 1.000000000000000000 ),
 .UNSPECIFIED. ) ;
#27733=CARTESIAN_POINT ( 'NONE',  ( 9.237204719595000668, 3.071719032003000116, -6.037263251225000182 ) ) ;
#27736=ORIENTED_EDGE ( 'NONE', *, *, #67014, .F. ) ;
#27737=DIRECTION ( 'NONE',  ( 0.000000000000000000, 1.000000000000000000, 0.000000000000000000 ) ) ;
#27741=CARTESIAN_POINT ( 'NONE',  ( 11.00000000000000000, 2.799999999999999822, -5.865766984179000332 ) ) ;
#27742=CARTESIAN_POINT ( 'NONE',  ( 1.011390132542624665, 3.499999999999998224, 0.4581489286485194157 ) ) ;
#27749=VERTEX_POINT ( 'NONE', #23829 ) ;
#27756=CARTESIAN_POINT ( 'NONE',  ( 8.573148997459998810, 5.167567567567999731, -6.822293592207000934 ) ) ;
#27767=DIRECTION ( 'NONE',  ( 1.000000000000000000, 0.000000000000000000, 0.000000000000000000 ) ) ;
#27769=FACE_OUTER_BOUND ( 'NONE', #61966, .T. ) ;
#27770=CARTESIAN_POINT ( 'NONE',  ( 1.050973465875000068, 3.500000000000000000, 0.000000000000000000 ) ) ;
#27777=CARTESIAN_POINT ( 'NONE',  ( 7.000000000000001776, 9.718048825484419950, 4.627116016484593253 ) ) ;
#27779=ORIENTED_EDGE ( 'NONE', *, *, #5306, .F. ) ;
#27784=DIRECTION ( 'NONE',  ( 0.000000000000000000, 0.7071067811865474617, -0.7071067811865474617 ) ) ;
#27785=CARTESIAN_POINT ( 'NONE',  ( 9.219964158774999419, 3.941185585667000169, -8.896279800194999865 ) ) ;
#27789=CARTESIAN_POINT ( 'NONE',  ( 7.373895280404999752, 4.512523768570999572, -9.154878768564000069 ) ) ;
#27800=CYLINDRICAL_SURFACE ( 'NONE', #12468, 1.999999999999999778 ) ;
#27802=ORIENTED_EDGE ( 'NONE', *, *, #59093, .T. ) ;
#27813=CARTESIAN_POINT ( 'NONE',  ( 10.43325471958999984, 5.596203146559000530, -8.042024377770999877 ) ) ;
#27815=CARTESIAN_POINT ( 'NONE',  ( 9.679055905794999859, 2.899999999999999911, 6.571291218949999902 ) ) ;
#27825=CARTESIAN_POINT ( 'NONE',  ( 10.27967883605999866, 5.739712809045000697, 7.774963411801000923 ) ) ;
#27830=CARTESIAN_POINT ( 'NONE',  ( 8.766851002546001581, 2.832432432432000269, 6.822293592207000934 ) ) ;
#27839=CARTESIAN_POINT ( 'NONE',  ( 8.473304831784332691, 5.100000000000000533, 6.564173320837334735 ) ) ;
#27844=CARTESIAN_POINT ( 'NONE',  ( 8.514954719592999766, 3.207599814920999659, -6.150466394809999571 ) ) ;
#27846=CARTESIAN_POINT ( 'NONE',  ( 0.7984915348666999924, -3.532786812989999969, -1.105428934477000080 ) ) ;
#27848=CARTESIAN_POINT ( 'NONE',  ( 10.84161084123000052, 2.641275823976000137, -7.444905437480000110 ) ) ;
#27852=DIRECTION ( 'NONE',  ( -1.000000000000000000, 0.000000000000000000, 0.000000000000000000 ) ) ;
#27855=CARTESIAN_POINT ( 'NONE',  ( 8.411454719592999396, 3.882020551409000042, 5.870058896428999695 ) ) ;
#27856=ORIENTED_EDGE ( 'NONE', *, *, #57307, .F. ) ;
#27858=CARTESIAN_POINT ( 'NONE',  ( 7.549170280409000178, 5.250007070404999254, -8.441605882928000071 ) ) ;
#27860=CARTESIAN_POINT ( 'NONE',  ( 10.87835931249066768, 5.126777126180478206, 6.752018918863570640 ) ) ;
#27865=ORIENTED_EDGE ( 'NONE', *, *, #24786, .T. ) ;
#27866=DIRECTION ( 'NONE',  ( 0.000000000000000000, 1.000000000000000000, 0.000000000000000000 ) ) ;
#27869=ORIENTED_EDGE ( 'NONE', *, *, #44142, .F. ) ;
#27876=CARTESIAN_POINT ( 'NONE',  ( 7.807364158771999740, 3.650414032626000171, 6.083147621602999600 ) ) ;
#27882=ORIENTED_EDGE ( 'NONE', *, *, #53434, .T. ) ;
#27886=CARTESIAN_POINT ( 'NONE',  ( 5.000030787343002103, 1.290525307673966449, 1.679270695423617399 ) ) ;
#27894=ORIENTED_EDGE ( 'NONE', *, *, #20937, .T. ) ;
#27897=CARTESIAN_POINT ( 'NONE',  ( 9.286929719595001131, 4.102804347295999854, -5.770625657082999460 ) ) ;
#27898=CARTESIAN_POINT ( 'NONE',  ( 10.19715290653000217, 4.982626294267999967, -6.124313696433000054 ) ) ;
#27902=CARTESIAN_POINT ( 'NONE',  ( 9.610944094206999466, 5.100000000000000533, -6.571291218949999902 ) ) ;
#27904=VERTEX_POINT ( 'NONE', #67157 ) ;
#27906=CARTESIAN_POINT ( 'NONE',  ( 9.504903297738000134, 3.934733353759999552, 5.704831249548000471 ) ) ;
#27907=CARTESIAN_POINT ( 'NONE',  ( 2.134306799209333416, 1.762666431298139713, 3.058252359239908458 ) ) ;
#27911=CARTESIAN_POINT ( 'NONE',  ( 10.40686970472170536, 2.482357117332503194, 8.418222078226063942 ) ) ;
#27917=CARTESIAN_POINT ( 'NONE',  ( 8.672510841228998402, 4.686731264770999772, -8.717075579553000608 ) ) ;
#27924=CARTESIAN_POINT ( 'NONE',  ( 8.913573341230998537, 2.550580605805000012, 8.854682662413999594 ) ) ;
#27925=CARTESIAN_POINT ( 'NONE',  ( 9.161379719595000637, 5.511689883260999956, -7.095113581311000672 ) ) ;
#27927=CARTESIAN_POINT ( 'NONE',  ( 10.74549836952449944, 3.055340480832492656, 4.827072375377776225 ) ) ;
#27931=CARTESIAN_POINT ( 'NONE',  ( 10.02201554968999986, 3.298015135926000152, 5.700522662207000657 ) ) ;
#27936=ORIENTED_EDGE ( 'NONE', *, *, #69052, .T. ) ;
#27940=AXIS2_PLACEMENT_3D ( 'NONE', #65937, #6522, #38692 ) ;
#27944=ORIENTED_EDGE ( 'NONE', *, *, #8194, .F. ) ;
#27947=CARTESIAN_POINT ( 'NONE',  ( 7.654876518126000562, 2.928962009306002479, 6.518628166992000317 ) ) ;
#27950=CARTESIAN_POINT ( 'NONE',  ( 9.717214158771000143, 3.990126737362999609, -8.809457313313998839 ) ) ;
#27955=VERTEX_POINT ( 'NONE', #48596 ) ;
#27956=CARTESIAN_POINT ( 'NONE',  ( 9.085607419977296928, 5.315139263812436177, -7.853694237287989210 ) ) ;
#27962=ORIENTED_EDGE ( 'NONE', *, *, #55487, .F. ) ;
#27966=CARTESIAN_POINT ( 'NONE',  ( 10.79839886931999970, 5.269366011605000288, -6.148705891248999578 ) ) ;
#27968=LINE ( 'NONE', #43359, #38606 ) ;
#27969=DIRECTION ( 'NONE',  ( -1.000000000000000000, 0.000000000000000000, 0.000000000000000000 ) ) ;
#27973=CARTESIAN_POINT ( 'NONE',  ( 9.406704719590001318, 3.705846972803000128, 9.096435887808000942 ) ) ;
#27977=FACE_OUTER_BOUND ( 'NONE', #27585, .T. ) ;
#27980=VECTOR ( 'NONE', #54933, 999.9999999999998863 ) ;
#27983=CARTESIAN_POINT ( 'NONE',  ( 10.58844943056000076, 3.754657019866000311, 5.545350295858999523 ) ) ;
#27986=EDGE_LOOP ( 'NONE', ( #50222, #57977, #13593, #655 ) ) ;
#27989=CARTESIAN_POINT ( 'NONE',  ( 11.09999999999999964, 2.700000000000000178, 5.160242713806000303 ) ) ;
#27993=B_SPLINE_SURFACE_WITH_KNOTS ( 'NONE', 3, 3, ( 
 ( #40597, #66471, #3868, #30128, #50404, #25202, #34681, #2504, #23828, #66127, #18247, #14037, #55995, #56685, #3528, #66822, #9120, #39569, #45166, #18935, #8784, #18595, #8099, #39921, #61240, #51092, #13355, #29443, #50749, #2846, #24174, #40259, #61579, #51431, #24863 ),
 ( #13695, #56339, #29790, #67502, #19619, #3195, #40941, #62262, #14383, #10494, #14720, #41974, #4902, #26243, #52110, #37076, #47571, #42659, #63967, #52809, #10839, #68876, #68184, #53150, #20993, #30797, #42329, #4213, #15748, #25551, #36035, #67843, #57351, #26590, #31834 ),
 ( #63631, #20302, #31485, #46876, #46537, #20648, #58387, #19965, #47223, #41628, #5586, #8, #5252, #47911, #21330, #62934, #16080, #37412, #63279, #36381, #58733, #41288, #62596, #15058, #32181, #53496, #9455, #15409, #57697, #9807, #31156, #68526, #52458, #36735, #58054 ),
 ( #4553, #25894, #10157, #16762, #49276, #33553, #27613, #17823, #12572, #59080, #48941, #27966, #60464, #38093, #33902, #11181, #11868, #65700, #55219, #26930, #32861, #39137, #48244, #37754, #1387, #54873, #6975, #22703, #38796, #59419, #53833, #697, #28303, #48595, #17471 ) ),
 .UNSPECIFIED., .F., .F., .F.,
 ( 4, 4 ),
 ( 4, 1, 1, 1, 1, 1, 1, 1, 1, 1, 1, 1, 1, 1, 1, 1, 1, 1, 1, 1, 1, 1, 1, 1, 1, 1, 1, 1, 1, 1, 1, 1, 4 ),
 ( -0.1039370721279000015, 1.103937072127999963 ),
 ( 0.1942321073450000157, 0.2199060843169000079, 0.2455800612886999967, 0.2712540382605999612, 0.2969280152323999777, 0.3226019922043000254, 0.3482759691761000420, 0.3739499461479999787, 0.3996239231197999953, 0.4252979000916999874, 0.4509718770635000040, 0.4766458540353999962, 0.5023198310072000128, 0.5279938079791000050, 0.5536677849509000771, 0.5793417619227999582, 0.6050157388945999193, 0.6306897158665000225, 0.6563636928382999836, 0.6820376698101999757, 0.7077116467820000478, 0.7333856237539000400, 0.7590596007256998901, 0.7847335776975999933, 0.8104075546693999543, 0.8360815316413000575, 0.8617555086131000186, 0.8874294855850000108, 0.9131034625568000829, 0.9387774395286999640, 0.9644514165004999251, 0.9901253934722999972, 1.015799370444000038 ),
 .UNSPECIFIED. ) ;
#27996=CARTESIAN_POINT ( 'NONE',  ( 8.919607780412000864, 5.165497731316000873, 8.645531386060000045 ) ) ;
#27997=CARTESIAN_POINT ( 'NONE',  ( 10.40227026081000083, 2.765684886876999649, 9.035354958280999327 ) ) ;
#27999=VERTEX_POINT ( 'NONE', #41975 ) ;
#28003=CARTESIAN_POINT ( 'NONE',  ( 8.076862807906000086, 5.120521186033995420, 6.727223554611003742 ) ) ;
#28008=CARTESIAN_POINT ( 'NONE',  ( 0.9192448634807000030, 3.532364098973999944, -0.6521526059094999717 ) ) ;
#28010=DIRECTION ( 'NONE',  ( 0.000000000000000000, 1.000000000000000000, 0.000000000000000000 ) ) ;
#28013=ADVANCED_FACE ( 'NONE', ( #11518 ), #1721, .F. ) ;
#28019=ORIENTED_EDGE ( 'NONE', *, *, #21432, .T. ) ;
#28021=CARTESIAN_POINT ( 'NONE',  ( 7.000000000000000000, 8.307879248642999315, -4.307879248643000203 ) ) ;
#28025=CARTESIAN_POINT ( 'NONE',  ( 1.180611034013999916, -1.296472565164999979, 3.528106597684999901 ) ) ;
#28026=CARTESIAN_POINT ( 'NONE',  ( 1.823890132539666586, -2.150913519912200478, -2.798833948393631754 ) ) ;
#28029=CARTESIAN_POINT ( 'NONE',  ( 9.792569055495000896, 3.463432304708999876, 6.184396499233999478 ) ) ;
#28031=CARTESIAN_POINT ( 'NONE',  ( 8.906851002547000462, 2.832432432432000269, -6.822293592207000934 ) ) ;
#28047=DIRECTION ( 'NONE',  ( 0.000000000000000000, 0.9565994702956990281, -0.2914059941558995726 ) ) ;
#28053=ORIENTED_EDGE ( 'NONE', *, *, #26635, .T. ) ;
#28055=VERTEX_POINT ( 'NONE', #55915 ) ;
#28056=CARTESIAN_POINT ( 'NONE',  ( 10.83581759994134863, 2.987285522957833894, -4.871130536556726121 ) ) ;
#28058=EDGE_CURVE ( 'NONE', #19641, #16280, #35986, .T. ) ;
#28066=ORIENTED_EDGE ( 'NONE', *, *, #32798, .T. ) ;
#28071=CARTESIAN_POINT ( 'NONE',  ( 10.12339528040999959, 3.988943694240999704, -8.966360307350999648 ) ) ;
#28079=FACE_OUTER_BOUND ( 'NONE', #25506, .T. ) ;
#28097=EDGE_CURVE ( 'NONE', #67407, #55115, #16782, .T. ) ;
#28107=CARTESIAN_POINT ( 'NONE',  ( 10.62947109217999930, 5.100000000000000533, 6.152188490330000370 ) ) ;
#28111=CARTESIAN_POINT ( 'NONE',  ( 8.191498566858999908, 3.399962487441000381, 6.146646668338000552 ) ) ;
#28112=CARTESIAN_POINT ( 'NONE',  ( 2.266329616852750473, -3.450786940248410151, -0.6753594422426504318 ) ) ;
#28115=CARTESIAN_POINT ( 'NONE',  ( 8.099999999999999645, 0.000000000000000000, 0.000000000000000000 ) ) ;
#28117=ORIENTED_EDGE ( 'NONE', *, *, #29901, .F. ) ;
#28120=ORIENTED_EDGE ( 'NONE', *, *, #39785, .T. ) ;
#28122=CARTESIAN_POINT ( 'NONE',  ( 11.09999999999999964, 6.593648130222000248, -5.598803514566000672 ) ) ;
#28123=CARTESIAN_POINT ( 'NONE',  ( 9.410004719593999312, 2.495531372253999791, -7.930944806125000746 ) ) ;
#28132=DIRECTION ( 'NONE',  ( 0.8660254037844288266, 0.000000000000000000, 0.5000000000000169864 ) ) ;
#28135=CARTESIAN_POINT ( 'NONE',  ( 9.780284676292000157, 3.021596928575999819, -8.450035627617001666 ) ) ;
#28149=CARTESIAN_POINT ( 'NONE',  ( 10.39539221959000059, 5.667182949051000840, -7.250689098107000241 ) ) ;
#28156=VERTEX_POINT ( 'NONE', #32437 ) ;
#28157=ORIENTED_EDGE ( 'NONE', *, *, #26269, .F. ) ;
#28158=CARTESIAN_POINT ( 'NONE',  ( 9.833904719592002408, 5.048004622677000341, -6.120508709481000231 ) ) ;
#28166=CARTESIAN_POINT ( 'NONE',  ( 8.620740978634000129, 4.599999999999999645, 5.898823289756999877 ) ) ;
#28170=CARTESIAN_POINT ( 'NONE',  ( 8.742477372938900260, 2.899999999999999467, -6.356265660156537045 ) ) ;
#28176=CARTESIAN_POINT ( 'NONE',  ( 10.88314899746000108, 5.167567567567999731, 6.822293592207000934 ) ) ;
#28178=CARTESIAN_POINT ( 'NONE',  ( 8.614404719593999005, 5.030502105212999453, -6.322203460290999999 ) ) ;
#28180=CARTESIAN_POINT ( 'NONE',  ( 8.568197172116430949, 5.125396288428779812, -6.749639981086953178 ) ) ;
#28182=CIRCLE ( 'NONE', #15891, 12.50000000000000000 ) ;
#28183=CARTESIAN_POINT ( 'NONE',  ( 0.4611081069563000012, 3.330914467393999878, 1.191613524625000142 ) ) ;
#28184=CARTESIAN_POINT ( 'NONE',  ( 9.520528907821001141, 2.899999999999999911, 6.152188490330000370 ) ) ;
#28186=CARTESIAN_POINT ( 'NONE',  ( 3.410659130938999972, 0.3807847720749999998, -3.739296779731999809 ) ) ;
#28191=CARTESIAN_POINT ( 'NONE',  ( 7.256079719589999755, 2.531201476950000195, 8.216704145297999418 ) ) ;
#28194=CARTESIAN_POINT ( 'NONE',  ( 10.91281150458596727, 9.717878385093197124, 5.838659047851286310 ) ) ;
#28203=EDGE_CURVE ( 'NONE', #23594, #34256, #54307, .T. ) ;
#28207=VERTEX_POINT ( 'NONE', #25805 ) ;
#28209=CARTESIAN_POINT ( 'NONE',  ( 5.500000000000000000, 11.95749337870000062, -3.642574926948999980 ) ) ;
#28212=CARTESIAN_POINT ( 'NONE',  ( 0.4529763571839853786, 3.676114825633475335E-06, -3.452897576335808072 ) ) ;
#28214=DIRECTION ( 'NONE',  ( 0.7071060865235063719, 0.7071074758489063194, 8.142185728694072879E-10 ) ) ;
#28218=CONICAL_SURFACE ( 'NONE', #38230, 1.600003888856000200, 0.7854004771980920285 ) ;
#28221=FACE_OUTER_BOUND ( 'NONE', #29875, .T. ) ;
#28223=CARTESIAN_POINT ( 'NONE',  ( 11.09999999999999964, 4.000000000000000000, -7.500000000000000000 ) ) ;
#28224=CARTESIAN_POINT ( 'NONE',  ( 5.000030787343000327, 2.099962892531006098, 0.2748844998327708011 ) ) ;
#28232=AXIS2_PLACEMENT_3D ( 'NONE', #48151, #32423, #22262 ) ;
#28234=CARTESIAN_POINT ( 'NONE',  ( 9.146614158775999925, 2.981992329588000423, -5.895876591910999664 ) ) ;
#28235=CARTESIAN_POINT ( 'NONE',  ( 3.488436892060000183, -3.068566966923000017, 0.5458777553189999576 ) ) ;
#28241=CARTESIAN_POINT ( 'NONE',  ( 1.946856900172333704, 0.9112004763889643977, -3.396138185504796958 ) ) ;
#28243=CARTESIAN_POINT ( 'NONE',  ( 9.753142190738998352, 4.104977339646000090, 9.293283246364000050 ) ) ;
#28245=LINE ( 'NONE', #43987, #67772 ) ;
#28253=ORIENTED_EDGE ( 'NONE', *, *, #52979, .T. ) ;
#28256=ADVANCED_FACE ( 'NONE', ( #5167 ), #37671, .F. ) ;
#28261=ORIENTED_EDGE ( 'NONE', *, *, #20266, .F. ) ;
#28264=CARTESIAN_POINT ( 'NONE',  ( 7.667607780408999929, 5.638704226117999596, 8.266404648244000342 ) ) ;
#28265=CARTESIAN_POINT ( 'NONE',  ( 9.093935841232999806, 2.156584729807999867, -7.959751745006000689 ) ) ;
#28267=CARTESIAN_POINT ( 'NONE',  ( 11.02418915877000138, 2.407889430138999920, -8.439554272735000140 ) ) ;
#28269=CARTESIAN_POINT ( 'NONE',  ( 10.63461554336999981, 5.668731883089999535, 6.527253515312000154 ) ) ;
#28287=EDGE_CURVE ( 'NONE', #16917, #33506, #61870, .T. ) ;
#28288=CARTESIAN_POINT ( 'NONE',  ( 8.266390833065004884, 2.877128322603998534, 6.332041950470006064 ) ) ;
#28290=CARTESIAN_POINT ( 'NONE',  ( 9.450870280412999591, 2.928319778732999978, -8.861178115809998701 ) ) ;
#28295=CARTESIAN_POINT ( 'NONE',  ( 27.64127793187000037, 5.599999999999999645, -6.571291218949999902 ) ) ;
#28299=EDGE_LOOP ( 'NONE', ( #23127, #20913, #27639, #51666, #60386 ) ) ;
#28303=CARTESIAN_POINT ( 'NONE',  ( 9.973493989215999278, 4.344963986309999804, -9.321593970653999861 ) ) ;
#28306=CARTESIAN_POINT ( 'NONE',  ( 8.957462135714999718, 5.100000000000000533, -6.571291218949999902 ) ) ;
#28310=CARTESIAN_POINT ( 'NONE',  ( 7.647239158771000689, 5.850290547079999293, 6.784176679236000318 ) ) ;
#28316=DIRECTION ( 'NONE',  ( 1.000000000000000000, 0.000000000000000000, 0.000000000000000000 ) ) ;
#28318=CARTESIAN_POINT ( 'NONE',  ( 10.29094007826000023, 2.903522982536999919, -8.310916170934000036 ) ) ;
#28320=EDGE_CURVE ( 'NONE', #46445, #28965, #47830, .T. ) ;
#28323=CARTESIAN_POINT ( 'NONE',  ( 10.27815081430999911, 5.521603098753999461, 8.751228458888000716 ) ) ;
#28325=DIRECTION ( 'NONE',  ( 0.000000000000000000, -1.000000000000000000, 0.000000000000000000 ) ) ;
#28337=CARTESIAN_POINT ( 'NONE',  ( 8.881823341230997926, 4.977909614887999545, 6.416776202806000029 ) ) ;
#28338=CARTESIAN_POINT ( 'NONE',  ( 10.58844943056000076, 3.754657019866000311, 5.545350295858999523 ) ) ;
#28341=CARTESIAN_POINT ( 'NONE',  ( 8.367589158771000513, 5.461114003844000031, -8.582501063019000398 ) ) ;
#28344=EDGE_CURVE ( 'NONE', #12675, #68596, #28182, .T. ) ;
#28346=CARTESIAN_POINT ( 'NONE',  ( 7.643735281411005111, 4.861037469149006363, 6.423817941563998879 ) ) ;
#28354=CARTESIAN_POINT ( 'NONE',  ( 1.782293291478000086, 2.470933839010999833, -2.372615558983000472 ) ) ;
#28360=CARTESIAN_POINT ( 'NONE',  ( 11.12921181303999951, 2.727588019252999985, 4.816967850745000668 ) ) ;
#28364=CARTESIAN_POINT ( 'NONE',  ( 6.933501042874380182, 3.037137096735000430, -6.379793420563999895 ) ) ;
#28368=CARTESIAN_POINT ( 'NONE',  ( 9.629471092178999214, 5.100000000000000533, 6.152188490330000370 ) ) ;
#28369=CARTESIAN_POINT ( 'NONE',  ( 0.6561095901646999407, -0.1662993809364999853, 3.755095982464999871 ) ) ;
#28372=EDGE_CURVE ( 'NONE', #51133, #40281, #43551, .T. ) ;
#28374=CARTESIAN_POINT ( 'NONE',  ( 10.57224177473000104, 4.020426023752999178, 8.920668579831000145 ) ) ;
#28382=CARTESIAN_POINT ( 'NONE',  ( 9.690635841230999858, 2.927176851028000293, -5.932007155957999878 ) ) ;
#28392=CARTESIAN_POINT ( 'NONE',  ( 10.21609109105999913, 5.961715741921000067, 7.319666990313999477 ) ) ;
#28395=FACE_OUTER_BOUND ( 'NONE', #54869, .T. ) ;
#28398=CARTESIAN_POINT ( 'NONE',  ( 3.050973465878000113, 3.500000000000000000, 0.000000000000000000 ) ) ;
#28399=DIRECTION ( 'NONE',  ( 0.000000000000000000, 0.8648648648648717963, -0.5020047465136829867 ) ) ;
#28410=B_SPLINE_SURFACE_WITH_KNOTS ( 'NONE', 3, 3, ( 
 ( #44114, #54232, #29075, #33618, #7382, #65412, #28029, #54937, #28723, #60525, #50385, #2484, #17884, #16826, #38150, #22766, #60184, #44804, #59476, #11576, #28374, #1797, #23115, #39550, #12634, #11932, #33964, #32919, #6331, #43760, #65054, #40922, #34661, #39902, #9437 ),
 ( #35687, #55974, #2824, #67137, #35004, #62581, #8424, #3176, #46519, #61559, #29767, #46173, #30110, #30779, #52091, #14017, #57001, #57335, #62245, #9103, #51413, #61221, #13337, #51072, #40241, #41267, #67822, #19248, #3508, #45826, #8081, #19603, #24505, #14702, #8768 ),
 ( #40576, #25184, #23810, #45143, #56662, #61903, #56319, #30441, #35346, #66804, #29422, #19946, #67481, #50731, #24155, #13675, #51752, #45489, #36020, #24846, #14363, #18916, #3846, #66453, #18575, #49721, #43589, #37056, #60005, #49168, #36717, #47553, #42311, #15389, #43937 ),
 ( #6515, #9787, #68855, #68507, #15039, #36365, #1280, #65241, #22594, #63613, #31469, #57678, #25871, #58371, #17358, #33098, #5233, #10137, #20630, #26570, #58038, #38684, #26224, #41954, #38331, #41612, #20975, #4195, #68164, #15729, #10473, #31814, #12117, #33445, #53133 ) ),
 .UNSPECIFIED., .F., .F., .F.,
 ( 4, 4 ),
 ( 4, 1, 1, 1, 1, 1, 1, 1, 1, 1, 1, 1, 1, 1, 1, 1, 1, 1, 1, 1, 1, 1, 1, 1, 1, 1, 1, 1, 1, 1, 1, 1, 4 ),
 ( -0.1039370721279000015, 1.103937072127999963 ),
 ( -0.01735257130020999988, 0.01084535706264999969, 0.03904328542550000031, 0.06724121378835999641, 0.09543914215121999944, 0.1236370705141000004, 0.1518349988768999959, 0.1800329272397999947, 0.2082308556026999935, 0.2364287839655000167, 0.2646267123283999601, 0.2928246406912000110, 0.3210225690540999821, 0.3492204974169000331, 0.3774184257798000042, 0.4056163541427000307, 0.4338142825054999707, 0.4620122108683999973, 0.4902101392311999928, 0.5184080675940999638, 0.5466059959569999904, 0.5748039243197999859, 0.6030018526827000125, 0.6311997810455000080, 0.6593977094084000345, 0.6875956377712000300, 0.7157935661340999456, 0.7439914944969999722, 0.7721894228597999676, 0.8003873512226999942, 0.8285852795854999897, 0.8567832079484000163, 0.8849811363112999318 ),
 .UNSPECIFIED. ) ;
#28413=CARTESIAN_POINT ( 'NONE',  ( 7.852796759037660834, 2.886226026955057034, -6.701059260334753631 ) ) ;
#28423=CARTESIAN_POINT ( 'NONE',  ( 9.585279719593998493, 2.928319778732999978, -8.861178115809998701 ) ) ;
#28428=DIRECTION ( 'NONE',  ( -1.000000000000000000, 0.000000000000000000, 0.000000000000000000 ) ) ;
#28430=DIRECTION ( 'NONE',  ( 0.7071067811865475727, 0.7071067811865475727, 0.000000000000000000 ) ) ;
#28431=CARTESIAN_POINT ( 'NONE',  ( 1.073890132542374864, 2.150913519912194705, 2.798833948393636639 ) ) ;
#28436=AXIS2_PLACEMENT_3D ( 'NONE', #49430, #59922, #17634 ) ;
#28437=DIRECTION ( 'NONE',  ( 1.000000000000000000, 0.000000000000000000, 0.000000000000000000 ) ) ;
#28445=CARTESIAN_POINT ( 'NONE',  ( 5.399998535875000449, -12.99045401563999924, -1.690592933733000125 ) ) ;
#28446=B_SPLINE_CURVE_WITH_KNOTS ( 'NONE', 3,
 ( #34537, #45019, #55848, #9309 ),
 .UNSPECIFIED., .F., .F.,
 ( 4, 4 ),
 ( 0.000000000000000000, 1.000000000000000000 ),
 .UNSPECIFIED. ) ;
#28472=EDGE_LOOP ( 'NONE', ( #55126, #25127, #65926 ) ) ;
#28473=DIRECTION ( 'NONE',  ( 1.000000000000000000, 0.000000000000000000, 0.000000000000000000 ) ) ;
#28486=CARTESIAN_POINT ( 'NONE',  ( 10.73506130198999919, 5.202496273738000276, -8.441412224440000500 ) ) ;
#28490=AXIS2_PLACEMENT_3D ( 'NONE', #59520, #58146, #26338 ) ;
#28494=ADVANCED_FACE ( 'NONE', ( #49197 ), #967, .F. ) ;
#28495=EDGE_CURVE ( 'NONE', #24471, #49930, #52704, .T. ) ;
#28497=EDGE_CURVE ( 'NONE', #57662, #10646, #11839, .T. ) ;
#28498=EDGE_CURVE ( 'NONE', #46731, #53432, #25956, .T. ) ;
#28501=CARTESIAN_POINT ( 'NONE',  ( 9.440795537696265782, 5.100000000000000533, 6.662590550601107608 ) ) ;
#28502=CARTESIAN_POINT ( 'NONE',  ( 10.28180471959000108, 3.991526675591000384, -5.814300410279999554 ) ) ;
#28512=CARTESIAN_POINT ( 'NONE',  ( 8.988579719593998263, 4.902869380824999901, -8.978557145469999057 ) ) ;
#28517=CARTESIAN_POINT ( 'NONE',  ( 9.266851002542999538, 2.832432432432000269, 6.822293592207000934 ) ) ;
#28518=EDGE_CURVE ( 'NONE', #37419, #38028, #49359, .T. ) ;
#28524=CARTESIAN_POINT ( 'NONE',  ( 7.481658233226216481, 4.679574733145784649, -6.320553983555220690 ) ) ;
#28532=CARTESIAN_POINT ( 'NONE',  ( 9.601268341696789221, 5.349866766629849835, -7.263147672793892617 ) ) ;
#28533=CARTESIAN_POINT ( 'NONE',  ( 8.316054719590999511, 3.826300099041999747, -9.055335252254000267 ) ) ;
#28539=EDGE_CURVE ( 'NONE', #16690, #35994, #65202, .T. ) ;
#28540=CARTESIAN_POINT ( 'NONE',  ( 9.484111209357660499, 2.372201727752532019, 6.771817387162120561 ) ) ;
#28541=CARTESIAN_POINT ( 'NONE',  ( 2.924292960406999597, -3.109127409734000036, 1.438104787010000107 ) ) ;
#28547=CARTESIAN_POINT ( 'NONE',  ( 8.283079719592000956, 2.376526778640999815, 7.686980884243000745 ) ) ;
#28550=CARTESIAN_POINT ( 'NONE',  ( 10.94048155334786010, 9.309399651271464293, 6.237067107879298966 ) ) ;
#28556=ORIENTED_EDGE ( 'NONE', *, *, #25731, .F. ) ;
#28576=CARTESIAN_POINT ( 'NONE',  ( 7.391647165042849466, 5.483386455157001294, -8.617406009823950441 ) ) ;
#28583=ORIENTED_EDGE ( 'NONE', *, *, #48925, .F. ) ;
#28586=B_SPLINE_CURVE_WITH_KNOTS ( 'NONE', 3,
 ( #44551, #17621, #48389, #32324, #841 ),
 .UNSPECIFIED., .F., .F.,
 ( 4, 1, 4 ),
 ( 0.000000000000000000, 0.5000000000000000000, 1.000000000000000000 ),
 .UNSPECIFIED. ) ;
#28589=CARTESIAN_POINT ( 'NONE',  ( 9.933354719590999693, 5.639765292528999829, -8.059103558718000215 ) ) ;
#28590=CARTESIAN_POINT ( 'NONE',  ( 2.538319053239000311, -2.896360734409999971, -1.395582542787000113 ) ) ;
#28594=CARTESIAN_POINT ( 'NONE',  ( 9.568197172114434323, 5.125396288428782476, -6.749639981086958507 ) ) ;
#28596=VERTEX_POINT ( 'NONE', #31292 ) ;
#28599=CARTESIAN_POINT ( 'NONE',  ( 10.31667774810000004, 3.819530253758000260, 6.062195927068000145 ) ) ;
#28601=EDGE_CURVE ( 'NONE', #54370, #26667, #4695, .T. ) ;
#28603=CARTESIAN_POINT ( 'NONE',  ( 4.950033214355999966, 0.000000000000000000, 0.000000000000000000 ) ) ;
#28605=DIRECTION ( 'NONE',  ( 1.000000000000000000, 0.000000000000000000, 0.000000000000000000 ) ) ;
#28608=CARTESIAN_POINT ( 'NONE',  ( 8.107831681780405475, 5.065903857563916368, -6.531537680950162184 ) ) ;
#28609=CARTESIAN_POINT ( 'NONE',  ( 10.31153584123000044, 2.716831823259000078, -7.950163994344000784 ) ) ;
#28610=ORIENTED_EDGE ( 'NONE', *, *, #42525, .T. ) ;
#28618=CARTESIAN_POINT ( 'NONE',  ( 7.678989158771000412, 2.599243720295000060, 7.909344432242998657 ) ) ;
#28619=CONICAL_SURFACE ( 'NONE', #17485, 2.049966935984999683, 0.7853819979415218588 ) ;
#28622=CARTESIAN_POINT ( 'NONE',  ( 10.91060165877000188, 4.702351492776999820, -9.210043641106000933 ) ) ;
#28624=CARTESIAN_POINT ( 'NONE',  ( 10.05691520198999989, 2.453477278391000382, 6.657104391228999773 ) ) ;
#28631=CARTESIAN_POINT ( 'NONE',  ( 6.899999689904000810, -12.43893549496000084, 2.828936992187000232 ) ) ;
#28646=CARTESIAN_POINT ( 'NONE',  ( 9.500595280412998278, 2.334550724494000029, -7.977056617806000283 ) ) ;
#28652=CARTESIAN_POINT ( 'NONE',  ( 7.536393842410557653, 4.984327542422680501, 8.445161314658211182 ) ) ;
#28659=CARTESIAN_POINT ( 'NONE',  ( 10.16000000000000014, 4.496968146123999865, -8.755198255949000696 ) ) ;
#28668=CARTESIAN_POINT ( 'NONE',  ( 9.294718325437999695, 4.148133901461999784, 9.337478696773001019 ) ) ;
#28673=CARTESIAN_POINT ( 'NONE',  ( 8.099999999999999645, 0.000000000000000000, -11.84999999999999964 ) ) ;
#28676=CARTESIAN_POINT ( 'NONE',  ( 11.02029022880999953, 5.784022792365999699, 5.014076608209000696 ) ) ;
#28677=CARTESIAN_POINT ( 'NONE',  ( 10.96080777006000062, 2.054568739078000306, 7.810084630238000258 ) ) ;
#28685=EDGE_CURVE ( 'NONE', #55873, #3842, #46023, .T. ) ;
#28692=CARTESIAN_POINT ( 'NONE',  ( 7.828420280408998622, 5.524123123935000379, 6.910361319981999095 ) ) ;
#28693=CARTESIAN_POINT ( 'NONE',  ( 9.347254965556000883, 4.028327103212000715, 9.469449669541999626 ) ) ;
#28696=CARTESIAN_POINT ( 'NONE',  ( 9.535554719593998030, 3.927090956378999742, -9.230892435423001530 ) ) ;
#28703=VERTEX_POINT ( 'NONE', #17968 ) ;
#28704=CARTESIAN_POINT ( 'NONE',  ( 2.020703038683000052, -2.100427248507999778, 2.706108474410000131 ) ) ;
#28714=CARTESIAN_POINT ( 'NONE',  ( 10.98768472638000127, 7.408460564924999936, -6.159405844198999169 ) ) ;
#28717=AXIS2_PLACEMENT_3D ( 'NONE', #54663, #2554, #2223 ) ;
#28718=CYLINDRICAL_SURFACE ( 'NONE', #25876, 2.000000000000001332 ) ;
#28720=EDGE_LOOP ( 'NONE', ( #65156, #41430, #38113 ) ) ;
#28723=CARTESIAN_POINT ( 'NONE',  ( 9.903950872528001881, 5.205009505618999555, 6.747225973806000532 ) ) ;
#28732=CARTESIAN_POINT ( 'NONE',  ( 3.500000000000000000, -3.200000000000000178, 0.000000000000000000 ) ) ;
#28735=CARTESIAN_POINT ( 'NONE',  ( 7.331802703852692282, 3.864187756835510967, 9.236377466553157944 ) ) ;
#28743=DIRECTION ( 'NONE',  ( 1.000000000000000000, 0.000000000000000000, 0.000000000000000000 ) ) ;
#28755=EDGE_LOOP ( 'NONE', ( #6969, #66097, #47878, #43606 ) ) ;
#28758=EDGE_CURVE ( 'NONE', #44831, #13445, #39287, .T. ) ;
#28759=CARTESIAN_POINT ( 'NONE',  ( 10.62716797183172268, 3.242337246279118013, -4.769350230161790272 ) ) ;
#28761=CARTESIAN_POINT ( 'NONE',  ( 7.492958774445000358, 8.174261230744999551, 4.512457914278000359 ) ) ;
#28766=CARTESIAN_POINT ( 'NONE',  ( 7.900104261408000816, 3.351183067932000270, -6.316134894229000096 ) ) ;
#28774=EDGE_CURVE ( 'NONE', #44210, #14053, #3720, .T. ) ;
#28775=CARTESIAN_POINT ( 'NONE',  ( 9.635004719593998956, 2.334550724494000029, -7.977056617806000283 ) ) ;
#28777=CARTESIAN_POINT ( 'NONE',  ( 10.95868203502999982, 8.167115842968998507, -6.508568339202000175 ) ) ;
#28790=CARTESIAN_POINT ( 'NONE',  ( 7.717918988116000634, 2.852331522235000083, 6.784355039830999523 ) ) ;
#28800=DIRECTION ( 'NONE',  ( 0.000000000000000000, -0.1218274111675002047, 0.9925512993736015366 ) ) ;
#28807=CARTESIAN_POINT ( 'NONE',  ( 10.33253786428999987, 2.899999999999999911, 6.571291218949999902 ) ) ;
#28808=CARTESIAN_POINT ( 'NONE',  ( 4.500000000000000000, 0.000000000000000000, 0.000000000000000000 ) ) ;
#28809=EDGE_CURVE ( 'NONE', #67604, #8734, #62052, .T. ) ;
#28812=CARTESIAN_POINT ( 'NONE',  ( 10.95319771135661391, 5.088176249045773147, 4.928389127490998334 ) ) ;
#28822=CARTESIAN_POINT ( 'NONE',  ( 6.999999999999999112, 10.39726215437233492, 4.179831230459656766 ) ) ;
#28828=CARTESIAN_POINT ( 'NONE',  ( 8.476519155276927009, 5.080278632455591747, 8.330433920097927825 ) ) ;
#28831=CARTESIAN_POINT ( 'NONE',  ( 8.307195280408999238, 5.473983809665999622, -8.180077404516000072 ) ) ;
#28835=STYLED_ITEM ( 'NONE', ( #6575 ), #52802 ) ;
#28838=CARTESIAN_POINT ( 'NONE',  ( 8.348093183609000434, 4.599999999999999645, -6.056236567608999977 ) ) ;
#28840=CARTESIAN_POINT ( 'NONE',  ( 8.549914158773001205, 2.141799395716999843, -7.895788736628000848 ) ) ;
#28841=EDGE_CURVE ( 'NONE', #69130, #60334, #15378, .T. ) ;
#28844=CARTESIAN_POINT ( 'NONE',  ( 10.60518955639999916, 5.343965917319999370, -7.731522121091999544 ) ) ;
#28852=AXIS2_PLACEMENT_3D ( 'NONE', #30776, #8765, #46516 ) ;
#28856=CARTESIAN_POINT ( 'NONE',  ( 6.899999691988000450, 12.20988339176000004, 3.111064831550000243 ) ) ;
#28857=CARTESIAN_POINT ( 'NONE',  ( 11.20537028040999949, 2.688545137295000220, -8.273930556758998023 ) ) ;
#28863=EDGE_CURVE ( 'NONE', #14563, #54068, #8846, .T. ) ;
#28866=EDGE_LOOP ( 'NONE', ( #25021, #32497, #41457, #21573 ) ) ;
#28868=CARTESIAN_POINT ( 'NONE',  ( 8.897989158775001073, 4.990139824845000405, -9.121472988377998803 ) ) ;
#28878=B_SPLINE_CURVE_WITH_KNOTS ( 'NONE', 3,
 ( #56589, #67404, #45075, #39827 ),
 .UNSPECIFIED., .F., .F.,
 ( 4, 4 ),
 ( 0.000000000000000000, 1.000000000000000000 ),
 .UNSPECIFIED. ) ;
#28879=CARTESIAN_POINT ( 'NONE',  ( 7.315000000000000391, 2.649999999999999911, -7.500000000000000000 ) ) ;
#28885=ORIENTED_EDGE ( 'NONE', *, *, #44843, .F. ) ;
#28888=CARTESIAN_POINT ( 'NONE',  ( 9.012204719595001023, 3.161445734422999809, -6.178649910536000434 ) ) ;
#28891=DIRECTION ( 'NONE',  ( 0.000000000000000000, -1.000000000000000000, 0.000000000000000000 ) ) ;
#28893=CARTESIAN_POINT ( 'NONE',  ( 3.362977181498000512, -1.794707112228999923, -3.302705535711000007 ) ) ;
#28895=CIRCLE ( 'NONE', #41155, 13.10000000000000320 ) ;
#28896=EDGE_CURVE ( 'NONE', #51514, #12675, #52781, .T. ) ;
#28906=CARTESIAN_POINT ( 'NONE',  ( 7.109360841228999917, 5.292420046468999217, -7.844702366751000966 ) ) ;
#28908=CARTESIAN_POINT ( 'NONE',  ( 10.79415884302793316, 2.685269952712994623, -7.853379249108686011 ) ) ;
#28909=AXIS2_PLACEMENT_3D ( 'NONE', #31076, #53424, #52032 ) ;
#28918=CARTESIAN_POINT ( 'NONE',  ( 10.97828475743834531, 8.385142400385850792, -6.553559007601123199 ) ) ;
#28919=CARTESIAN_POINT ( 'NONE',  ( 8.361784252019500485, 5.107027770526263666, 6.686924863581454659 ) ) ;
#28920=CARTESIAN_POINT ( 'NONE',  ( 7.839139158769000026, 2.603157881926999817, -7.543458285860999979 ) ) ;
#28921=CARTESIAN_POINT ( 'NONE',  ( 5.500000000000000000, -11.00717859340000082, -1.432487142323000118 ) ) ;
#28936=AXIS2_PLACEMENT_3D ( 'NONE', #25679, #63416, #15540 ) ;
#28939=ORIENTED_EDGE ( 'NONE', *, *, #9597, .T. ) ;
#28943=CARTESIAN_POINT ( 'NONE',  ( 9.684729719592999331, 2.370176859044999862, -6.912649125838000508 ) ) ;
#28944=CARTESIAN_POINT ( 'NONE',  ( 2.789820834103999836, 2.869509198118999738, 1.449990717411999919 ) ) ;
#28954=CARTESIAN_POINT ( 'NONE',  ( 9.848730799670999403, 2.769737997918999994, 6.441853401936000090 ) ) ;
#28956=CARTESIAN_POINT ( 'NONE',  ( 11.09999999999999964, 5.299999999999999822, 5.160242730440000258 ) ) ;
#28957=CARTESIAN_POINT ( 'NONE',  ( 9.175261536096115833, 2.907197492737139122, 8.295168095921209073 ) ) ;
#28963=CARTESIAN_POINT ( 'NONE',  ( 0.9590630006697127286, 3.046066035227705804, -1.769131241224070950 ) ) ;
#28964=CARTESIAN_POINT ( 'NONE',  ( 11.18237334122999904, 4.516636732814999888, -8.757876389238999693 ) ) ;
#28965=VERTEX_POINT ( 'NONE', #52870 ) ;
#28972=CARTESIAN_POINT ( 'NONE',  ( 8.596685841231000325, 2.141799395716999843, -7.895788736628000848 ) ) ;
#28975=VERTEX_POINT ( 'NONE', #42038 ) ;
#28977=CARTESIAN_POINT ( 'NONE',  ( 10.44675156161000018, 2.885046387990999772, 8.863482298832000339 ) ) ;
#28983=DIRECTION ( 'NONE',  ( 0.000000000000000000, -0.8648648648648720183, -0.5020047465136825426 ) ) ;
#28995=CARTESIAN_POINT ( 'NONE',  ( 9.610944094206999466, 5.100000000000000533, -6.571291218949999902 ) ) ;
#28998=CARTESIAN_POINT ( 'NONE',  ( 9.292835841232999883, 5.200883864107000321, -6.027780766890000308 ) ) ;
#29005=ORIENTED_EDGE ( 'NONE', *, *, #8223, .T. ) ;
#29007=CARTESIAN_POINT ( 'NONE',  ( 7.000000000000000000, 0.3230303992915000144, 3.000000000000000000 ) ) ;
#29011=EDGE_LOOP ( 'NONE', ( #10930, #51877, #36606, #51379 ) ) ;
#29021=CYLINDRICAL_SURFACE ( 'NONE', #13912, 11.84999999999999964 ) ;
#29022=CARTESIAN_POINT ( 'NONE',  ( 9.149954719592001240, 4.175915362023999933, 5.699506188181000077 ) ) ;
#29026=CARTESIAN_POINT ( 'NONE',  ( 7.178735624121773462, 2.852824245031727379, 8.262394631885278784 ) ) ;
#29030=CARTESIAN_POINT ( 'NONE',  ( 9.629022744239000176, 5.794335169544999609, 7.414871903737999759 ) ) ;
#29031=EDGE_CURVE ( 'NONE', #34779, #51086, #39905, .T. ) ;
#29034=ORIENTED_EDGE ( 'NONE', *, *, #47518, .T. ) ;
#29037=CARTESIAN_POINT ( 'NONE',  ( 10.90638722582999875, 5.227488226180000197, 6.784465725675999259 ) ) ;
#29041=CARTESIAN_POINT ( 'NONE',  ( 8.893204719592999297, 3.977267228909999730, 9.308925224542001331 ) ) ;
#29042=CARTESIAN_POINT ( 'NONE',  ( 9.442843574488000158, 2.691255504502000129, 6.269523028052000235 ) ) ;
#29044=ORIENTED_EDGE ( 'NONE', *, *, #61009, .T. ) ;
#29051=AXIS2_PLACEMENT_3D ( 'NONE', #29090, #30452, #20989 ) ;
#29054=CARTESIAN_POINT ( 'NONE',  ( 0.9717001509839999773, -0.1515593316830000370, 3.422260710200999867 ) ) ;
#29058=B_SPLINE_CURVE_WITH_KNOTS ( 'NONE', 3,
 ( #6638, #54185, #23063, #11530 ),
 .UNSPECIFIED., .F., .F.,
 ( 4, 4 ),
 ( 0.000000000000000000, 1.000000000000000000 ),
 .UNSPECIFIED. ) ;
#29064=VERTEX_POINT ( 'NONE', #56667 ) ;
#29065=CARTESIAN_POINT ( 'NONE',  ( 7.700045280408999382, 3.346262376537000094, 6.002251090845000192 ) ) ;
#29066=EDGE_CURVE ( 'NONE', #22260, #29486, #4757, .T. ) ;
#29071=CARTESIAN_POINT ( 'NONE',  ( 0.6036543026616000285, 3.532364098973999944, -0.6521526059094999717 ) ) ;
#29073=CARTESIAN_POINT ( 'NONE',  ( 1.792640132539665698, -3.058252359239901796, -1.762666431298149039 ) ) ;
#29075=CARTESIAN_POINT ( 'NONE',  ( 9.569805421428000614, 4.064052243276000453, 8.919241792616000808 ) ) ;
#29080=CARTESIAN_POINT ( 'NONE',  ( 10.10000011340999926, 12.39999890530000037, 0.000000000000000000 ) ) ;
#29083=CARTESIAN_POINT ( 'NONE',  ( 7.506887093506311892, 2.659857595113553241, 6.362335448027723217 ) ) ;
#29084=ORIENTED_EDGE ( 'NONE', *, *, #7764, .F. ) ;
#29086=CARTESIAN_POINT ( 'NONE',  ( 7.779445392134999082, 3.186710064579999724, 6.422248840039000761 ) ) ;
#29088=ORIENTED_EDGE ( 'NONE', *, *, #45453, .F. ) ;
#29089=EDGE_CURVE ( 'NONE', #66241, #4821, #53761, .T. ) ;
#29090=CARTESIAN_POINT ( 'NONE',  ( 5.500000000000000000, 13.87069231928999891, -4.225386915259999654 ) ) ;
#29092=AXIS2_PLACEMENT_3D ( 'NONE', #66571, #13454, #67252 ) ;
#29093=LINE ( 'NONE', #50402, #34477 ) ;
#29094=CARTESIAN_POINT ( 'NONE',  ( 10.71256887705999894, 5.951815279772000089, 7.233043586354999555 ) ) ;
#29095=LINE ( 'NONE', #24522, #20965 ) ;
#29107=CARTESIAN_POINT ( 'NONE',  ( 5.000030787343001215, 0.5496608443529860111, -2.045306479342562156 ) ) ;
#29114=ORIENTED_EDGE ( 'NONE', *, *, #14414, .F. ) ;
#29117=CARTESIAN_POINT ( 'NONE',  ( 7.115095033390245405, 5.350161709276040511, -7.499994210608702083 ) ) ;
#29118=CARTESIAN_POINT ( 'NONE',  ( 8.491253953972980995, 3.097373565453227506, 6.091084184371706733 ) ) ;
#29119=CARTESIAN_POINT ( 'NONE',  ( 5.500000000000000000, 0.000000000000000000, 0.000000000000000000 ) ) ;
#29120=CARTESIAN_POINT ( 'NONE',  ( 11.01668724082999873, 7.361611265918999614, -6.178327710506999360 ) ) ;
#29122=CARTESIAN_POINT ( 'NONE',  ( 8.106591486974918936, 5.204875969127657598, -8.204933670002066748 ) ) ;
#29123=CARTESIAN_POINT ( 'NONE',  ( -15.86200481174999943, 5.599999999999999645, 6.571291218949999902 ) ) ;
#29124=CARTESIAN_POINT ( 'NONE',  ( 11.09999999999999964, 2.649999999999999911, -7.500000000000000000 ) ) ;
#29127=LINE ( 'NONE', #12688, #58976 ) ;
#29143=EDGE_CURVE ( 'NONE', #57692, #53328, #31473, .T. ) ;
#29154=CARTESIAN_POINT ( 'NONE',  ( 0.8218067992086085516, -3.408904368339104263, -0.9161175952574813763 ) ) ;
#29155=EDGE_LOOP ( 'NONE', ( #66813, #66037, #49924, #21687, #41032, #27936, #27627, #59382, #42991, #68153, #30356, #10688, #21975, #35602, #13376 ) ) ;
#29161=CARTESIAN_POINT ( 'NONE',  ( 8.324914158772999784, 2.633142096252999664, -7.791134854666999843 ) ) ;
#29170=CARTESIAN_POINT ( 'NONE',  ( 9.881820280408998514, 4.325866256860000369, -9.125812605905000652 ) ) ;
#29174=CIRCLE ( 'NONE', #65975, 12.39999890530000037 ) ;
#29180=CARTESIAN_POINT ( 'NONE',  ( 10.25165889348999926, 3.418644779562000302, -8.733642166016998942 ) ) ;
#29185=CARTESIAN_POINT ( 'NONE',  ( 8.225195096046167720, 2.649880853682612614, 7.500010424662513664 ) ) ;
#29186=DIRECTION ( 'NONE',  ( -0.8660254037844288266, 0.000000000000000000, -0.5000000000000169864 ) ) ;
#29193=CARTESIAN_POINT ( 'NONE',  ( 10.81187971959000116, 4.614148948243999904, -5.930135044105000475 ) ) ;
#29200=CARTESIAN_POINT ( 'NONE',  ( 10.20920446231349921, 2.899999999999999911, 6.662590550579914783 ) ) ;
#29204=ORIENTED_EDGE ( 'NONE', *, *, #23663, .T. ) ;
#29205=CARTESIAN_POINT ( 'NONE',  ( 8.739954719592999410, 3.122811675949999977, -6.006064052396999919 ) ) ;
#29206=PLANE ( 'NONE',  #63533 ) ;
#29212=CARTESIAN_POINT ( 'NONE',  ( 1.800973465875000068, -3.500000000000000000, 0.000000000000000000 ) ) ;
#29213=CARTESIAN_POINT ( 'NONE',  ( 9.099999999999999645, 0.000000000000000000, -11.84999999999999964 ) ) ;
#29215=B_SPLINE_CURVE_WITH_KNOTS ( 'NONE', 3,
 ( #53112, #11147, #21630, #11481 ),
 .UNSPECIFIED., .F., .F.,
 ( 4, 4 ),
 ( 0.000000000000000000, 1.000000000000000000 ),
 .UNSPECIFIED. ) ;
#29220=CARTESIAN_POINT ( 'NONE',  ( 4.149992563292000725, 1.947893036340042627, 0.5234817089163691373 ) ) ;
#29224=CARTESIAN_POINT ( 'NONE',  ( 9.360279719594000625, 3.031907308384000022, -8.729608011560001657 ) ) ;
#29229=EDGE_CURVE ( 'NONE', #21989, #19777, #52893, .T. ) ;
#29230=LINE ( 'NONE', #2641, #8803 ) ;
#29232=CARTESIAN_POINT ( 'NONE',  ( 2.595292652382999776, 3.444664203886000031, -1.018890266960999824 ) ) ;
#29235=CARTESIAN_POINT ( 'NONE',  ( 5.399998535875000449, 12.99045401563999924, -1.690592933733000125 ) ) ;
#29237=CARTESIAN_POINT ( 'NONE',  ( 10.10000011340999926, -1.190159082397999942E-13, -1.214010018759999782E-13 ) ) ;
#29238=CARTESIAN_POINT ( 'NONE',  ( 7.486426658771000220, 5.321913229613000063, 8.118244847118999630 ) ) ;
#29240=ORIENTED_EDGE ( 'NONE', *, *, #57016, .F. ) ;
#29243=CARTESIAN_POINT ( 'NONE',  ( 8.186735841226001398, 4.459320617394000763, -8.819879155908999735 ) ) ;
#29245=PLANE ( 'NONE',  #43293 ) ;
#29247=CARTESIAN_POINT ( 'NONE',  ( 8.486008579191000933, 3.399999999999999911, 5.976611076844000614 ) ) ;
#29250=ORIENTED_EDGE ( 'NONE', *, *, #60447, .T. ) ;
#29256=CARTESIAN_POINT ( 'NONE',  ( 10.93115808116164445, 9.461016078471338631, -6.116472974095783499 ) ) ;
#29258=CARTESIAN_POINT ( 'NONE',  ( 10.57314899745999881, 5.167567567567999731, -6.822293592207000934 ) ) ;
#29260=CYLINDRICAL_SURFACE ( 'NONE', #64146, 1.350000000000000533 ) ;
#29265=DIRECTION ( 'NONE',  ( 0.000000000000000000, 0.8648648648648717963, -0.5020047465136829867 ) ) ;
#29267=ORIENTED_EDGE ( 'NONE', *, *, #267, .T. ) ;
#29268=CARTESIAN_POINT ( 'NONE',  ( 0.000000000000000000, 0.000000000000000000, 0.000000000000000000 ) ) ;
#29269=FACE_OUTER_BOUND ( 'NONE', #38695, .T. ) ;
#29270=CARTESIAN_POINT ( 'NONE',  ( 7.093297165044828212, 2.144184834596416511, -7.429419625897773827 ) ) ;
#29277=VERTEX_POINT ( 'NONE', #47208 ) ;
#29278=CARTESIAN_POINT ( 'NONE',  ( 0.1499942179679999987, 1.689975037551096015, 2.199046806507072294 ) ) ;
#29279=CARTESIAN_POINT ( 'NONE',  ( 8.631645280409999899, 3.826300099041999747, -9.055335252254000267 ) ) ;
#29281=CARTESIAN_POINT ( 'NONE',  ( 2.454485126283999730, -2.645348439211000269, 1.827207675772000162 ) ) ;
#29283=CARTESIAN_POINT ( 'NONE',  ( 7.000000000000000000, 7.526486366024999874, 3.526486366024999874 ) ) ;
#29285=ADVANCED_FACE ( 'NONE', ( #63265 ), #7203, .T. ) ;
#29290=CARTESIAN_POINT ( 'NONE',  ( 9.944319408602000365, 5.443001719280999851, 7.367350382395000175 ) ) ;
#29293=CARTESIAN_POINT ( 'NONE',  ( 9.753142190738998352, 4.104977339646000090, 9.293283246364000050 ) ) ;
#29294=CARTESIAN_POINT ( 'NONE',  ( 9.092672482587163429, 4.128061954255975330, 8.851215505526871752 ) ) ;
#29295=VECTOR ( 'NONE', #26353, 1000.000000000000000 ) ;
#29303=CARTESIAN_POINT ( 'NONE',  ( 10.27367334122999942, 3.065551304793999510, -8.487910413489000661 ) ) ;
#29310=CARTESIAN_POINT ( 'NONE',  ( 9.181704719590001673, 3.734279507827999556, 8.942126004519000304 ) ) ;
#29311=CARTESIAN_POINT ( 'NONE',  ( 9.988985841228000595, 3.986577607995999806, -9.280166295424001177 ) ) ;
#29312=CARTESIAN_POINT ( 'NONE',  ( 0.5765531495413795948, 3.350104404781542033, 1.142356188860006228 ) ) ;
#29313=CARTESIAN_POINT ( 'NONE',  ( 10.75915165876999957, 5.387277012365999873, -6.278112168454999420 ) ) ;
#29314=ORIENTED_EDGE ( 'NONE', *, *, #45453, .T. ) ;
#29315=CARTESIAN_POINT ( 'NONE',  ( 10.72520610419000064, 5.521650664120000940, 6.612990918765000004 ) ) ;
#29322=CARTESIAN_POINT ( 'NONE',  ( 1.417640132541000186, 1.762666431298152370, -3.058252359239900464 ) ) ;
#29332=VERTEX_POINT ( 'NONE', #4108 ) ;
#29337=CARTESIAN_POINT ( 'NONE',  ( 9.550320280412000429, 2.370176859044999862, -6.912649125838000508 ) ) ;
#29338=EDGE_CURVE ( 'NONE', #37404, #56515, #22923, .T. ) ;
#29345=FACE_OUTER_BOUND ( 'NONE', #14711, .T. ) ;
#29350=CARTESIAN_POINT ( 'NONE',  ( 7.954299074928001367, 3.414461172233999697, -6.283593702261001113 ) ) ;
#29351=ORIENTED_EDGE ( 'NONE', *, *, #22813, .T. ) ;
#29362=CARTESIAN_POINT ( 'NONE',  ( 8.700642219592999993, 5.212261578733999201, 6.157186134061999994 ) ) ;
#29364=B_SPLINE_CURVE_WITH_KNOTS ( 'NONE', 3,
 ( #8796, #66831, #56696, #61589 ),
 .UNSPECIFIED., .F., .F.,
 ( 4, 4 ),
 ( 0.000000000000000000, 1.000000000000000000 ),
 .UNSPECIFIED. ) ;
#29368=CARTESIAN_POINT ( 'NONE',  ( 10.84087666499999969, 2.636288985756999992, -7.512643730465999425 ) ) ;
#29371=CARTESIAN_POINT ( 'NONE',  ( 9.657553581808000942, 5.333455947841000189, 6.049916795084000043 ) ) ;
#29380=CARTESIAN_POINT ( 'NONE',  ( 10.85069631730999973, 4.478098874537000285, 6.162039661770999821 ) ) ;
#29387=CARTESIAN_POINT ( 'NONE',  ( 7.994579719591000000, 2.263558315407000254, 8.007442119518000112 ) ) ;
#29388=CARTESIAN_POINT ( 'NONE',  ( 9.034110134264999203, 4.695345051283999815, 8.660667941667000491 ) ) ;
#29391=CARTESIAN_POINT ( 'NONE',  ( 8.500189158773000742, 2.724453559418999582, -8.908010318766001134 ) ) ;
#29399=ORIENTED_EDGE ( 'NONE', *, *, #37311, .F. ) ;
#29400=AXIS2_PLACEMENT_3D ( 'NONE', #8439, #14034, #35360 ) ;
#29401=CARTESIAN_POINT ( 'NONE',  ( 1.162427948746999951, -2.208354302538000358, -2.618776384398000090 ) ) ;
#29402=DIRECTION ( 'NONE',  ( 1.000000000000000000, 0.000000000000000000, 0.000000000000000000 ) ) ;
#29403=AXIS2_PLACEMENT_3D ( 'NONE', #68031, #26782, #20147 ) ;
#29411=CARTESIAN_POINT ( 'NONE',  ( 0.1499942179679999987, 5.893556041935713383E-16, -2.749976859058071543 ) ) ;
#29413=ORIENTED_EDGE ( 'NONE', *, *, #45806, .T. ) ;
#29414=CARTESIAN_POINT ( 'NONE',  ( 8.149357780409999918, 2.583668273793999770, 6.684750595573999199 ) ) ;
#29418=CARTESIAN_POINT ( 'NONE',  ( 1.891066937564000128, -3.444624976169999631, -1.019033653642999804 ) ) ;
#29419=VERTEX_POINT ( 'NONE', #15984 ) ;
#29420=CARTESIAN_POINT ( 'NONE',  ( 1.761390132539666808, -3.499999999999999556, -0.4581489286485119772 ) ) ;
#29422=CARTESIAN_POINT ( 'NONE',  ( 9.834151567923001380, 5.173929249342999803, 8.813048229486998508 ) ) ;
#29425=CARTESIAN_POINT ( 'NONE',  ( 5.000000000000000000, 0.2999999999999999889, 9.776630298829998011 ) ) ;
#29427=ADVANCED_FACE ( 'NONE', ( #43249 ), #32723, .T. ) ;
#29429=CARTESIAN_POINT ( 'NONE',  ( 8.474485200571999499, 5.100000000000000533, 6.560614371780999043 ) ) ;
#29431=AXIS2_PLACEMENT_3D ( 'NONE', #57342, #62255, #66815 ) ;
#29432=CARTESIAN_POINT ( 'NONE',  ( 8.536950018568271403, 3.172726136472098446, 5.956131468116810268 ) ) ;
#29434=CONICAL_SURFACE ( 'NONE', #4841, 12.44999944941000081, 0.7853981146832407223 ) ;
#29442=CARTESIAN_POINT ( 'NONE',  ( 9.781673028307999118, 5.464749740720999505, 8.817329433105999925 ) ) ;
#29443=CARTESIAN_POINT ( 'NONE',  ( 9.898128230592000421, 2.965931985296999862, -6.610871072364999712 ) ) ;
#29455=AXIS2_PLACEMENT_3D ( 'NONE', #56016, #39945, #51116 ) ;
#29456=CARTESIAN_POINT ( 'NONE',  ( 5.000030787342999439, 1.834918991542626499, -1.057581170753191913 ) ) ;
#29470=FACE_OUTER_BOUND ( 'NONE', #7857, .T. ) ;
#29471=CARTESIAN_POINT ( 'NONE',  ( 8.761020418847346392, 3.646575901141349885, -8.850808559580910284 ) ) ;
#29473=CARTESIAN_POINT ( 'NONE',  ( 0.4936698601467999770, 3.273731968234999901, -1.479853775367000246 ) ) ;
#29474=DIRECTION ( 'NONE',  ( 0.000000000000000000, 0.8648648648648717963, -0.5020047465136829867 ) ) ;
#29478=CARTESIAN_POINT ( 'NONE',  ( 6.999998971696826722, -12.01547034654744195, -3.452253082527627637 ) ) ;
#29480=DIRECTION ( 'NONE',  ( -1.000000000000000000, 0.000000000000000000, 0.000000000000000000 ) ) ;
#29486=VERTEX_POINT ( 'NONE', #69124 ) ;
#29489=B_SPLINE_CURVE_WITH_KNOTS ( 'NONE', 3,
 ( #67610, #36154, #35481, #41058, #67960, #19737 ),
 .UNSPECIFIED., .F., .F.,
 ( 4, 2, 4 ),
 ( 0.000000000000000000, 0.4999999999999995559, 1.000000000000000000 ),
 .UNSPECIFIED. ) ;
#29496=ORIENTED_EDGE ( 'NONE', *, *, #4347, .T. ) ;
#29497=AXIS2_PLACEMENT_3D ( 'NONE', #21549, #15963, #53717 ) ;
#29510=CONICAL_SURFACE ( 'NONE', #26142, 12.49999584805000019, 0.7853981146832407223 ) ;
#29512=CARTESIAN_POINT ( 'NONE',  ( 8.406851002545000284, 2.832432432432000269, -6.822293592207000934 ) ) ;
#29516=CARTESIAN_POINT ( 'NONE',  ( 9.617764158771999305, 5.322769172805999816, -7.951018786192998178 ) ) ;
#29518=ORIENTED_EDGE ( 'NONE', *, *, #26269, .T. ) ;
#29519=B_SPLINE_CURVE_WITH_KNOTS ( 'NONE', 3,
 ( #34456, #59971, #18368, #12777 ),
 .UNSPECIFIED., .F., .F.,
 ( 4, 4 ),
 ( 0.000000000000000000, 1.000000000000000000 ),
 .UNSPECIFIED. ) ;
#29523=CARTESIAN_POINT ( 'NONE',  ( 8.528661480133287398, 4.352698949118988025, 8.815590613233503348 ) ) ;
#29525=CARTESIAN_POINT ( 'NONE',  ( 9.898395280408998076, 3.987760651117999711, -9.123263301387000368 ) ) ;
#29531=CARTESIAN_POINT ( 'NONE',  ( 7.773105724985851950, 3.449994720449756525, -8.750200106293087643 ) ) ;
#29532=CARTESIAN_POINT ( 'NONE',  ( 7.732053843957007899, 3.067861388767125774, 6.507875342627428950 ) ) ;
#29533=CARTESIAN_POINT ( 'NONE',  ( 8.997439158776000312, 2.773858540272000184, -8.951250717848999727 ) ) ;
#29536=CARTESIAN_POINT ( 'NONE',  ( 10.34224945431000009, 3.348985101650000296, -8.881460768006000706 ) ) ;
#29537=FACE_OUTER_BOUND ( 'NONE', #29538, .T. ) ;
#29538=EDGE_LOOP ( 'NONE', ( #66118, #22696, #60433, #65275 ) ) ;
#29542=DIRECTION ( 'NONE',  ( 0.000000000000000000, 1.000000000000000000, 0.000000000000000000 ) ) ;
#29545=EDGE_CURVE ( 'NONE', #15877, #61826, #17099, .T. ) ;
#29550=CARTESIAN_POINT ( 'NONE',  ( 10.17270667456000055, 4.650145611776999921, -8.655516756809999990 ) ) ;
#29556=CARTESIAN_POINT ( 'NONE',  ( 7.836894192211024013, 4.974970171335808544, 6.505028920865267850 ) ) ;
#29559=CARTESIAN_POINT ( 'NONE',  ( 9.784179719593000257, 4.042991257420999851, -5.768106221333000327 ) ) ;
#29560=LINE ( 'NONE', #67957, #8844 ) ;
#29564=EDGE_CURVE ( 'NONE', #64040, #25016, #49181, .T. ) ;
#29576=ORIENTED_EDGE ( 'NONE', *, *, #39245, .F. ) ;
#29577=FACE_OUTER_BOUND ( 'NONE', #47296, .T. ) ;
#29579=CARTESIAN_POINT ( 'NONE',  ( 9.292835841232999883, 5.200883864107000321, -6.027780766890000308 ) ) ;
#29584=CARTESIAN_POINT ( 'NONE',  ( 3.358203843436000202, -3.564015676669000321, 0.4490691151644999879 ) ) ;
#29591=ORIENTED_EDGE ( 'NONE', *, *, #32912, .T. ) ;
#29593=CARTESIAN_POINT ( 'NONE',  ( 10.86501009699162701, 2.649983380500041008, -7.500000587580665901 ) ) ;
#29594=B_SPLINE_CURVE_WITH_KNOTS ( 'NONE', 3,
 ( #16387, #11830, #1008, #37717, #59045, #12188, #27927, #64619, #6587, #27577 ),
 .UNSPECIFIED., .F., .F.,
 ( 4, 2, 2, 2, 4 ),
 ( 0.000000000000000000, 0.2500000000000000000, 0.5000000000000000000, 0.7500000000000000000, 1.000000000000000000 ),
 .UNSPECIFIED. ) ;
#29595=CARTESIAN_POINT ( 'NONE',  ( 7.882273351303999753, 4.670607894679000616, 6.328281252841999382 ) ) ;
#29606=ORIENTED_EDGE ( 'NONE', *, *, #2564, .T. ) ;
#29607=CARTESIAN_POINT ( 'NONE',  ( 10.96365577692472293, 8.824255620808143519, -6.481155636164055878 ) ) ;
#29609=DIRECTION ( 'NONE',  ( -1.000000000000000000, 0.000000000000000000, 0.000000000000000000 ) ) ;
#29613=CARTESIAN_POINT ( 'NONE',  ( 2.084306799206667282, 1.762666431298138825, 3.058252359239908014 ) ) ;
#29616=CARTESIAN_POINT ( 'NONE',  ( 10.99284770222452323, 5.204191398046943640, 6.666795694131347538 ) ) ;
#29621=CARTESIAN_POINT ( 'NONE',  ( 3.500000000000000000, 2.593303125396967168, 2.221279084403522841 ) ) ;
#29622=LINE ( 'NONE', #2684, #7362 ) ;
#29630=ORIENTED_EDGE ( 'NONE', *, *, #22867, .T. ) ;
#29631=CARTESIAN_POINT ( 'NONE',  ( 10.03612394578000000, 3.011788727150999989, 8.746962581836999817 ) ) ;
#29633=CARTESIAN_POINT ( 'NONE',  ( 10.16426084122999995, 4.808846957865000604, -8.639578604182998944 ) ) ;
#29634=EDGE_CURVE ( 'NONE', #10305, #2626, #33805, .T. ) ;
#29635=CARTESIAN_POINT ( 'NONE',  ( 2.496402089761999843, -3.205343848849000032, 0.2496534946583000014 ) ) ;
#29642=CARTESIAN_POINT ( 'NONE',  ( 10.77962664842000073, 2.397507474987000009, 7.755423212350999407 ) ) ;
#29645=CARTESIAN_POINT ( 'NONE',  ( 11.18051582549000145, 5.340073783367000892, 8.416152717850000187 ) ) ;
#29646=CARTESIAN_POINT ( 'NONE',  ( 10.96666666666765622, 4.766458981285071062, 8.714450223969652853 ) ) ;
#29654=CARTESIAN_POINT ( 'NONE',  ( 0.9047787742017877610, 1.249023173894558303, -3.293673443241941445 ) ) ;
#29655=CARTESIAN_POINT ( 'NONE',  ( 11.03092334123000029, 5.020455242919999783, -6.601201971309999195 ) ) ;
#29662=CARTESIAN_POINT ( 'NONE',  ( 9.053329719590999858, 5.618384167307999277, 7.727742442702000503 ) ) ;
#29663=CARTESIAN_POINT ( 'NONE',  ( 9.972410841228999345, 4.357364160690000432, -9.282962013144999247 ) ) ;
#29667=B_SPLINE_CURVE_WITH_KNOTS ( 'NONE', 3,
 ( #49138, #22908, #64858, #1945 ),
 .UNSPECIFIED., .F., .F.,
 ( 4, 4 ),
 ( 0.000000000000000000, 0.1254224513349476711 ),
 .UNSPECIFIED. ) ;
#29672=CARTESIAN_POINT ( 'NONE',  ( 9.739312519577246974, 2.650230560758055187, 7.263871480528552915 ) ) ;
#29677=AXIS2_PLACEMENT_3D ( 'NONE', #55477, #34515, #29265 ) ;
#29683=CARTESIAN_POINT ( 'NONE',  ( 0.5181103717477000270, 3.205765437135000173, -1.404659375816999844 ) ) ;
#29684=VERTEX_POINT ( 'NONE', #50566 ) ;
#29686=VERTEX_POINT ( 'NONE', #28209 ) ;
#29690=CARTESIAN_POINT ( 'NONE',  ( 8.365779719592000063, 2.949305648881000330, -8.659807625323999503 ) ) ;
#29695=CARTESIAN_POINT ( 'NONE',  ( 8.785198341231000185, 5.414918126383000185, 8.890678916765999418 ) ) ;
#29720=LINE ( 'NONE', #51023, #812 ) ;
#29723=CARTESIAN_POINT ( 'NONE',  ( 10.15902941591999920, 4.166415211384999040, 9.114163806478000396 ) ) ;
#29728=CARTESIAN_POINT ( 'NONE',  ( 9.611387933856001098, 3.334846092635999959, 5.869117602953000556 ) ) ;
#29731=EDGE_CURVE ( 'NONE', #35162, #48584, #32834, .T. ) ;
#29734=CARTESIAN_POINT ( 'NONE',  ( 8.187142219590999304, 4.968147183437999992, 5.971792472497999604 ) ) ;
#29735=CARTESIAN_POINT ( 'NONE',  ( 9.124700695083998170, 4.778663323155000420, 8.799742559280000265 ) ) ;
#29739=CARTESIAN_POINT ( 'NONE',  ( 9.146614158775999925, 2.981992329588000423, -5.895876591910999664 ) ) ;
#29741=CARTESIAN_POINT ( 'NONE',  ( 11.09999058424224394, 2.671414376110711864, 6.690776694877815345 ) ) ;
#29748=CARTESIAN_POINT ( 'NONE',  ( 2.015929700617999920, 1.841731729107999982, 3.084132442762999915 ) ) ;
#29752=CARTESIAN_POINT ( 'NONE',  ( 11.09999999999999964, 2.399999999999999911, 6.571291218949999902 ) ) ;
#29758=CARTESIAN_POINT ( 'NONE',  ( 9.266948341230998309, 3.049618631524000367, 6.392542946894000266 ) ) ;
#29762=CARTESIAN_POINT ( 'NONE',  ( 0.8849726612439999807, -2.055220836715000221, 2.740599349591000156 ) ) ;
#29764=DIRECTION ( 'NONE',  ( 1.000000000000000000, 0.000000000000000000, 0.000000000000000000 ) ) ;
#29767=CARTESIAN_POINT ( 'NONE',  ( 9.924742128742000347, 5.060458431729999873, 8.686130311522999747 ) ) ;
#29769=EDGE_CURVE ( 'NONE', #4993, #10018, #13176, .T. ) ;
#29774=EDGE_CURVE ( 'NONE', #46445, #23086, #57832, .T. ) ;
#29775=ADVANCED_FACE ( 'NONE', ( #65254 ), #7018, .T. ) ;
#29778=CARTESIAN_POINT ( 'NONE',  ( 7.597202546497848985, 4.478004213731558991, 5.818027706311307945 ) ) ;
#29780=AXIS2_PLACEMENT_3D ( 'NONE', #40759, #8945, #25025 ) ;
#29786=CARTESIAN_POINT ( 'NONE',  ( 4.149992563292000725, 2.000000000000000000, 0.000000000000000000 ) ) ;
#29789=CARTESIAN_POINT ( 'NONE',  ( 9.166073843917999397, 4.023333628930999772, 9.122276991855001071 ) ) ;
#29790=CARTESIAN_POINT ( 'NONE',  ( 10.97074841058999972, 2.648521302318000092, -6.788870928221999890 ) ) ;
#29796=CARTESIAN_POINT ( 'NONE',  ( 7.919010841228001141, 5.361039412362000434, 6.973453640356000349 ) ) ;
#29798=AXIS2_PLACEMENT_3D ( 'NONE', #12804, #23628, #51232 ) ;
#29800=DIRECTION ( 'NONE',  ( 0.000000000000000000, 0.3258275053806940491, -0.9454292341245820186 ) ) ;
#29801=CARTESIAN_POINT ( 'NONE',  ( 5.000030787343000327, 2.099962892530999881, 0.000000000000000000 ) ) ;
#29806=ORIENTED_EDGE ( 'NONE', *, *, #29774, .F. ) ;
#29817=CARTESIAN_POINT ( 'NONE',  ( 7.935182732229910663, 5.348502701843190543, 7.676951299079826541 ) ) ;
#29818=EDGE_CURVE ( 'NONE', #10337, #1602, #30964, .T. ) ;
#29822=CARTESIAN_POINT ( 'NONE',  ( 1.250973465874999802, -3.500000000000000000, 0.000000000000000000 ) ) ;
#29823=CARTESIAN_POINT ( 'NONE',  ( 11.06205165877000063, 2.154392227069000132, -7.605898171884000192 ) ) ;
#29827=DIRECTION ( 'NONE',  ( 0.000000000000000000, 0.8648648261949251070, 0.5020048131351152465 ) ) ;
#29836=CIRCLE ( 'NONE', #54356, 12.39999890530000037 ) ;
#29842=CIRCLE ( 'NONE', #25373, 11.35000000000000497 ) ;
#29847=CARTESIAN_POINT ( 'NONE',  ( 7.939460911587998382, 2.865023798136999922, 6.766038833998996971 ) ) ;
#29849=CARTESIAN_POINT ( 'NONE',  ( 0.8009734658753000502, -3.500000000000000000, 0.000000000000000000 ) ) ;
#29852=ADVANCED_FACE ( 'NONE', ( #24339 ), #46354, .T. ) ;
#29854=ADVANCED_FACE ( 'NONE', ( #52277 ), #3349, .T. ) ;
#29858=CARTESIAN_POINT ( 'NONE',  ( 9.310554719594000161, 3.934138271021000222, -9.063586117809000697 ) ) ;
#29861=CARTESIAN_POINT ( 'NONE',  ( 4.000000000000000000, -1.082950885222932147, 1.878608423871279687 ) ) ;
#29863=ORIENTED_EDGE ( 'NONE', *, *, #34667, .T. ) ;
#29866=CARTESIAN_POINT ( 'NONE',  ( 9.600045280412000892, 3.021734963141999852, -6.070209284876999511 ) ) ;
#29870=CARTESIAN_POINT ( 'NONE',  ( -15.86200481174999943, 5.599999999999999645, 6.571291218949999902 ) ) ;
#29874=CARTESIAN_POINT ( 'NONE',  ( 9.128895280414001334, 3.880154689736000417, -9.060377011187000562 ) ) ;
#29875=EDGE_LOOP ( 'NONE', ( #45621, #4101, #13909 ) ) ;
#29878=CARTESIAN_POINT ( 'NONE',  ( 10.87696123885999810, 5.827079664135999870, -7.814747088295999511 ) ) ;
#29890=CARTESIAN_POINT ( 'NONE',  ( 8.687922088694000067, 3.419384128876999718, -5.860036257779999147 ) ) ;
#29891=DIRECTION ( 'NONE',  ( -0.4682208595142289265, -0.4682208595142289265, 0.7493586947727458591 ) ) ;
#29896=CARTESIAN_POINT ( 'NONE',  ( 7.837706995175509839, 4.985640386982826300, 6.515278850541923461 ) ) ;
#29900=CARTESIAN_POINT ( 'NONE',  ( 8.441604719589999917, 5.473983809665999622, -8.180077404516000072 ) ) ;
#29901=EDGE_CURVE ( 'NONE', #27904, #43460, #67000, .T. ) ;
#29902=CARTESIAN_POINT ( 'NONE',  ( 9.299999999999998934, 4.537600397704999899, 9.154563893594000135 ) ) ;
#29908=CARTESIAN_POINT ( 'NONE',  ( 8.752020595170648676, 5.414340795661968464, 8.580369625954880064 ) ) ;
#29909=CARTESIAN_POINT ( 'NONE',  ( 0.6679169396051075624, 2.967698684047975544, -1.300341253696400301 ) ) ;
#29910=ORIENTED_EDGE ( 'NONE', *, *, #62271, .F. ) ;
#29914=DIRECTION ( 'NONE',  ( 0.000000000000000000, 1.000000000000000000, 0.000000000000000000 ) ) ;
#29920=DIRECTION ( 'NONE',  ( -1.000000000000000000, 0.000000000000000000, 0.000000000000000000 ) ) ;
#29922=CARTESIAN_POINT ( 'NONE',  ( 0.3738300074506999970, -3.373808768376999723, -1.182108054635000026E-09 ) ) ;
#29923=CARTESIAN_POINT ( 'NONE',  ( 3.496476353695999961, -3.048162822197999944, -1.563142635087000132 ) ) ;
#29932=VERTEX_POINT ( 'NONE', #4024 ) ;
#29936=EDGE_CURVE ( 'NONE', #10927, #11525, #46215, .T. ) ;
#29937=CARTESIAN_POINT ( 'NONE',  ( 10.97857890969851979, 8.376940913775774433, 6.556924013712003507 ) ) ;
#29939=CARTESIAN_POINT ( 'NONE',  ( 1.615556799206875116, 0.4581489286485002088, 3.500000000000001776 ) ) ;
#29949=CARTESIAN_POINT ( 'NONE',  ( 10.97209615884046485, 8.593900732908855034, -6.535061034646649780 ) ) ;
#29951=LINE ( 'NONE', #29258, #19226 ) ;
#29952=DIRECTION ( 'NONE',  ( -1.000000000000000000, 0.000000000000000000, 0.000000000000000000 ) ) ;
#29964=EDGE_CURVE ( 'NONE', #69017, #62685, #6942, .T. ) ;
#29970=ORIENTED_EDGE ( 'NONE', *, *, #25485, .F. ) ;
#29973=CARTESIAN_POINT ( 'NONE',  ( 9.442087588264000075, 4.742492734433000123, 8.809983635807000724 ) ) ;
#29976=CARTESIAN_POINT ( 'NONE',  ( 9.865910841232000905, 2.685250982074999904, -7.026194612421999608 ) ) ;
#29977=CARTESIAN_POINT ( 'NONE',  ( 3.054835882697000127, 0.1750656501049999980, 3.539389852118999702 ) ) ;
#29979=CARTESIAN_POINT ( 'NONE',  ( 3.500000000000000000, -2.946081722130999836, 0.9972449351501998516 ) ) ;
#29984=CARTESIAN_POINT ( 'NONE',  ( 9.013423559847998590, 4.933953210258000155, 8.417881984655998906 ) ) ;
#29988=CARTESIAN_POINT ( 'NONE',  ( 10.99433665574000152, 3.697618584609999814, 5.729302299903000772 ) ) ;
#29996=LINE ( 'NONE', #18458, #18789 ) ;
#29998=ORIENTED_EDGE ( 'NONE', *, *, #5387, .T. ) ;
#30004=CARTESIAN_POINT ( 'NONE',  ( 7.807364158771999740, 3.650414032626000171, 6.083147621602999600 ) ) ;
#30007=CARTESIAN_POINT ( 'NONE',  ( 10.47111721959000086, 5.170640285885000687, -8.712953516124999354 ) ) ;
#30010=CARTESIAN_POINT ( 'NONE',  ( 1.467640132540666498, 1.762666431298152148, -3.058252359239900908 ) ) ;
#30011=LINE ( 'NONE', #61122, #68831 ) ;
#30015=ORIENTED_EDGE ( 'NONE', *, *, #7092, .T. ) ;
#30024=CARTESIAN_POINT ( 'NONE',  ( 2.865556799209791894, -0.4581489286485082579, -3.500000000000000888 ) ) ;
#30026=ORIENTED_EDGE ( 'NONE', *, *, #10084, .T. ) ;
#30029=VERTEX_POINT ( 'NONE', #51587 ) ;
#30031=CARTESIAN_POINT ( 'NONE',  ( 8.397785841227999981, 5.616457598545999907, -8.245813000738998255 ) ) ;
#30036=CARTESIAN_POINT ( 'NONE',  ( 8.721010841230999233, 5.983047240001000411, 7.440798119034999658 ) ) ;
#30040=FACE_OUTER_BOUND ( 'NONE', #55022, .T. ) ;
#30046=CARTESIAN_POINT ( 'NONE',  ( 6.875000000000000000, 5.574137966889000317, -8.240733100917999820 ) ) ;
#30053=CARTESIAN_POINT ( 'NONE',  ( 2.750973465876000557, -3.500000000000000000, 0.000000000000000000 ) ) ;
#30059=CARTESIAN_POINT ( 'NONE',  ( 11.01002959534999981, 3.180718072098000171, -6.283812549199000230 ) ) ;
#30063=CARTESIAN_POINT ( 'NONE',  ( 11.11845610223999969, 5.767025078915000158, 7.178418469370999588 ) ) ;
#30064=DIRECTION ( 'NONE',  ( -1.000000000000000000, 0.000000000000000000, 0.000000000000000000 ) ) ;
#30068=CARTESIAN_POINT ( 'NONE',  ( 9.980433037259000884, 4.047223446241999589, 9.090360698422999874 ) ) ;
#30070=CARTESIAN_POINT ( 'NONE',  ( 8.640504719592000171, 2.305580295895999665, -7.860904109308999743 ) ) ;
#30073=ADVANCED_FACE ( 'NONE', ( #49704 ), #33637, .T. ) ;
#30075=CARTESIAN_POINT ( 'NONE',  ( 9.021579719592999425, 2.193665972875999959, 7.400591513898000073 ) ) ;
#30076=CARTESIAN_POINT ( 'NONE',  ( 9.600491906670001185, 5.206545077004999911, 8.585111878242999595 ) ) ;
#30077=AXIS2_PLACEMENT_3D ( 'NONE', #67205, #22925, #67547 ) ;
#30080=CARTESIAN_POINT ( 'NONE',  ( 10.01508584123000034, 4.845406482350000488, -6.387189183984999907 ) ) ;
#30081=CARTESIAN_POINT ( 'NONE',  ( -2.444943969992999916E-05, 2.899969545325999931, 0.000000000000000000 ) ) ;
#30088=CARTESIAN_POINT ( 'NONE',  ( 1.062290711803000054, -0.1589293563100999951, 3.588678346333000313 ) ) ;
#30090=CARTESIAN_POINT ( 'NONE',  ( 9.768156128192828191, 5.148428864295390817, 8.818541960853263362 ) ) ;
#30095=LINE ( 'NONE', #35671, #43135 ) ;
#30096=CARTESIAN_POINT ( 'NONE',  ( 9.679055905794999859, 2.899999999999999911, 6.571291218949999902 ) ) ;
#30099=CARTESIAN_POINT ( 'NONE',  ( 9.074385841230999006, 3.981661882377999895, 8.959227447876999761 ) ) ;
#30104=CARTESIAN_POINT ( 'NONE',  ( 0.7896087623623999630, 1.804890371571000074, 2.911542930280999641 ) ) ;
#30106=CARTESIAN_POINT ( 'NONE',  ( 1.429412799688042801, -1.139198292438498017, 3.100114201899466959 ) ) ;
#30107=ADVANCED_FACE ( 'NONE', ( #55992 ), #45506, .T. ) ;
#30110=CARTESIAN_POINT ( 'NONE',  ( 10.03612394578000000, 3.011788727150999989, 8.746962581836999817 ) ) ;
#30117=CARTESIAN_POINT ( 'NONE',  ( 7.665091595931846413, 5.584449939165478938, 6.749525577098944851 ) ) ;
#30125=EDGE_CURVE ( 'NONE', #32067, #12035, #19616, .T. ) ;
#30127=CARTESIAN_POINT ( 'NONE',  ( 9.691082467489000152, 5.335647408863999352, 8.701220655673999715 ) ) ;
#30128=CARTESIAN_POINT ( 'NONE',  ( 10.84087666499999969, 2.636288985756999992, -7.512643730465999425 ) ) ;
#30135=ORIENTED_EDGE ( 'NONE', *, *, #33626, .F. ) ;
#30141=DIRECTION ( 'NONE',  ( 0.000000000000000000, 1.000000000000000000, 0.000000000000000000 ) ) ;
#30145=ORIENTED_EDGE ( 'NONE', *, *, #59990, .T. ) ;
#30146=CARTESIAN_POINT ( 'NONE',  ( 10.97499895057999986, -2.398081733189999864E-14, 0.000000000000000000 ) ) ;
#30148=AXIS2_PLACEMENT_3D ( 'NONE', #53556, #26990, #59138 ) ;
#30149=CARTESIAN_POINT ( 'NONE',  ( 5.500000000000000000, 0.000000000000000000, 0.000000000000000000 ) ) ;
#30154=EDGE_CURVE ( 'NONE', #47074, #50591, #64508, .T. ) ;
#30156=CARTESIAN_POINT ( 'NONE',  ( 8.029017301488167391, 4.353549739958994635, 8.815463536202678085 ) ) ;
#30161=CARTESIAN_POINT ( 'NONE',  ( 9.709999999999999076, 4.496968146123999865, -8.755198255949000696 ) ) ;
#30162=CARTESIAN_POINT ( 'NONE',  ( 10.60770165877000082, 2.392327800351000011, -6.587345916039000215 ) ) ;
#30167=ORIENTED_EDGE ( 'NONE', *, *, #43344, .T. ) ;
#30174=CARTESIAN_POINT ( 'NONE',  ( 6.916399753370999548, -12.19468927157999971, 3.104275419013000192 ) ) ;
#30184=CARTESIAN_POINT ( 'NONE',  ( 10.63706886433642573, 2.899999999999999911, 6.444141223494331605 ) ) ;
#30190=AXIS2_PLACEMENT_3D ( 'NONE', #26584, #4208, #62592 ) ;
#30191=CARTESIAN_POINT ( 'NONE',  ( 8.474089158773999486, 4.131080973160000447, -6.108642999115999395 ) ) ;
#30194=CARTESIAN_POINT ( 'NONE',  ( 4.000000000000000000, 1.082895748633089683, 1.878475312369199957 ) ) ;
#30200=CARTESIAN_POINT ( 'NONE',  ( 9.152520280414000453, 4.102804347295999854, -5.770625657082999460 ) ) ;
#30201=CARTESIAN_POINT ( 'NONE',  ( 9.715116888608552159, 4.417514547833707894, -8.786659901436729925 ) ) ;
#30206=EDGE_LOOP ( 'NONE', ( #1520, #49867, #42502 ) ) ;
#30207=CARTESIAN_POINT ( 'NONE',  ( 7.906851002540999929, 2.832432432432000269, -6.822293592207000934 ) ) ;
#30209=CARTESIAN_POINT ( 'NONE',  ( 8.491329719591000469, 4.851303550474000303, -9.008742670124000540 ) ) ;
#30211=CARTESIAN_POINT ( 'NONE',  ( 9.870875237110999123, 2.904361819252000210, -8.563871667095998674 ) ) ;
#30215=B_SPLINE_CURVE_WITH_KNOTS ( 'NONE', 3,
 ( #37521, #31599, #42430, #42089, #48356, #36151 ),
 .UNSPECIFIED., .F., .F.,
 ( 4, 2, 4 ),
 ( 0.000000000000000000, 0.3470882326038999266, 0.6941764652077998532 ),
 .UNSPECIFIED. ) ;
#30216=CARTESIAN_POINT ( 'NONE',  ( 9.342770489224111685, 2.713249534563407561, -7.026737643655856402 ) ) ;
#30221=DIRECTION ( 'NONE',  ( 0.000000000000000000, -1.000000000000000000, 0.000000000000000000 ) ) ;
#30222=B_SPLINE_CURVE_WITH_KNOTS ( 'NONE', 3,
 ( #18812, #61452, #56894, #45722 ),
 .UNSPECIFIED., .F., .F.,
 ( 4, 4 ),
 ( 0.000000000000000000, 1.000000000000000000 ),
 .UNSPECIFIED. ) ;
#30229=EDGE_CURVE ( 'NONE', #58875, #62483, #34457, .T. ) ;
#30231=ORIENTED_EDGE ( 'NONE', *, *, #22783, .F. ) ;
#30232=CARTESIAN_POINT ( 'NONE',  ( 8.532195280408998883, 5.331510020787000315, -8.114341808290998159 ) ) ;
#30233=CARTESIAN_POINT ( 'NONE',  ( 4.149992563292000725, -2.000000000000000000, 0.000000000000000000 ) ) ;
#30234=EDGE_CURVE ( 'NONE', #29932, #37966, #53623, .T. ) ;
#30240=CIRCLE ( 'NONE', #31332, 1.900000000000001021 ) ;
#30245=B_SPLINE_CURVE_WITH_KNOTS ( 'NONE', 3,
 ( #30161, #19999, #51803, #30833 ),
 .UNSPECIFIED., .F., .F.,
 ( 4, 4 ),
 ( 0.000000000000000000, 1.000000000000000000 ),
 .UNSPECIFIED. ) ;
#30249=LINE ( 'NONE', #41069, #11277 ) ;
#30250=CARTESIAN_POINT ( 'NONE',  ( 4.933367189779430895, 2.033301450227492424, -8.777144014527002974E-10 ) ) ;
#30251=CARTESIAN_POINT ( 'NONE',  ( 8.601296034414005476, 5.350254842529069244, -7.263180132971093883 ) ) ;
#30252=CARTESIAN_POINT ( 'NONE',  ( 8.696135841231001251, 3.038023536984999939, -5.861661709981000001 ) ) ;
#30257=CARTESIAN_POINT ( 'NONE',  ( 2.299654279612000085, 3.259062154207000184, 0.01210126588865999969 ) ) ;
#30258=ORIENTED_EDGE ( 'NONE', *, *, #23439, .F. ) ;
#30261=CARTESIAN_POINT ( 'NONE',  ( 8.765417767663000959, 5.029951493281999753, -6.097931603992000404 ) ) ;
#30262=CARTESIAN_POINT ( 'NONE',  ( 7.358051658771000092, 4.561643343497000735, 6.153061759127000485 ) ) ;
#30265=CARTESIAN_POINT ( 'NONE',  ( 11.04384236319999957, 5.374509385214000012, -5.035088906224999938 ) ) ;
#30267=CARTESIAN_POINT ( 'NONE',  ( 10.96277061797134955, 8.847246680402779617, 6.474667694356146974 ) ) ;
#30269=CARTESIAN_POINT ( 'NONE',  ( 1.750973465873000068, -3.500000000000000000, 0.000000000000000000 ) ) ;
#30274=ORIENTED_EDGE ( 'NONE', *, *, #2485, .T. ) ;
#30275=CIRCLE ( 'NONE', #9049, 12.50000000000000000 ) ;
#30284=CARTESIAN_POINT ( 'NONE',  ( 7.531929719588999816, 3.511256298105000173, -6.013302684100999329 ) ) ;
#30288=EDGE_LOOP ( 'NONE', ( #1711, #18825, #41520, #31956 ) ) ;
#30293=CARTESIAN_POINT ( 'NONE',  ( 11.09999999999999964, 5.299999999999999822, -5.160242713806000303 ) ) ;
#30295=CARTESIAN_POINT ( 'NONE',  ( 10.62947109217999930, 5.100000000000000533, 6.152188490330000370 ) ) ;
#30297=DIRECTION ( 'NONE',  ( -1.000000000000000000, 0.000000000000000000, -6.365544662581999450E-14 ) ) ;
#30304=CARTESIAN_POINT ( 'NONE',  ( 10.42596030538999941, 5.042177533603999784, 8.702224267793999601 ) ) ;
#30306=CARTESIAN_POINT ( 'NONE',  ( 9.178620280414001797, 2.990001567622999623, -8.695425648791999862 ) ) ;
#30307=CARTESIAN_POINT ( 'NONE',  ( 2.446810385560000078, 2.013401216687999984, -2.977891740175000024 ) ) ;
#30309=DIRECTION ( 'NONE',  ( 0.5298945043518936693, -0.5996714848441926371, -0.5996715138493925457 ) ) ;
#30312=EDGE_CURVE ( 'NONE', #45966, #7152, #15745, .T. ) ;
#30314=CARTESIAN_POINT ( 'NONE',  ( 10.33467135001178860, 5.744925381912087126, -7.383168082734888671 ) ) ;
#30318=CARTESIAN_POINT ( 'NONE',  ( 10.71256887705999894, 5.951815279772000089, 7.233043586354999555 ) ) ;
#30321=CARTESIAN_POINT ( 'NONE',  ( 11.02452225494999993, 2.775477745048999800, -6.571291218949999902 ) ) ;
#30333=CARTESIAN_POINT ( 'NONE',  ( 8.536962618768443534, 5.285878940952796867, -7.027227351473634975 ) ) ;
#30335=ORIENTED_EDGE ( 'NONE', *, *, #59901, .F. ) ;
#30339=AXIS2_PLACEMENT_3D ( 'NONE', #6450, #54002, #47742 ) ;
#30340=CARTESIAN_POINT ( 'NONE',  ( 10.73615471958999912, 3.078044734341000233, -6.088740491863000592 ) ) ;
#30346=CARTESIAN_POINT ( 'NONE',  ( 8.162581873609997984, 3.457979189883997329, 6.166988478103001547 ) ) ;
#30347=VERTEX_POINT ( 'NONE', #43696 ) ;
#30349=CARTESIAN_POINT ( 'NONE',  ( 7.268539158768000163, 5.563598295091999546, -6.420781807775999717 ) ) ;
#30355=DIRECTION ( 'NONE',  ( 0.000000000000000000, 0.000000000000000000, -1.000000000000000000 ) ) ;
#30356=ORIENTED_EDGE ( 'NONE', *, *, #42234, .T. ) ;
#30358=ORIENTED_EDGE ( 'NONE', *, *, #41513, .T. ) ;
#30360=CARTESIAN_POINT ( 'NONE',  ( 8.546960841229999772, 2.724453559418999582, -8.908010318766001134 ) ) ;
#30365=CARTESIAN_POINT ( 'NONE',  ( 9.298698341228998743, 5.159258275969999197, 9.109498396691998678 ) ) ;
#30367=CARTESIAN_POINT ( 'NONE',  ( 3.500000000000000000, -3.070497928137199128, 0.6771155813265552492 ) ) ;
#30370=DIRECTION ( 'NONE',  ( 1.000000000000000000, 0.000000000000000000, 1.736057635189999993E-14 ) ) ;
#30375=CARTESIAN_POINT ( 'NONE',  ( 6.401834305184006091, 10.52691165332000089, -4.501978947072999837 ) ) ;
#30388=CARTESIAN_POINT ( 'NONE',  ( 9.792312867577999569, 4.284154069364999984, -9.000485152170000447 ) ) ;
#30389=DIRECTION ( 'NONE',  ( -1.000000000000000000, 0.000000000000000000, 0.000000000000000000 ) ) ;
#30393=CARTESIAN_POINT ( 'NONE',  ( 11.06923869026000062, 5.425682056982999768, 8.012911262916999178 ) ) ;
#30397=CARTESIAN_POINT ( 'NONE',  ( 9.409314688805999083, 2.634692233435000031, 8.920311306029999443 ) ) ;
#30400=CARTESIAN_POINT ( 'NONE',  ( 10.79500540879000070, 3.503955365545999623, 6.168588659884999714 ) ) ;
#30402=CARTESIAN_POINT ( 'NONE',  ( 8.672510841228998402, 4.686731264770999772, -8.717075579553000608 ) ) ;
#30405=CARTESIAN_POINT ( 'NONE',  ( 7.711426658771000753, 5.797099724369999763, 8.340484548805999765 ) ) ;
#30406=CARTESIAN_POINT ( 'NONE',  ( 9.166073843917999397, 4.023333628930999772, 9.122276991855001071 ) ) ;
#30408=ORIENTED_EDGE ( 'NONE', *, *, #40190, .F. ) ;
#30409=CARTESIAN_POINT ( 'NONE',  ( 10.10682028041000002, 4.294368353031000396, -8.968663198664000191 ) ) ;
#30416=ORIENTED_EDGE ( 'NONE', *, *, #20847, .T. ) ;
#30418=CARTESIAN_POINT ( 'NONE',  ( 2.302021397264000235, -0.3042438094541999871, -3.579344195347000213 ) ) ;
#30422=CARTESIAN_POINT ( 'NONE',  ( 8.921614158776000281, 3.251172436837000301, -6.320036569851000152 ) ) ;
#30431=CARTESIAN_POINT ( 'NONE',  ( 7.828420280408998622, 5.524123123935000379, 6.910361319981999095 ) ) ;
#30436=CARTESIAN_POINT ( 'NONE',  ( 1.223519645392000088, 0.8784043042010000191, 3.483138632238000021 ) ) ;
#30438=CARTESIAN_POINT ( 'NONE',  ( 4.500000000000000000, 0.000000000000000000, 0.000000000000000000 ) ) ;
#30441=CARTESIAN_POINT ( 'NONE',  ( 9.667078842372998082, 4.541623431405000133, 5.824038024834000460 ) ) ;
#30446=CARTESIAN_POINT ( 'NONE',  ( 8.518741573454621019, 2.828840032196707988, 6.174218200494118847 ) ) ;
#30450=VERTEX_POINT ( 'NONE', #53411 ) ;
#30451=ORIENTED_EDGE ( 'NONE', *, *, #55055, .F. ) ;
#30452=DIRECTION ( 'NONE',  ( 1.000000000000000000, 0.000000000000000000, 0.000000000000000000 ) ) ;
#30454=CARTESIAN_POINT ( 'NONE',  ( 8.999999695565000124, 12.49999969551000056, -3.568585573319000265E-10 ) ) ;
#30456=CARTESIAN_POINT ( 'NONE',  ( 10.43579914648999996, 2.587602126999999808, 6.390037244031000263 ) ) ;
#30458=LINE ( 'NONE', #13009, #55606 ) ;
#30465=DIRECTION ( 'NONE',  ( -1.000000000000000000, 0.000000000000000000, 0.000000000000000000 ) ) ;
#30477=ORIENTED_EDGE ( 'NONE', *, *, #26611, .F. ) ;
#30484=CARTESIAN_POINT ( 'NONE',  ( 9.447288403127886980, 2.899999999999999911, 6.305985889523069154 ) ) ;
#30490=CARTESIAN_POINT ( 'NONE',  ( 6.966665878461012262, -12.09896511371897176, -3.276379751798359052 ) ) ;
#30493=FACE_OUTER_BOUND ( 'NONE', #39831, .T. ) ;
#30506=CARTESIAN_POINT ( 'NONE',  ( 5.500000000000000000, 0.000000000000000000, 0.000000000000000000 ) ) ;
#30510=CARTESIAN_POINT ( 'NONE',  ( 11.09999999999999964, 2.649999999999999911, -7.500000000000000000 ) ) ;
#30513=CARTESIAN_POINT ( 'NONE',  ( 2.646806799209334482, -0.9161175952574931447, 3.408904368339100710 ) ) ;
#30515=B_SPLINE_CURVE_WITH_KNOTS ( 'NONE', 3,
 ( #42779, #53612, #38216, #64426, #59545, #63747, #16548, #37528, #63403, #32304, #47342, #32639, #6052, #22137, #21111, #20765, #53949, #27391, #43478, #15859, #32981, #54295, #6397 ),
 .UNSPECIFIED., .F., .F.,
 ( 4, 2, 2, 2, 2, 2, 2, 2, 2, 1, 2, 4 ),
 ( 0.000000000000000000, 0.2499999999999990008, 0.3749999999999970579, 0.4374999999999952816, 0.4687499999999953926, 0.4999999999999955591, 0.7499999999999988898, 0.8749999999999990008, 0.9374999999999977796, 0.9687499999999971134, 0.9843749999999986677, 1.000000000000000000 ),
 .UNSPECIFIED. ) ;
#30520=CARTESIAN_POINT ( 'NONE',  ( 8.972537864292000620, 2.899999999999999911, -6.571291218949999902 ) ) ;
#30523=CARTESIAN_POINT ( 'NONE',  ( 11.09999999999000053, 7.516533755232999603, 6.492360339384999790 ) ) ;
#30524=CARTESIAN_POINT ( 'NONE',  ( 2.435247277619000172, 2.372532593102000043, -2.573147701680999599 ) ) ;
#30525=CARTESIAN_POINT ( 'NONE',  ( 9.791229719590001324, 4.294368353031000396, -8.968663198664000191 ) ) ;
#30528=ORIENTED_EDGE ( 'NONE', *, *, #66350, .T. ) ;
#30536=CARTESIAN_POINT ( 'NONE',  ( 9.837290039650055107, 2.697792955639530810, -7.971619481532576934 ) ) ;
#30537=ADVANCED_FACE ( 'NONE', ( #65953 ), #45683, .F. ) ;
#30541=ORIENTED_EDGE ( 'NONE', *, *, #20828, .F. ) ;
#30543=CARTESIAN_POINT ( 'NONE',  ( 9.933354719590999693, 5.639765292528999829, -8.059103558718000215 ) ) ;
#30544=ORIENTED_EDGE ( 'NONE', *, *, #45539, .F. ) ;
#30545=CARTESIAN_POINT ( 'NONE',  ( 10.48414939117999900, 4.098653981087000631, -9.351365234892998757 ) ) ;
#30554=CARTESIAN_POINT ( 'NONE',  ( 10.31153584123000044, 2.716831823259000078, -7.950163994344000784 ) ) ;
#30562=ORIENTED_EDGE ( 'NONE', *, *, #32992, .T. ) ;
#30564=CARTESIAN_POINT ( 'NONE',  ( 9.825045280412000537, 3.116293075258000478, -6.208411413796000033 ) ) ;
#30565=CARTESIAN_POINT ( 'NONE',  ( 4.399997082757115763, -2.000000000000000000, 2.821984141243951889E-09 ) ) ;
#30566=CARTESIAN_POINT ( 'NONE',  ( 1.050973465875000068, 3.500000000000000000, 0.000000000000000000 ) ) ;
#30571=CARTESIAN_POINT ( 'NONE',  ( 8.634347174277479553, 5.179539635115185447, 6.206398391140019122 ) ) ;
#30576=ADVANCED_FACE ( 'NONE', ( #40099 ), #33818, .F. ) ;
#30584=CARTESIAN_POINT ( 'NONE',  ( 10.20448674122272337, 2.648429362731234082, 7.853061647120905597 ) ) ;
#30586=CARTESIAN_POINT ( 'NONE',  ( 7.960542845103298681, 2.951378269640129393, -6.549292586381456616 ) ) ;
#30587=B_SPLINE_CURVE_WITH_KNOTS ( 'NONE', 3,
 ( #35945, #42569, #36986, #68780 ),
 .UNSPECIFIED., .F., .F.,
 ( 4, 4 ),
 ( 0.000000000000000000, 1.000000000000000000 ),
 .UNSPECIFIED. ) ;
#30589=DIRECTION ( 'NONE',  ( -1.000000000000000000, 0.000000000000000000, 0.000000000000000000 ) ) ;
#30590=CARTESIAN_POINT ( 'NONE',  ( 3.348657167312000027, 2.653411138596999841, 1.892272653627999901 ) ) ;
#30598=DIRECTION ( 'NONE',  ( -2.317113318597000329E-09, -7.301652274642000223E-12, -1.000000000000000000 ) ) ;
#30602=CARTESIAN_POINT ( 'NONE',  ( 7.806695108664264637, 3.013278973495211677, 6.528997597326380742 ) ) ;
#30604=ORIENTED_EDGE ( 'NONE', *, *, #37813, .T. ) ;
#30608=CARTESIAN_POINT ( 'NONE',  ( 9.299999999999998934, 4.537600397704999899, 9.154563893594000135 ) ) ;
#30614=ADVANCED_FACE ( 'NONE', ( #28221 ), #1648, .T. ) ;
#30616=CARTESIAN_POINT ( 'NONE',  ( 6.835779719590999726, 3.450042761745999886, -8.965148246193999526 ) ) ;
#30628=CARTESIAN_POINT ( 'NONE',  ( 7.954299074928001367, 3.414461172233999697, -6.283593702261001113 ) ) ;
#30629=EDGE_LOOP ( 'NONE', ( #49646, #30720, #278 ) ) ;
#30630=CARTESIAN_POINT ( 'NONE',  ( 10.74163761344578738, 5.515432212743636597, 8.372100252378068319 ) ) ;
#30634=CARTESIAN_POINT ( 'NONE',  ( 3.209306799211167238, -3.058252359239909790, 1.762666431298136382 ) ) ;
#30639=EDGE_LOOP ( 'NONE', ( #52714, #5887 ) ) ;
#30640=CARTESIAN_POINT ( 'NONE',  ( 9.792569055495000896, 3.463432304708999876, 6.184396499233999478 ) ) ;
#30641=EDGE_CURVE ( 'NONE', #3842, #58572, #39393, .T. ) ;
#30642=CYLINDRICAL_SURFACE ( 'NONE', #63502, 1.350000000000000533 ) ;
#30643=CARTESIAN_POINT ( 'NONE',  ( 10.10682028041000002, 4.294368353031000396, -8.968663198664000191 ) ) ;
#30644=CARTESIAN_POINT ( 'NONE',  ( 3.641673371380000024, -3.059358981837999814, 1.788244077786999897 ) ) ;
#30648=ORIENTED_EDGE ( 'NONE', *, *, #24535, .T. ) ;
#30650=CARTESIAN_POINT ( 'NONE',  ( 3.134306799210999195, 1.762666431298139713, 3.058252359239908458 ) ) ;
#30653=CARTESIAN_POINT ( 'NONE',  ( 9.724611353170001138, 2.928305163963000446, 8.718478150869000132 ) ) ;
#30675=CARTESIAN_POINT ( 'NONE',  ( 10.41025778040999938, 4.690688562647999937, -6.142866736126999960 ) ) ;
#30676=ORIENTED_EDGE ( 'NONE', *, *, #64935, .F. ) ;
#30691=EDGE_LOOP ( 'NONE', ( #10602, #42235, #2258, #14772 ) ) ;
#30695=CARTESIAN_POINT ( 'NONE',  ( 2.509306799210165639, 3.058252359239904905, -1.762666431298142600 ) ) ;
#30701=CARTESIAN_POINT ( 'NONE',  ( 7.437260841228000352, 2.216873702600000051, 8.370081218683999680 ) ) ;
#30702=EDGE_CURVE ( 'NONE', #32067, #61556, #32773, .T. ) ;
#30707=ORIENTED_EDGE ( 'NONE', *, *, #42138, .T. ) ;
#30717=CARTESIAN_POINT ( 'NONE',  ( 10.67500447327519097, 2.650284540010591439, 7.500001951671590561 ) ) ;
#30718=CARTESIAN_POINT ( 'NONE',  ( 10.84999882987999875, -2.398081733189999864E-14, -12.49999929738252114 ) ) ;
#30720=ORIENTED_EDGE ( 'NONE', *, *, #56712, .F. ) ;
#30726=CARTESIAN_POINT ( 'NONE',  ( 9.753031682810998859, 4.922927894835999574, -8.639534507509999628 ) ) ;
#30732=CARTESIAN_POINT ( 'NONE',  ( 11.08992526467999973, 5.210543602612999869, 8.327598319864998544 ) ) ;
#30734=CARTESIAN_POINT ( 'NONE',  ( 8.946604883137396769, 4.403857067667214409, -9.229209525869062958 ) ) ;
#30735=VERTEX_POINT ( 'NONE', #35634 ) ;
#30738=CARTESIAN_POINT ( 'NONE',  ( 11.02445190299000011, 3.404087387974999768, 5.822483872269000216 ) ) ;
#30745=CARTESIAN_POINT ( 'NONE',  ( 10.90374609491999891, 3.726846467344000047, 5.900456154266000119 ) ) ;
#30749=CARTESIAN_POINT ( 'NONE',  ( 9.377520280414000098, 4.092867382745001059, -5.937785237406000505 ) ) ;
#30757=CARTESIAN_POINT ( 'NONE',  ( 1.872883852295999851, 2.591090368091000240, -2.487991068387999771 ) ) ;
#30759=CARTESIAN_POINT ( 'NONE',  ( 8.672989158774999652, 4.728328492779000136, -8.692725459657999920 ) ) ;
#30768=ORIENTED_EDGE ( 'NONE', *, *, #58492, .F. ) ;
#30769=CARTESIAN_POINT ( 'NONE',  ( 8.224926658773000554, 5.629399530851999955, 8.631829656822000985 ) ) ;
#30774=CARTESIAN_POINT ( 'NONE',  ( 0.8801993231815000707, 1.717122193005000019, 2.769960469742999809 ) ) ;
#30776=CARTESIAN_POINT ( 'NONE',  ( -15.86200481174999943, -13.87069231928999891, -4.225386915259999654 ) ) ;
#30778=DIRECTION ( 'NONE',  ( -0.000000000000000000, 1.000000000000000000, 0.000000000000000000 ) ) ;
#30779=CARTESIAN_POINT ( 'NONE',  ( 10.09181485429000169, 2.440912084162000006, 7.817367409531000177 ) ) ;
#30786=EDGE_CURVE ( 'NONE', #54722, #46011, #61809, .T. ) ;
#30793=ORIENTED_EDGE ( 'NONE', *, *, #29964, .F. ) ;
#30796=CARTESIAN_POINT ( 'NONE',  ( 9.662551629919999385, 4.094830335839000135, 9.119946295870999364 ) ) ;
#30797=CARTESIAN_POINT ( 'NONE',  ( 10.06728116094000036, 4.192860729918999496, -5.985054792427000336 ) ) ;
#30801=CARTESIAN_POINT ( 'NONE',  ( 9.010251885924715154, 5.224530136624865762, 8.068208678207518858 ) ) ;
#30808=DIRECTION ( 'NONE',  ( 0.000000000000000000, -0.9916377111174247139, 0.1290528957048031888 ) ) ;
#30810=B_SPLINE_CURVE_WITH_KNOTS ( 'NONE', 3,
 ( #42705, #52502, #16129, #58775 ),
 .UNSPECIFIED., .F., .F.,
 ( 4, 4 ),
 ( 0.000000000000000000, 1.000000000000000000 ),
 .UNSPECIFIED. ) ;
#30814=CARTESIAN_POINT ( 'NONE',  ( 10.97571094393200042, 2.824289056067999848, 6.306988371318333897 ) ) ;
#30817=DIRECTION ( 'NONE',  ( -0.8987684456439055669, 0.000000000000000000, -0.4384236320214022764 ) ) ;
#30821=B_SPLINE_CURVE_WITH_KNOTS ( 'NONE', 3,
 ( #48003, #47321, #57799, #32283 ),
 .UNSPECIFIED., .F., .F.,
 ( 4, 4 ),
 ( 0.000000000000000000, 1.000000000000000000 ),
 .UNSPECIFIED. ) ;
#30825=CONICAL_SURFACE ( 'NONE', #68733, 1.949999999867999767, 0.7853981633972997312 ) ;
#30828=CARTESIAN_POINT ( 'NONE',  ( 0.3266986677754999957, 3.021985743044000028, 1.081096232840000004 ) ) ;
#30833=CARTESIAN_POINT ( 'NONE',  ( 9.934999999999998721, 4.640430492595999823, -9.117542781427999898 ) ) ;
#30834=B_SPLINE_CURVE_WITH_KNOTS ( 'NONE', 3,
 ( #22809, #33315, #18270, #65456 ),
 .UNSPECIFIED., .F., .F.,
 ( 4, 4 ),
 ( 0.000000000000000000, 1.000000000000000000 ),
 .UNSPECIFIED. ) ;
#30835=CARTESIAN_POINT ( 'NONE',  ( 11.12964528040999923, 3.869081149487999749, -9.017143166339000260 ) ) ;
#30837=CARTESIAN_POINT ( 'NONE',  ( 7.100000000000000533, 4.000000000000000000, -7.500000000000000000 ) ) ;
#30839=CARTESIAN_POINT ( 'NONE',  ( 8.817462135714999150, 5.100000000000000533, 6.571291218949999902 ) ) ;
#30850=CARTESIAN_POINT ( 'NONE',  ( 8.154557834963361174, 3.119004674881718397, 6.266135323581367267 ) ) ;
#30871=CARTESIAN_POINT ( 'NONE',  ( 9.301695280414000067, 5.619431609641999614, -8.115423117607999615 ) ) ;
#30874=CIRCLE ( 'NONE', #24132, 1.999999999999999556 ) ;
#30876=CARTESIAN_POINT ( 'NONE',  ( 7.974113208588001100, 4.561154361229000642, -6.272154006859000930 ) ) ;
#30878=ORIENTED_EDGE ( 'NONE', *, *, #55793, .F. ) ;
#30888=CARTESIAN_POINT ( 'NONE',  ( 8.441604719589999917, 5.473983809665999622, -8.180077404516000072 ) ) ;
#30890=CARTESIAN_POINT ( 'NONE',  ( 10.70780830849999887, 5.157484706885999692, -6.267808298721999627 ) ) ;
#30896=DIRECTION ( 'NONE',  ( 0.000000000000000000, 0.8897496663238059211, -0.4564488265695026969 ) ) ;
#30901=CARTESIAN_POINT ( 'NONE',  ( 8.699680597014879169, 3.656951845173556315, -5.776565596854453588 ) ) ;
#30910=CARTESIAN_POINT ( 'NONE',  ( 9.874770280412001000, 4.038835765825999680, -5.935509327774999733 ) ) ;
#30919=CARTESIAN_POINT ( 'NONE',  ( 8.701589129073576956, 5.750364994161538235, 7.524138884631350166 ) ) ;
#30920=LINE ( 'NONE', #26363, #34163 ) ;
#30923=CARTESIAN_POINT ( 'NONE',  ( 10.13706886426420084, 2.899999999999999911, 6.444141223280826836 ) ) ;
#30928=CARTESIAN_POINT ( 'NONE',  ( 7.951755279714369351, 4.908718838353461678, 6.393521497924140817 ) ) ;
#30932=CARTESIAN_POINT ( 'NONE',  ( 10.05882936267886940, 4.704418606475568865, 8.703716202581716743 ) ) ;
#30938=CARTESIAN_POINT ( 'NONE',  ( 2.633427925697999772, -1.603367949813999882, -2.837339924868000463 ) ) ;
#30943=CARTESIAN_POINT ( 'NONE',  ( 3.499564475844618272, 0.6826263220198214299, -3.360566866257050922 ) ) ;
#30957=ORIENTED_EDGE ( 'NONE', *, *, #68504, .T. ) ;
#30961=CARTESIAN_POINT ( 'NONE',  ( 9.050000000000000711, 7.679126935408000065, 5.093340497782000043 ) ) ;
#30964=LINE ( 'NONE', #62757, #41652 ) ;
#30965=CARTESIAN_POINT ( 'NONE',  ( 7.871145280405000833, 4.569394889178999719, -9.136182695123999054 ) ) ;
#30971=B_SPLINE_CURVE_WITH_KNOTS ( 'NONE', 3,
 ( #49838, #21877, #12089, #60672 ),
 .UNSPECIFIED., .F., .F.,
 ( 4, 4 ),
 ( 0.000000000000000000, 1.000000000000000000 ),
 .UNSPECIFIED. ) ;
#30974=VERTEX_POINT ( 'NONE', #35167 ) ;
#30977=CARTESIAN_POINT ( 'NONE',  ( 8.972537864292000620, 2.899999999999999911, -6.571291218949999902 ) ) ;
#30983=CARTESIAN_POINT ( 'NONE',  ( 8.753040873196827221, 3.779878465243081465, -5.822439910017921605 ) ) ;
#30989=ORIENTED_EDGE ( 'NONE', *, *, #52271, .T. ) ;
#30991=ORIENTED_EDGE ( 'NONE', *, *, #33706, .F. ) ;
#30992=CARTESIAN_POINT ( 'NONE',  ( 10.57224177473000104, 4.020426023752999178, 8.920668579831000145 ) ) ;
#30993=CARTESIAN_POINT ( 'NONE',  ( 9.074999999999999289, 4.417172942406000224, 8.783926296998000538 ) ) ;
#30995=CARTESIAN_POINT ( 'NONE',  ( 3.264420700083999982, -1.874241925158999900, -3.007514872430000263 ) ) ;
#31002=CARTESIAN_POINT ( 'NONE',  ( 3.228056799210624384, -2.150913519912213800, 2.798833948393621540 ) ) ;
#31004=LINE ( 'NONE', #40793, #56718 ) ;
#31005=CARTESIAN_POINT ( 'NONE',  ( 9.261662452849000360, 2.944259351255000379, 6.507396354981000108 ) ) ;
#31012=EDGE_CURVE ( 'NONE', #6055, #57932, #17440, .T. ) ;
#31018=CARTESIAN_POINT ( 'NONE',  ( 0.2554390818521176665, 0.8426791852790889159, -3.173196348029862612 ) ) ;
#31023=CARTESIAN_POINT ( 'NONE',  ( 5.000030787343000327, -2.099962892530999881, 0.000000000000000000 ) ) ;
#31026=CARTESIAN_POINT ( 'NONE',  ( 0.3210591298330999765, 2.092960143115000005, 2.433246087927000367 ) ) ;
#31028=CARTESIAN_POINT ( 'NONE',  ( 10.81187971959000116, 4.614148948243999904, -5.930135044105000475 ) ) ;
#31031=CONICAL_SURFACE ( 'NONE', #25481, 13.04999999969999891, 0.7853981633972997312 ) ;
#31035=CARTESIAN_POINT ( 'NONE',  ( 9.341490007895000502, 4.148133901461999784, 9.337478696773001019 ) ) ;
#31036=VERTEX_POINT ( 'NONE', #22674 ) ;
#31049=CARTESIAN_POINT ( 'NONE',  ( 8.646410841231000788, 2.261390688294000029, -6.733978371730000134 ) ) ;
#31054=CARTESIAN_POINT ( 'NONE',  ( 8.116920280410999666, 5.773189794777000117, 7.141495931231999883 ) ) ;
#31072=EDGE_LOOP ( 'NONE', ( #20421, #63091, #30274, #13200, #42873, #57944, #10405, #50487, #51425, #19491, #31311, #27865, #1078, #34729, #54283, #56129, #4957, #49459, #58270, #25979, #51449, #49787, #14533 ) ) ;
#31076=CARTESIAN_POINT ( 'NONE',  ( 10.90000658885999840, -1.199999999999999956, 9.776630298829998011 ) ) ;
#31077=CARTESIAN_POINT ( 'NONE',  ( 4.900006121742000786, 2.000000000000000888, 0.2617993877991453555 ) ) ;
#31078=CARTESIAN_POINT ( 'NONE',  ( 11.08752642792000032, 2.871528932589999972, -6.302908019754999813 ) ) ;
#31080=CARTESIAN_POINT ( 'NONE',  ( 8.616995677562000466, 4.876077402042000131, 5.996974966532000018 ) ) ;
#31083=CARTESIAN_POINT ( 'NONE',  ( 9.696080515601000371, 2.554416243104999928, 7.600685069647000525 ) ) ;
#31087=ORIENTED_EDGE ( 'NONE', *, *, #65898, .T. ) ;
#31090=CARTESIAN_POINT ( 'NONE',  ( 10.55813337864000090, 2.466561068647000532, 6.633529813744000414 ) ) ;
#31099=CARTESIAN_POINT ( 'NONE',  ( 9.882259685352000389, 4.932708901218999742, 6.390989635557000170 ) ) ;
#31102=CARTESIAN_POINT ( 'NONE',  ( 9.079170280414000871, 4.815598936798999752, -8.835641302565999666 ) ) ;
#31107=CARTESIAN_POINT ( 'NONE',  ( 9.261037412837582750, 3.646685539694229039, -8.850715144363563880 ) ) ;
#31112=CARTESIAN_POINT ( 'NONE',  ( 7.950760841228999176, 2.095715612964000218, 8.056490963156001328 ) ) ;
#31114=CARTESIAN_POINT ( 'NONE',  ( 10.01279489264886458, 2.761698732461363104, 6.264380212190736152 ) ) ;
#31119=CARTESIAN_POINT ( 'NONE',  ( 9.532678149083000818, 4.663044775770000427, 8.669813205957000335 ) ) ;
#31124=ORIENTED_EDGE ( 'NONE', *, *, #58477, .F. ) ;
#31125=CARTESIAN_POINT ( 'NONE',  ( 8.930989158774000458, 2.019067547072999957, 7.390982789861999969 ) ) ;
#31128=CARTESIAN_POINT ( 'NONE',  ( 10.02314899745999988, 5.167567567567999731, -6.822293592207000934 ) ) ;
#31136=CARTESIAN_POINT ( 'NONE',  ( 9.781673028307999118, 5.464749740720999505, 8.817329433105999925 ) ) ;
#31139=EDGE_LOOP ( 'NONE', ( #61234, #53453, #20928, #12122, #1979, #32427 ) ) ;
#31155=CARTESIAN_POINT ( 'NONE',  ( 9.228133567168001150, 2.875367362387999837, 8.669940206484001877 ) ) ;
#31156=CARTESIAN_POINT ( 'NONE',  ( 9.961465797930001642, 2.787126709928999801, -8.677707706574000923 ) ) ;
#31161=CARTESIAN_POINT ( 'NONE',  ( 9.044058817429487362, 4.875265736440850262, 8.528255781230162924 ) ) ;
#31164=ORIENTED_EDGE ( 'NONE', *, *, #48377, .F. ) ;
#31171=VECTOR ( 'NONE', #59291, 1000.000000000000114 ) ;
#31174=VERTEX_POINT ( 'NONE', #41250 ) ;
#31177=LINE ( 'NONE', #1071, #58265 ) ;
#31182=FACE_OUTER_BOUND ( 'NONE', #40843, .T. ) ;
#31189=CARTESIAN_POINT ( 'NONE',  ( 10.22907665877000127, 4.838498214728000235, -5.852435699035000383 ) ) ;
#31195=ORIENTED_EDGE ( 'NONE', *, *, #2485, .F. ) ;
#31200=CYLINDRICAL_SURFACE ( 'NONE', #33259, 1.999999999999999556 ) ;
#31203=DIRECTION ( 'NONE',  ( 1.000000000000000000, 0.000000000000000000, 0.000000000000000000 ) ) ;
#31214=CARTESIAN_POINT ( 'NONE',  ( 7.895830451470996714, 3.177662910779999628, 6.240430379278997464 ) ) ;
#31220=CARTESIAN_POINT ( 'NONE',  ( 11.10000000031000056, 8.466679424687001188, 6.746294355622000083 ) ) ;
#31221=CARTESIAN_POINT ( 'NONE',  ( 2.800973465877999669, -3.500000000000000000, 0.000000000000000000 ) ) ;
#31223=CARTESIAN_POINT ( 'NONE',  ( 9.202245280414000916, 5.095038542659000136, -6.157541456184000062 ) ) ;
#31225=EDGE_LOOP ( 'NONE', ( #43247, #7643, #63200, #60817 ) ) ;
#31231=CARTESIAN_POINT ( 'NONE',  ( 9.989493109327902687, 3.453294174495602054, -9.227563350567775657 ) ) ;
#31234=DIRECTION ( 'NONE',  ( -2.820458616744058146E-07, 2.816894698951058879E-07, -0.9999999999999205080 ) ) ;
#31235=CARTESIAN_POINT ( 'NONE',  ( 11.09999999999999964, 6.351820664109999903, 5.386194068259000822 ) ) ;
#31238=CARTESIAN_POINT ( 'NONE',  ( 9.228345280414000484, 2.481540185810000132, -7.878707153279001396 ) ) ;
#31241=CARTESIAN_POINT ( 'NONE',  ( 9.961465797930001642, 2.787126709928999801, -8.677707706574000923 ) ) ;
#31247=CARTESIAN_POINT ( 'NONE',  ( 8.564263637668691587, 2.982766295838745307, 6.174911310893544503 ) ) ;
#31252=CARTESIAN_POINT ( 'NONE',  ( 11.09999999999999964, 4.000000000000000000, 7.500000000000000000 ) ) ;
#31258=CARTESIAN_POINT ( 'NONE',  ( 8.880270280412998929, 4.146787477634999775, -5.941926545671999627 ) ) ;
#31262=EDGE_CURVE ( 'NONE', #13611, #7244, #3754, .T. ) ;
#31263=ADVANCED_FACE ( 'NONE', ( #9420 ), #8918, .F. ) ;
#31267=CARTESIAN_POINT ( 'NONE',  ( 8.903314993461870941, 2.546304713195970848, 8.472542641376174188 ) ) ;
#31269=ORIENTED_EDGE ( 'NONE', *, *, #53449, .T. ) ;
#31278=AXIS2_PLACEMENT_3D ( 'NONE', #19181, #18849, #34243 ) ;
#31279=CARTESIAN_POINT ( 'NONE',  ( 7.993989691196518699, 3.116233090823458340, -6.353578959360522305 ) ) ;
#31286=CARTESIAN_POINT ( 'NONE',  ( 2.204290380730999921, 1.127589919772999938, -2.855189883873000323 ) ) ;
#31291=CARTESIAN_POINT ( 'NONE',  ( 3.499604618624656105, -0.6504880270822478439, -3.309912210867942850 ) ) ;
#31292=CARTESIAN_POINT ( 'NONE',  ( 4.500000125099000492, 1.829647544581999737E-13, -12.99999867215000116 ) ) ;
#31294=DIRECTION ( 'NONE',  ( 0.8480635683783770418, 0.000000000000000000, 0.5298945026977860406 ) ) ;
#31298=CARTESIAN_POINT ( 'NONE',  ( 7.735197674916334698, 3.263818714402415111, -8.649421172292802495 ) ) ;
#31307=CARTESIAN_POINT ( 'NONE',  ( 8.265163602278375876, 3.125207522424720885, -6.192262357212721113 ) ) ;
#31308=CARTESIAN_POINT ( 'NONE',  ( 8.078904719588999583, 4.421485762723999180, -5.992852494763999616 ) ) ;
#31311=ORIENTED_EDGE ( 'NONE', *, *, #5306, .T. ) ;
#31331=CARTESIAN_POINT ( 'NONE',  ( 11.18706938844999854, 3.186790175674999670, 6.232702730851999995 ) ) ;
#31332=AXIS2_PLACEMENT_3D ( 'NONE', #17072, #315, #21974 ) ;
#31334=CARTESIAN_POINT ( 'NONE',  ( 8.821685841230998193, 2.633142096252999664, -7.791134854666999843 ) ) ;
#31337=CARTESIAN_POINT ( 'NONE',  ( 8.073389927753067852, 5.122947197419580156, -6.729807961493258439 ) ) ;
#31344=EDGE_CURVE ( 'NONE', #38028, #31922, #38513, .T. ) ;
#31346=CARTESIAN_POINT ( 'NONE',  ( 10.81315553411000074, 3.756074350075000012, 6.071610008629000355 ) ) ;
#31349=EDGE_CURVE ( 'NONE', #20987, #68613, #10164, .T. ) ;
#31358=CARTESIAN_POINT ( 'NONE',  ( 8.142589158771000868, 5.074768364528000397, -8.296267706722000312 ) ) ;
#31359=B_SPLINE_CURVE_WITH_KNOTS ( 'NONE', 3,
 ( #16911, #5399, #153, #64449 ),
 .UNSPECIFIED., .F., .F.,
 ( 4, 4 ),
 ( 0.000000000000000000, 1.000000000000000000 ),
 .UNSPECIFIED. ) ;
#31360=CARTESIAN_POINT ( 'NONE',  ( 8.158337970077000990E-06, 0.000000000000000000, -2.999989272562999965 ) ) ;
#31363=CARTESIAN_POINT ( 'NONE',  ( 0.2059889680762000130, -0.5148121778627998690, -3.334029978310999898 ) ) ;
#31367=CARTESIAN_POINT ( 'NONE',  ( 10.10735778041000010, 4.293584699549000128, -8.994197232567001876 ) ) ;
#31372=DIRECTION ( 'NONE',  ( 1.000000000000000000, 0.000000000000000000, 0.000000000000000000 ) ) ;
#31373=CARTESIAN_POINT ( 'NONE',  ( 7.330281674562000305, 4.426928431836000044, 9.293321981113999541 ) ) ;
#31376=CARTESIAN_POINT ( 'NONE',  ( 6.920464158770999852, 4.499022151374000522, -9.333214642871000777 ) ) ;
#31384=CARTESIAN_POINT ( 'NONE',  ( 7.613512347206999209, 10.68273724490999932, -3.841609246918000320 ) ) ;
#31393=CARTESIAN_POINT ( 'NONE',  ( 8.347267219593000220, 2.741641653469999884, 6.457329666915000210 ) ) ;
#31394=VERTEX_POINT ( 'NONE', #46069 ) ;
#31395=CARTESIAN_POINT ( 'NONE',  ( 10.85685100254000091, 2.832432432432000269, -6.822293592207000934 ) ) ;
#31400=CARTESIAN_POINT ( 'NONE',  ( 10.86919096481999780, 8.268617798044999745, -7.016197574546996663 ) ) ;
#31403=CARTESIAN_POINT ( 'NONE',  ( 10.90000004630000063, 9.856474695503001371, 5.627825000517000298 ) ) ;
#31410=ORIENTED_EDGE ( 'NONE', *, *, #35618, .F. ) ;
#31416=CARTESIAN_POINT ( 'NONE',  ( 10.85290485628999946, 3.170386876061999537, -8.782184998573001167 ) ) ;
#31420=CARTESIAN_POINT ( 'NONE',  ( 10.87521525736000072, 4.831064930369000088, 6.312796576761000367 ) ) ;
#31425=CARTESIAN_POINT ( 'NONE',  ( 9.657553581808000942, 5.333455947841000189, 6.049916795084000043 ) ) ;
#31427=CARTESIAN_POINT ( 'NONE',  ( 10.61382428715999993, 3.385080336122999967, 5.849521480782000182 ) ) ;
#31429=CARTESIAN_POINT ( 'NONE',  ( 9.816185841232000442, 2.656512020013999997, -7.884832994446999699 ) ) ;
#31430=CARTESIAN_POINT ( 'NONE',  ( 11.14445592698000098, 10.08445635709999877, -5.720398172012999716 ) ) ;
#31433=AXIS2_PLACEMENT_3D ( 'NONE', #40935, #13689, #3520 ) ;
#31434=CARTESIAN_POINT ( 'NONE',  ( 9.251926658770999623, 5.159258275969999197, 9.109498396691998678 ) ) ;
#31435=CARTESIAN_POINT ( 'NONE',  ( 10.19255830160000009, 2.560287027313000063, 7.664549200117999561 ) ) ;
#31437=EDGE_LOOP ( 'NONE', ( #52675, #2997, #18769, #20123 ) ) ;
#31438=CARTESIAN_POINT ( 'NONE',  ( 8.532195280408998883, 5.331510020787000315, -8.114341808290998159 ) ) ;
#31439=FACE_OUTER_BOUND ( 'NONE', #35751, .T. ) ;
#31441=CARTESIAN_POINT ( 'NONE',  ( 9.354766166764603597, 2.650157509278342705, -7.676821081800753177 ) ) ;
#31446=CARTESIAN_POINT ( 'NONE',  ( 8.528448341230999930, 2.472348777564000066, 6.234194744024999402 ) ) ;
#31448=CARTESIAN_POINT ( 'NONE',  ( 8.573539158775000502, 5.361622798585000460, -7.185294144754000634 ) ) ;
#31452=CARTESIAN_POINT ( 'NONE',  ( 9.646287586158999616, 2.591467678478000192, 6.760055064032999717 ) ) ;
#31459=CARTESIAN_POINT ( 'NONE',  ( 8.353301658773000682, 2.800103557244999930, 9.079946116129001155 ) ) ;
#31460=CARTESIAN_POINT ( 'NONE',  ( 9.317462135714000837, 5.100000000000000533, 6.571291218949999902 ) ) ;
#31461=CARTESIAN_POINT ( 'NONE',  ( 10.36503728015293646, 2.650011783304074164, -7.500002219258057323 ) ) ;
#31464=CARTESIAN_POINT ( 'NONE',  ( 2.119930008642999741, -2.059315964850999769, -2.525946829712999886 ) ) ;
#31468=CARTESIAN_POINT ( 'NONE',  ( 0.000000000000000000, 5.100000000000000533, 7.500000000000000000 ) ) ;
#31469=CARTESIAN_POINT ( 'NONE',  ( 9.743561007103998861, 5.287400066955999733, 8.939966147452000911 ) ) ;
#31473=LINE ( 'NONE', #68510, #22628 ) ;
#31476=CARTESIAN_POINT ( 'NONE',  ( 8.609219020791252674, 4.708310599750610947, 5.912357210627167348 ) ) ;
#31480=CARTESIAN_POINT ( 'NONE',  ( 9.725191424783275806, 2.649754699899339538, 7.500009801425228773 ) ) ;
#31481=ORIENTED_EDGE ( 'NONE', *, *, #20828, .T. ) ;
#31485=CARTESIAN_POINT ( 'NONE',  ( 11.06133897141000055, 2.503910831767000023, -6.712778933675999760 ) ) ;
#31487=EDGE_CURVE ( 'NONE', #23058, #22260, #16092, .T. ) ;
#31489=ADVANCED_FACE ( 'NONE', ( #57933 ), #66299, .T. ) ;
#31491=CARTESIAN_POINT ( 'NONE',  ( 9.040103201076165718, 4.925662930945876816, 8.482493365444813804 ) ) ;
#31495=CARTESIAN_POINT ( 'NONE',  ( 8.662857780412000608, 2.741641653469999884, 6.457329666915000210 ) ) ;
#31496=ORIENTED_EDGE ( 'NONE', *, *, #50938, .F. ) ;
#31497=CARTESIAN_POINT ( 'NONE',  ( 11.10000000000000142, 2.290061757222789041, -7.204632786817215084 ) ) ;
#31498=CARTESIAN_POINT ( 'NONE',  ( 9.231612604287846580, 2.652298733595448432, 7.391242544803094283 ) ) ;
#31503=DIRECTION ( 'NONE',  ( -1.782458877139945186E-07, 1.777825404087945614E-07, -0.9999999999999682476 ) ) ;
#31508=CARTESIAN_POINT ( 'NONE',  ( 11.09999233421999953, -1.199999999999999956, -9.776630298829998011 ) ) ;
#31514=CARTESIAN_POINT ( 'NONE',  ( 0.7380201129275000271, 2.302377811826000098, -2.236047032684999714 ) ) ;
#31515=B_SPLINE_CURVE_WITH_KNOTS ( 'NONE', 3,
 ( #63640, #5943, #4567, #10849, #63977 ),
 .UNSPECIFIED., .F., .F.,
 ( 4, 1, 4 ),
 ( 0.000000000000000000, 0.5000000000000000000, 1.000000000000000000 ),
 .UNSPECIFIED. ) ;
#31520=CARTESIAN_POINT ( 'NONE',  ( 8.066302634316002695, 3.111242948840002409, -6.203702194951995708 ) ) ;
#31521=CARTESIAN_POINT ( 'NONE',  ( 11.15264221959000146, 2.317063201199000222, -7.596564358366999947 ) ) ;
#31527=AXIS2_PLACEMENT_3D ( 'NONE', #46221, #51459, #19651 ) ;
#31530=EDGE_CURVE ( 'NONE', #9263, #23594, #68593, .T. ) ;
#31542=CARTESIAN_POINT ( 'NONE',  ( 6.999999692251999583, -12.89129024476000041, -1.677687640358999976 ) ) ;
#31546=CARTESIAN_POINT ( 'NONE',  ( 8.601133948506207716, 4.977182018904446892, 6.107802660072452205 ) ) ;
#31549=CARTESIAN_POINT ( 'NONE',  ( 9.112942518363999156, 5.100000000000000533, 6.192000867487999827 ) ) ;
#31559=CARTESIAN_POINT ( 'NONE',  ( 9.699495280410998177, 5.048004622677000341, -6.120508709481000231 ) ) ;
#31573=ORIENTED_EDGE ( 'NONE', *, *, #28372, .T. ) ;
#31575=EDGE_CURVE ( 'NONE', #33797, #32376, #55243, .T. ) ;
#31577=CARTESIAN_POINT ( 'NONE',  ( 8.871410841230998656, 2.721111233225000259, -6.936528696292000085 ) ) ;
#31580=DIRECTION ( 'NONE',  ( 1.000000000000000000, 0.000000000000000000, 7.549516567279000659E-14 ) ) ;
#31597=ORIENTED_EDGE ( 'NONE', *, *, #36662, .T. ) ;
#31599=CARTESIAN_POINT ( 'NONE',  ( 10.14395937989721652, 4.746860684429531574, -8.656482714661228428 ) ) ;
#31609=CARTESIAN_POINT ( 'NONE',  ( 2.716664739337339540, 2.750000000000000000, 3.881524028221258434E-10 ) ) ;
#31614=ADVANCED_FACE ( 'NONE', ( #3422 ), #10503, .T. ) ;
#31618=CARTESIAN_POINT ( 'NONE',  ( 7.986960674332891585, 3.285250301221325664, -6.274837602397500547 ) ) ;
#31632=ORIENTED_EDGE ( 'NONE', *, *, #58477, .T. ) ;
#31637=CARTESIAN_POINT ( 'NONE',  ( 10.70440763476387680, 2.684940916868421734, 7.852706794445638572 ) ) ;
#31639=ORIENTED_EDGE ( 'NONE', *, *, #20780, .T. ) ;
#31647=CARTESIAN_POINT ( 'NONE',  ( 8.657436137450503111, 2.838366281656380608, -6.183390965021622776 ) ) ;
#31649=CARTESIAN_POINT ( 'NONE',  ( 7.432479719588999778, 2.435036720175999925, -7.494591853605999887 ) ) ;
#31651=CARTESIAN_POINT ( 'NONE',  ( 7.156825054363874727, 5.205086695061690527, -8.205119277360076069 ) ) ;
#31658=CARTESIAN_POINT ( 'NONE',  ( 5.500000000000000000, -13.87069231928999891, 4.225386915259999654 ) ) ;
#31659=ORIENTED_EDGE ( 'NONE', *, *, #18280, .T. ) ;
#31661=LINE ( 'NONE', #51596, #57120 ) ;
#31663=CARTESIAN_POINT ( 'NONE',  ( 2.250973465874000379, -3.500000000000000000, 0.000000000000000000 ) ) ;
#31673=CARTESIAN_POINT ( 'NONE',  ( 11.03856029907000114, 2.974095820320000083, 8.716122353065999917 ) ) ;
#31674=LINE ( 'NONE', #43190, #41799 ) ;
#31677=CARTESIAN_POINT ( 'NONE',  ( 8.639360841228999277, 5.074768364528000397, -8.296267706722000312 ) ) ;
#31678=CARTESIAN_POINT ( 'NONE',  ( 10.08728840308773300, 2.899999999999999911, -6.305985889617788942 ) ) ;
#31686=CARTESIAN_POINT ( 'NONE',  ( 3.196806799210749617, -0.9161175952574931447, 3.408904368339101598 ) ) ;
#31689=DIRECTION ( 'NONE',  ( 1.000000000000000000, 0.000000000000000000, 0.000000000000000000 ) ) ;
#31700=CARTESIAN_POINT ( 'NONE',  ( 8.971339158776000744, 4.082930418187999955, -6.104944817728999773 ) ) ;
#31702=B_SPLINE_CURVE_WITH_KNOTS ( 'NONE', 3,
 ( #2945, #24278, #41727, #30901, #29890 ),
 .UNSPECIFIED., .F., .F.,
 ( 4, 1, 4 ),
 ( 0.000000000000000000, 0.3074238982151080157, 1.000000000000000000 ),
 .UNSPECIFIED. ) ;
#31706=VECTOR ( 'NONE', #52400, 1000.000000000000000 ) ;
#31709=CARTESIAN_POINT ( 'NONE',  ( 11.25809834123000108, 3.275514549383000240, -8.650774600386998969 ) ) ;
#31710=EDGE_CURVE ( 'NONE', #44976, #21492, #2601, .T. ) ;
#31717=EDGE_LOOP ( 'NONE', ( #43516, #25827, #48402, #56155, #66021, #63506, #60008, #61119 ) ) ;
#31719=CARTESIAN_POINT ( 'NONE',  ( 8.403354719590000244, 5.730434958826999825, -7.416203477251000820 ) ) ;
#31721=VECTOR ( 'NONE', #15638, 1000.000000000000000 ) ;
#31728=CARTESIAN_POINT ( 'NONE',  ( 10.57226862415000035, 9.951161148090999831, -5.461992367169999696 ) ) ;
#31739=CARTESIAN_POINT ( 'NONE',  ( 8.502045280412000139, 3.869396554003000421, 5.695652484872999466 ) ) ;
#31744=EDGE_CURVE ( 'NONE', #15298, #20015, #42219, .T. ) ;
#31745=CARTESIAN_POINT ( 'NONE',  ( 8.910378124222624763, 5.351542105685659578, 7.263808684111331182 ) ) ;
#31746=CARTESIAN_POINT ( 'NONE',  ( 11.12373268272000004, 5.763386772010999692, -5.184271159621000713 ) ) ;
#31747=ORIENTED_EDGE ( 'NONE', *, *, #59509, .T. ) ;
#31762=CARTESIAN_POINT ( 'NONE',  ( 10.16989991304999918, 2.594216849811000092, -6.291257009166999481 ) ) ;
#31765=LINE ( 'NONE', #32112, #56263 ) ;
#31766=CARTESIAN_POINT ( 'NONE',  ( 8.224593659958996383, 3.074059020428998146, -6.140725432342995838 ) ) ;
#31772=CARTESIAN_POINT ( 'NONE',  ( 10.41185190929999926, 2.101586107686999938, 7.856266936613998553 ) ) ;
#31774=CARTESIAN_POINT ( 'NONE',  ( 9.368660841232999914, 2.702406276695999754, -6.981052078638000147 ) ) ;
#31776=CARTESIAN_POINT ( 'NONE',  ( 11.06165563537000018, 9.156947157375000756, -6.511651601598999584 ) ) ;
#31782=CARTESIAN_POINT ( 'NONE',  ( 9.070310841232000598, 5.361622798585000460, -7.185294144754000634 ) ) ;
#31787=VECTOR ( 'NONE', #46784, 1000.000000000000000 ) ;
#31789=ORIENTED_EDGE ( 'NONE', *, *, #36929, .T. ) ;
#31793=CARTESIAN_POINT ( 'NONE',  ( 8.664129719593997692, 5.524776413195999325, -7.147585171405999915 ) ) ;
#31795=CARTESIAN_POINT ( 'NONE',  ( 10.79353630809276687, 2.899999999999999911, 6.665341197409489382 ) ) ;
#31798=EDGE_CURVE ( 'NONE', #15587, #38721, #65992, .T. ) ;
#31799=CARTESIAN_POINT ( 'NONE',  ( 9.701978494675000064, 3.399139198672999740, 6.026757051093999173 ) ) ;
#31805=CARTESIAN_POINT ( 'NONE',  ( 7.262114158771001193, 4.847807297114000491, 9.065373753110998578 ) ) ;
#31814=CARTESIAN_POINT ( 'NONE',  ( 10.91307008594999850, 2.096286256021000050, 7.827189715349000210 ) ) ;
#31822=CARTESIAN_POINT ( 'NONE',  ( 11.07729151584000071, 2.725326910309999739, -5.088622218232000449 ) ) ;
#31827=CARTESIAN_POINT ( 'NONE',  ( 7.100000000000000533, 5.349999999999999645, 7.500000000000000000 ) ) ;
#31831=VECTOR ( 'NONE', #47347, 1000.000000000000000 ) ;
#31834=CARTESIAN_POINT ( 'NONE',  ( 9.753031682810998859, 4.922927894835999574, -8.639534507509999628 ) ) ;
#31838=CARTESIAN_POINT ( 'NONE',  ( 9.005624905851385975, 5.254615185761620566, 7.997778784833124099 ) ) ;
#31840=CARTESIAN_POINT ( 'NONE',  ( 7.956795280408998750, 4.524487726177000013, 9.047753146378999745 ) ) ;
#31844=CARTESIAN_POINT ( 'NONE',  ( 9.242199581279592735, 2.679961688974304757, 7.218432988884748269 ) ) ;
#31848=B_SPLINE_CURVE_WITH_KNOTS ( 'NONE', 3,
 ( #39200, #55972, #49686, #45141, #1447, #7380, #39548, #60870, #61219, #66451, #1795, #66105, #60523, #34309, #54935, #23112, #18914, #50038 ),
 .UNSPECIFIED., .F., .F.,
 ( 4, 2, 2, 2, 2, 2, 2, 2, 4 ),
 ( 0.1280414556252505165, 0.2236515624513979450, 0.3192616692775453457, 0.4148717761036927465, 0.5104818829298402028, 0.6060919897559874370, 0.7017020965821346712, 0.7973122034082819054, 0.8929223102344291396 ),
 .UNSPECIFIED. ) ;
#31850=CARTESIAN_POINT ( 'NONE',  ( 11.06995268536000054, 8.134787565625000383, 6.681297597381000486 ) ) ;
#31859=B_SPLINE_SURFACE_WITH_KNOTS ( 'NONE', 3, 3, ( 
 ( #5930, #27272, #1731, #60120 ),
 ( #12226, #38444, #44047, #22010 ),
 ( #1049, #64658, #43357, #49626 ),
 ( #44400, #348, #11517, #54174 ),
 ( #17110, #65352, #21665, #42999 ),
 ( #6272, #64307, #16425, #22361 ) ),
 .UNSPECIFIED., .F., .F., .F.,
 ( 4, 1, 1, 4 ),
 ( 4, 4 ),
 ( -0.007877447430640999518, 0.000000000000000000, 0.07142857142856999519, 0.1006818857400000045 ),
 ( -0.1835627100093999986, 1.183562709872999941 ),
 .UNSPECIFIED. ) ;
#31861=B_SPLINE_CURVE_WITH_KNOTS ( 'NONE', 3,
 ( #64524, #45301, #50537, #20012 ),
 .UNSPECIFIED., .F., .F.,
 ( 4, 4 ),
 ( 0.000000000000000000, 1.000000000000000000 ),
 .UNSPECIFIED. ) ;
#31862=CARTESIAN_POINT ( 'NONE',  ( 0.4417688295323000114, -3.296907118028000294, 0.7152224222591000435 ) ) ;
#31868=CARTESIAN_POINT ( 'NONE',  ( 7.686616257283001907, 3.172402717919002413, -6.371572564913001280 ) ) ;
#31869=CARTESIAN_POINT ( 'NONE',  ( 10.43325471958999984, 5.596203146559000530, -8.042024377770999877 ) ) ;
#31873=CARTESIAN_POINT ( 'NONE',  ( 10.10107565221368375, 5.349884357715816385, -7.263395957186810747 ) ) ;
#31882=EDGE_CURVE ( 'NONE', #53057, #61390, #36783, .T. ) ;
#31905=CARTESIAN_POINT ( 'NONE',  ( 8.605545280412000508, 3.122811675949999977, -6.006064052396999919 ) ) ;
#31909=CARTESIAN_POINT ( 'NONE',  ( 11.09999999999999964, 5.299999999999999822, 5.160242730440000258 ) ) ;
#31921=CARTESIAN_POINT ( 'NONE',  ( 9.269210841233000764, 3.098073081301000009, -8.567513114264999174 ) ) ;
#31922=VERTEX_POINT ( 'NONE', #63439 ) ;
#31923=B_SPLINE_CURVE_WITH_KNOTS ( 'NONE', 3,
 ( #48739, #38587, #58879, #22849 ),
 .UNSPECIFIED., .F., .F.,
 ( 4, 4 ),
 ( 0.000000000000000000, 1.000000000000000000 ),
 .UNSPECIFIED. ) ;
#31925=FILL_AREA_STYLE_COLOUR ( '', #48816 ) ;
#31930=ADVANCED_FACE ( 'NONE', ( #54682 ), #422, .T. ) ;
#31940=CARTESIAN_POINT ( 'NONE',  ( 8.549914158773001205, 2.141799395716999843, -7.895788736628000848 ) ) ;
#31943=VERTEX_POINT ( 'NONE', #853 ) ;
#31944=ORIENTED_EDGE ( 'NONE', *, *, #64155, .T. ) ;
#31956=ORIENTED_EDGE ( 'NONE', *, *, #39785, .F. ) ;
#31961=CARTESIAN_POINT ( 'NONE',  ( 8.200000304434999165, -12.49999969551000056, 3.568585274154000017E-10 ) ) ;
#31965=FACE_OUTER_BOUND ( 'NONE', #51866, .T. ) ;
#31966=EDGE_CURVE ( 'NONE', #44325, #61815, #52980, .T. ) ;
#31967=EDGE_CURVE ( 'NONE', #22650, #35088, #65114, .T. ) ;
#31968=B_SPLINE_CURVE_WITH_KNOTS ( 'NONE', 3,
 ( #40663, #8168, #41013, #25275 ),
 .UNSPECIFIED., .F., .F.,
 ( 4, 4 ),
 ( 0.000000000000000000, 1.000000000000000000 ),
 .UNSPECIFIED. ) ;
#31982=CARTESIAN_POINT ( 'NONE',  ( 10.34423739839300715, 2.685214518267480699, -7.853261023685005782 ) ) ;
#31986=CARTESIAN_POINT ( 'NONE',  ( 10.81905590578999998, 2.899999999999999911, -6.571291218949999902 ) ) ;
#31989=CARTESIAN_POINT ( 'NONE',  ( 5.399999743830999677, 12.99045401563999924, 1.690592933733000125 ) ) ;
#31991=ORIENTED_EDGE ( 'NONE', *, *, #29545, .T. ) ;
#32001=B_SPLINE_CURVE_WITH_KNOTS ( 'NONE', 3,
 ( #25009, #20795, #9959, #4011 ),
 .UNSPECIFIED., .F., .F.,
 ( 4, 4 ),
 ( 0.8929223102344291396, 1.000000000000000000 ),
 .UNSPECIFIED. ) ;
#32005=LINE ( 'NONE', #42146, #3865 ) ;
#32019=CARTESIAN_POINT ( 'NONE',  ( 7.907275465492005218, 4.844754857023993999, -6.256456030303002791 ) ) ;
#32020=DIRECTION ( 'NONE',  ( 0.000000000000000000, -1.000000000000000000, 0.000000000000000000 ) ) ;
#32021=DIRECTION ( 'NONE',  ( 0.000000000000000000, 0.000000000000000000, -1.000000000000000000 ) ) ;
#32023=EDGE_CURVE ( 'NONE', #43600, #26545, #40694, .T. ) ;
#32027=CARTESIAN_POINT ( 'NONE',  ( 10.18908827523999960, 5.907871695079999874, 7.801541097952000570 ) ) ;
#32028=CARTESIAN_POINT ( 'NONE',  ( 10.64556415877000006, 2.988929467935999895, -5.952329570726999641 ) ) ;
#32031=CARTESIAN_POINT ( 'NONE',  ( 8.921135841230999119, 3.292387953886000140, -6.294868737226000377 ) ) ;
#32035=EDGE_LOOP ( 'NONE', ( #35237, #50228, #50242, #35256 ) ) ;
#32041=DIRECTION ( 'NONE',  ( -1.000000000000000000, 0.000000000000000000, 0.000000000000000000 ) ) ;
#32048=ORIENTED_EDGE ( 'NONE', *, *, #29936, .T. ) ;
#32051=ADVANCED_FACE ( 'NONE', ( #16918 ), #59576, .F. ) ;
#32053=FACE_OUTER_BOUND ( 'NONE', #44031, .T. ) ;
#32054=DIRECTION ( 'NONE',  ( -1.000000000000000000, 0.000000000000000000, 0.000000000000000000 ) ) ;
#32057=CARTESIAN_POINT ( 'NONE',  ( 0.8092604209659999270, 2.983562695318000113, -1.348686013867999911 ) ) ;
#32059=CARTESIAN_POINT ( 'NONE',  ( 10.50084834123000022, 4.616783736607999344, -6.288082254674000282 ) ) ;
#32066=CARTESIAN_POINT ( 'NONE',  ( 8.849385841230999361, 3.975069902178000270, 9.483774112875002160 ) ) ;
#32067=VERTEX_POINT ( 'NONE', #45583 ) ;
#32069=CARTESIAN_POINT ( 'NONE',  ( 7.399995280410000653, 4.524560801752999240, -6.025559345696000157 ) ) ;
#32070=EDGE_CURVE ( 'NONE', #5981, #11316, #48414, .T. ) ;
#32081=DIRECTION ( 'NONE',  ( 0.000000000000000000, 0.000000000000000000, -1.000000000000000000 ) ) ;
#32082=ORIENTED_EDGE ( 'NONE', *, *, #4121, .F. ) ;
#32089=CARTESIAN_POINT ( 'NONE',  ( 9.117517219591000810, 4.954905351382000944, 8.825777580285999235 ) ) ;
#32094=ORIENTED_EDGE ( 'NONE', *, *, #5136, .T. ) ;
#32109=CARTESIAN_POINT ( 'NONE',  ( 10.44486820642000069, 4.964088085664999817, -9.083609801695999408 ) ) ;
#32112=CARTESIAN_POINT ( 'NONE',  ( 7.000035920415999868, -12.36732175638999998, 2.759089158555000143 ) ) ;
#32117=AXIS2_PLACEMENT_3D ( 'NONE', #19056, #2974, #24988 ) ;
#32119=CARTESIAN_POINT ( 'NONE',  ( 10.77462860031000069, 5.575476001419000127, 8.682676628339999425 ) ) ;
#32120=CARTESIAN_POINT ( 'NONE',  ( 2.165556799209332528, 0.4581489286485003198, 3.500000000000000444 ) ) ;
#32122=CARTESIAN_POINT ( 'NONE',  ( 9.225036466121004253, 2.649952287134117235, 7.500002258928285315 ) ) ;
#32126=CARTESIAN_POINT ( 'NONE',  ( 9.059364158773000497, 4.192919163547999872, 5.525472271700999194 ) ) ;
#32127=B_SPLINE_CURVE_WITH_KNOTS ( 'NONE', 3,
 ( #4345, #52940, #31618, #36171, #9943, #5036, #63061, #31279, #25678, #62053, #35495, #51898, #62395, #63414, #42109, #41419, #20433, #67977, #3654, #41761, #30586, #15538, #36865, #3996 ),
 .UNSPECIFIED., .F., .F.,
 ( 4, 2, 2, 2, 2, 2, 2, 1, 1, 2, 2, 2, 4 ),
 ( 0.000000000000000000, 0.2499999999999440448, 0.3749999999999168443, 0.4374999999999040767, 0.4999999999998913092, 0.6249999999998667732, 0.6874999999998523403, 0.7187499999998447908, 0.7343749999998396838, 0.7421874999998377964, 0.7499999999998357980, 0.8749999999999178435, 1.000000000000000000 ),
 .UNSPECIFIED. ) ;
#32128=CARTESIAN_POINT ( 'NONE',  ( 10.93727498060999892, 5.425427353909999972, 7.240585962396000497 ) ) ;
#32130=( NAMED_UNIT ( * ) SI_UNIT ( $, .STERADIAN. ) SOLID_ANGLE_UNIT ( ) );
#32132=ORIENTED_EDGE ( 'NONE', *, *, #31487, .T. ) ;
#32138=CARTESIAN_POINT ( 'NONE',  ( 11.09999999999999964, 2.649999999999999911, -7.500000000000000000 ) ) ;
#32143=CARTESIAN_POINT ( 'NONE',  ( 9.053070280414001303, 2.391443348526999912, -6.856688371964000162 ) ) ;
#32144=CARTESIAN_POINT ( 'NONE',  ( 5.000030787343000327, -2.099962892530999881, 0.000000000000000000 ) ) ;
#32146=ORIENTED_EDGE ( 'NONE', *, *, #21381, .F. ) ;
#32147=CARTESIAN_POINT ( 'NONE',  ( 11.20563302462000088, 3.509134285281999777, 6.118194788334999856 ) ) ;
#32153=CARTESIAN_POINT ( 'NONE',  ( 8.187142219590999304, 4.968147183437999992, 5.971792472497999604 ) ) ;
#32166=VERTEX_POINT ( 'NONE', #5323 ) ;
#32167=CARTESIAN_POINT ( 'NONE',  ( 8.614404719593999005, 5.030502105212999453, -6.322203460290999999 ) ) ;
#32175=CARTESIAN_POINT ( 'NONE',  ( 9.642108463020802489, 3.293853022144934695, 8.705313308395453475 ) ) ;
#32177=ORIENTED_EDGE ( 'NONE', *, *, #20780, .F. ) ;
#32180=CARTESIAN_POINT ( 'NONE',  ( 10.28912155192344535, 2.704284023348198396, -7.938084390888771047 ) ) ;
#32181=CARTESIAN_POINT ( 'NONE',  ( 10.19715290653000217, 4.982626294267999967, -6.124313696433000054 ) ) ;
#32182=CARTESIAN_POINT ( 'NONE',  ( 8.086080172061008042, 4.921420473137001927, 6.235316328396007357 ) ) ;
#32185=CONICAL_SURFACE ( 'NONE', #42207, 1.449999999967999553, 0.7853981633972997312 ) ;
#32186=CARTESIAN_POINT ( 'NONE',  ( 9.038118784902701819, 4.950731182098148331, 8.458238308662791027 ) ) ;
#32188=CARTESIAN_POINT ( 'NONE',  ( 7.828420280408998622, 5.524123123935000379, 6.910361319981999095 ) ) ;
#32190=AXIS2_PLACEMENT_3D ( 'NONE', #10267, #10609, #64422 ) ;
#32196=EDGE_CURVE ( 'NONE', #50903, #49108, #63354, .T. ) ;
#32199=CARTESIAN_POINT ( 'NONE',  ( 10.96591775263000024, 9.690018913608000162, 5.974571089057000073 ) ) ;
#32211=CARTESIAN_POINT ( 'NONE',  ( 0.2772402514715000543, 2.199938726422999924, 2.557617887446999916 ) ) ;
#32219=EDGE_CURVE ( 'NONE', #23338, #30974, #34320, .T. ) ;
#32220=CARTESIAN_POINT ( 'NONE',  ( 11.28109528040999976, 2.660125405577999924, -6.904121770750999865 ) ) ;
#32238=AXIS2_PLACEMENT_3D ( 'NONE', #12846, #3372, #19459 ) ;
#32241=LINE ( 'NONE', #26297, #56735 ) ;
#32242=B_SPLINE_CURVE_WITH_KNOTS ( 'NONE', 3,
 ( #67665, #9630, #4724, #30977 ),
 .UNSPECIFIED., .F., .F.,
 ( 4, 4 ),
 ( 0.000000000000000000, 1.000000000000000000 ),
 .UNSPECIFIED. ) ;
#32252=CYLINDRICAL_SURFACE ( 'NONE', #8619, 0.5000000000000000000 ) ;
#32254=CARTESIAN_POINT ( 'NONE',  ( 9.790085841230000696, 5.149303692842000402, -5.987168472229000393 ) ) ;
#32261=CARTESIAN_POINT ( 'NONE',  ( 7.550000000000000711, 4.000000000000000000, 8.849999999999999645 ) ) ;
#32262=CARTESIAN_POINT ( 'NONE',  ( 5.000000000000000000, 0.000000000000000000, 0.000000000000000000 ) ) ;
#32264=DIRECTION ( 'NONE',  ( 1.000000000000000000, 0.000000000000000000, 0.000000000000000000 ) ) ;
#32268=CONICAL_SURFACE ( 'NONE', #25516, 13.04999934368000147, 0.7853981075146502233 ) ;
#32272=CARTESIAN_POINT ( 'NONE',  ( 8.496516550600000883, 5.350579948490858051, 7.852800305270208447 ) ) ;
#32273=ORIENTED_EDGE ( 'NONE', *, *, #60387, .F. ) ;
#32274=CARTESIAN_POINT ( 'NONE',  ( 0.3446312255616370557, 2.120796480409111506, 2.465608222985203213 ) ) ;
#32275=ORIENTED_EDGE ( 'NONE', *, *, #22813, .F. ) ;
#32282=B_SPLINE_SURFACE_WITH_KNOTS ( 'NONE', 3, 3, ( 
 ( #68143, #52067, #4172, #25508, #10115, #20260, #41587, #58348, #15017, #9762, #4511, #31112, #10451, #25850, #53109, #68483, #20606, #41932, #63239, #47529, #31446, #68834, #20953, #47872, #69179, #49583, #27924, #64956, #1005, #6232, #54135, #12184, #22317, #27573, #37714 ),
 ( #43311, #44358, #1691, #43659, #54483, #48900, #11145, #22661, #28264, #59042, #42962, #17069, #39098, #48205, #33860, #23009, #38401, #33167, #32818, #60423, #311, #26891, #65658, #59725, #59378, #64269, #60080, #11827, #21627, #6584, #16724, #49234, #1344, #55175, #33514 ),
 ( #54830, #38054, #12529, #44004, #65311, #17780, #16384, #32479, #658, #5890, #17425, #38754, #53793, #27230, #6929, #48555, #21971, #64616, #11479, #2380, #45725, #50278, #39791, #3062, #61115, #67369, #55868, #35238, #8317, #13232, #23703, #29662, #34558, #46064, #29310 ),
 ( #67032, #61795, #34207, #35582, #50622, #7976, #49932, #45382, #50963, #2724, #24047, #28618, #40811, #30004, #62133, #66692, #44703, #13911, #18815, #39443, #13572, #23363, #65998, #40140, #45039, #24737, #51306, #61454, #34894, #56210, #60763, #24395, #8657, #18123, #12879 ) ),
 .UNSPECIFIED., .F., .F., .F.,
 ( 4, 4 ),
 ( 4, 1, 1, 1, 1, 1, 1, 1, 1, 1, 1, 1, 1, 1, 1, 1, 1, 1, 1, 1, 1, 1, 1, 1, 1, 1, 1, 1, 1, 1, 1, 1, 4 ),
 ( -0.1039370721279000015, 1.103937072127999963 ),
 ( -0.02000000000000000042, 0.01250000000000000069, 0.04499999999999999833, 0.07749999999999999944, 0.1100000000000000006, 0.1424999999999999878, 0.1749999999999999889, 0.2074999999999999900, 0.2399999999999999911, 0.2725000000000000200, 0.3049999999999999933, 0.3375000000000000222, 0.3699999999999999956, 0.4025000000000000244, 0.4349999999999999978, 0.4675000000000000266, 0.5000000000000000000, 0.5324999999999999734, 0.5649999999999999467, 0.5975000000000000311, 0.6300000000000000044, 0.6624999999999999778, 0.6949999999999999512, 0.7275000000000000355, 0.7600000000000000089, 0.7924999999999999822, 0.8249999999999999556, 0.8575000000000000400, 0.8900000000000000133, 0.9224999999999999867, 0.9549999999999999600, 0.9875000000000000444, 1.020000000000000018 ),
 .UNSPECIFIED. ) ;
#32283=CARTESIAN_POINT ( 'NONE',  ( 4.149992563292000725, 2.000000000000000000, 0.000000000000000000 ) ) ;
#32296=CARTESIAN_POINT ( 'NONE',  ( 10.98417232529000032, 5.106037833414999838, -4.881461580086000396 ) ) ;
#32304=CARTESIAN_POINT ( 'NONE',  ( 8.347900245721101342, 4.939084050600958342, -6.209245198555986001 ) ) ;
#32313=CARTESIAN_POINT ( 'NONE',  ( 6.875001042874380630, 2.534482666265000184, -7.314862106114000007 ) ) ;
#32317=CARTESIAN_POINT ( 'NONE',  ( 6.999999999999999112, 8.396653025789797553, -4.391099154829968931 ) ) ;
#32322=ADVANCED_FACE ( 'NONE', ( #57341 ), #6181, .F. ) ;
#32324=CARTESIAN_POINT ( 'NONE',  ( 8.351645692843000290, 5.100874653827000671, 6.601413402487000148 ) ) ;
#32335=VERTEX_POINT ( 'NONE', #59678 ) ;
#32340=CARTESIAN_POINT ( 'NONE',  ( 8.115081613917173087, 5.350113345104855256, -7.499995474391613293 ) ) ;
#32344=CARTESIAN_POINT ( 'NONE',  ( 6.793770280410000417, 5.602143124542999786, -7.927308852422999763 ) ) ;
#32346=CARTESIAN_POINT ( 'NONE',  ( 9.451728970891553061, 5.272005692884806471, 7.951869525468983291 ) ) ;
#32361=CARTESIAN_POINT ( 'NONE',  ( 7.474999999999999645, 5.349999999999999645, 7.500000000000000000 ) ) ;
#32365=ORIENTED_EDGE ( 'NONE', *, *, #14699, .F. ) ;
#32367=ORIENTED_EDGE ( 'NONE', *, *, #67014, .T. ) ;
#32368=CARTESIAN_POINT ( 'NONE',  ( 10.13339736671999880, 5.653645990693000556, 6.501823474484000442 ) ) ;
#32372=CARTESIAN_POINT ( 'NONE',  ( 3.760208574517000191, -3.539102845952000198, 0.6295829741491000275 ) ) ;
#32376=VERTEX_POINT ( 'NONE', #56851 ) ;
#32384=CARTESIAN_POINT ( 'NONE',  ( 9.075483283097998566, 4.020836891789999257, 8.948690653012000951 ) ) ;
#32388=DIRECTION ( 'NONE',  ( 0.000000000000000000, -1.000000000000000000, 4.054615592038000306E-13 ) ) ;
#32394=DIRECTION ( 'NONE',  ( 0.000000000000000000, 0.000000000000000000, -1.000000000000000000 ) ) ;
#32395=B_SPLINE_CURVE_WITH_KNOTS ( 'NONE', 3,
 ( #54943, #65766, #55640, #34666, #7737, #3850 ),
 .UNSPECIFIED., .F., .F.,
 ( 4, 2, 4 ),
 ( 0.3058235430633697294, 0.6529117715316847814, 1.000000000000000000 ),
 .UNSPECIFIED. ) ;
#32397=CARTESIAN_POINT ( 'NONE',  ( 10.90000000296000060, 5.100000000009000445, -5.160242730682999657 ) ) ;
#32398=CARTESIAN_POINT ( 'NONE',  ( 0.2554473843801999822, -2.101315454803999838, -2.652019770012000066 ) ) ;
#32400=CARTESIAN_POINT ( 'NONE',  ( 10.38726084123000071, 2.888676266723000374, -6.716337836090000124 ) ) ;
#32401=ORIENTED_EDGE ( 'NONE', *, *, #34667, .F. ) ;
#32405=EDGE_CURVE ( 'NONE', #20142, #35353, #48416, .T. ) ;
#32410=CARTESIAN_POINT ( 'NONE',  ( 8.295045280407999044, 2.702884610408000210, -6.624425519483001068 ) ) ;
#32417=ORIENTED_EDGE ( 'NONE', *, *, #14825, .T. ) ;
#32418=LINE ( 'NONE', #43944, #48493 ) ;
#32423=DIRECTION ( 'NONE',  ( -1.000000000000000000, 0.000000000000000000, 0.000000000000000000 ) ) ;
#32427=ORIENTED_EDGE ( 'NONE', *, *, #42696, .T. ) ;
#32428=CARTESIAN_POINT ( 'NONE',  ( 7.577017219590000074, 5.480308727866000318, 8.192324747680999053 ) ) ;
#32430=CARTESIAN_POINT ( 'NONE',  ( 8.479753663705539068, 5.101882484038004151, -8.673404222138428210 ) ) ;
#32431=DIRECTION ( 'NONE',  ( 0.8660254037844289376, 0.000000000000000000, 0.5000000000000169864 ) ) ;
#32432=CARTESIAN_POINT ( 'NONE',  ( 10.96237823296000080, 6.768026792119000490, -5.462786416141000245 ) ) ;
#32433=VERTEX_POINT ( 'NONE', #53665 ) ;
#32437=CARTESIAN_POINT ( 'NONE',  ( 7.856851002541000106, 2.832432432432000269, -6.822293592207000934 ) ) ;
#32449=DIRECTION ( 'NONE',  ( -1.000000000000000000, 0.000000000000000000, 0.000000000000000000 ) ) ;
#32454=CARTESIAN_POINT ( 'NONE',  ( 10.75109581085999899, 2.822145500011000063, 6.655897464539000552 ) ) ;
#32457=CARTESIAN_POINT ( 'NONE',  ( 11.05639637898999972, 5.030226177531999632, 6.028288223959999748 ) ) ;
#32462=CARTESIAN_POINT ( 'NONE',  ( 10.96568151726000018, 9.694042294195000409, -5.969392498067000119 ) ) ;
#32467=CARTESIAN_POINT ( 'NONE',  ( 10.99933470386000067, 5.081013421858999735, 8.239043921879998678 ) ) ;
#32471=CARTESIAN_POINT ( 'NONE',  ( 9.905375278050065901, 5.100000000000000533, -6.445686799065932782 ) ) ;
#32479=CARTESIAN_POINT ( 'NONE',  ( 7.512829719590000010, 5.524123123935000379, 6.910361319981999095 ) ) ;
#32480=CARTESIAN_POINT ( 'NONE',  ( 9.749220280410998640, 5.656948148960999845, -6.994239053114000626 ) ) ;
#32481=LINE ( 'NONE', #26550, #52168 ) ;
#32482=CARTESIAN_POINT ( 'NONE',  ( 2.394284045767109514, 0.2836190127161131169, 3.245552818120243543 ) ) ;
#32484=CARTESIAN_POINT ( 'NONE',  ( 9.534905769125000319, 3.030948166328000237, 8.761984216465000586 ) ) ;
#32487=EDGE_CURVE ( 'NONE', #19773, #66241, #45943, .T. ) ;
#32496=CARTESIAN_POINT ( 'NONE',  ( 1.500064665912000050, -2.653487697479000040, 1.892165331686999963 ) ) ;
#32497=ORIENTED_EDGE ( 'NONE', *, *, #63111, .T. ) ;
#32502=CARTESIAN_POINT ( 'NONE',  ( 8.465229719592999302, 2.567871051582000241, -6.869011921437000012 ) ) ;
#32503=VECTOR ( 'NONE', #41662, 1000.000000000000114 ) ;
#32506=ORIENTED_EDGE ( 'NONE', *, *, #64155, .F. ) ;
#32507=CARTESIAN_POINT ( 'NONE',  ( 9.148130259829166278, 4.680070470244416470, -8.679971105817726240 ) ) ;
#32511=CARTESIAN_POINT ( 'NONE',  ( 11.09999999999999964, -4.755975669291000300E-06, 1.428076682242000113E-06 ) ) ;
#32516=CARTESIAN_POINT ( 'NONE',  ( 9.944319408602000365, 5.443001719280999851, 7.367350382395000175 ) ) ;
#32518=CARTESIAN_POINT ( 'NONE',  ( 8.493369886551995762, 5.097498803759001440, 6.607670056088003285 ) ) ;
#32521=CIRCLE ( 'NONE', #16881, 3.500000000000000000 ) ;
#32524=EDGE_CURVE ( 'NONE', #23367, #66228, #58217, .T. ) ;
#32525=CARTESIAN_POINT ( 'NONE',  ( 8.020982780409999791, 3.245534453799999941, 8.949623695221001540 ) ) ;
#32530=PLANE ( 'NONE',  #22417 ) ;
#32531=CARTESIAN_POINT ( 'NONE',  ( 9.243270085646278389, 2.683788241851253531, 7.201163913334668543 ) ) ;
#32532=CARTESIAN_POINT ( 'NONE',  ( 0.07497316781761000082, 0.000000000000000000, -2.824973347946000413 ) ) ;
#32534=CARTESIAN_POINT ( 'NONE',  ( 10.96855433372000022, 5.800069981862000290, 4.929813314009000358 ) ) ;
#32535=CARTESIAN_POINT ( 'NONE',  ( 10.96261261415000021, 7.423557921018999473, 6.118074476279000251 ) ) ;
#32548=CARTESIAN_POINT ( 'NONE',  ( 8.534482780410998615, 3.011620138462000273, 8.801434747080000065 ) ) ;
#32553=CARTESIAN_POINT ( 'NONE',  ( 8.163776391448005043, 3.396249911995000481, -6.162465440825001473 ) ) ;
#32555=CARTESIAN_POINT ( 'NONE',  ( 10.63743278041000018, 3.721476136598000028, -8.997092462634000753 ) ) ;
#32556=CARTESIAN_POINT ( 'NONE',  ( 9.612308556530413384, 3.034755127822595266, 8.468084591989956778 ) ) ;
#32557=CARTESIAN_POINT ( 'NONE',  ( 7.758693699415004197, 5.085317049932003286, 6.543835681441004581 ) ) ;
#32559=DIRECTION ( 'NONE',  ( 0.5298945027589778700, -0.5996715052829758585, -0.5996714948181758320 ) ) ;
#32560=EDGE_LOOP ( 'NONE', ( #7327, #3859, #40788, #36232 ) ) ;
#32567=CARTESIAN_POINT ( 'NONE',  ( 11.04499918297000072, 2.754540059510000027, 5.176258675770000650 ) ) ;
#32568=FACE_OUTER_BOUND ( 'NONE', #7705, .T. ) ;
#32572=CARTESIAN_POINT ( 'NONE',  ( 9.842730320956407652, 2.713277070382849043, -7.026830998939262329 ) ) ;
#32585=DIRECTION ( 'NONE',  ( -0.8660254037844289376, 0.000000000000000000, -0.5000000000000169864 ) ) ;
#32587=CARTESIAN_POINT ( 'NONE',  ( 9.093935841232999806, 2.156584729807999867, -7.959751745006000689 ) ) ;
#32589=ORIENTED_EDGE ( 'NONE', *, *, #59901, .T. ) ;
#32595=CARTESIAN_POINT ( 'NONE',  ( 9.051550650638001017, 2.899999999999999911, 6.227445478845999638 ) ) ;
#32602=CARTESIAN_POINT ( 'NONE',  ( 11.09999965054999826, 12.24999851416000141, 0.000000000000000000 ) ) ;
#32605=CARTESIAN_POINT ( 'NONE',  ( 9.567560841232999991, 5.349936549139000519, -7.138437102151999447 ) ) ;
#32608=CARTESIAN_POINT ( 'NONE',  ( 11.09999999999999964, 5.299999999999999822, -5.160242713806000303 ) ) ;
#32609=SHAPE_REPRESENTATION_RELATIONSHIP ( 'NONE' , 'NONE' ,  #15732, #61967 ) ;
#32611=VERTEX_POINT ( 'NONE', #35110 ) ;
#32619=ORIENTED_EDGE ( 'NONE', *, *, #28539, .F. ) ;
#32620=CARTESIAN_POINT ( 'NONE',  ( 6.613728317541999857, 5.172411450403999744, -8.246583185469999577 ) ) ;
#32624=AXIS2_PLACEMENT_3D ( 'NONE', #31508, #26613, #52830 ) ;
#32631=CARTESIAN_POINT ( 'NONE',  ( 10.97197891098000078, 5.142532440135999749, -4.995747455712000296 ) ) ;
#32639=CARTESIAN_POINT ( 'NONE',  ( 8.363921074485642038, 5.017958344788086222, -6.290581482856832274 ) ) ;
#32640=CARTESIAN_POINT ( 'NONE',  ( 4.500000000000000000, 0.000000000000000000, 0.000000000000000000 ) ) ;
#32641=ORIENTED_EDGE ( 'NONE', *, *, #49304, .T. ) ;
#32656=EDGE_CURVE ( 'NONE', #66492, #64300, #15111, .T. ) ;
#32661=DIRECTION ( 'NONE',  ( 0.7071067811865475727, -0.7071067811865475727, 0.000000000000000000 ) ) ;
#32662=CARTESIAN_POINT ( 'NONE',  ( 1.009306799208383065, 3.058252359239904905, -1.762666431298142600 ) ) ;
#32663=ORIENTED_EDGE ( 'NONE', *, *, #11007, .F. ) ;
#32672=ORIENTED_EDGE ( 'NONE', *, *, #51778, .F. ) ;
#32676=DIRECTION ( 'NONE',  ( 1.000000000000000000, 0.000000000000000000, 0.000000000000000000 ) ) ;
#32678=CARTESIAN_POINT ( 'NONE',  ( 8.126014158770999529, 5.189036231907000030, -8.048606212067999977 ) ) ;
#32681=CARTESIAN_POINT ( 'NONE',  ( 6.926370280408000291, 3.391196421714000042, -9.121921547671998809 ) ) ;
#32682=CARTESIAN_POINT ( 'NONE',  ( 8.645206806413895606, 4.733533093241248935, -8.663332967138325458 ) ) ;
#32683=CARTESIAN_POINT ( 'NONE',  ( 9.458877515925783186, 5.224829427659542169, 8.067569713668623521 ) ) ;
#32688=FACE_OUTER_BOUND ( 'NONE', #5139, .T. ) ;
#32695=CARTESIAN_POINT ( 'NONE',  ( 8.021095686590996365, 4.867149410870005077, -6.207068544376001640 ) ) ;
#32697=CARTESIAN_POINT ( 'NONE',  ( 5.449999267937000624, 6.217248937900999058E-14, 3.708144902247999495E-14 ) ) ;
#32698=B_SPLINE_SURFACE_WITH_KNOTS ( 'NONE', 3, 3, ( 
 ( #52049, #67783, #9397, #13385 ),
 ( #4152, #29120, #2530, #14662 ),
 ( #25492, #41569, #55683, #68464 ),
 ( #44851, #25145, #56018, #20244 ),
 ( #41230, #4493, #7429, #39597 ),
 ( #28777, #50089, #18619, #66500 ),
 ( #66158, #60919, #13035, #7781 ),
 ( #34707, #59027, #10435, #37698 ),
 ( #5875, #43294, #31776, #42603 ),
 ( #36675, #57995, #42946, #32805 ),
 ( #27214, #32462, #992, #21953 ),
 ( #11130, #48884, #54119, #22302 ),
 ( #15348, #63218, #10095, #58678 ),
 ( #6217, #52746, #20936, #31430 ) ),
 .UNSPECIFIED., .F., .F., .F.,
 ( 4, 1, 1, 1, 1, 1, 1, 1, 1, 1, 1, 4 ),
 ( 4, 4 ),
 ( -0.01123015465801999874, 0.000000000000000000, 0.1111111111111000027, 0.2222222222222000054, 0.3333333333333000081, 0.4444444444444000109, 0.5555555555555999891, 0.6666666666667000474, 0.7777777777777999946, 0.8888888888888999418, 1.000000000000000000, 1.008787911365999879 ),
 ( -0.2206650672665999846, 1.220665067267000081 ),
 .UNSPECIFIED. ) ;
#32702=CARTESIAN_POINT ( 'NONE',  ( 10.30047009227000032, 4.027768540959000276, 9.431354536774000152 ) ) ;
#32703=CARTESIAN_POINT ( 'NONE',  ( 9.964039158770999549, 3.485905350467000119, -9.275749134703000109 ) ) ;
#32707=CYLINDRICAL_SURFACE ( 'NONE', #10311, 1.350000000000000533 ) ;
#32708=B_SPLINE_CURVE_WITH_KNOTS ( 'NONE', 3,
 ( #52584, #26019, #62720, #20772, #4339 ),
 .UNSPECIFIED., .F., .F.,
 ( 4, 1, 4 ),
 ( 0.000000000000000000, 0.5000000000000000000, 1.000000000000000000 ),
 .UNSPECIFIED. ) ;
#32712=FACE_OUTER_BOUND ( 'NONE', #68884, .T. ) ;
#32713=ORIENTED_EDGE ( 'NONE', *, *, #24053, .F. ) ;
#32723=CONICAL_SURFACE ( 'NONE', #28232, 12.44999944941000081, 0.7853981146832407223 ) ;
#32726=CARTESIAN_POINT ( 'NONE',  ( 10.90000000000000036, 0.2999999999999999889, 4.902439024389999567 ) ) ;
#32728=CARTESIAN_POINT ( 'NONE',  ( 8.472124462996665883, 5.100000000000000533, 6.567732269893666874 ) ) ;
#32732=CARTESIAN_POINT ( 'NONE',  ( 8.374639158773000247, 2.721111233225000259, -6.936528696292000085 ) ) ;
#32735=CARTESIAN_POINT ( 'NONE',  ( 0.6173104132283999679, -3.219656052487999798, -1.007448552055000057 ) ) ;
#32737=CARTESIAN_POINT ( 'NONE',  ( 2.457020142123000461, 2.375218314457999913, -2.913196738027000077 ) ) ;
#32742=DIRECTION ( 'NONE',  ( 0.000000000000000000, -1.000000000000000000, 0.000000000000000000 ) ) ;
#32745=CARTESIAN_POINT ( 'NONE',  ( 8.924954719592001595, 4.158911560497999815, 5.873540104660999184 ) ) ;
#32751=CARTESIAN_POINT ( 'NONE',  ( 7.648620280409000216, 3.500992739020000410, -8.983283880004998778 ) ) ;
#32758=ORIENTED_EDGE ( 'NONE', *, *, #60920, .T. ) ;
#32764=CARTESIAN_POINT ( 'NONE',  ( 7.000000000000000000, 8.307879248642999315, 4.307879248643000203 ) ) ;
#32768=ORIENTED_EDGE ( 'NONE', *, *, #33229, .T. ) ;
#32769=CARTESIAN_POINT ( 'NONE',  ( 9.143920280410000601, 5.791553967443999973, 7.752111263209999770 ) ) ;
#32770=EDGE_CURVE ( 'NONE', #54361, #38721, #53502, .T. ) ;
#32771=ORIENTED_EDGE ( 'NONE', *, *, #39665, .T. ) ;
#32773=CIRCLE ( 'NONE', #35033, 2.749999999999999556 ) ;
#32774=CARTESIAN_POINT ( 'NONE',  ( 8.350387243830999395, 4.599999999999999645, -6.632262360512000576 ) ) ;
#32775=CARTESIAN_POINT ( 'NONE',  ( 10.96237843380999877, 5.422598724373000501, -4.905487645836000610 ) ) ;
#32780=DIRECTION ( 'NONE',  ( 1.000000000000000000, 0.000000000000000000, 0.000000000000000000 ) ) ;
#32781=CARTESIAN_POINT ( 'NONE',  ( 6.999999691988000095, 0.000000000000000000, 0.000000000000000000 ) ) ;
#32790=CARTESIAN_POINT ( 'NONE',  ( 9.535554719593998030, 3.927090956378999742, -9.230892435423001530 ) ) ;
#32791=CARTESIAN_POINT ( 'NONE',  ( 10.95552360838999917, 4.744046441415999738, -9.198140387677000263 ) ) ;
#32797=ORIENTED_EDGE ( 'NONE', *, *, #9654, .T. ) ;
#32798=EDGE_CURVE ( 'NONE', #3842, #20189, #40008, .T. ) ;
#32800=CARTESIAN_POINT ( 'NONE',  ( 9.600491906670001185, 5.206545077004999911, 8.585111878242999595 ) ) ;
#32805=CARTESIAN_POINT ( 'NONE',  ( 11.13611325966000010, 9.539967198755999078, -6.380887600928000225 ) ) ;
#32806=CARTESIAN_POINT ( 'NONE',  ( 10.16210844129514790, 5.577934564358349334, 6.690706121504116588 ) ) ;
#32811=CARTESIAN_POINT ( 'NONE',  ( 9.617285841233000454, 5.306366356490000769, -7.996450761531000317 ) ) ;
#32818=CARTESIAN_POINT ( 'NONE',  ( 8.309482780410998970, 2.905861847853000057, 8.940690431604000565 ) ) ;
#32820=CARTESIAN_POINT ( 'NONE',  ( 9.260829719593999698, 4.861259245430999520, -8.806664389576001284 ) ) ;
#32822=CARTESIAN_POINT ( 'NONE',  ( 3.274540278792131165, 3.257195673479903686, -0.06878223238550713881 ) ) ;
#32824=CARTESIAN_POINT ( 'NONE',  ( 9.757669403192000601, 4.489270656625000022, 5.986034819543999852 ) ) ;
#32828=CARTESIAN_POINT ( 'NONE',  ( 7.432076984665996200, 3.524670056070998037, 6.650527748631001046 ) ) ;
#32829=AXIS2_PLACEMENT_3D ( 'NONE', #28808, #16566, #1186 ) ;
#32833=EDGE_CURVE ( 'NONE', #2928, #8734, #31674, .T. ) ;
#32834=B_SPLINE_CURVE_WITH_KNOTS ( 'NONE', 3,
 ( #13519, #34150, #55469, #1987 ),
 .UNSPECIFIED., .F., .F.,
 ( 4, 4 ),
 ( 0.000000000000000000, 1.000000000000000000 ),
 .UNSPECIFIED. ) ;
#32844=CARTESIAN_POINT ( 'NONE',  ( 8.325004567511003373, 2.868524053507002236, 6.316175840085996640 ) ) ;
#32848=CARTESIAN_POINT ( 'NONE',  ( 9.211104719594999324, 5.462898983065000102, -8.055936939571999744 ) ) ;
#32852=CARTESIAN_POINT ( 'NONE',  ( 9.210653099680683908, 3.646553657477270782, -8.850805462952818559 ) ) ;
#32855=CARTESIAN_POINT ( 'NONE',  ( 9.621289888149652469, 3.647081445668302724, 8.849739427182289120 ) ) ;
#32860=CARTESIAN_POINT ( 'NONE',  ( 9.385781899350000401, 4.980865465981000106, 6.433345686594999613 ) ) ;
#32861=CARTESIAN_POINT ( 'NONE',  ( 10.44486820642000069, 4.964088085664999817, -9.083609801695999408 ) ) ;
#32862=CARTESIAN_POINT ( 'NONE',  ( 8.187982051047001164, 4.942702676859997979, 6.196150354213001421 ) ) ;
#32868=CARTESIAN_POINT ( 'NONE',  ( 7.609454719589999527, 3.276311362504999991, 5.841989464160999290 ) ) ;
#32869=ORIENTED_EDGE ( 'NONE', *, *, #28372, .F. ) ;
#32872=CARTESIAN_POINT ( 'NONE',  ( 7.225632159681131483, 2.625029116607175972, 7.496691097032143425 ) ) ;
#32874=VECTOR ( 'NONE', #21483, 1000.000000000000227 ) ;
#32876=CARTESIAN_POINT ( 'NONE',  ( 11.07243245105999918, 6.084025226422999921, 5.191545849810999869 ) ) ;
#32877=CARTESIAN_POINT ( 'NONE',  ( 11.12952936848999919, 8.831357469829999474, 6.732325948479999767 ) ) ;
#32880=DIRECTION ( 'NONE',  ( 0.000000000000000000, -1.000000000000000000, 0.000000000000000000 ) ) ;
#32881=ORIENTED_EDGE ( 'NONE', *, *, #43371, .T. ) ;
#32884=CARTESIAN_POINT ( 'NONE',  ( 10.34947814066000049, 4.457562099971999814, 6.154877938302999674 ) ) ;
#32887=B_SPLINE_CURVE_WITH_KNOTS ( 'NONE', 3,
 ( #55019, #65142, #28812, #13067 ),
 .UNSPECIFIED., .F., .F.,
 ( 4, 4 ),
 ( 0.000000000000000000, 1.000000000000000000 ),
 .UNSPECIFIED. ) ;
#32890=CARTESIAN_POINT ( 'NONE',  ( 7.854823341228001077, 4.561643343497000735, 6.153061759127000485 ) ) ;
#32891=CARTESIAN_POINT ( 'NONE',  ( 9.533434135307000901, 2.564753581125000181, 6.150586364588000343 ) ) ;
#32893=CARTESIAN_POINT ( 'NONE',  ( 7.598073341229000022, 3.554857159507999853, 8.889479859586000288 ) ) ;
#32896=CARTESIAN_POINT ( 'NONE',  ( 10.46298584122999920, 3.993164721578000176, -6.140176455708999725 ) ) ;
#32898=CARTESIAN_POINT ( 'NONE',  ( 9.724226531639931892, 2.899999999999999911, -6.304440313831950249 ) ) ;
#32900=CARTESIAN_POINT ( 'NONE',  ( 8.941941226754561711, 5.237474851784025276, 6.943363493799808772 ) ) ;
#32905=CARTESIAN_POINT ( 'NONE',  ( 3.500000000000000000, 1.113524292603000010, -3.231029921506000324 ) ) ;
#32908=CARTESIAN_POINT ( 'NONE',  ( 11.12988950403999944, 2.715405747272999548, 4.847983218306000097 ) ) ;
#32911=ADVANCED_FACE ( 'NONE', ( #5776 ), #22814, .T. ) ;
#32912=EDGE_CURVE ( 'NONE', #7311, #63350, #31702, .T. ) ;
#32919=CARTESIAN_POINT ( 'NONE',  ( 10.96207813434000045, 5.399835028078000754, 7.743264559064000352 ) ) ;
#32921=CARTESIAN_POINT ( 'NONE',  ( 8.328909422836733967, 2.650170743412998409, -7.263558743223875958 ) ) ;
#32928=EDGE_CURVE ( 'NONE', #32611, #57225, #40860, .T. ) ;
#32929=VECTOR ( 'NONE', #54434, 1000.000000000000000 ) ;
#32930=ORIENTED_EDGE ( 'NONE', *, *, #801, .F. ) ;
#32931=CARTESIAN_POINT ( 'NONE',  ( 7.452411699453480587, 2.247457503992560390, 7.471653287871163229 ) ) ;
#32936=EDGE_LOOP ( 'NONE', ( #42583, #57689, #49245, #37734 ) ) ;
#32937=ADVANCED_FACE ( 'NONE', ( #56788 ), #19721, .T. ) ;
#32943=CARTESIAN_POINT ( 'NONE',  ( 11.10000000115999974, 8.827960611545998759, -6.689729118101999994 ) ) ;
#32946=CARTESIAN_POINT ( 'NONE',  ( 11.06622274902552405, 4.530851388969875160, -8.944471867876563564 ) ) ;
#32948=CARTESIAN_POINT ( 'NONE',  ( 8.970860841232001448, 4.131080973160000447, -6.108642999115999395 ) ) ;
#32949=ORIENTED_EDGE ( 'NONE', *, *, #50073, .T. ) ;
#32951=EDGE_LOOP ( 'NONE', ( #66242, #67703, #17066, #67799 ) ) ;
#32955=CARTESIAN_POINT ( 'NONE',  ( 7.974113208588001100, 4.561154361229000642, -6.272154006859000930 ) ) ;
#32958=CARTESIAN_POINT ( 'NONE',  ( 4.900006121741999010, 2.000000000000000000, 0.000000000000000000 ) ) ;
#32961=ORIENTED_EDGE ( 'NONE', *, *, #53515, .T. ) ;
#32962=CARTESIAN_POINT ( 'NONE',  ( 7.190590560818999499, 2.534482666265000184, -7.314862106114000007 ) ) ;
#32966=CARTESIAN_POINT ( 'NONE',  ( 9.128895280414001334, 3.880154689736000417, -9.060377011187000562 ) ) ;
#32967=AXIS2_PLACEMENT_3D ( 'NONE', #65562, #17686, #32388 ) ;
#32968=DIRECTION ( 'NONE',  ( 0.000000000000000000, 1.000000000000000000, 0.000000000000000000 ) ) ;
#32973=LINE ( 'NONE', #36844, #29295 ) ;
#32976=CARTESIAN_POINT ( 'NONE',  ( 5.399999743830999677, 0.000000000000000000, 0.000000000000000000 ) ) ;
#32981=CARTESIAN_POINT ( 'NONE',  ( 8.455089073534951538, 5.099985254049173022, -6.566459068862928738 ) ) ;
#32982=CARTESIAN_POINT ( 'NONE',  ( 6.999998782146999332, 11.95749337870000062, -3.642574926947999892 ) ) ;
#32992=EDGE_CURVE ( 'NONE', #67585, #65548, #23983, .T. ) ;
#32998=B_SPLINE_SURFACE_WITH_KNOTS ( 'NONE', 3, 3, ( 
 ( #49447, #39312, #65520, #50486, #34428, #66559, #13443, #1556, #60633, #2588, #18678, #22878, #60981, #17648, #23918, #23230, #55740, #55391, #60290, #13093, #29533, #33728, #7843, #7487, #55045, #19017, #50836, #61664, #45253, #28840, #13779, #7147, #3953, #19708, #68615 ),
 ( #51513, #24609, #20388, #30543, #15147, #51854, #19358, #25291, #20047, #63368, #41028, #41716, #46625, #8871, #62011, #4643, #63016, #58140, #36466, #41375, #25636, #40681, #67931, #62684, #67584, #14123, #52545, #35449, #25981, #47310, #14468, #56774, #30209, #14806, #30888 ),
 ( #57787, #36124, #46966, #3613, #57439, #9544, #62351, #24947, #20734, #46280, #42063, #15495, #35787, #57102, #9200, #52201, #4302, #9900, #68268, #31238, #36821, #29874, #51183, #3279, #45932, #67241, #68968, #787, #64050, #63716, #4992, #53581, #27710, #47654, #27358 ),
 ( #21412, #43786, #42408, #64392, #49025, #65082, #17204, #16172, #22445, #10240, #21079, #53918, #38178, #59508, #32605, #22100, #42746, #37158, #53235, #16855, #31921, #43444, #6019, #37495, #5335, #38532, #32948, #58821, #31577, #11606, #54260, #48332, #11267, #10929, #5675 ) ),
 .UNSPECIFIED., .F., .F., .F.,
 ( 4, 4 ),
 ( 4, 1, 1, 1, 1, 1, 1, 1, 1, 1, 1, 1, 1, 1, 1, 1, 1, 1, 1, 1, 1, 1, 1, 1, 1, 1, 1, 1, 1, 1, 1, 1, 4 ),
 ( -0.1039370721279000015, 1.103937072127999963 ),
 ( -0.02000000000000000042, 0.01250000000000000069, 0.04499999999999999833, 0.07749999999999999944, 0.1100000000000000006, 0.1424999999999999878, 0.1749999999999999889, 0.2074999999999999900, 0.2399999999999999911, 0.2725000000000000200, 0.3049999999999999933, 0.3375000000000000222, 0.3699999999999999956, 0.4025000000000000244, 0.4349999999999999978, 0.4675000000000000266, 0.5000000000000000000, 0.5324999999999999734, 0.5649999999999999467, 0.5975000000000000311, 0.6300000000000000044, 0.6624999999999999778, 0.6949999999999999512, 0.7275000000000000355, 0.7600000000000000089, 0.7924999999999999822, 0.8249999999999999556, 0.8575000000000000400, 0.8900000000000000133, 0.9224999999999999867, 0.9549999999999999600, 0.9875000000000000444, 1.020000000000000018 ),
 .UNSPECIFIED. ) ;
#32999=CARTESIAN_POINT ( 'NONE',  ( 7.000000000000001776, 10.08082116580678367, -4.449062842274066121 ) ) ;
#33003=CARTESIAN_POINT ( 'NONE',  ( 9.266851002542999538, 2.832432432432000269, 6.822293592207000934 ) ) ;
#33006=EDGE_LOOP ( 'NONE', ( #31164, #5847, #53406, #66956 ) ) ;
#33011=CARTESIAN_POINT ( 'NONE',  ( 6.999999999999998224, 10.44690841785601698, 4.123972661126250827 ) ) ;
#33013=VERTEX_POINT ( 'NONE', #63385 ) ;
#33014=AXIS2_PLACEMENT_3D ( 'NONE', #2217, #55006, #1869 ) ;
#33020=LINE ( 'NONE', #28122, #48035 ) ;
#33022=CARTESIAN_POINT ( 'NONE',  ( 9.509454719593000149, 3.116293075258000478, -6.208411413796000033 ) ) ;
#33024=CARTESIAN_POINT ( 'NONE',  ( -0.000000000000000000, 2.824745580908275766, -0.7586348975822421181 ) ) ;
#33026=CARTESIAN_POINT ( 'NONE',  ( 8.458985841228999547, 4.642843096736999797, -9.160097874508000615 ) ) ;
#33028=CARTESIAN_POINT ( 'NONE',  ( 9.432982363827456140, 5.350302034667164364, 7.637571449422903669 ) ) ;
#33036=ORIENTED_EDGE ( 'NONE', *, *, #29545, .F. ) ;
#33038=DIRECTION ( 'NONE',  ( 1.000000000000000000, 0.000000000000000000, 0.000000000000000000 ) ) ;
#33041=CARTESIAN_POINT ( 'NONE',  ( 8.472537864290000442, 2.899999999999999911, -6.571291218949999902 ) ) ;
#33042=CARTESIAN_POINT ( 'NONE',  ( 10.67008267378785646, 2.650318246679984391, 7.583525964882096737 ) ) ;
#33053=VECTOR ( 'NONE', #3296, 1000.000000000000000 ) ;
#33056=EDGE_CURVE ( 'NONE', #10018, #23381, #57452, .T. ) ;
#33057=ORIENTED_EDGE ( 'NONE', *, *, #51224, .T. ) ;
#33059=CARTESIAN_POINT ( 'NONE',  ( 10.96876099447000108, 2.333339469804000199, 6.524055942683999021 ) ) ;
#33079=CARTESIAN_POINT ( 'NONE',  ( 9.344351860772725615, 2.684670005318823716, -7.853455765640516617 ) ) ;
#33080=CARTESIAN_POINT ( 'NONE',  ( 9.898395280408998076, 3.987760651117999711, -9.123263301387000368 ) ) ;
#33084=EDGE_CURVE ( 'NONE', #29332, #68416, #30834, .T. ) ;
#33085=CARTESIAN_POINT ( 'NONE',  ( 0.3788438179258999949, 2.727922606149000284, -2.252402744047000471 ) ) ;
#33087=CARTESIAN_POINT ( 'NONE',  ( 10.16008584122999991, 4.812959680871000678, -8.526582921144999716 ) ) ;
#33090=CARTESIAN_POINT ( 'NONE',  ( 9.933148997456999751, 5.167567567567999731, 6.822293592207000934 ) ) ;
#33093=CARTESIAN_POINT ( 'NONE',  ( 7.769579719591000355, 2.431401017850999935, 7.958393275880999873 ) ) ;
#33096=CARTESIAN_POINT ( 'NONE',  ( 7.408854719586000392, 5.732054911314000023, -7.535918460973999977 ) ) ;
#33098=CARTESIAN_POINT ( 'NONE',  ( 10.02201554968999986, 3.298015135926000152, 5.700522662207000657 ) ) ;
#33102=AXIS2_PLACEMENT_3D ( 'NONE', #28921, #43252, #11425 ) ;
#33103=CARTESIAN_POINT ( 'NONE',  ( 8.232750256034279346, 4.666560802815586051, 6.122829837893929650 ) ) ;
#33104=EDGE_LOOP ( 'NONE', ( #31269, #29998, #30015, #25360 ) ) ;
#33116=ORIENTED_EDGE ( 'NONE', *, *, #58492, .T. ) ;
#33124=CARTESIAN_POINT ( 'NONE',  ( 0.4266613450451046674, -1.726519499994412454, -2.993820366163598923 ) ) ;
#33125=CARTESIAN_POINT ( 'NONE',  ( 7.292197165043062590, 5.528435618896470949, -6.445051596221718526 ) ) ;
#33137=CARTESIAN_POINT ( 'NONE',  ( 9.096889158776001238, 2.235961884443999459, -6.794506518623999902 ) ) ;
#33138=CARTESIAN_POINT ( 'NONE',  ( 10.27571527605999968, 5.689443924112000062, -7.562019866568999049 ) ) ;
#33140=CARTESIAN_POINT ( 'NONE',  ( 0.000000000000000000, 5.100000000000000533, -7.500000000000000000 ) ) ;
#33141=CARTESIAN_POINT ( 'NONE',  ( 7.572352458090005456, 3.472372354340000911, -6.527657354165006254 ) ) ;
#33146=CARTESIAN_POINT ( 'NONE',  ( 1.862398069789666710, -2.519008840803133698, -2.453290717214521521 ) ) ;
#33148=CARTESIAN_POINT ( 'NONE',  ( 10.24961997674000003, 4.184221916050000267, 9.286882020979000174 ) ) ;
#33159=CARTESIAN_POINT ( 'NONE',  ( 9.766460841231999979, 3.135494838036999798, -8.598037907310999373 ) ) ;
#33167=CARTESIAN_POINT ( 'NONE',  ( 8.245295280410999794, 4.283000592898000392, 9.286795422009001655 ) ) ;
#33168=CARTESIAN_POINT ( 'NONE',  ( 9.410004719593999312, 2.495531372253999791, -7.930944806125000746 ) ) ;
#33170=CARTESIAN_POINT ( 'NONE',  ( 2.215865467774827735, 2.262839795465755977, -2.144213487925047623 ) ) ;
#33172=CARTESIAN_POINT ( 'NONE',  ( 9.854942824136999846, 2.800308224477999985, 9.013816726157999781 ) ) ;
#33176=CARTESIAN_POINT ( 'NONE',  ( 7.885003087483005046, 2.917683036408002195, 6.444041402419006914 ) ) ;
#33183=CARTESIAN_POINT ( 'NONE',  ( 10.98768472639999949, 5.139099012905000485, 4.945212061661000469 ) ) ;
#33191=CARTESIAN_POINT ( 'NONE',  ( 8.225464158772000545, 3.844886277615000125, -8.888911790991000927 ) ) ;
#33215=CARTESIAN_POINT ( 'NONE',  ( 8.122954719591000128, 3.566637212418000136, 5.743604853744000316 ) ) ;
#33216=ORIENTED_EDGE ( 'NONE', *, *, #36802, .F. ) ;
#33219=CYLINDRICAL_SURFACE ( 'NONE', #58416, 1.350000000000000533 ) ;
#33223=CARTESIAN_POINT ( 'NONE',  ( 9.318724127987000116, 2.755029797911999978, 8.795125756257000660 ) ) ;
#33227=EDGE_CURVE ( 'NONE', #958, #16538, #19192, .T. ) ;
#33229=EDGE_CURVE ( 'NONE', #66034, #1019, #9153, .T. ) ;
#33237=CARTESIAN_POINT ( 'NONE',  ( 8.598670280411999656, 2.376526778640999815, 7.686980884243000745 ) ) ;
#33238=CARTESIAN_POINT ( 'NONE',  ( 10.21609109105999913, 5.961715741921000067, 7.319666990313999477 ) ) ;
#33241=CARTESIAN_POINT ( 'NONE',  ( 7.919010841228001141, 5.361039412362000434, 6.973453640356000349 ) ) ;
#33253=CARTESIAN_POINT ( 'NONE',  ( 1.496201594832999859, -1.181558911493999942, 3.215390670984000554 ) ) ;
#33259=AXIS2_PLACEMENT_3D ( 'NONE', #52505, #4604, #25939 ) ;
#33261=CARTESIAN_POINT ( 'NONE',  ( 7.947784805528978147, 5.286778829772822874, 7.027374276529180896 ) ) ;
#33266=CARTESIAN_POINT ( 'NONE',  ( 8.610875063856999745, 4.757997781751000410, 5.934102420827000124 ) ) ;
#33270=CARTESIAN_POINT ( 'NONE',  ( 2.000973465872999846, 3.500000000000000000, 0.000000000000000000 ) ) ;
#33282=CARTESIAN_POINT ( 'NONE',  ( 7.489726418404281993, 2.461536839440352065, 6.668271594188382778 ) ) ;
#33291=CARTESIAN_POINT ( 'NONE',  ( 10.52638970730999901, 2.451081172664000274, 6.282749363171999946 ) ) ;
#33294=FACE_BOUND ( 'NONE', #1216, .T. ) ;
#33299=VERTEX_POINT ( 'NONE', #24196 ) ;
#33301=ORIENTED_EDGE ( 'NONE', *, *, #39936, .T. ) ;
#33313=ORIENTED_EDGE ( 'NONE', *, *, #60477, .F. ) ;
#33314=CARTESIAN_POINT ( 'NONE',  ( 6.976090560819000252, 5.172411450403999744, -8.246583185469999577 ) ) ;
#33315=CARTESIAN_POINT ( 'NONE',  ( 9.342711596876126734, 5.100000000000000533, -6.305985889523087806 ) ) ;
#33316=DIRECTION ( 'NONE',  ( 0.000000000000000000, -1.000000000000000000, 0.000000000000000000 ) ) ;
#33319=CARTESIAN_POINT ( 'NONE',  ( 9.626145280412998773, 3.934138271021000222, -9.063586117809000697 ) ) ;
#33328=CARTESIAN_POINT ( 'NONE',  ( 1.053056799209125094, 2.798833948393625537, 2.150913519912209360 ) ) ;
#33347=DIRECTION ( 'NONE',  ( 1.000000000000000000, 0.000000000000000000, 0.000000000000000000 ) ) ;
#33350=AXIS2_PLACEMENT_3D ( 'NONE', #56701, #8801, #30141 ) ;
#33356=CARTESIAN_POINT ( 'NONE',  ( 5.449999267937000624, 6.217248937900999058E-14, -13.04999927352996281 ) ) ;
#33364=CARTESIAN_POINT ( 'NONE',  ( 7.000000000000002665, 8.394866283432396159, 4.394866297543325473 ) ) ;
#33372=CARTESIAN_POINT ( 'NONE',  ( 8.175739158770999992, 4.686731264770999772, -8.717075579553000608 ) ) ;
#33375=CARTESIAN_POINT ( 'NONE',  ( 7.016960841228000234, 3.332350081667999842, -9.278694849147001378 ) ) ;
#33379=CARTESIAN_POINT ( 'NONE',  ( 10.59999999999999964, 3.399999999999999911, -4.756097560976000338 ) ) ;
#33389=CARTESIAN_POINT ( 'NONE',  ( 8.138783675073003820, 5.105454305967005446, -6.386197971998996969 ) ) ;
#33390=CARTESIAN_POINT ( 'NONE',  ( 4.500000000000000000, 0.000000000000000000, 0.000000000000000000 ) ) ;
#33398=CARTESIAN_POINT ( 'NONE',  ( 10.84974221959000218, 5.265003089217000998, -6.385808769407000263 ) ) ;
#33405=ORIENTED_EDGE ( 'NONE', *, *, #21482, .F. ) ;
#33407=VECTOR ( 'NONE', #49928, 1000.000000000000000 ) ;
#33408=CARTESIAN_POINT ( 'NONE',  ( 10.03280471959000231, 3.987760651117999711, -9.123263301387000368 ) ) ;
#33423=CARTESIAN_POINT ( 'NONE',  ( 6.911134836320000474, -12.43100038668999829, -2.821124938267000282 ) ) ;
#33424=CARTESIAN_POINT ( 'NONE',  ( 4.149992563291999836, -1.747525841223986465, 1.007210908820208140 ) ) ;
#33425=ORIENTED_EDGE ( 'NONE', *, *, #22122, .F. ) ;
#33427=CARTESIAN_POINT ( 'NONE',  ( 9.313108942797164502, 2.920708135355637225, -8.329534079918376577 ) ) ;
#33428=CARTESIAN_POINT ( 'NONE',  ( 8.863029719594999634, 2.990001567622999623, -8.695425648791999862 ) ) ;
#33429=DIRECTION ( 'NONE',  ( 0.000000000000000000, 1.000000000000000000, 0.000000000000000000 ) ) ;
#33430=CARTESIAN_POINT ( 'NONE',  ( 6.999999691988000095, -12.11716380430000051, 3.069905306952000146 ) ) ;
#33431=CARTESIAN_POINT ( 'NONE',  ( 0.5105665232603000536, 3.646234950436999966, -0.6383912046097000026 ) ) ;
#33434=CARTESIAN_POINT ( 'NONE',  ( 3.024430197351000160, 1.374756561418999823, -3.318718615493999824 ) ) ;
#33437=DIRECTION ( 'NONE',  ( 0.000000000000000000, 0.000000000000000000, -1.000000000000000000 ) ) ;
#33439=CARTESIAN_POINT ( 'NONE',  ( 7.165489158771000788, 2.688365364125000045, 8.140015608605001063 ) ) ;
#33443=CARTESIAN_POINT ( 'NONE',  ( 10.93466815658861613, 9.405386378085696109, 6.163902746065222260 ) ) ;
#33445=CARTESIAN_POINT ( 'NONE',  ( 11.00588826681000043, 3.012760565655999923, 5.961496895743000124 ) ) ;
#33447=EDGE_LOOP ( 'NONE', ( #49588, #20542, #13029, #48684, #65198 ) ) ;
#33450=CARTESIAN_POINT ( 'NONE',  ( 8.241912900173000267, 4.599999999999999645, 6.117539782833000928 ) ) ;
#33451=ORIENTED_EDGE ( 'NONE', *, *, #28863, .T. ) ;
#33468=B_SPLINE_CURVE_WITH_KNOTS ( 'NONE', 3,
 ( #42914, #12136, #54782, #609 ),
 .UNSPECIFIED., .F., .F.,
 ( 4, 4 ),
 ( 0.000000000000000000, 1.000000000000000000 ),
 .UNSPECIFIED. ) ;
#33472=CARTESIAN_POINT ( 'NONE',  ( 7.640272165042063079, 2.497528546856052412, -6.408390592194270319 ) ) ;
#33484=CARTESIAN_POINT ( 'NONE',  ( 3.999971066382000284, -2.149963194831999935, 0.000000000000000000 ) ) ;
#33486=EDGE_CURVE ( 'NONE', #38790, #47849, #18955, .T. ) ;
#33487=CARTESIAN_POINT ( 'NONE',  ( 2.796577467967999997, 2.816309704165000039, -1.867789267639999862 ) ) ;
#33495=CARTESIAN_POINT ( 'NONE',  ( 9.815201913989998417, 2.813632032385000148, 8.848857341496000117 ) ) ;
#33500=EDGE_CURVE ( 'NONE', #29486, #5467, #15843, .T. ) ;
#33501=CARTESIAN_POINT ( 'NONE',  ( 10.34160003447459708, 3.644395320192564736, 9.238506757596626429 ) ) ;
#33506=VERTEX_POINT ( 'NONE', #57376 ) ;
#33514=CARTESIAN_POINT ( 'NONE',  ( 9.272295280408998863, 3.705846972803000128, 9.096435887808000942 ) ) ;
#33515=CARTESIAN_POINT ( 'NONE',  ( 8.356920280409999791, 4.851303550474000303, -9.008742670124000540 ) ) ;
#33517=CARTESIAN_POINT ( 'NONE',  ( 2.855370644018131010, 1.774957683866571490, 2.731955323636169553 ) ) ;
#33519=CARTESIAN_POINT ( 'NONE',  ( 9.743561007103998861, 5.287400066955999733, 8.939966147452000911 ) ) ;
#33523=CARTESIAN_POINT ( 'NONE',  ( 8.057199896074001444, 2.877672799700000450, 6.732802633655004421 ) ) ;
#33524=VERTEX_POINT ( 'NONE', #9478 ) ;
#33540=CARTESIAN_POINT ( 'NONE',  ( 9.848670280409999478, 5.002683760508999988, -8.912673867568997821 ) ) ;
#33542=EDGE_CURVE ( 'NONE', #15832, #29686, #54932, .T. ) ;
#33553=CARTESIAN_POINT ( 'NONE',  ( 11.03408597791999846, 2.992846905312999795, -9.056576857348998644 ) ) ;
#33560=CARTESIAN_POINT ( 'NONE',  ( 9.385308886257000438, 4.135077451221000011, 9.175524215473998879 ) ) ;
#33566=CARTESIAN_POINT ( 'NONE',  ( 7.856038276909000473, 2.869044596334999753, -6.744487387516000076 ) ) ;
#33580=B_SPLINE_SURFACE_WITH_KNOTS ( 'NONE', 3, 3, ( 
 ( #32775, #43615, #58996, #53062 ),
 ( #6185, #16340, #38356, #11780 ),
 ( #37666, #21924, #54436, #48161 ),
 ( #42571, #27184, #17024, #31746 ),
 ( #16680, #15993, #43262, #64910 ),
 ( #47826, #27527, #11434, #69136 ),
 ( #11098, #5163, #962, #5507 ),
 ( #54088, #42916, #26847, #26496 ),
 ( #32432, #37324, #22273, #59682 ) ),
 .UNSPECIFIED., .F., .F., .F.,
 ( 4, 1, 1, 1, 1, 1, 4 ),
 ( 4, 4 ),
 ( -0.01864526228370000024, 0.000000000000000000, 0.2500000000000000000, 0.5000000000000000000, 0.7500000000000000000, 1.000000000000000000, 1.019255357118999950 ),
 ( -0.2206650646280000072, 1.220665064628000174 ),
 .UNSPECIFIED. ) ;
#33585=CARTESIAN_POINT ( 'NONE',  ( 9.395323341230000125, 5.146726419831999522, 6.597424767138000412 ) ) ;
#33589=CARTESIAN_POINT ( 'NONE',  ( 8.748814158775001459, 5.251032986819000214, -6.070151079272999795 ) ) ;
#33591=FACE_OUTER_BOUND ( 'NONE', #67276, .T. ) ;
#33592=CARTESIAN_POINT ( 'NONE',  ( 8.500383147356993518, 5.097359707274998541, 6.605634423517003029 ) ) ;
#33597=ORIENTED_EDGE ( 'NONE', *, *, #66632, .F. ) ;
#33598=CARTESIAN_POINT ( 'NONE',  ( 1.353155746511000235, 3.398721108301999916, 0.4283847067656000318 ) ) ;
#33605=CARTESIAN_POINT ( 'NONE',  ( 10.95213788363000162, 2.845858105723999998, 5.181730564763999958 ) ) ;
#33611=CARTESIAN_POINT ( 'NONE',  ( 9.550814556648244746, 5.350066006687046460, -7.263181378929296272 ) ) ;
#33616=AXIS2_PLACEMENT_3D ( 'NONE', #9817, #64315, #58741 ) ;
#33618=CARTESIAN_POINT ( 'NONE',  ( 9.625496329943999285, 3.134638325776999856, 8.626949804392001653 ) ) ;
#33621=EDGE_CURVE ( 'NONE', #58219, #14861, #49380, .T. ) ;
#33625=EDGE_CURVE ( 'NONE', #51298, #4821, #63303, .T. ) ;
#33626=EDGE_CURVE ( 'NONE', #18530, #17232, #869, .T. ) ;
#33629=ORIENTED_EDGE ( 'NONE', *, *, #68166, .T. ) ;
#33630=CARTESIAN_POINT ( 'NONE',  ( 8.845310841232000953, 5.851083642416999631, -7.072167224702999633 ) ) ;
#33635=ORIENTED_EDGE ( 'NONE', *, *, #58227, .F. ) ;
#33637=CYLINDRICAL_SURFACE ( 'NONE', #42748, 0.4999999999999998335 ) ;
#33639=CARTESIAN_POINT ( 'NONE',  ( 9.305881816721999655, 4.945299866898000829, 9.077891794505999812 ) ) ;
#33641=CARTESIAN_POINT ( 'NONE',  ( 11.09999993992000000, 9.806598331764000420, -6.066326716004000197 ) ) ;
#33646=ORIENTED_EDGE ( 'NONE', *, *, #41271, .F. ) ;
#33647=ADVANCED_FACE ( 'NONE', ( #63990 ), #2478, .F. ) ;
#33650=CARTESIAN_POINT ( 'NONE',  ( 10.81218444402201584, 3.003105123708600388, -4.859602167815589624 ) ) ;
#33656=VERTEX_POINT ( 'NONE', #4577 ) ;
#33657=CARTESIAN_POINT ( 'NONE',  ( 7.878292898358790097, 3.256492674266815435, -6.335713178755712605 ) ) ;
#33665=CARTESIAN_POINT ( 'NONE',  ( 9.874770280412001000, 4.038835765825999680, -5.935509327774999733 ) ) ;
#33669=CARTESIAN_POINT ( 'NONE',  ( 8.064958992852089281, 5.350069970865218849, -7.500002487662858819 ) ) ;
#33672=ADVANCED_FACE ( 'NONE', ( #36404 ), #25575, .T. ) ;
#33674=FACE_OUTER_BOUND ( 'NONE', #59199, .T. ) ;
#33675=DIRECTION ( 'NONE',  ( -1.000000000000000000, 0.000000000000000000, 0.000000000000000000 ) ) ;
#33683=AXIS2_PLACEMENT_3D ( 'NONE', #34848, #50920, #3019 ) ;
#33691=VERTEX_POINT ( 'NONE', #10860 ) ;
#33695=CARTESIAN_POINT ( 'NONE',  ( 6.999998971696786754, 12.01547034654740109, 3.452253082527627637 ) ) ;
#33702=ORIENTED_EDGE ( 'NONE', *, *, #27078, .T. ) ;
#33706=EDGE_CURVE ( 'NONE', #13653, #45966, #46899, .T. ) ;
#33710=CARTESIAN_POINT ( 'NONE',  ( 10.57960558317114774, 4.353252721116626311, 8.851706718789662531 ) ) ;
#33715=CARTESIAN_POINT ( 'NONE',  ( 3.500000000000000000, 0.000000000000000000, 0.000000000000000000 ) ) ;
#33720=CARTESIAN_POINT ( 'NONE',  ( 8.772439158776000667, 3.098073081301000009, -8.567513114264999174 ) ) ;
#33726=CARTESIAN_POINT ( 'NONE',  ( 8.368787704064557076, 3.808649829341963056, -6.044288580653415899 ) ) ;
#33728=CARTESIAN_POINT ( 'NONE',  ( 8.947714158774999760, 3.854507394315999758, -9.394302886912999639 ) ) ;
#33731=CARTESIAN_POINT ( 'NONE',  ( 9.701722306758000514, 4.253749110891999585, -8.839930742927998963 ) ) ;
#33745=CARTESIAN_POINT ( 'NONE',  ( 10.69030645188999884, 5.903031974240000146, 7.830710565751001440 ) ) ;
#33746=CARTESIAN_POINT ( 'NONE',  ( 10.22094528040999961, 2.563078870232999851, -8.004103956955001209 ) ) ;
#33755=CARTESIAN_POINT ( 'NONE',  ( 9.594139158774000364, 2.212639797530000063, -6.855876382544999537 ) ) ;
#33756=EDGE_CURVE ( 'NONE', #37026, #13153, #22469, .T. ) ;
#33762=DIRECTION ( 'NONE',  ( -1.000000000000000000, 0.000000000000000000, 0.000000000000000000 ) ) ;
#33774=CARTESIAN_POINT ( 'NONE',  ( 11.09999999999999964, 5.299999999999999822, -5.160242713806000303 ) ) ;
#33775=CARTESIAN_POINT ( 'NONE',  ( 9.061929719594999710, 4.092867382745001059, -5.937785237406000505 ) ) ;
#33780=LINE ( 'NONE', #51227, #44550 ) ;
#33783=CARTESIAN_POINT ( 'NONE',  ( 2.685883213202000075, 3.284924929773000102, -0.9716413097203999705 ) ) ;
#33784=ORIENTED_EDGE ( 'NONE', *, *, #47858, .T. ) ;
#33788=CARTESIAN_POINT ( 'NONE',  ( 7.833767219591000419, 2.583668273793999770, 6.684750595573999199 ) ) ;
#33791=EDGE_CURVE ( 'NONE', #41535, #22650, #31177, .T. ) ;
#33793=CARTESIAN_POINT ( 'NONE',  ( 7.987835841226000433, 4.422660346525999486, -6.167928437610999737 ) ) ;
#33795=CARTESIAN_POINT ( 'NONE',  ( 10.80457650502821387, 2.650115154242055127, -7.676668932391350175 ) ) ;
#33797=VERTEX_POINT ( 'NONE', #39164 ) ;
#33804=CARTESIAN_POINT ( 'NONE',  ( 10.94095842555437059, 9.300938419463392393, -6.243091547608035086 ) ) ;
#33805=LINE ( 'NONE', #50224, #328 ) ;
#33807=LINE ( 'NONE', #65942, #68313 ) ;
#33818=CYLINDRICAL_SURFACE ( 'NONE', #48378, 2.750000000000000000 ) ;
#33821=CARTESIAN_POINT ( 'NONE',  ( 7.938622165042806600, 4.610389606898620762, -9.253982923057691323 ) ) ;
#33822=CARTESIAN_POINT ( 'NONE',  ( 5.000030787343001215, -1.057581170753187694, 1.834918991542629163 ) ) ;
#33824=CARTESIAN_POINT ( 'NONE',  ( 6.999998782146999332, -11.95749337870000062, -3.642574926947999892 ) ) ;
#33826=ORIENTED_EDGE ( 'NONE', *, *, #31967, .F. ) ;
#33828=ORIENTED_EDGE ( 'NONE', *, *, #36018, .T. ) ;
#33831=CARTESIAN_POINT ( 'NONE',  ( 9.983079719591000156, 5.002683760508999988, -8.912673867568997821 ) ) ;
#33832=CARTESIAN_POINT ( 'NONE',  ( 3.208990468877999991, 2.744503479086000119, -1.674591564687999856 ) ) ;
#33835=CARTESIAN_POINT ( 'NONE',  ( 8.220124669774001802, 3.381964873247001790, -6.130490311850000928 ) ) ;
#33840=CARTESIAN_POINT ( 'NONE',  ( 9.571961069101000419, 4.084683332033999470, 8.946609345378000455 ) ) ;
#33841=DIRECTION ( 'NONE',  ( -1.000000000000000000, 0.000000000000000000, 0.000000000000000000 ) ) ;
#33842=DIRECTION ( 'NONE',  ( 1.000000000000000000, 0.000000000000000000, 0.000000000000000000 ) ) ;
#33845=CARTESIAN_POINT ( 'NONE',  ( 7.100000000000060041, 5.084948259510642110, -8.362010274963123990 ) ) ;
#33847=ADVANCED_FACE ( 'NONE', ( #12596 ), #34597, .F. ) ;
#33850=CARTESIAN_POINT ( 'NONE',  ( 11.02452225494999993, 2.775477745048999800, -6.571291218949999902 ) ) ;
#33860=CARTESIAN_POINT ( 'NONE',  ( 8.052732780410000402, 4.968147183437999992, 5.971792472497999604 ) ) ;
#33863=CARTESIAN_POINT ( 'NONE',  ( 10.45625165877000029, 3.661871102473000406, -9.317475234260999883 ) ) ;
#33865=CARTESIAN_POINT ( 'NONE',  ( 9.632179190069999564, 5.638172764974000550, 6.476627236431999890 ) ) ;
#33869=CARTESIAN_POINT ( 'NONE',  ( 8.332048273611004419, 2.867478057767001154, 6.314276212112998721 ) ) ;
#33872=ADVANCED_FACE ( 'NONE', ( #22554 ), #13950, .T. ) ;
#33879=ORIENTED_EDGE ( 'NONE', *, *, #55235, .T. ) ;
#33885=AXIS2_PLACEMENT_3D ( 'NONE', #25212, #41300, #44583 ) ;
#33887=CARTESIAN_POINT ( 'NONE',  ( 9.193385841233000733, 2.981992329588000423, -5.895876591910999664 ) ) ;
#33889=CARTESIAN_POINT ( 'NONE',  ( 9.115118560745049336, 5.349923934101355805, -7.499992884230159973 ) ) ;
#33895=CARTESIAN_POINT ( 'NONE',  ( 9.496378438922302934, 5.350075508921114498, 7.852928877054549339 ) ) ;
#33899=ADVANCED_FACE ( 'NONE', ( #64765 ), #61949, .F. ) ;
#33901=CARTESIAN_POINT ( 'NONE',  ( 10.18576633586645031, 4.069734382926330163, -8.865705745737809451 ) ) ;
#33902=CARTESIAN_POINT ( 'NONE',  ( 10.68055531501999944, 2.768167480619000198, -6.114404645958000373 ) ) ;
#33904=LINE ( 'NONE', #17112, #19648 ) ;
#33911=AXIS2_PLACEMENT_3D ( 'NONE', #33140, #6205, #64244 ) ;
#33914=CARTESIAN_POINT ( 'NONE',  ( 11.18484176840999922, 2.599663474744000169, 7.740674686800000259 ) ) ;
#33918=CARTESIAN_POINT ( 'NONE',  ( 9.566963020987998334, 5.215925787220999865, 6.177726425586999248 ) ) ;
#33920=CARTESIAN_POINT ( 'NONE',  ( 2.328734235851999568, 1.852089340889000013, 2.627990287460999941 ) ) ;
#33932=CARTESIAN_POINT ( 'NONE',  ( 7.635857780409000206, 2.466388272391000225, 6.935562100014999842 ) ) ;
#33944=CARTESIAN_POINT ( 'NONE',  ( 1.067064049866000008, -3.242811033061999915, 1.104080751309999942 ) ) ;
#33950=CARTESIAN_POINT ( 'NONE',  ( 10.90728308714999883, 2.969488398748000080, 4.935980545376000173 ) ) ;
#33954=CARTESIAN_POINT ( 'NONE',  ( 10.02790872788999899, 7.656519725853999425, -5.745353671516999938 ) ) ;
#33955=DIRECTION ( 'NONE',  ( -1.000000000000000000, 0.000000000000000000, 0.000000000000000000 ) ) ;
#33957=CIRCLE ( 'NONE', #3792, 1.700000201121000032 ) ;
#33959=CARTESIAN_POINT ( 'NONE',  ( 1.800476376745000051, -3.604362431180999859, -1.066289260138999939 ) ) ;
#33962=EDGE_CURVE ( 'NONE', #36930, #50903, #5016, .T. ) ;
#33963=DIRECTION ( 'NONE',  ( -1.000000000000000000, 0.000000000000000000, 0.000000000000000000 ) ) ;
#33964=CARTESIAN_POINT ( 'NONE',  ( 10.90638722582999875, 5.227488226180000197, 6.784465725675999259 ) ) ;
#33973=CARTESIAN_POINT ( 'NONE',  ( 7.377259056795572256, 2.936797553513828873, 8.875456578139957031 ) ) ;
#33975=ORIENTED_EDGE ( 'NONE', *, *, #53515, .F. ) ;
#33985=FACE_OUTER_BOUND ( 'NONE', #18048, .T. ) ;
#33990=CARTESIAN_POINT ( 'NONE',  ( 11.07503769033409746, 4.268003910470056894, -9.025037683628568175 ) ) ;
#33991=DIRECTION ( 'NONE',  ( 1.000000000000000000, 0.000000000000000000, 0.000000000000000000 ) ) ;
#33992=ORIENTED_EDGE ( 'NONE', *, *, #57349, .T. ) ;
#33997=CARTESIAN_POINT ( 'NONE',  ( 5.000015393671500163, -2.571712834666313134E-16, -2.099962892531002545 ) ) ;
#34004=CARTESIAN_POINT ( 'NONE',  ( 7.849093588702794833, 2.941815248762500890, -6.601834848426078040 ) ) ;
#34007=CYLINDRICAL_SURFACE ( 'NONE', #37624, 3.500000000000000000 ) ;
#34011=AXIS2_PLACEMENT_3D ( 'NONE', #62382, #8561, #36157 ) ;
#34013=CARTESIAN_POINT ( 'NONE',  ( 9.327795280414001411, 3.161445734422999809, -6.178649910536000434 ) ) ;
#34016=EDGE_CURVE ( 'NONE', #32335, #42555, #32973, .T. ) ;
#34018=DIRECTION ( 'NONE',  ( 0.000000000000000000, 1.000000000000000000, 0.000000000000000000 ) ) ;
#34025=CARTESIAN_POINT ( 'NONE',  ( 1.178056799208624827, -2.150913519912214245, 2.798833948393621984 ) ) ;
#34031=ORIENTED_EDGE ( 'NONE', *, *, #9596, .F. ) ;
#34032=B_SPLINE_CURVE_WITH_KNOTS ( 'NONE', 3,
 ( #30233, #30565, #41402, #24289 ),
 .UNSPECIFIED., .F., .F.,
 ( 4, 4 ),
 ( 0.000000000000000000, 1.000000000000000000 ),
 .UNSPECIFIED. ) ;
#34041=EDGE_LOOP ( 'NONE', ( #59663, #52286, #29250, #18054 ) ) ;
#34049=DIRECTION ( 'NONE',  ( -1.000000000000000000, 0.000000000000000000, 0.000000000000000000 ) ) ;
#34057=CARTESIAN_POINT ( 'NONE',  ( 4.900006121741999010, 0.5234957687185600728, -1.947945353336631102 ) ) ;
#34060=ORIENTED_EDGE ( 'NONE', *, *, #17050, .T. ) ;
#34065=ADVANCED_FACE ( 'NONE', ( #7783 ), #39254, .T. ) ;
#34066=CARTESIAN_POINT ( 'NONE',  ( 8.356920280409999791, 4.851303550474000303, -9.008742670124000540 ) ) ;
#34076=VERTEX_POINT ( 'NONE', #18279 ) ;
#34077=CARTESIAN_POINT ( 'NONE',  ( 10.84087666499999969, 2.636288985756999992, -7.512643730465999425 ) ) ;
#34078=B_SPLINE_CURVE_WITH_KNOTS ( 'NONE', 3,
 ( #54689, #1209, #43860, #13087 ),
 .UNSPECIFIED., .F., .F.,
 ( 4, 4 ),
 ( 0.000000000000000000, 1.000000000000000000 ),
 .UNSPECIFIED. ) ;
#34083=CARTESIAN_POINT ( 'NONE',  ( 10.85685100254000091, 2.832432432432000269, -6.822293592207000934 ) ) ;
#34085=FACE_BOUND ( 'NONE', #46385, .T. ) ;
#34088=VERTEX_POINT ( 'NONE', #50429 ) ;
#34089=CARTESIAN_POINT ( 'NONE',  ( 9.428197172113266689, 5.125396288426561142, 6.749639981083131346 ) ) ;
#34090=CARTESIAN_POINT ( 'NONE',  ( 10.44812028041000040, 5.235600787608000850, -6.609970743661000903 ) ) ;
#34098=ORIENTED_EDGE ( 'NONE', *, *, #4184, .T. ) ;
#34100=CARTESIAN_POINT ( 'NONE',  ( 9.246064158776000852, 5.200883864107000321, -6.027780766890000308 ) ) ;
#34101=CARTESIAN_POINT ( 'NONE',  ( 9.129428851719998406, 5.099284414202999827, 6.151604790022999758 ) ) ;
#34110=CARTESIAN_POINT ( 'NONE',  ( 5.399998535875000449, 6.217248937900999058E-14, 3.708144902247999495E-14 ) ) ;
#34112=ORIENTED_EDGE ( 'NONE', *, *, #18790, .F. ) ;
#34113=CARTESIAN_POINT ( 'NONE',  ( 7.564999999998999414, 5.349999999999999645, -7.500000000000000000 ) ) ;
#34114=CARTESIAN_POINT ( 'NONE',  ( 8.126014158770999529, 5.189036231907000030, -8.048606212067999977 ) ) ;
#34115=CARTESIAN_POINT ( 'NONE',  ( 9.361802827890667089, 2.874603711572071951, -6.749639981085484131 ) ) ;
#34116=CARTESIAN_POINT ( 'NONE',  ( 11.09999999999999964, 5.538898460221000519, 7.685179721164000277 ) ) ;
#34120=CARTESIAN_POINT ( 'NONE',  ( 10.88867070183947483, 5.215510510159838020, 6.904563811839100396 ) ) ;
#34122=CARTESIAN_POINT ( 'NONE',  ( 9.111654719595000174, 4.989193221215000307, -6.287302145481000082 ) ) ;
#34123=CARTESIAN_POINT ( 'NONE',  ( 8.580795537699431819, 5.100000000000000533, -6.662590550605527184 ) ) ;
#34127=AXIS2_PLACEMENT_3D ( 'NONE', #26274, #68908, #41321 ) ;
#34128=CARTESIAN_POINT ( 'NONE',  ( 8.203568157088000135, 3.399999998409999780, 6.139678131101000247 ) ) ;
#34129=CARTESIAN_POINT ( 'NONE',  ( 3.262839944555000038, -0.8785454485268000546, 3.483102888041999634 ) ) ;
#34135=CARTESIAN_POINT ( 'NONE',  ( 8.539829719592999524, 5.633477595780999714, 7.451234169193000412 ) ) ;
#34138=CARTESIAN_POINT ( 'NONE',  ( 10.95521427414540128, 9.021152868672782432, 6.404909939993181034 ) ) ;
#34140=CARTESIAN_POINT ( 'NONE',  ( 10.73165287102628085, 3.320185038362386098, -8.679412628036420330 ) ) ;
#34148=VERTEX_POINT ( 'NONE', #13037 ) ;
#34149=CARTESIAN_POINT ( 'NONE',  ( 10.92633922843239169, 9.535098715412203774, -6.046881589190145512 ) ) ;
#34150=CARTESIAN_POINT ( 'NONE',  ( 8.270987821524766304, 2.867662864822190016, 6.761597825165790887 ) ) ;
#34151=CARTESIAN_POINT ( 'NONE',  ( 10.90000154029999990, 0.000000000000000000, 0.000000000000000000 ) ) ;
#34156=LINE ( 'NONE', #50229, #34339 ) ;
#34163=VECTOR ( 'NONE', #26711, 999.9999999999998863 ) ;
#34164=CARTESIAN_POINT ( 'NONE',  ( 0.1744510438295829302, -0.5461907802877905560, -3.174431049355146861 ) ) ;
#34165=CARTESIAN_POINT ( 'NONE',  ( 8.038072165043022466, 2.528277501517397940, -8.632724327209173154 ) ) ;
#34174=CARTESIAN_POINT ( 'NONE',  ( 0.1499942179679999710, -1.384928887584818469, 2.402872127494066756 ) ) ;
#34177=CARTESIAN_POINT ( 'NONE',  ( 2.370651199330000125, 0.2798869272278999842, 3.202845242003000248 ) ) ;
#34187=CARTESIAN_POINT ( 'NONE',  ( 10.46932803217000085, 4.988495740890000363, 6.213106455073000411 ) ) ;
#34196=CARTESIAN_POINT ( 'NONE',  ( 0.9319208874357501893, 2.278816592008448882, -2.686138227945438217 ) ) ;
#34197=CARTESIAN_POINT ( 'NONE',  ( 11.25809834123000108, 3.275514549383000240, -8.650774600386998969 ) ) ;
#34207=CARTESIAN_POINT ( 'NONE',  ( 7.101301658771000724, 3.554857159507999853, 8.889479859586000288 ) ) ;
#34209=CARTESIAN_POINT ( 'NONE',  ( 8.795585841232000490, 5.251032986819000214, -6.070151079272999795 ) ) ;
#34210=CARTESIAN_POINT ( 'NONE',  ( 0.7179470766575658525, -1.805094916197470312, 3.044603405180807965 ) ) ;
#34213=CARTESIAN_POINT ( 'NONE',  ( 10.00122429346999908, 2.274087081648999753, 7.851326250696001097 ) ) ;
#34219=DIRECTION ( 'NONE',  ( 1.000000000000000000, 0.000000000000000000, 0.000000000000000000 ) ) ;
#34220=CARTESIAN_POINT ( 'NONE',  ( 1.459306799207500172, 3.058252359239905793, -1.762666431298143488 ) ) ;
#34230=CARTESIAN_POINT ( 'NONE',  ( 9.314928906318884927, 2.650140463285438397, -7.499996151983930659 ) ) ;
#34233=CARTESIAN_POINT ( 'NONE',  ( 8.655270280412999284, 4.162493982103000256, -5.775210092227999858 ) ) ;
#34235=FACE_OUTER_BOUND ( 'NONE', #68779, .T. ) ;
#34240=DIRECTION ( 'NONE',  ( 0.000000000000000000, -1.000000000000000000, 0.000000000000000000 ) ) ;
#34243=DIRECTION ( 'NONE',  ( 0.000000000000000000, 0.000000000000000000, -1.000000000000000000 ) ) ;
#34249=CARTESIAN_POINT ( 'NONE',  ( 6.308905548400004726, 8.386554649686992491, -3.907920053779999847 ) ) ;
#34255=CARTESIAN_POINT ( 'NONE',  ( 8.610051658774001027, 5.329437560656000272, 6.027391099688998999 ) ) ;
#34256=VERTEX_POINT ( 'NONE', #35052 ) ;
#34263=CARTESIAN_POINT ( 'NONE',  ( 11.01812914314999858, 5.553047824615000572, 4.991737071610000243 ) ) ;
#34264=CARTESIAN_POINT ( 'NONE',  ( 10.02991192131000098, 2.506457833269999824, 6.215406506815000398 ) ) ;
#34269=EDGE_CURVE ( 'NONE', #37026, #53667, #35006, .T. ) ;
#34274=CARTESIAN_POINT ( 'NONE',  ( 9.848259964010999568, 4.436917881843999822, 6.148031614254000132 ) ) ;
#34279=CARTESIAN_POINT ( 'NONE',  ( 7.545267219589999463, 2.302289264429000504, 6.875166305059000393 ) ) ;
#34280=CARTESIAN_POINT ( 'NONE',  ( 9.256664404737000140, 4.025830366070999311, 9.295863330698999505 ) ) ;
#34283=CARTESIAN_POINT ( 'NONE',  ( 9.585279719593998493, 2.928319778732999978, -8.861178115809998701 ) ) ;
#34291=CARTESIAN_POINT ( 'NONE',  ( 1.644020781218000105, 0.6682336154344999946, -3.189788463028000454 ) ) ;
#34297=CARTESIAN_POINT ( 'NONE',  ( 4.900006121741999898, -0.2617993877991499074, -2.000000000000000444 ) ) ;
#34303=CARTESIAN_POINT ( 'NONE',  ( 11.13731690804999985, 5.336290732615000643, 5.187964585069000378 ) ) ;
#34307=CARTESIAN_POINT ( 'NONE',  ( 1.752794427304000147, -3.577811800725999802, 1.152232014823999950 ) ) ;
#34309=CARTESIAN_POINT ( 'NONE',  ( 10.81294898260098947, 2.920599542024987727, -8.329474447052378494 ) ) ;
#34318=CARTESIAN_POINT ( 'NONE',  ( 0.4529763571839853786, 3.676114825633475335E-06, -3.452897576335808072 ) ) ;
#34320=B_SPLINE_CURVE_WITH_KNOTS ( 'NONE', 3,
 ( #42397, #47297, #42734, #20377, #4981, #30876 ),
 .UNSPECIFIED., .F., .F.,
 ( 4, 2, 4 ),
 ( 0.000000000000000000, 0.5000000000000005551, 1.000000000000000000 ),
 .UNSPECIFIED. ) ;
#34322=CARTESIAN_POINT ( 'NONE',  ( 8.401779134048657838, 2.565904574551121975, 8.507432892281750370 ) ) ;
#34333=EDGE_CURVE ( 'NONE', #29419, #61078, #9899, .T. ) ;
#34334=CARTESIAN_POINT ( 'NONE',  ( 10.34021053755999908, 4.202028620710000162, 9.459600235481000041 ) ) ;
#34335=ADVANCED_FACE ( 'NONE', ( #2877 ), #46566, .T. ) ;
#34339=VECTOR ( 'NONE', #28214, 1000.000000000000114 ) ;
#34341=CARTESIAN_POINT ( 'NONE',  ( 4.000000000000000000, -2.136325177875821435, -0.2822470469891263378 ) ) ;
#34346=DIRECTION ( 'NONE',  ( 1.000000000000000000, 0.000000000000000000, 0.000000000000000000 ) ) ;
#34348=CARTESIAN_POINT ( 'NONE',  ( 5.000030787343001215, 0.2748844998327731326, -2.099962892531005654 ) ) ;
#34357=ADVANCED_FACE ( 'NONE', ( #8474 ), #56716, .T. ) ;
#34358=CARTESIAN_POINT ( 'NONE',  ( 10.60000000000016485, 4.647604842474216902, -4.756097560975663718 ) ) ;
#34364=CARTESIAN_POINT ( 'NONE',  ( 9.356463691919302050, 5.100000000000000533, 6.665341197421592589 ) ) ;
#34365=CARTESIAN_POINT ( 'NONE',  ( 8.231612003192127602, 3.320411601377035726, -8.679267246414919867 ) ) ;
#34372=CARTESIAN_POINT ( 'NONE',  ( 10.96888392554999925, 5.599999999999999645, 6.571291218949999902 ) ) ;
#34377=ORIENTED_EDGE ( 'NONE', *, *, #21684, .T. ) ;
#34386=CYLINDRICAL_SURFACE ( 'NONE', #10696, 1.350000000000000533 ) ;
#34394=CARTESIAN_POINT ( 'NONE',  ( 7.000000000000000000, 9.904500808576843340, -4.554970072511064672 ) ) ;
#34395=CARTESIAN_POINT ( 'NONE',  ( 7.000002934099999408, -1.865174681369999698E-13, 1.040631535496999952E-13 ) ) ;
#34407=CARTESIAN_POINT ( 'NONE',  ( 4.900006121741999898, 1.229093439949828781, -1.599333684796360844 ) ) ;
#34413=DIRECTION ( 'NONE',  ( 0.000000000000000000, -1.000000000000000000, 0.000000000000000000 ) ) ;
#34416=CARTESIAN_POINT ( 'NONE',  ( 9.798945280410000791, 5.639765292528999829, -8.059103558718000215 ) ) ;
#34422=MECHANICAL_DESIGN_GEOMETRIC_PRESENTATION_REPRESENTATION('',(#28835),#24372);
#34423=EDGE_CURVE ( 'NONE', #34720, #19975, #19131, .T. ) ;
#34425=ORIENTED_EDGE ( 'NONE', *, *, #40584, .F. ) ;
#34428=CARTESIAN_POINT ( 'NONE',  ( 9.793039158772000263, 5.817107086401000160, -6.945352709928000579 ) ) ;
#34430=CARTESIAN_POINT ( 'NONE',  ( 10.05525296965999971, 5.223856410664000194, -6.898317050646999959 ) ) ;
#34431=ORIENTED_EDGE ( 'NONE', *, *, #21606, .F. ) ;
#34435=DIRECTION ( 'NONE',  ( 0.000000000000000000, 0.000000000000000000, 1.000000000000000000 ) ) ;
#34436=CARTESIAN_POINT ( 'NONE',  ( 9.023148997459999876, 5.167567567567999731, -6.822293592207000934 ) ) ;
#34443=CARTESIAN_POINT ( 'NONE',  ( 10.69829221958999987, 2.534027248431999890, -6.667786804432999759 ) ) ;
#34453=CARTESIAN_POINT ( 'NONE',  ( 9.038304719595000591, 3.867331042029999999, -9.227339949050001877 ) ) ;
#34454=FACE_OUTER_BOUND ( 'NONE', #64821, .T. ) ;
#34456=CARTESIAN_POINT ( 'NONE',  ( 10.98768472639999949, 2.860900986606000007, -4.945212061661000469 ) ) ;
#34457=B_SPLINE_CURVE_WITH_KNOTS ( 'NONE', 3,
 ( #62259, #14380, #47568, #57347, #25889, #51767, #20644, #35700, #4899 ),
 .UNSPECIFIED., .F., .F.,
 ( 4, 1, 2, 2, 4 ),
 ( 0.000000000000000000, 0.2500000000000000555, 0.3750000000000000000, 0.5000000000000000000, 1.000000000000000000 ),
 .UNSPECIFIED. ) ;
#34459=CARTESIAN_POINT ( 'NONE',  ( 6.899999691988000450, 0.000000000000000000, 0.000000000000000000 ) ) ;
#34462=DIRECTION ( 'NONE',  ( 0.7071067811865475727, -0.7071067811865475727, 0.000000000000000000 ) ) ;
#34469=EDGE_CURVE ( 'NONE', #12694, #45049, #3215, .T. ) ;
#34472=CARTESIAN_POINT ( 'NONE',  ( 10.90000000000000036, 5.283926297003000094, 7.082827057608000132 ) ) ;
#34474=CARTESIAN_POINT ( 'NONE',  ( 8.912754719595000097, 2.481540185810000132, -7.878707153279001396 ) ) ;
#34477=VECTOR ( 'NONE', #23826, 1000.000000000000000 ) ;
#34480=CARTESIAN_POINT ( 'NONE',  ( 2.876611010965999693, -1.756444158189999882, 2.941041065258999776 ) ) ;
#34483=B_SPLINE_CURVE_WITH_KNOTS ( 'NONE', 3,
 ( #62345, #8865, #14801, #15143 ),
 .UNSPECIFIED., .F., .F.,
 ( 4, 4 ),
 ( 0.000000000000000000, 1.000000000000000000 ),
 .UNSPECIFIED. ) ;
#34487=CARTESIAN_POINT ( 'NONE',  ( 9.069718325438000051, 4.108964550738000376, 8.851615252874999840 ) ) ;
#34491=CARTESIAN_POINT ( 'NONE',  ( 8.435360841226998474, 3.517942668285999996, -6.188254172171000711 ) ) ;
#34494=AXIS2_PLACEMENT_3D ( 'NONE', #47067, #9301, #25387 ) ;
#34499=CARTESIAN_POINT ( 'NONE',  ( 0.04997405931213007302, 2.849971983161022848, 1.472630648340316603E-09 ) ) ;
#34502=ORIENTED_EDGE ( 'NONE', *, *, #49188, .T. ) ;
#34503=CARTESIAN_POINT ( 'NONE',  ( 10.96186279128636620, 8.868890186250860452, -6.466688578834012269 ) ) ;
#34506=CARTESIAN_POINT ( 'NONE',  ( 7.590514158769000375, 5.397384434738000003, -7.480682713844000631 ) ) ;
#34515=DIRECTION ( 'NONE',  ( 1.000000000000000000, 0.000000000000000000, 0.000000000000000000 ) ) ;
#34518=DIRECTION ( 'NONE',  ( 0.000000000000000000, 0.000000000000000000, -1.000000000000000000 ) ) ;
#34520=CARTESIAN_POINT ( 'NONE',  ( 6.993847165045809611, 3.347364397022671856, -9.238695015924625054 ) ) ;
#34530=CARTESIAN_POINT ( 'NONE',  ( 9.079170280414000871, 4.815598936798999752, -8.835641302565999666 ) ) ;
#34531=CARTESIAN_POINT ( 'NONE',  ( 2.628909614058000166, -3.044403958803000076, -1.466915694452000096 ) ) ;
#34537=CARTESIAN_POINT ( 'NONE',  ( 10.11094409420000062, 5.100000000000000533, -6.571291218949999902 ) ) ;
#34540=CARTESIAN_POINT ( 'NONE',  ( 11.25041981190000051, 5.730782764036999488, 8.122675980938000251 ) ) ;
#34541=CARTESIAN_POINT ( 'NONE',  ( 9.167131993064588258, 2.992074715526335194, 8.398797324404764453 ) ) ;
#34543=CARTESIAN_POINT ( 'NONE',  ( 10.95930679442663269, 2.825993392401128901, -6.684172063606795611 ) ) ;
#34550=EDGE_CURVE ( 'NONE', #718, #10646, #43728, .T. ) ;
#34551=CARTESIAN_POINT ( 'NONE',  ( 11.22023584123000006, 3.883089684441999978, -8.854806321849000739 ) ) ;
#34558=CARTESIAN_POINT ( 'NONE',  ( 9.117517219591000810, 4.954905351382000944, 8.825777580285999235 ) ) ;
#34561=CARTESIAN_POINT ( 'NONE',  ( 10.03976415876999972, 2.255572964181999929, -8.111983882175000105 ) ) ;
#34563=CARTESIAN_POINT ( 'NONE',  ( 10.24477918374999952, 5.265206995764999398, 8.959504263949002123 ) ) ;
#34564=CARTESIAN_POINT ( 'NONE',  ( 5.000030787343000327, -2.099962892530999881, 0.000000000000000000 ) ) ;
#34569=DIRECTION ( 'NONE',  ( 0.000000000000000000, 1.000000000000000000, 0.000000000000000000 ) ) ;
#34575=VERTEX_POINT ( 'NONE', #55252 ) ;
#34580=ORIENTED_EDGE ( 'NONE', *, *, #9311, .F. ) ;
#34582=CARTESIAN_POINT ( 'NONE',  ( 9.093935841232999806, 2.156584729807999867, -7.959751745006000689 ) ) ;
#34591=AXIS2_PLACEMENT_3D ( 'NONE', #65415, #49339, #54940 ) ;
#34592=CARTESIAN_POINT ( 'NONE',  ( 7.718334321649531482, 2.593359702620003038, 7.633860556273081244 ) ) ;
#34596=VERTEX_POINT ( 'NONE', #44431 ) ;
#34597=B_SPLINE_SURFACE_WITH_KNOTS ( 'NONE', 3, 3, ( 
 ( #2112, #48620, #12946, #23429, #44767, #66068, #60833, #34274, #11541, #721, #48962, #43380, #64680, #16787, #38117, #59442, #32884, #54195, #6297, #2446, #40533, #55593, #24804, #14322, #30400, #29380, #29037, #62201, #24463, #45788, #2788, #19559, #23770, #51032, #7695 ),
 ( #3132, #13979, #51708, #3804, #61858, #8725, #34962, #67099, #39860, #18878, #13300, #30068, #56279, #46128, #61181, #45105, #50346, #62538, #25142, #50692, #51371, #46473, #67779, #3469, #66414, #67435, #35304, #34624, #18533, #14659, #35647, #55937, #19209, #40881, #8039 ),
 ( #56620, #66761, #40204, #61522, #24114, #56959, #29728, #9061, #45448, #19901, #41227, #13637, #8386, #47853, #36672, #47160, #4838, #20583, #27825, #20931, #52046, #9392, #10092, #31090, #31427, #52743, #9742, #52398, #4490, #26179, #25830, #15683, #68460, #57992, #41909 ),
 ( #11717, #63214, #62875, #68122, #35975, #15344, #47506, #63571, #36320, #58329, #68811, #54373, #64849, #16960, #42267, #65199, #38293, #4149, #37017, #5189, #41566, #10431, #31772, #59622, #53089, #26526, #20241, #14995, #57637, #901, #22213, #43549, #33059, #6476, #30738 ) ),
 .UNSPECIFIED., .F., .F., .F.,
 ( 4, 4 ),
 ( 4, 1, 1, 1, 1, 1, 1, 1, 1, 1, 1, 1, 1, 1, 1, 1, 1, 1, 1, 1, 1, 1, 1, 1, 1, 1, 1, 1, 1, 1, 1, 1, 4 ),
 ( -0.1039370721279000015, 1.103937072127999963 ),
 ( -0.01735257130020999988, 0.01084535706264999969, 0.03904328542550000031, 0.06724121378835999641, 0.09543914215121999944, 0.1236370705141000004, 0.1518349988768999959, 0.1800329272397999947, 0.2082308556026999935, 0.2364287839655000167, 0.2646267123283999601, 0.2928246406912000110, 0.3210225690540999821, 0.3492204974169000331, 0.3774184257798000042, 0.4056163541427000307, 0.4338142825054999707, 0.4620122108683999973, 0.4902101392311999928, 0.5184080675940999638, 0.5466059959569999904, 0.5748039243197999859, 0.6030018526827000125, 0.6311997810455000080, 0.6593977094084000345, 0.6875956377712000300, 0.7157935661340999456, 0.7439914944969999722, 0.7721894228597999676, 0.8003873512226999942, 0.8285852795854999897, 0.8567832079484000163, 0.8849811363112999318 ),
 .UNSPECIFIED. ) ;
#34603=CARTESIAN_POINT ( 'NONE',  ( 9.838567964380441566, 5.764523275123773161, -7.468534388609791463 ) ) ;
#34607=CARTESIAN_POINT ( 'NONE',  ( 10.25000000000000000, 0.000000000000000000, 0.000000000000000000 ) ) ;
#34608=CARTESIAN_POINT ( 'NONE',  ( 8.315517219592001297, 5.485785046334999748, 8.532070739720001740 ) ) ;
#34610=ADVANCED_FACE ( 'NONE', ( #17502 ), #62511, .F. ) ;
#34613=CARTESIAN_POINT ( 'NONE',  ( 8.027701659444428373, 5.080332885338247451, 8.330387188615796745 ) ) ;
#34614=FACE_OUTER_BOUND ( 'NONE', #59347, .T. ) ;
#34618=CARTESIAN_POINT ( 'NONE',  ( 11.20904666305999875, 5.937823941418000295, 7.147334722859000067 ) ) ;
#34624=CARTESIAN_POINT ( 'NONE',  ( 10.87148757351999961, 5.567567343464999929, 7.772413227960999649 ) ) ;
#34628=CARTESIAN_POINT ( 'NONE',  ( 8.700642219592999993, 5.212261578733999201, 6.157186134061999994 ) ) ;
#34629=CARTESIAN_POINT ( 'NONE',  ( 10.99433665574000152, 3.697618584609999814, 5.729302299903000772 ) ) ;
#34631=EDGE_CURVE ( 'NONE', #24517, #63941, #47513, .T. ) ;
#34633=CARTESIAN_POINT ( 'NONE',  ( 9.743314158772999889, 5.149303692842000402, -5.987168472229000393 ) ) ;
#34643=CARTESIAN_POINT ( 'NONE',  ( 0.8286543026616000063, 3.368557921162000479, -0.6219103594335000373 ) ) ;
#34648=CARTESIAN_POINT ( 'NONE',  ( 4.900006121741999010, -2.000000000000000000, 0.000000000000000000 ) ) ;
#34652=ORIENTED_EDGE ( 'NONE', *, *, #13506, .T. ) ;
#34653=CARTESIAN_POINT ( 'NONE',  ( 8.983795280412000039, 3.979464555644999901, 9.134076336209998814 ) ) ;
#34654=CARTESIAN_POINT ( 'NONE',  ( 11.12983972095000063, 5.283814160399000315, 4.845726857105999485 ) ) ;
#34656=CARTESIAN_POINT ( 'NONE',  ( 9.050000000000000711, 7.679126935408000065, -5.093340497782000043 ) ) ;
#34657=CARTESIAN_POINT ( 'NONE',  ( 0.8325173737407000063, 2.980225901380999964, 1.319047437492999908 ) ) ;
#34659=CARTESIAN_POINT ( 'NONE',  ( 1.834306799206333549, -1.762666431298145708, -3.058252359239904461 ) ) ;
#34661=CARTESIAN_POINT ( 'NONE',  ( 11.24053267693000002, 2.774035422596999645, 6.782113650547000105 ) ) ;
#34666=CARTESIAN_POINT ( 'NONE',  ( 9.678552719866329923, 4.965075498814901955, -8.480910291410426183 ) ) ;
#34667=EDGE_CURVE ( 'NONE', #58783, #34762, #56666, .T. ) ;
#34670=CARTESIAN_POINT ( 'NONE',  ( 8.472609142682756556, 2.304035199181565297, 7.029818754297329164 ) ) ;
#34673=CARTESIAN_POINT ( 'NONE',  ( 7.800894426331000275, 3.218815461055000160, 6.398977422524000147 ) ) ;
#34680=CARTESIAN_POINT ( 'NONE',  ( 11.25041981190000051, 5.730782764036999488, 8.122675980938000251 ) ) ;
#34681=CARTESIAN_POINT ( 'NONE',  ( 10.72303311070000120, 3.890114357827999747, -8.859327677199999584 ) ) ;
#34685=LINE ( 'NONE', #51435, #12948 ) ;
#34690=AXIS2_PLACEMENT_3D ( 'NONE', #27741, #28430, #1160 ) ;
#34691=CARTESIAN_POINT ( 'NONE',  ( 0.5914240926529371611, -2.218416840111444355, -2.378158849281455822 ) ) ;
#34692=DIRECTION ( 'NONE',  ( -0.7071067735209209948, -0.6115516217690190048, -0.3549713013083110047 ) ) ;
#34693=ADVANCED_FACE ( 'NONE', ( #5540 ), #29434, .T. ) ;
#34702=FACE_OUTER_BOUND ( 'NONE', #67477, .T. ) ;
#34706=CARTESIAN_POINT ( 'NONE',  ( 8.781845775272032029, 3.294641396360323604, -8.705015079476726925 ) ) ;
#34707=CARTESIAN_POINT ( 'NONE',  ( 10.93634361804999955, 8.767998367038000396, -6.465339435565999437 ) ) ;
#34708=CARTESIAN_POINT ( 'NONE',  ( 0.1783234188636000084, -1.176389486124999939, 3.509795687408999942 ) ) ;
#34715=CARTESIAN_POINT ( 'NONE',  ( 10.87273915876999908, 5.407616985330000681, -8.698399706473999515 ) ) ;
#34720=VERTEX_POINT ( 'NONE', #297 ) ;
#34722=FACE_OUTER_BOUND ( 'NONE', #68839, .T. ) ;
#34729=ORIENTED_EDGE ( 'NONE', *, *, #63373, .F. ) ;
#34738=CARTESIAN_POINT ( 'NONE',  ( 0.8530567992085708040, -2.798833948393629534, -2.150913519912204031 ) ) ;
#34745=EDGE_CURVE ( 'NONE', #4821, #21830, #51621, .T. ) ;
#34746=CARTESIAN_POINT ( 'NONE',  ( 2.281685767831499234, -3.258006849854496512, -1.322661048612402412 ) ) ;
#34751=CARTESIAN_POINT ( 'NONE',  ( 3.999999999999999112, 0.5626148410807583211, 2.094138670346520570 ) ) ;
#34754=DIRECTION ( 'NONE',  ( 1.000000000000000000, 0.000000000000000000, 0.000000000000000000 ) ) ;
#34756=CARTESIAN_POINT ( 'NONE',  ( 8.903895280414001689, 3.867331042029999999, -9.227339949050001877 ) ) ;
#34760=CONICAL_SURFACE ( 'NONE', #60401, 2.049966935984999683, 0.7853819979415218588 ) ;
#34762=VERTEX_POINT ( 'NONE', #60069 ) ;
#34763=LINE ( 'NONE', #55738, #25380 ) ;
#34766=ORIENTED_EDGE ( 'NONE', *, *, #55190, .T. ) ;
#34767=CARTESIAN_POINT ( 'NONE',  ( 10.09453415443000068, 5.362844031509000686, -7.550030311027999375 ) ) ;
#34773=ADVANCED_FACE ( 'NONE', ( #18113 ), #10434, .T. ) ;
#34775=CARTESIAN_POINT ( 'NONE',  ( 9.023148997459999876, 5.167567567567999731, -6.822293592207000934 ) ) ;
#34779=VERTEX_POINT ( 'NONE', #64943 ) ;
#34781=CARTESIAN_POINT ( 'NONE',  ( 11.35906500789999996, 2.719101288111000159, -7.157645240044000268 ) ) ;
#34789=ORIENTED_EDGE ( 'NONE', *, *, #1099, .F. ) ;
#34790=CARTESIAN_POINT ( 'NONE',  ( 9.096889158776001238, 2.235961884443999459, -6.794506518623999902 ) ) ;
#34799=ORIENTED_EDGE ( 'NONE', *, *, #17354, .F. ) ;
#34800=DIRECTION ( 'NONE',  ( -0.8660254037844289376, -1.431232957501532063E-11, -0.5000000000000169864 ) ) ;
#34801=CARTESIAN_POINT ( 'NONE',  ( 9.349204462308000174, 2.899999999999999911, -6.662590550603827211 ) ) ;
#34807=ORIENTED_EDGE ( 'NONE', *, *, #67689, .F. ) ;
#34809=CARTESIAN_POINT ( 'NONE',  ( 8.957462135714999718, 5.100000000000000533, -6.571291218949999902 ) ) ;
#34810=CARTESIAN_POINT ( 'NONE',  ( 9.996404771875296191, 5.349457780298017440, 7.853068642099864327 ) ) ;
#34815=CARTESIAN_POINT ( 'NONE',  ( 9.337344653340027278, 3.744151942263672872, 9.232870615261292713 ) ) ;
#34816=CARTESIAN_POINT ( 'NONE',  ( 3.315295232058000252, -3.344614842881000527, -1.715167582504999899 ) ) ;
#34826=CARTESIAN_POINT ( 'NONE',  ( 7.142510841228999929, 5.086541985415000688, -8.378805615758999181 ) ) ;
#34828=CARTESIAN_POINT ( 'NONE',  ( 7.000000000000000000, 7.526486366024999874, 3.526486366024999874 ) ) ;
#34830=EDGE_LOOP ( 'NONE', ( #30335, #50589, #45333, #60731 ) ) ;
#34836=VECTOR ( 'NONE', #46291, 1000.000000000000000 ) ;
#34839=CARTESIAN_POINT ( 'NONE',  ( 10.98851211193927035, 7.849834481462382385, -6.454919206791046804 ) ) ;
#34841=DIRECTION ( 'NONE',  ( 0.000000000000000000, -1.000000000000000000, 0.000000000000000000 ) ) ;
#34843=DIRECTION ( 'NONE',  ( 0.000000000000000000, 1.000000000000000000, 0.000000000000000000 ) ) ;
#34844=ORIENTED_EDGE ( 'NONE', *, *, #60659, .F. ) ;
#34845=CARTESIAN_POINT ( 'NONE',  ( 2.011390132539708997, 3.499999999999998224, 0.4581489286485194157 ) ) ;
#34848=CARTESIAN_POINT ( 'NONE',  ( 4.000000000000000000, 0.000000000000000000, 0.000000000000000000 ) ) ;
#34853=CARTESIAN_POINT ( 'NONE',  ( 3.499999999999999556, 0.6014456285219068610, 3.255366668256093554 ) ) ;
#34861=CARTESIAN_POINT ( 'NONE',  ( 0.1499942179680000542, 2.199046806507070961, 1.689975037551098680 ) ) ;
#34862=CARTESIAN_POINT ( 'NONE',  ( 9.187479719595000205, 2.391443348526999912, -6.856688371964000162 ) ) ;
#34863=CARTESIAN_POINT ( 'NONE',  ( 3.125156541922999853, -0.09820418113198998988, -3.213551318459999973 ) ) ;
#34867=B_SPLINE_CURVE_WITH_KNOTS ( 'NONE', 3,
 ( #57994, #10433, #4840, #47508 ),
 .UNSPECIFIED., .F., .F.,
 ( 4, 4 ),
 ( 0.000000000000000000, 1.000000000000000000 ),
 .UNSPECIFIED. ) ;
#34871=CARTESIAN_POINT ( 'NONE',  ( 9.075483283097998566, 4.020836891789999257, 8.948690653012000951 ) ) ;
#34874=CARTESIAN_POINT ( 'NONE',  ( 9.538432183420001209, 5.620896541217999420, 7.423100299691999915 ) ) ;
#34875=FACE_OUTER_BOUND ( 'NONE', #40564, .T. ) ;
#34877=CARTESIAN_POINT ( 'NONE',  ( 10.97513183233909473, 2.816994567542234318, -6.653220807580209950 ) ) ;
#34878=AXIS2_PLACEMENT_3D ( 'NONE', #43019, #64322, #16444 ) ;
#34884=CARTESIAN_POINT ( 'NONE',  ( 0.9228735163577627132, 1.956520987066745931, -2.929226735302376206 ) ) ;
#34894=CARTESIAN_POINT ( 'NONE',  ( 8.770176658772999900, 3.049618631524000367, 6.392542946894000266 ) ) ;
#34897=CARTESIAN_POINT ( 'NONE',  ( 10.41838915877000105, 4.531912033713999755, -9.270484952459998595 ) ) ;
#34899=CARTESIAN_POINT ( 'NONE',  ( 1.509306799207333460, 3.058252359239904905, -1.762666431298142600 ) ) ;
#34903=CARTESIAN_POINT ( 'NONE',  ( 10.10000011340999926, -1.714184350020999865E-13, 8.687683754368000722E-14 ) ) ;
#34921=CARTESIAN_POINT ( 'NONE',  ( 8.754720280412998434, 5.687930027805999877, -7.109876198051000351 ) ) ;
#34923=CARTESIAN_POINT ( 'NONE',  ( 10.90000000000000036, 2.899999999999999911, 6.414037451299000381 ) ) ;
#34926=CARTESIAN_POINT ( 'NONE',  ( 7.501448341228000416, 2.138190256467000339, 6.814770510101999967 ) ) ;
#34927=B_SPLINE_CURVE_WITH_KNOTS ( 'NONE', 3,
 ( #16345, #20216, #26853, #14972 ),
 .UNSPECIFIED., .F., .F.,
 ( 4, 4 ),
 ( 0.8746030603449276297, 1.000000000000000000 ),
 .UNSPECIFIED. ) ;
#34940=CARTESIAN_POINT ( 'NONE',  ( 9.921464875192169686, 4.920967364567339963, -9.006643819163958398 ) ) ;
#34957=CARTESIAN_POINT ( 'NONE',  ( 11.15982925107999968, 5.578232410510000072, 8.067793621926998782 ) ) ;
#34962=CARTESIAN_POINT ( 'NONE',  ( 9.701978494675000064, 3.399139198672999740, 6.026757051093999173 ) ) ;
#34963=CARTESIAN_POINT ( 'NONE',  ( 8.158337970077000990E-06, 0.000000000000000000, 0.000000000000000000 ) ) ;
#34968=CARTESIAN_POINT ( 'NONE',  ( 7.454676658771000497, 2.138190256467000339, 6.814770510101999967 ) ) ;
#34969=CARTESIAN_POINT ( 'NONE',  ( 10.80815748598999981, 2.937526572573000205, 8.948458885032000154 ) ) ;
#34972=CARTESIAN_POINT ( 'NONE',  ( 9.833904719592002408, 5.048004622677000341, -6.120508709481000231 ) ) ;
#34983=CARTESIAN_POINT ( 'NONE',  ( 2.106520261437999864, 1.927138280259999892, 3.227152792068999965 ) ) ;
#34988=CARTESIAN_POINT ( 'NONE',  ( 9.903950872528001881, 5.205009505618999555, 6.747225973806000532 ) ) ;
#34994=CARTESIAN_POINT ( 'NONE',  ( 8.919607780412000864, 5.165497731316000873, 8.645531386060000045 ) ) ;
#34999=CARTESIAN_POINT ( 'NONE',  ( 1.266428256771000127, 2.565043520226999885, 2.270544068615000022 ) ) ;
#35001=FACE_OUTER_BOUND ( 'NONE', #61930, .T. ) ;
#35004=CARTESIAN_POINT ( 'NONE',  ( 9.590596677641999079, 2.445964682955000136, 7.841184989245001624 ) ) ;
#35006=B_SPLINE_CURVE_WITH_KNOTS ( 'NONE', 3,
 ( #45876, #24553, #67186, #3897, #41318 ),
 .UNSPECIFIED., .F., .F.,
 ( 4, 1, 4 ),
 ( 0.000000000000000000, 0.5000000000000000000, 1.000000000000000000 ),
 .UNSPECIFIED. ) ;
#35007=DIRECTION ( 'NONE',  ( 1.000000000000000000, 0.000000000000000000, 0.000000000000000000 ) ) ;
#35013=CARTESIAN_POINT ( 'NONE',  ( 7.632009264042212138, 5.138780499484131070, 6.167916169763508094 ) ) ;
#35014=EDGE_LOOP ( 'NONE', ( #22590, #14941, #57587, #27197 ) ) ;
#35018=ORIENTED_EDGE ( 'NONE', *, *, #21482, .T. ) ;
#35023=CARTESIAN_POINT ( 'NONE',  ( 9.877261637240000169, 2.207988120125000009, 7.624813826992999921 ) ) ;
#35033=AXIS2_PLACEMENT_3D ( 'NONE', #64482, #33038, #54350 ) ;
#35035=DIRECTION ( 'NONE',  ( 0.000000000000000000, 1.000000000000000000, 0.000000000000000000 ) ) ;
#35051=CARTESIAN_POINT ( 'NONE',  ( 0.4334425577436000210, -2.413104819777999843, -2.586865767356999690 ) ) ;
#35052=CARTESIAN_POINT ( 'NONE',  ( 9.020964430773000586, 2.907392932634000005, 6.146188468825999784 ) ) ;
#35064=CARTESIAN_POINT ( 'NONE',  ( 11.09999999999999964, 4.000000000000000000, -7.500000000000000000 ) ) ;
#35078=DIRECTION ( 'NONE',  ( -1.000000000000000000, 0.000000000000000000, 0.000000000000000000 ) ) ;
#35079=EDGE_CURVE ( 'NONE', #26809, #45133, #21602, .T. ) ;
#35081=CARTESIAN_POINT ( 'NONE',  ( 2.542640132542666631, 3.058252359239899132, 1.762666431298154146 ) ) ;
#35088=VERTEX_POINT ( 'NONE', #43564 ) ;
#35089=DIRECTION ( 'NONE',  ( 0.7071067796723968790, 0.6140599801297969007, -0.3506142366537984834 ) ) ;
#35093=FACE_OUTER_BOUND ( 'NONE', #35174, .T. ) ;
#35098=CARTESIAN_POINT ( 'NONE',  ( 4.000000000000000000, 2.136325177875821435, 0.2822470469891264488 ) ) ;
#35100=ORIENTED_EDGE ( 'NONE', *, *, #21219, .F. ) ;
#35102=CARTESIAN_POINT ( 'NONE',  ( 6.899999691988000450, -12.20988339176000004, -3.111064831550000243 ) ) ;
#35103=CARTESIAN_POINT ( 'NONE',  ( 8.664129719593997692, 5.524776413195999325, -7.147585171405999915 ) ) ;
#35109=CARTESIAN_POINT ( 'NONE',  ( 8.883148997460001084, 5.167567567567999731, 6.822293592207000934 ) ) ;
#35110=CARTESIAN_POINT ( 'NONE',  ( 7.325000000000000178, 4.000000000000000000, 9.239711431703000244 ) ) ;
#35111=CARTESIAN_POINT ( 'NONE',  ( 6.899999691988000450, 0.000000000000000000, 0.000000000000000000 ) ) ;
#35112=ORIENTED_EDGE ( 'NONE', *, *, #6293, .T. ) ;
#35113=AXIS2_PLACEMENT_3D ( 'NONE', #38564, #49749, #2209 ) ;
#35114=CARTESIAN_POINT ( 'NONE',  ( 10.68375192593000023, 4.547306763790999184, -8.749120576764999768 ) ) ;
#35115=DIRECTION ( 'NONE',  ( 0.000000000000000000, -1.000000000000000000, 0.000000000000000000 ) ) ;
#35132=CARTESIAN_POINT ( 'NONE',  ( 7.840808840898988663, 5.014465085856414817, 6.545777694986461448 ) ) ;
#35133=ORIENTED_EDGE ( 'NONE', *, *, #11866, .F. ) ;
#35135=CARTESIAN_POINT ( 'NONE',  ( 9.965360841230999966, 4.034680274230000308, -6.102912434217000026 ) ) ;
#35136=CARTESIAN_POINT ( 'NONE',  ( 7.000000000000000000, 0.3230303992915000144, 3.000000000000000000 ) ) ;
#35139=EDGE_CURVE ( 'NONE', #25073, #33524, #46635, .T. ) ;
#35144=CARTESIAN_POINT ( 'NONE',  ( 8.709994373423086245, 5.736668034480788769, 7.709616018064762599 ) ) ;
#35146=ORIENTED_EDGE ( 'NONE', *, *, #33486, .F. ) ;
#35147=CARTESIAN_POINT ( 'NONE',  ( 7.419155789456778116, 3.646555675397749940, -6.184975449998299624 ) ) ;
#35153=CARTESIAN_POINT ( 'NONE',  ( 9.193385841233000733, 2.981992329588000423, -5.895876591910999664 ) ) ;
#35159=CARTESIAN_POINT ( 'NONE',  ( 0.2153359931920000025, 3.215315751876999695, 1.126573897625000029E-09 ) ) ;
#35162=VERTEX_POINT ( 'NONE', #12438 ) ;
#35167=CARTESIAN_POINT ( 'NONE',  ( 7.974113208588001100, 4.561154361229000642, -6.272154006859000930 ) ) ;
#35174=EDGE_LOOP ( 'NONE', ( #14545, #9058, #39068, #9617, #46787 ) ) ;
#35179=CONICAL_SURFACE ( 'NONE', #47495, 13.04999927352999833, 0.7853981075146502233 ) ;
#35181=EDGE_LOOP ( 'NONE', ( #41714, #39575, #7123, #14465 ) ) ;
#35182=CARTESIAN_POINT ( 'NONE',  ( 10.95867266763608328, 8.944080322854695453, -6.438115898787937219 ) ) ;
#35190=B_SPLINE_CURVE_WITH_KNOTS ( 'NONE', 3,
 ( #49114, #58920, #21506, #68102, #22199, #48428, #26774, #33042, #30717 ),
 .UNSPECIFIED., .F., .F.,
 ( 4, 1, 1, 1, 1, 1, 4 ),
 ( 0.1253746098019370980, 0.1627898251898792226, 0.3296782782853378002, 0.4965667313813880712, 0.6634551844774385643, 0.8303436375728971974, 0.8746155046758248286 ),
 .UNSPECIFIED. ) ;
#35193=CARTESIAN_POINT ( 'NONE',  ( 11.01684168656612961, 5.218333533724945461, 6.608889323344318889 ) ) ;
#35202=CARTESIAN_POINT ( 'NONE',  ( 3.136390132544209397, -0.4581489286485235790, 3.499999999999998224 ) ) ;
#35206=ORIENTED_EDGE ( 'NONE', *, *, #58578, .T. ) ;
#35209=CARTESIAN_POINT ( 'NONE',  ( 9.980433037259000884, 4.047223446241999589, 9.090360698422999874 ) ) ;
#35211=CARTESIAN_POINT ( 'NONE',  ( 8.889129719593999113, 5.687930027805999877, -7.109876198051000351 ) ) ;
#35212=CARTESIAN_POINT ( 'NONE',  ( 2.971001955742000433, 3.162850693241999966, 1.598219008581000189 ) ) ;
#35218=CARTESIAN_POINT ( 'NONE',  ( 9.323722176100000425, 3.947350570199999797, 6.051869652381999920 ) ) ;
#35220=EDGE_CURVE ( 'NONE', #19244, #23058, #61794, .T. ) ;
#35222=CARTESIAN_POINT ( 'NONE',  ( 9.815201913989998417, 2.813632032385000148, 8.848857341496000117 ) ) ;
#35226=CARTESIAN_POINT ( 'NONE',  ( 10.96040066253607037, 2.825454854422092765, -6.681915423809532406 ) ) ;
#35230=CARTESIAN_POINT ( 'NONE',  ( 8.087104536824956114, 4.663776001496819923, -6.206918359655642092 ) ) ;
#35236=CARTESIAN_POINT ( 'NONE',  ( 8.331682176603999679, 5.101289360622999425, 6.607176324693000424 ) ) ;
#35237=ORIENTED_EDGE ( 'NONE', *, *, #22162, .F. ) ;
#35238=CARTESIAN_POINT ( 'NONE',  ( 8.796579719592999780, 2.368264398678999516, 7.410200237937000445 ) ) ;
#35242=CARTESIAN_POINT ( 'NONE',  ( 11.05392028041000074, 5.159483628325999938, -8.487146968478000986 ) ) ;
#35250=DIRECTION ( 'NONE',  ( -1.000000000000000000, 0.000000000000000000, 0.000000000000000000 ) ) ;
#35256=ORIENTED_EDGE ( 'NONE', *, *, #43191, .F. ) ;
#35260=CARTESIAN_POINT ( 'NONE',  ( 10.98768472569999943, 6.720753179915999631, -5.471698458723999181 ) ) ;
#35261=AXIS2_PLACEMENT_3D ( 'NONE', #41409, #34462, #3982 ) ;
#35262=VERTEX_POINT ( 'NONE', #55780 ) ;
#35269=CARTESIAN_POINT ( 'NONE',  ( 7.629823341228000544, 4.763536573491999881, 5.668879554882000349 ) ) ;
#35272=CARTESIAN_POINT ( 'NONE',  ( 9.475279990687596410, 5.350441389720215213, 7.499985493516660107 ) ) ;
#35286=LINE ( 'NONE', #3445, #41929 ) ;
#35289=CARTESIAN_POINT ( 'NONE',  ( 6.999999691988000095, 12.89129024452999950, 1.677687644161999891 ) ) ;
#35290=VERTEX_POINT ( 'NONE', #48288 ) ;
#35294=CARTESIAN_POINT ( 'NONE',  ( 10.97074841058999972, 2.648521302318000092, -6.788870928221999890 ) ) ;
#35299=CARTESIAN_POINT ( 'NONE',  ( 9.786671076420999427, 2.381202181614999525, 7.612749448318000489 ) ) ;
#35304=CARTESIAN_POINT ( 'NONE',  ( 10.81579666500999970, 5.374569445151000657, 6.698728322222000209 ) ) ;
#35306=CARTESIAN_POINT ( 'NONE',  ( 9.775320280412000074, 2.527713920559999661, -6.969421869128999525 ) ) ;
#35309=AXIS2_PLACEMENT_3D ( 'NONE', #4107, #69123, #21231 ) ;
#35310=CARTESIAN_POINT ( 'NONE',  ( 7.930392219590000735, 3.164805384346000228, 9.104735843897000080 ) ) ;
#35311=CARTESIAN_POINT ( 'NONE',  ( 10.37373942323999998, 2.215265813302000009, 7.703982730183001060 ) ) ;
#35314=CARTESIAN_POINT ( 'NONE',  ( 8.880270280412998929, 4.146787477634999775, -5.941926545671999627 ) ) ;
#35318=CARTESIAN_POINT ( 'NONE',  ( 3.323606204996916613, -2.160720528238035953, -2.790977566173463931 ) ) ;
#35323=CARTESIAN_POINT ( 'NONE',  ( 1.396064357887999874, 3.196468001211000054, -1.639036658905000055 ) ) ;
#35326=CARTESIAN_POINT ( 'NONE',  ( 8.424364158774000799, 3.292387953886000140, -6.294868737226000377 ) ) ;
#35330=CARTESIAN_POINT ( 'NONE',  ( 10.34947814066000049, 4.457562099971999814, 6.154877938302999674 ) ) ;
#35331=ADVANCED_FACE ( 'NONE', ( #54216 ), #2195, .F. ) ;
#35337=CARTESIAN_POINT ( 'NONE',  ( 7.802017219589999719, 5.638704226117999596, 8.266404648244000342 ) ) ;
#35338=CARTESIAN_POINT ( 'NONE',  ( 10.95203274928999804, 5.154111710649999623, 5.182718807703999175 ) ) ;
#35341=CARTESIAN_POINT ( 'NONE',  ( 2.124703346705999696, 1.685541059001999908, -2.982097634516000184 ) ) ;
#35343=CARTESIAN_POINT ( 'NONE',  ( 1.095639153602063987, -2.129181563504743746, -2.524889412081005258 ) ) ;
#35346=CARTESIAN_POINT ( 'NONE',  ( 9.722769750889000306, 5.493785011855999656, 6.566826815556000341 ) ) ;
#35352=CARTESIAN_POINT ( 'NONE',  ( 8.039315972864844895, 3.244806080982685526, 5.913190043580576649 ) ) ;
#35353=VERTEX_POINT ( 'NONE', #58691 ) ;
#35358=ORIENTED_EDGE ( 'NONE', *, *, #68558, .T. ) ;
#35360=DIRECTION ( 'NONE',  ( 0.000000000000000000, -1.000000000000000000, 0.000000000000000000 ) ) ;
#35362=CARTESIAN_POINT ( 'NONE',  ( 10.96580581817999978, 4.930645553951000792, 6.170542400361000546 ) ) ;
#35363=FACE_OUTER_BOUND ( 'NONE', #10667, .T. ) ;
#35372=CARTESIAN_POINT ( 'NONE',  ( 8.255239991808057454, 5.012978268976954865, -8.578693711955805767 ) ) ;
#35374=AXIS2_PLACEMENT_3D ( 'NONE', #38321, #27852, #32742 ) ;
#35376=CARTESIAN_POINT ( 'NONE',  ( 10.66922466689405269, 3.154184221645670139, -4.789865691167801920 ) ) ;
#35377=CARTESIAN_POINT ( 'NONE',  ( 10.67437910952998870, 7.450072830998997198, 5.983005019645002420 ) ) ;
#35381=ORIENTED_EDGE ( 'NONE', *, *, #53847, .T. ) ;
#35387=ADVANCED_FACE ( 'NONE', ( #5889 ), #42782, .F. ) ;
#35391=CARTESIAN_POINT ( 'NONE',  ( 0.4662484304700000304, 2.655425791298000160, -2.578923811134000044 ) ) ;
#35392=CARTESIAN_POINT ( 'NONE',  ( 8.174990947233153449, 2.650692654198087972, 7.500004443805798005 ) ) ;
#35396=FACE_OUTER_BOUND ( 'NONE', #1395, .T. ) ;
#35401=DIRECTION ( 'NONE',  ( 1.000000000000000000, 5.773164121932000354E-14, 0.000000000000000000 ) ) ;
#35411=FACE_OUTER_BOUND ( 'NONE', #54570, .T. ) ;
#35415=CONICAL_SURFACE ( 'NONE', #37643, 13.04999934368000147, 0.7853981075146502233 ) ;
#35416=CARTESIAN_POINT ( 'NONE',  ( 8.576923877145999242, 3.399999999999999911, 5.924121105096999962 ) ) ;
#35419=CARTESIAN_POINT ( 'NONE',  ( 2.698890132542666631, -2.798833948393640192, 2.150913519912191152 ) ) ;
#35420=CARTESIAN_POINT ( 'NONE',  ( 10.98768472639999949, 0.3876847264043000174, 4.945212061661000469 ) ) ;
#35426=CARTESIAN_POINT ( 'NONE',  ( 6.294818531611999781E-06, -2.999993704296999741, -7.007531981267999457E-10 ) ) ;
#35429=CARTESIAN_POINT ( 'NONE',  ( 11.10000000001999965, 7.806347126537000136, 6.642166469876999990 ) ) ;
#35430=CARTESIAN_POINT ( 'NONE',  ( 2.884306799211333594, -1.762666431298145930, -3.058252359239904905 ) ) ;
#35431=CARTESIAN_POINT ( 'NONE',  ( 9.219964158774999419, 3.941185585667000169, -8.896279800194999865 ) ) ;
#35436=ORIENTED_EDGE ( 'NONE', *, *, #50107, .F. ) ;
#35439=CARTESIAN_POINT ( 'NONE',  ( 8.365779719592000063, 2.949305648881000330, -8.659807625323999503 ) ) ;
#35440=CARTESIAN_POINT ( 'NONE',  ( 9.958268565653391136, 4.155869445530794515, -9.269508239148089856 ) ) ;
#35446=EDGE_CURVE ( 'NONE', #66620, #7152, #9327, .T. ) ;
#35449=CARTESIAN_POINT ( 'NONE',  ( 8.739954719592999410, 3.122811675949999977, -6.006064052396999919 ) ) ;
#35450=ORIENTED_EDGE ( 'NONE', *, *, #5393, .F. ) ;
#35451=VECTOR ( 'NONE', #51822, 1000.000000000000114 ) ;
#35452=CARTESIAN_POINT ( 'NONE',  ( 10.35427764559999986, 4.879113829302000660, -8.944031201701999834 ) ) ;
#35459=VECTOR ( 'NONE', #63205, 1000.000000000000000 ) ;
#35464=CARTESIAN_POINT ( 'NONE',  ( 7.100000000000000533, 4.000000000000000000, 8.849999999999999645 ) ) ;
#35471=CARTESIAN_POINT ( 'NONE',  ( 10.20271159698171815, 5.100000000000000533, 6.305985889763628727 ) ) ;
#35476=AXIS2_PLACEMENT_3D ( 'NONE', #34903, #8329, #19503 ) ;
#35477=CARTESIAN_POINT ( 'NONE',  ( 9.716735841232001292, 3.941185585667000169, -8.896279800194999865 ) ) ;
#35478=CARTESIAN_POINT ( 'NONE',  ( 10.58718478751670666, 5.286440948694374420, -7.026985308887427450 ) ) ;
#35481=CARTESIAN_POINT ( 'NONE',  ( 7.830819424294336528, 3.674999207176894878, 6.165344395466317629 ) ) ;
#35484=CARTESIAN_POINT ( 'NONE',  ( 9.020964430773000586, 2.907392932634000005, 6.146188468825999784 ) ) ;
#35486=VERTEX_POINT ( 'NONE', #15364 ) ;
#35493=FACE_OUTER_BOUND ( 'NONE', #30288, .T. ) ;
#35495=CARTESIAN_POINT ( 'NONE',  ( 7.986889964180154955, 3.051162356207695492, -6.411554890354049796 ) ) ;
#35499=CARTESIAN_POINT ( 'NONE',  ( 3.115020758170000015, 1.311005030890000089, -3.164819811060000099 ) ) ;
#35500=ORIENTED_EDGE ( 'NONE', *, *, #43191, .T. ) ;
#35504=AXIS2_PLACEMENT_3D ( 'NONE', #67351, #62116, #40123 ) ;
#35505=CARTESIAN_POINT ( 'NONE',  ( 7.871551658771999804, 4.780986922229000236, 6.267222470044999660 ) ) ;
#35510=CARTESIAN_POINT ( 'NONE',  ( 10.95645069460308108, 8.994232988617600455, 6.417022446611309938 ) ) ;
#35511=CARTESIAN_POINT ( 'NONE',  ( 11.09999999999999964, 2.685305999535000154, 6.664030027596000494 ) ) ;
#35512=CARTESIAN_POINT ( 'NONE',  ( 7.832456446343600831, 2.667230532683134481, -7.203453600678752622 ) ) ;
#35515=EDGE_LOOP ( 'NONE', ( #19437, #53422, #52270 ) ) ;
#35521=VERTEX_POINT ( 'NONE', #53792 ) ;
#35522=CARTESIAN_POINT ( 'NONE',  ( 8.525869573596782658, 2.785289313170467462, -8.768765148542382093 ) ) ;
#35524=AXIS2_PLACEMENT_3D ( 'NONE', #16484, #37129, #58448 ) ;
#35525=CARTESIAN_POINT ( 'NONE',  ( 8.128629719589000047, 5.223492654083000453, -6.524203877525000195 ) ) ;
#35533=CARTESIAN_POINT ( 'NONE',  ( 8.099999999999999645, 0.000000000000000000, 0.000000000000000000 ) ) ;
#35536=DIRECTION ( 'NONE',  ( 1.000000000000000000, 0.000000000000000000, 0.000000000000000000 ) ) ;
#35543=B_SPLINE_CURVE_WITH_KNOTS ( 'NONE', 3,
 ( #56806, #40047, #24296, #24645 ),
 .UNSPECIFIED., .F., .F.,
 ( 4, 4 ),
 ( 0.8745245747709967654, 1.000000000000000000 ),
 .UNSPECIFIED. ) ;
#35548=ORIENTED_EDGE ( 'NONE', *, *, #45280, .T. ) ;
#35549=CARTESIAN_POINT ( 'NONE',  ( 10.96207813434000045, 5.399835028078000754, 7.743264559064000352 ) ) ;
#35551=CARTESIAN_POINT ( 'NONE',  ( 9.576420280414000175, 4.861259245430999520, -8.806664389576001284 ) ) ;
#35552=CARTESIAN_POINT ( 'NONE',  ( 2.467998394013000141, 3.220898723588000223, 1.477727276234999998 ) ) ;
#35560=CARTESIAN_POINT ( 'NONE',  ( 10.48131298037437453, 3.643872424580264724, -9.239416608973755274 ) ) ;
#35563=CARTESIAN_POINT ( 'NONE',  ( 10.89874804681000064, 2.834828962328999502, 9.088465460431999432 ) ) ;
#35564=CARTESIAN_POINT ( 'NONE',  ( 11.09999999999999964, 2.700683852703999577, 5.124965750789000296 ) ) ;
#35565=VECTOR ( 'NONE', #27349, 999.9999999999998863 ) ;
#35574=EDGE_LOOP ( 'NONE', ( #41461, #47707, #43176, #638, #20723, #68133, #13079, #26227, #13456, #1533, #54962, #30793, #62705, #39077, #23287, #31632, #29863 ) ) ;
#35580=ORIENTED_EDGE ( 'NONE', *, *, #50407, .F. ) ;
#35582=CARTESIAN_POINT ( 'NONE',  ( 7.165489158771000788, 2.688365364125000045, 8.140015608605001063 ) ) ;
#35584=CARTESIAN_POINT ( 'NONE',  ( 10.67529528041000120, 3.066676902634999813, -8.703232886886000941 ) ) ;
#35589=CARTESIAN_POINT ( 'NONE',  ( 8.609967445932182883, 4.707159105297979096, 5.915074581558411815 ) ) ;
#35591=CARTESIAN_POINT ( 'NONE',  ( 11.09999999999999964, 4.000000000000000000, 7.500000000000000000 ) ) ;
#35595=CARTESIAN_POINT ( 'NONE',  ( 7.218814158767999700, 4.636818559850000909, -5.710024136463999866 ) ) ;
#35602=ORIENTED_EDGE ( 'NONE', *, *, #45024, .F. ) ;
#35608=VECTOR ( 'NONE', #19406, 1000.000000000000114 ) ;
#35617=CARTESIAN_POINT ( 'NONE',  ( 9.461621083092172313, 5.351423275947217562, 7.263649724570491628 ) ) ;
#35618=EDGE_CURVE ( 'NONE', #53044, #59076, #24098, .T. ) ;
#35626=CARTESIAN_POINT ( 'NONE',  ( 2.435247277619000172, 2.372532593102000043, -2.573147701680999599 ) ) ;
#35634=CARTESIAN_POINT ( 'NONE',  ( 8.082873386424997975, 5.111739203374999541, -6.679001318365999751 ) ) ;
#35637=CARTESIAN_POINT ( 'NONE',  ( 10.22440590001000160, 5.317411003666999925, -8.272452263128000638 ) ) ;
#35642=CARTESIAN_POINT ( 'NONE',  ( 10.28314886242000092, 2.387776420306999992, 7.684265965147999644 ) ) ;
#35647=CARTESIAN_POINT ( 'NONE',  ( 11.03856029907000114, 2.974095820320000083, 8.716122353065999917 ) ) ;
#35649=CARTESIAN_POINT ( 'NONE',  ( 10.06481084123000080, 5.336630274082000192, -7.092011739486999922 ) ) ;
#35652=CARTESIAN_POINT ( 'NONE',  ( 8.764829719592999169, 5.808262417891000062, 7.446016144116000213 ) ) ;
#35653=CARTESIAN_POINT ( 'NONE',  ( 10.00138108374000012, 3.855364958793999985, 5.709478909302000638 ) ) ;
#35656=CARTESIAN_POINT ( 'NONE',  ( 9.137754719594999742, 2.319062457810000311, -7.919229449146000022 ) ) ;
#35663=CARTESIAN_POINT ( 'NONE',  ( 1.486654918706999950, 3.344697682836000219, -1.715043639744999959 ) ) ;
#35665=CARTESIAN_POINT ( 'NONE',  ( 9.931248637830082160, 2.301670995521332141, 7.915216903584279429 ) ) ;
#35667=CARTESIAN_POINT ( 'NONE',  ( 6.999999691988000095, 12.89129024452999950, -1.677687644161999891 ) ) ;
#35670=DIRECTION ( 'NONE',  ( 0.000000000000000000, 0.000000000000000000, -1.000000000000000000 ) ) ;
#35671=CARTESIAN_POINT ( 'NONE',  ( 11.09999999999999964, 2.700000000000000178, 5.160242713806000303 ) ) ;
#35676=CARTESIAN_POINT ( 'NONE',  ( 8.817635841231000526, 3.894644548817000285, 6.044465307984999924 ) ) ;
#35679=AXIS2_PLACEMENT_3D ( 'NONE', #60265, #32661, #43498 ) ;
#35681=DIRECTION ( 'NONE',  ( 0.000000000000000000, -1.000000000000000000, 0.000000000000000000 ) ) ;
#35682=CARTESIAN_POINT ( 'NONE',  ( 1.128155746510000057, 3.563994061069000185, 0.4492161910706000127 ) ) ;
#35684=CARTESIAN_POINT ( 'NONE',  ( 1.667822546892261393, 0.6772077056339234069, -3.232625950882237031 ) ) ;
#35686=PLANE ( 'NONE',  #9590 ) ;
#35687=CARTESIAN_POINT ( 'NONE',  ( 9.423523952092001110, 4.993991073313000406, 8.578107851305000864 ) ) ;
#35692=CARTESIAN_POINT ( 'NONE',  ( 7.717636619252205676, 5.722644694260130116, 7.867024080253358420 ) ) ;
#35700=CARTESIAN_POINT ( 'NONE',  ( 8.491228313223627922, 4.376000986002790860, 5.973597461995679758 ) ) ;
#35702=CARTESIAN_POINT ( 'NONE',  ( 10.24961997674000003, 4.184221916050000267, 9.286882020979000174 ) ) ;
#35712=CARTESIAN_POINT ( 'NONE',  ( 9.018359312501498692, 5.126777126186109257, -6.752018918873272213 ) ) ;
#35714=ADVANCED_FACE ( 'NONE', ( #44498 ), #24991, .F. ) ;
#35715=CARTESIAN_POINT ( 'NONE',  ( 8.206872618705004285, 10.60779917172999376, 4.026525179214997863 ) ) ;
#35723=DIRECTION ( 'NONE',  ( 0.000000000000000000, 1.000000000000000000, -3.576848554708999905E-13 ) ) ;
#35729=CARTESIAN_POINT ( 'NONE',  ( 0.06325325710666998558, 2.727922606149000284, -2.252402744047000471 ) ) ;
#35730=CARTESIAN_POINT ( 'NONE',  ( 7.997739111735369555, 4.828320830117592166, 8.578514095141908768 ) ) ;
#35735=CARTESIAN_POINT ( 'NONE',  ( 1.240556799208374805, -3.500000000000003109, 0.4581489286484972667 ) ) ;
#35743=CARTESIAN_POINT ( 'NONE',  ( 9.285767973100965023, 5.375727035179655111, -6.377217275772713023 ) ) ;
#35747=EDGE_CURVE ( 'NONE', #64753, #18982, #25215, .T. ) ;
#35751=EDGE_LOOP ( 'NONE', ( #60900, #7373, #46783, #38496 ) ) ;
#35757=B_SPLINE_CURVE_WITH_KNOTS ( 'NONE', 3,
 ( #35159, #63065, #62397, #14852, #24995, #14171, #41079, #36174, #67979, #57840 ),
 .UNSPECIFIED., .F., .F.,
 ( 4, 2, 2, 2, 4 ),
 ( 0.000000000000000000, 0.1886333293263050825, 0.3772666586526101651, 0.5658999879789150533, 0.7545333173052201081 ),
 .UNSPECIFIED. ) ;
#35770=B_SPLINE_CURVE_WITH_KNOTS ( 'NONE', 3,
 ( #46124, #40200, #18528, #61174 ),
 .UNSPECIFIED., .F., .F.,
 ( 4, 4 ),
 ( 0.8745969165622392572, 1.000000000000000000 ),
 .UNSPECIFIED. ) ;
#35778=CARTESIAN_POINT ( 'NONE',  ( 2.571806799210416550, 3.408904368339104263, 0.9161175952574878156 ) ) ;
#35787=CARTESIAN_POINT ( 'NONE',  ( 9.576420280414000175, 4.861259245430999520, -8.806664389576001284 ) ) ;
#35789=CARTESIAN_POINT ( 'NONE',  ( 10.51140238467000110, 2.326714339996000191, -7.741210149842999932 ) ) ;
#35791=ORIENTED_EDGE ( 'NONE', *, *, #25309, .T. ) ;
#35801=CARTESIAN_POINT ( 'NONE',  ( 10.80374834123000127, 2.766954612461999918, -8.073381085840999560 ) ) ;
#35807=LINE ( 'NONE', #13121, #33053 ) ;
#35810=CARTESIAN_POINT ( 'NONE',  ( 9.468110841233000841, 4.082930418187999955, -6.104944817728999773 ) ) ;
#35811=CARTESIAN_POINT ( 'NONE',  ( 9.201178352479098876, 5.768932051408849127, 7.515051652316785180 ) ) ;
#35818=CARTESIAN_POINT ( 'NONE',  ( 2.285684048949442104, 2.196238783330880739, -2.381962904619033594 ) ) ;
#35819=PLANE ( 'NONE',  #35261 ) ;
#35820=ORIENTED_EDGE ( 'NONE', *, *, #9052, .T. ) ;
#35829=EDGE_CURVE ( 'NONE', #35353, #51133, #1317, .T. ) ;
#35833=CARTESIAN_POINT ( 'NONE',  ( 0.2417516622353175770, 2.832911453320530626, 1.631798746758986285 ) ) ;
#35834=CARTESIAN_POINT ( 'NONE',  ( 2.919519622344000087, 0.1980832466146000004, 3.253006245077000091 ) ) ;
#35839=CARTESIAN_POINT ( 'NONE',  ( 8.577614158774000686, 3.981661882377999895, 8.959227447876999761 ) ) ;
#35845=EDGE_CURVE ( 'NONE', #43188, #47743, #31765, .T. ) ;
#35847=CARTESIAN_POINT ( 'NONE',  ( 7.810846861326904644, 3.150764258446524746, 6.417811892696772880 ) ) ;
#35853=CARTESIAN_POINT ( 'NONE',  ( 9.374309343116463467, 4.497301283948258899, 9.030649165034382975 ) ) ;
#35860=CARTESIAN_POINT ( 'NONE',  ( 7.780554719587999379, 4.514357753279999663, -8.978030925517998639 ) ) ;
#35861=B_SPLINE_CURVE_WITH_KNOTS ( 'NONE', 3,
 ( #23682, #25056, #56876, #40791, #68378, #36234, #41145, #26094, #9656, #10005, #35560, #20845, #15258, #25747, #46387, #8975, #62454, #30314, #10350, #47077, #20499, #57552 ),
 .UNSPECIFIED., .F., .F.,
 ( 4, 2, 2, 2, 2, 2, 2, 2, 2, 2, 4 ),
 ( 0.000000000000000000, 0.1249999999999992506, 0.2499999999999985012, 0.3124999999999983902, 0.3749999999999982792, 0.4999999999999984457, 0.6249999999999985567, 0.7499999999999986677, 0.8124999999999990008, 0.8749999999999993339, 1.000000000000000000 ),
 .UNSPECIFIED. ) ;
#35872=CARTESIAN_POINT ( 'NONE',  ( 10.73362722026812932, 5.594669424171384797, 8.214019094825715683 ) ) ;
#35881=ORIENTED_EDGE ( 'NONE', *, *, #20937, .F. ) ;
#35882=CARTESIAN_POINT ( 'NONE',  ( 10.68362359175999998, 2.603561947343000060, 7.762063351517999976 ) ) ;
#35883=DIRECTION ( 'NONE',  ( 0.000000000000000000, -0.9539392014169415512, -0.3000000000000128120 ) ) ;
#35884=CARTESIAN_POINT ( 'NONE',  ( 9.427245280414000561, 4.989193221215000307, -6.287302145481000082 ) ) ;
#35885=CARTESIAN_POINT ( 'NONE',  ( 3.180586773128999845, -3.540884173372999655, 0.1416607846616000088 ) ) ;
#35891=CARTESIAN_POINT ( 'NONE',  ( 3.092640132544500098, 3.058252359239899132, 1.762666431298155034 ) ) ;
#35894=B_SPLINE_CURVE_WITH_KNOTS ( 'NONE', 3,
 ( #58188, #65756, #60520, #12629 ),
 .UNSPECIFIED., .F., .F.,
 ( 4, 4 ),
 ( 0.000000000000000000, 1.000000000000000000 ),
 .UNSPECIFIED. ) ;
#35895=CARTESIAN_POINT ( 'NONE',  ( 11.20904666305999875, 5.937823941418000295, 7.147334722859000067 ) ) ;
#35910=CARTESIAN_POINT ( 'NONE',  ( 6.900019030169000089, 12.43894676821000012, -2.828897736577999922 ) ) ;
#35911=CARTESIAN_POINT ( 'NONE',  ( 5.000030787343001215, -0.2748844998327745759, -2.099962892531005210 ) ) ;
#35913=CARTESIAN_POINT ( 'NONE',  ( 0.4033234188635999584, -1.019984463426999888, 3.043156295769000153 ) ) ;
#35915=AXIS2_PLACEMENT_3D ( 'NONE', #17564, #66137, #55662 ) ;
#35916=CARTESIAN_POINT ( 'NONE',  ( 11.01605778040999972, 5.482856203356999636, -7.846408531951999166 ) ) ;
#35919=CARTESIAN_POINT ( 'NONE',  ( 1.550973465874000201, 3.500000000000000000, 0.000000000000000000 ) ) ;
#35926=CARTESIAN_POINT ( 'NONE',  ( 8.113864158768999246, 2.425297598239999797, -6.437049665397999831 ) ) ;
#35927=EDGE_CURVE ( 'NONE', #26293, #51926, #50714, .T. ) ;
#35933=ORIENTED_EDGE ( 'NONE', *, *, #56908, .T. ) ;
#35934=ADVANCED_FACE ( 'NONE', ( #981 ), #26866, .T. ) ;
#35936=ORIENTED_EDGE ( 'NONE', *, *, #51146, .F. ) ;
#35938=CARTESIAN_POINT ( 'NONE',  ( 2.373890132542958220, -2.150913519912200922, -2.798833948393631754 ) ) ;
#35943=CARTESIAN_POINT ( 'NONE',  ( 9.341490007895000502, 4.148133901461999784, 9.337478696773001019 ) ) ;
#35945=CARTESIAN_POINT ( 'NONE',  ( 7.766851002543999627, 2.832432432432000269, 6.822293592207000934 ) ) ;
#35947=CARTESIAN_POINT ( 'NONE',  ( 11.09999999999999964, 5.350000000000000533, -7.500000000000000000 ) ) ;
#35948=ORIENTED_EDGE ( 'NONE', *, *, #29089, .F. ) ;
#35954=CARTESIAN_POINT ( 'NONE',  ( 7.954299074928001367, 3.414461172233999697, -6.283593702261001113 ) ) ;
#35964=CARTESIAN_POINT ( 'NONE',  ( 9.766125411066999717, 4.735428155407000794, -8.791393655830999521 ) ) ;
#35970=CARTESIAN_POINT ( 'NONE',  ( 9.910790522921001156, 3.869345236050000025, 5.882548872612999524 ) ) ;
#35972=ORIENTED_EDGE ( 'NONE', *, *, #6064, .T. ) ;
#35975=CARTESIAN_POINT ( 'NONE',  ( 9.409415556003999370, 2.113395950889999764, 7.914199712930999553 ) ) ;
#35977=CARTESIAN_POINT ( 'NONE',  ( 9.269210841233000764, 3.098073081301000009, -8.567513114264999174 ) ) ;
#35978=DIRECTION ( 'NONE',  ( -1.000000000000000000, 0.000000000000000000, 0.000000000000000000 ) ) ;
#35982=CARTESIAN_POINT ( 'NONE',  ( 10.62197831623999988, 5.779783227492000464, 7.256572995198999898 ) ) ;
#35985=CARTESIAN_POINT ( 'NONE',  ( 8.889129719593999113, 5.687930027805999877, -7.109876198051000351 ) ) ;
#35986=B_SPLINE_CURVE_WITH_KNOTS ( 'NONE', 3,
 ( #44744, #18514, #6976, #49277 ),
 .UNSPECIFIED., .F., .F.,
 ( 4, 4 ),
 ( 0.000000000000000000, 1.000000000000000000 ),
 .UNSPECIFIED. ) ;
#35987=CARTESIAN_POINT ( 'NONE',  ( 0.000000000000000000, 2.319305672483364056, 1.781768641235244921 ) ) ;
#35988=ADVANCED_FACE ( 'NONE', ( #42936 ), #16358, .T. ) ;
#35994=VERTEX_POINT ( 'NONE', #18786 ) ;
#35997=CARTESIAN_POINT ( 'NONE',  ( 2.058838311996999959, 3.411444769430000079, 1.578107062294999974 ) ) ;
#36000=CARTESIAN_POINT ( 'NONE',  ( 9.518314158773000244, 4.845406482350000488, -6.387189183984999907 ) ) ;
#36001=DIRECTION ( 'NONE',  ( 1.000000000000000000, 0.000000000000000000, 0.000000000000000000 ) ) ;
#36002=LINE ( 'NONE', #14344, #61469 ) ;
#36006=DIRECTION ( 'NONE',  ( 0.000000000000000000, 0.000000000000000000, -1.000000000000000000 ) ) ;
#36009=CARTESIAN_POINT ( 'NONE',  ( 9.176357780411999343, 2.935741164366000522, 6.259844213126999790 ) ) ;
#36013=DIRECTION ( 'NONE',  ( -1.000000000000000000, 0.000000000000000000, 0.000000000000000000 ) ) ;
#36014=CARTESIAN_POINT ( 'NONE',  ( 1.123382408447999747, 1.635708097465000010, -3.009863393104000195 ) ) ;
#36016=FACE_OUTER_BOUND ( 'NONE', #24635, .T. ) ;
#36018=EDGE_CURVE ( 'NONE', #28156, #7065, #22344, .T. ) ;
#36019=CARTESIAN_POINT ( 'NONE',  ( 10.46432998405999903, 2.042755206296999582, 7.723699495214000343 ) ) ;
#36020=CARTESIAN_POINT ( 'NONE',  ( 10.27967883605999866, 5.739712809045000697, 7.774963411801000923 ) ) ;
#36024=DIRECTION ( 'NONE',  ( 0.000000000000000000, 0.000000000000000000, 1.000000000000000000 ) ) ;
#36028=ORIENTED_EDGE ( 'NONE', *, *, #56907, .T. ) ;
#36029=CARTESIAN_POINT ( 'NONE',  ( 7.307500000000000107, 0.2999999999999999889, -3.149999999999999911 ) ) ;
#36034=CARTESIAN_POINT ( 'NONE',  ( 10.93227693248999977, 2.539877577705000000, 6.453611809651000009 ) ) ;
#36035=CARTESIAN_POINT ( 'NONE',  ( 9.870875237110999123, 2.904361819252000210, -8.563871667095998674 ) ) ;
#36046=CARTESIAN_POINT ( 'NONE',  ( 9.769471092180999960, 5.100000000000000533, -6.152188490330000370 ) ) ;
#36048=CARTESIAN_POINT ( 'NONE',  ( 8.960616452296999768, 2.899999999999999911, 6.279946362737000243 ) ) ;
#36054=CARTESIAN_POINT ( 'NONE',  ( 10.93785547196599950, 2.862144528033999880, 6.360512911308666695 ) ) ;
#36055=VERTEX_POINT ( 'NONE', #29283 ) ;
#36057=LINE ( 'NONE', #9475, #44868 ) ;
#36058=EDGE_LOOP ( 'NONE', ( #68966, #31639, #20098, #7814 ) ) ;
#36066=CARTESIAN_POINT ( 'NONE',  ( 0.4251162859547999995, 1.034012873651999787, -3.554373790709000058 ) ) ;
#36067=CARTESIAN_POINT ( 'NONE',  ( 7.924878289113897800, 5.349357204871084903, 7.500005630225526687 ) ) ;
#36069=CARTESIAN_POINT ( 'NONE',  ( 11.09999999999999964, 2.700000000742000417, -5.148510365175999581 ) ) ;
#36073=CARTESIAN_POINT ( 'NONE',  ( 11.20537028040999949, 2.688545137295000220, -8.273930556758998023 ) ) ;
#36077=CARTESIAN_POINT ( 'NONE',  ( 10.08712270112418885, 5.286531262339692283, -7.026829543710713111 ) ) ;
#36081=CARTESIAN_POINT ( 'NONE',  ( 10.98768472638000127, 7.408460564924999936, -6.159405844198999169 ) ) ;
#36107=CARTESIAN_POINT ( 'NONE',  ( 9.053070280414001303, 2.391443348526999912, -6.856688371964000162 ) ) ;
#36114=CARTESIAN_POINT ( 'NONE',  ( 8.653803059789224150, 2.648172424375619727, 7.852957271308079079 ) ) ;
#36117=CARTESIAN_POINT ( 'NONE',  ( 4.149992563292000725, -2.000000000000000000, 0.000000000000000000 ) ) ;
#36124=CARTESIAN_POINT ( 'NONE',  ( 10.10682028041000002, 4.294368353031000396, -8.968663198664000191 ) ) ;
#36126=B_SPLINE_CURVE_WITH_KNOTS ( 'NONE', 3,
 ( #67671, #20137, #46370, #51268, #24699 ),
 .UNSPECIFIED., .F., .F.,
 ( 4, 1, 4 ),
 ( 0.000000000000000000, 0.2283572645236016108, 1.000000000000000000 ),
 .UNSPECIFIED. ) ;
#36127=CARTESIAN_POINT ( 'NONE',  ( 11.10062015617000064, 3.093053541899000169, -6.153678467293999255 ) ) ;
#36136=EDGE_CURVE ( 'NONE', #39016, #62424, #42294, .T. ) ;
#36138=CARTESIAN_POINT ( 'NONE',  ( 8.642077642326000841, 2.899999999999999911, 6.463854830420999953 ) ) ;
#36139=ORIENTED_EDGE ( 'NONE', *, *, #13803, .T. ) ;
#36146=CARTESIAN_POINT ( 'NONE',  ( 0.5000220334827000235, 2.806761118207999672, -2.090954811877999919 ) ) ;
#36150=CARTESIAN_POINT ( 'NONE',  ( 9.368660841232999914, 2.702406276695999754, -6.981052078638000147 ) ) ;
#36151=CARTESIAN_POINT ( 'NONE',  ( 10.06489140842196406, 5.349900232312646331, -7.500006335289779003 ) ) ;
#36154=CARTESIAN_POINT ( 'NONE',  ( 7.815856925312669290, 3.425834468749924699, 6.252095740542113589 ) ) ;
#36157=DIRECTION ( 'NONE',  ( 0.000000000000000000, 1.000000000000000000, 0.000000000000000000 ) ) ;
#36162=AXIS2_PLACEMENT_3D ( 'NONE', #21680, #10509, #68889 ) ;
#36166=CARTESIAN_POINT ( 'NONE',  ( 8.200000998245998929, -12.50000000000000000, 0.000000000000000000 ) ) ;
#36168=CARTESIAN_POINT ( 'NONE',  ( 10.18367854428788633, 2.796579479970431326, 8.204151721975319944 ) ) ;
#36169=B_SPLINE_CURVE_WITH_KNOTS ( 'NONE', 3,
 ( #36899, #865, #31651, #22181, #517, #69049, #48070, #43521, #21157, #21491, #42484, #63794, #42825, #15903 ),
 .UNSPECIFIED., .F., .F.,
 ( 4, 2, 2, 2, 2, 2, 4 ),
 ( 0.05661757269142905086, 0.2924631795185714256, 0.4103859829321429564, 0.5283087863457146538, 0.6462315897592861846, 0.7641543931728578265, 1.000000000000000000 ),
 .UNSPECIFIED. ) ;
#36171=CARTESIAN_POINT ( 'NONE',  ( 7.994077351562546951, 3.211953255579858446, -6.298056302553895591 ) ) ;
#36173=EDGE_CURVE ( 'NONE', #227, #14714, #22983, .T. ) ;
#36174=CARTESIAN_POINT ( 'NONE',  ( 0.1492968197647682738, 0.8235178986539704038, -3.067640566204680397 ) ) ;
#36176=CARTESIAN_POINT ( 'NONE',  ( 3.539384965075000000, -3.233467766375999641, 0.4074197872470000092 ) ) ;
#36183=CARTESIAN_POINT ( 'NONE',  ( 10.32340023520120020, 2.820488420191645584, -8.179866073662113379 ) ) ;
#36199=CARTESIAN_POINT ( 'NONE',  ( 7.563304092220104025, 3.763842522021197290, 8.850238422624055801 ) ) ;
#36200=CARTESIAN_POINT ( 'NONE',  ( 8.219220280408000789, 5.354408404900999230, -6.419792067946000103 ) ) ;
#36211=VERTEX_POINT ( 'NONE', #62450 ) ;
#36222=ADVANCED_FACE ( 'NONE', ( #19464 ), #68373, .T. ) ;
#36223=ORIENTED_EDGE ( 'NONE', *, *, #60659, .T. ) ;
#36226=CARTESIAN_POINT ( 'NONE',  ( 10.07102359808000003, 4.042170458878000083, 8.920189456109998360 ) ) ;
#36229=CARTESIAN_POINT ( 'NONE',  ( 2.761417138354999690, -1.986395360111999908, -2.934648526694999759 ) ) ;
#36232=ORIENTED_EDGE ( 'NONE', *, *, #11468, .F. ) ;
#36234=CARTESIAN_POINT ( 'NONE',  ( 10.55463379556076831, 2.421258825577123464, -8.251507791233850142 ) ) ;
#36235=CARTESIAN_POINT ( 'NONE',  ( 10.83253786428999987, 2.899999999999999911, 6.571291218949999902 ) ) ;
#36238=CARTESIAN_POINT ( 'NONE',  ( 10.46932803217000085, 4.988495740890000363, 6.213106455073000411 ) ) ;
#36248=ORIENTED_EDGE ( 'NONE', *, *, #58665, .T. ) ;
#36250=CARTESIAN_POINT ( 'NONE',  ( 4.000000000000000888, 2.094138670346413100, -0.5626148410812732426 ) ) ;
#36251=CARTESIAN_POINT ( 'NONE',  ( 8.679055905797000037, 2.899999999999999911, 6.571291218949999902 ) ) ;
#36252=B_SPLINE_CURVE_WITH_KNOTS ( 'NONE', 3,
 ( #37038, #24828, #31795, #67459 ),
 .UNSPECIFIED., .F., .F.,
 ( 4, 4 ),
 ( 0.000000000000000000, 1.000000000000000000 ),
 .UNSPECIFIED. ) ;
#36258=CARTESIAN_POINT ( 'NONE',  ( 10.88760471959000142, 5.634847467408999222, -7.088990678556999825 ) ) ;
#36264=DIRECTION ( 'NONE',  ( 0.000000000000000000, 1.000000000000000000, 0.000000000000000000 ) ) ;
#36265=LINE ( 'NONE', #58619, #3321 ) ;
#36268=CARTESIAN_POINT ( 'NONE',  ( 7.566889158767000190, 2.100129367691999871, -7.493434492293999938 ) ) ;
#36269=AXIS2_PLACEMENT_3D ( 'NONE', #28295, #64984, #12215 ) ;
#36280=CARTESIAN_POINT ( 'NONE',  ( 2.405140132543083897, -0.9161175952574773795, -3.408904368339105595 ) ) ;
#36285=CARTESIAN_POINT ( 'NONE',  ( 7.239691113742999562, 4.389299166881000858, 9.135259451319999613 ) ) ;
#36301=EDGE_CURVE ( 'NONE', #57692, #67708, #62109, .T. ) ;
#36304=ORIENTED_EDGE ( 'NONE', *, *, #15221, .F. ) ;
#36308=CARTESIAN_POINT ( 'NONE',  ( 10.70780830849999887, 5.157484706885999692, -6.267808298721999627 ) ) ;
#36309=B_SPLINE_CURVE_WITH_KNOTS ( 'NONE', 3,
 ( #47997, #96, #64052, #16174, #37500, #58823, #10931, #32274, #38180, #5678, #48335, #21755, #59512, #34691, #22795, #56003, #44832, #6715, #65442 ),
 .UNSPECIFIED., .F., .F.,
 ( 4, 1, 1, 1, 1, 1, 1, 1, 1, 1, 1, 1, 1, 1, 1, 1, 4 ),
 ( 0.000000000000000000, 0.04500088138722610487, 0.1100007829711507901, 0.1750006845550757251, 0.2400005861392325857, 0.3050004877231572986, 0.3700003893070824557, 0.4350002908912390942, 0.5000001924751640292, 0.5650000940590889087, 0.6299999956432456027, 0.6949998972271704822, 0.7599997988110954728, 0.8249997003950201302, 0.8899996019791770463, 0.9549995035631019258, 1.000000000000000000 ),
 .UNSPECIFIED. ) ;
#36310=CARTESIAN_POINT ( 'NONE',  ( 8.674844125071947687, 5.060684314967137887, 6.220133919708653814 ) ) ;
#36314=CARTESIAN_POINT ( 'NONE',  ( 10.55991859298999991, 5.094266430778000121, 6.075406703384000018 ) ) ;
#36319=CARTESIAN_POINT ( 'NONE',  ( 8.575665180404380195, 5.349989392515093201, -7.683710349381269289 ) ) ;
#36320=CARTESIAN_POINT ( 'NONE',  ( 9.632179190069999564, 5.638172764974000550, 6.476627236431999890 ) ) ;
#36323=CARTESIAN_POINT ( 'NONE',  ( 9.020585841232000135, 4.920236664407999783, -6.448229650796999834 ) ) ;
#36333=CARTESIAN_POINT ( 'NONE',  ( 8.491329719591000469, 4.851303550474000303, -9.008742670124000540 ) ) ;
#36335=VECTOR ( 'NONE', #29891, 1000.000000000000114 ) ;
#36341=CARTESIAN_POINT ( 'NONE',  ( 2.440293907525000083, 1.849469983415999996, -3.272124421528999960 ) ) ;
#36343=CARTESIAN_POINT ( 'NONE',  ( 9.841547757529466978, 3.644489497211603535, 9.239081501414979414 ) ) ;
#36353=CARTESIAN_POINT ( 'NONE',  ( 8.764829719592999169, 5.808262417891000062, 7.446016144116000213 ) ) ;
#36361=CARTESIAN_POINT ( 'NONE',  ( 11.09999999999999964, 0.5000000000000000000, 5.124965750789000296 ) ) ;
#36362=B_SPLINE_CURVE_WITH_KNOTS ( 'NONE', 3,
 ( #15547, #16224, #16570, #36876, #58878, #10294 ),
 .UNSPECIFIED., .F., .F.,
 ( 4, 1, 1, 4 ),
 ( 0.000000000000000000, 0.3333333333333000081, 0.6666666666667000474, 1.000000000000000000 ),
 .UNSPECIFIED. ) ;
#36364=CARTESIAN_POINT ( 'NONE',  ( 9.905792474809000936, 2.698958900805999761, 8.979236532123000103 ) ) ;
#36365=CARTESIAN_POINT ( 'NONE',  ( 9.465106464520001595, 2.290037071913000322, 6.601704384062999864 ) ) ;
#36366=VECTOR ( 'NONE', #22705, 999.9999999999998863 ) ;
#36375=DIRECTION ( 'NONE',  ( -1.000000000000000000, 0.000000000000000000, 0.000000000000000000 ) ) ;
#36377=ORIENTED_EDGE ( 'NONE', *, *, #31798, .F. ) ;
#36380=CARTESIAN_POINT ( 'NONE',  ( 9.600491906670001185, 5.206545077004999911, 8.585111878242999595 ) ) ;
#36381=CARTESIAN_POINT ( 'NONE',  ( 10.39355883036999906, 4.089958667033000594, -9.188186800857998549 ) ) ;
#36389=EDGE_CURVE ( 'NONE', #26858, #30735, #4747, .T. ) ;
#36395=CONICAL_SURFACE ( 'NONE', #38639, 12.44999944941000081, 0.7853981146832407223 ) ;
#36396=CARTESIAN_POINT ( 'NONE',  ( 6.981185917753003345, 10.82755309799000010, 3.400726541711003748 ) ) ;
#36401=ORIENTED_EDGE ( 'NONE', *, *, #19365, .F. ) ;
#36404=FACE_OUTER_BOUND ( 'NONE', #45701, .T. ) ;
#36412=CARTESIAN_POINT ( 'NONE',  ( 9.009297488802992859, 5.100000000000000533, 6.455145051482742424 ) ) ;
#36413=CARTESIAN_POINT ( 'NONE',  ( 8.133277933996836850, 2.820894615410977746, 8.178702166371902393 ) ) ;
#36418=CARTESIAN_POINT ( 'NONE',  ( 10.81187971959000116, 4.614148948243999904, -5.930135044105000475 ) ) ;
#36420=DIRECTION ( 'NONE',  ( 0.000000000000000000, 0.9048270524660052549, -0.4257792915651026910 ) ) ;
#36426=DIRECTION ( 'NONE',  ( 0.8660254006610920152, 3.948310870465965241E-12, 0.5000000054097949453 ) ) ;
#36440=EDGE_CURVE ( 'NONE', #12675, #26552, #19117, .T. ) ;
#36451=CARTESIAN_POINT ( 'NONE',  ( 9.848670280409999478, 5.002683760508999988, -8.912673867568997821 ) ) ;
#36459=CARTESIAN_POINT ( 'NONE',  ( 9.491735841231999871, 3.920043641733999884, -9.398198753036000497 ) ) ;
#36463=DIRECTION ( 'NONE',  ( 0.7071068156326932863, 0.000000000000000000, -0.7071067467404001938 ) ) ;
#36464=VERTEX_POINT ( 'NONE', #29979 ) ;
#36466=CARTESIAN_POINT ( 'NONE',  ( 9.187479719595000205, 2.391443348526999912, -6.856688371964000162 ) ) ;
#36469=CARTESIAN_POINT ( 'NONE',  ( 11.17811698873999937, 2.762452057009999962, -6.187198315927000536 ) ) ;
#36476=LINE ( 'NONE', #57800, #34836 ) ;
#36485=CARTESIAN_POINT ( 'NONE',  ( 8.450464158772000189, 3.789127741898000057, -9.388182174781999123 ) ) ;
#36486=CIRCLE ( 'NONE', #26461, 12.50000000000000000 ) ;
#36491=CARTESIAN_POINT ( 'NONE',  ( 9.070310841232000598, 5.361622798585000460, -7.185294144754000634 ) ) ;
#36493=DIRECTION ( 'NONE',  ( 1.000000000000000000, 0.000000000000000000, 0.000000000000000000 ) ) ;
#36495=DIRECTION ( 'NONE',  ( 0.7071059447856029578, 0.7071076175865028679, -3.669605936760013587E-09 ) ) ;
#36499=CARTESIAN_POINT ( 'NONE',  ( 7.760448372719867649, 3.361655312119658401, 6.300695999402769587 ) ) ;
#36511=CARTESIAN_POINT ( 'NONE',  ( 8.856851002545001350, 2.832432432432000269, -6.822293592207000934 ) ) ;
#36517=CARTESIAN_POINT ( 'NONE',  ( 2.776473774021000374, 3.125185655655999817, -0.9243923524902999400 ) ) ;
#36526=ORIENTED_EDGE ( 'NONE', *, *, #6212, .F. ) ;
#36530=CARTESIAN_POINT ( 'NONE',  ( 0.6048333392154046084, 0.9397506571931915076, 3.402778030820548416 ) ) ;
#36532=CARTESIAN_POINT ( 'NONE',  ( 10.71480780573045699, 2.649489222497333429, 7.676606295960487714 ) ) ;
#36535=AXIS2_PLACEMENT_3D ( 'NONE', #61599, #13716, #24195 ) ;
#36544=CARTESIAN_POINT ( 'NONE',  ( 6.984954719590999339, 2.766448485756999975, -6.536937350656000234 ) ) ;
#36552=ORIENTED_EDGE ( 'NONE', *, *, #8541, .F. ) ;
#36555=CYLINDRICAL_SURFACE ( 'NONE', #25891, 1.999999999999999778 ) ;
#36569=CARTESIAN_POINT ( 'NONE',  ( 10.72520610419000064, 5.521650664120000940, 6.612990918765000004 ) ) ;
#36572=CARTESIAN_POINT ( 'NONE',  ( 2.810090735696999964, -3.340490407592999755, -1.609581997777000062 ) ) ;
#36574=EDGE_CURVE ( 'NONE', #62089, #61638, #8972, .T. ) ;
#36581=CARTESIAN_POINT ( 'NONE',  ( 3.217640132543999165, -1.762666431298159475, 3.058252359239895135 ) ) ;
#36584=CARTESIAN_POINT ( 'NONE',  ( 10.90374609491999891, 3.726846467344000047, 5.900456154266000119 ) ) ;
#36599=CARTESIAN_POINT ( 'NONE',  ( 4.000000000000000000, 0.2816038378556621202, -2.150035234257813510 ) ) ;
#36603=CARTESIAN_POINT ( 'NONE',  ( 0.6501162859548000883, 0.8965373106020000371, -3.081807587122999958 ) ) ;
#36605=CARTESIAN_POINT ( 'NONE',  ( 10.37239528041000014, 3.992345698584000235, -5.977238432995000572 ) ) ;
#36606=ORIENTED_EDGE ( 'NONE', *, *, #62563, .T. ) ;
#36612=CARTESIAN_POINT ( 'NONE',  ( 8.721010841230999233, 5.983047240001000411, 7.440798119034999658 ) ) ;
#36616=ADVANCED_FACE ( 'NONE', ( #15844 ), #7779, .T. ) ;
#36622=B_SPLINE_CURVE_WITH_KNOTS ( 'NONE', 3,
 ( #60696, #1977, #2994, #29595, #50213 ),
 .UNSPECIFIED., .F., .F.,
 ( 4, 1, 4 ),
 ( 0.000000000000000000, 0.5000000000000000000, 1.000000000000000000 ),
 .UNSPECIFIED. ) ;
#36630=CARTESIAN_POINT ( 'NONE',  ( 8.497235841230001085, 3.789127741898000057, -9.388182174781999123 ) ) ;
#36635=CARTESIAN_POINT ( 'NONE',  ( 7.641204719590000138, 4.524487726177000013, 9.047753146378999745 ) ) ;
#36660=CARTESIAN_POINT ( 'NONE',  ( 10.30296826955000000, 4.081263352980999848, -9.025008366823000117 ) ) ;
#36662=EDGE_CURVE ( 'NONE', #49930, #65620, #34867, .T. ) ;
#36665=AXIS2_PLACEMENT_3D ( 'NONE', #11760, #61643, #61992 ) ;
#36669=ORIENTED_EDGE ( 'NONE', *, *, #15752, .F. ) ;
#36672=CARTESIAN_POINT ( 'NONE',  ( 10.05691520198999989, 2.453477278391000382, 6.657104391228999773 ) ) ;
#36675=CARTESIAN_POINT ( 'NONE',  ( 10.90023029886999950, 9.364047981009999688, -6.155772864046999970 ) ) ;
#36680=CARTESIAN_POINT ( 'NONE',  ( 9.758140238852000437, 2.901378080241999946, 6.555076849497999625 ) ) ;
#36682=ORIENTED_EDGE ( 'NONE', *, *, #7882, .F. ) ;
#36683=CARTESIAN_POINT ( 'NONE',  ( 9.278070280414000948, 2.546924812613000189, -6.918870225297999887 ) ) ;
#36686=CARTESIAN_POINT ( 'NONE',  ( 9.125651434942099627, 5.349687154987381454, -7.676802464757987110 ) ) ;
#36693=CARTESIAN_POINT ( 'NONE',  ( 8.871889158775999817, 2.702406276695999754, -6.981052078638000147 ) ) ;
#36698=CARTESIAN_POINT ( 'NONE',  ( 10.79500540879000070, 3.503955365545999623, 6.168588659884999714 ) ) ;
#36699=AXIS2_PLACEMENT_3D ( 'NONE', #18045, #39362, #28891 ) ;
#36705=CARTESIAN_POINT ( 'NONE',  ( 8.289114158772999730, 4.310355144869000732, 9.459505265942000918 ) ) ;
#36707=EDGE_CURVE ( 'NONE', #5489, #62147, #14997, .T. ) ;
#36716=CARTESIAN_POINT ( 'NONE',  ( 10.40227026081000083, 2.765684886876999649, 9.035354958280999327 ) ) ;
#36717=CARTESIAN_POINT ( 'NONE',  ( 10.94796973825000030, 2.864322365205000054, 8.846249469408000721 ) ) ;
#36720=B_SPLINE_SURFACE_WITH_KNOTS ( 'NONE', 3, 3, ( 
 ( #51042, #23087, #60844, #12260, #38828, #34633, #49660, #66771, #56290, #8394, #55945, #7009, #2798, #1769, #17855, #12956, #50010, #29739, #23437, #18197, #13645, #7351, #44776, #13311, #66423, #33589, #24472, #50355, #24124, #3143, #29391, #45459, #18544, #28341, #65732 ),
 ( #18889, #39519, #66076, #7706, #40214, #34972, #39173, #60496, #2455, #12605, #34283, #28696, #55604, #23780, #39871, #14333, #9406, #62213, #68134, #35656, #19913, #25153, #52754, #46829, #35985, #46485, #40891, #20252, #25842, #67447, #63229, #41578, #36333, #56970, #25499 ),
 ( #47170, #30409, #4849, #62886, #9071, #67792, #19218, #47516, #51721, #19569, #15007, #14672, #20595, #24815, #57303, #3816, #30749, #57648, #36683, #9754, #58004, #41238, #31102, #52408, #52057, #4501, #35314, #62549, #4161, #68473, #41920, #26193, #15357, #10103, #31438 ),
 ( #40544, #61869, #13988, #56632, #8735, #30080, #51380, #3479, #46141, #20945, #33159, #22309, #48893, #32811, #58339, #37362, #21281, #42611, #63921, #58684, #43650, #47864, #10442, #16714, #31782, #15696, #54476, #54126, #10788, #5198, #38045, #17061, #27917, #63581, #38393 ) ),
 .UNSPECIFIED., .F., .F., .F.,
 ( 4, 4 ),
 ( 4, 1, 1, 1, 1, 1, 1, 1, 1, 1, 1, 1, 1, 1, 1, 1, 1, 1, 1, 1, 1, 1, 1, 1, 1, 1, 1, 1, 1, 1, 1, 1, 4 ),
 ( -0.1039370721279000015, 1.103937072127999963 ),
 ( -0.02000000000000000042, 0.01250000000000000069, 0.04499999999999999833, 0.07749999999999999944, 0.1100000000000000006, 0.1424999999999999878, 0.1749999999999999889, 0.2074999999999999900, 0.2399999999999999911, 0.2725000000000000200, 0.3049999999999999933, 0.3375000000000000222, 0.3699999999999999956, 0.4025000000000000244, 0.4349999999999999978, 0.4675000000000000266, 0.5000000000000000000, 0.5324999999999999734, 0.5649999999999999467, 0.5975000000000000311, 0.6300000000000000044, 0.6624999999999999778, 0.6949999999999999512, 0.7275000000000000355, 0.7600000000000000089, 0.7924999999999999822, 0.8249999999999999556, 0.8575000000000000400, 0.8900000000000000133, 0.9224999999999999867, 0.9549999999999999600, 0.9875000000000000444, 1.020000000000000018 ),
 .UNSPECIFIED. ) ;
#36734=CARTESIAN_POINT ( 'NONE',  ( 10.97864812944000157, 5.273131703456000352, 7.958028903907000462 ) ) ;
#36735=CARTESIAN_POINT ( 'NONE',  ( 9.856715971886000460, 4.814120192353000149, -8.929574926876000518 ) ) ;
#36736=CARTESIAN_POINT ( 'NONE',  ( 7.613778970466999141, 4.858908887722000358, 6.437635593844006188 ) ) ;
#36740=B_SPLINE_CURVE_WITH_KNOTS ( 'NONE', 3,
 ( #68554, #15088, #36412, #37103 ),
 .UNSPECIFIED., .F., .F.,
 ( 4, 4 ),
 ( 0.000000000000000000, 1.000000000000000000 ),
 .UNSPECIFIED. ) ;
#36742=CARTESIAN_POINT ( 'NONE',  ( 9.202760841230999134, 2.542862824481000317, 7.419808961972999661 ) ) ;
#36743=ORIENTED_EDGE ( 'NONE', *, *, #66836, .T. ) ;
#36745=FACE_OUTER_BOUND ( 'NONE', #44443, .T. ) ;
#36747=CARTESIAN_POINT ( 'NONE',  ( 11.31510034929000241, 9.451872599583003520, 6.816406955572995585 ) ) ;
#36752=LINE ( 'NONE', #20665, #52667 ) ;
#36761=CARTESIAN_POINT ( 'NONE',  ( 7.790635841228000125, 3.416213390569000197, 6.162512717529000206 ) ) ;
#36767=CARTESIAN_POINT ( 'NONE',  ( 9.991525552923999243, 4.805950298207000593, -8.932431532051998246 ) ) ;
#36774=CARTESIAN_POINT ( 'NONE',  ( 7.744950122392999958, 2.855953552844000320, 6.776551829089000556 ) ) ;
#36781=ORIENTED_EDGE ( 'NONE', *, *, #49273, .F. ) ;
#36783=B_SPLINE_CURVE_WITH_KNOTS ( 'NONE', 3,
 ( #2317, #1980, #33103, #33450 ),
 .UNSPECIFIED., .F., .F.,
 ( 4, 4 ),
 ( 0.000000000000000000, 1.000000000000000000 ),
 .UNSPECIFIED. ) ;
#36784=EDGE_CURVE ( 'NONE', #51368, #67585, #48418, .T. ) ;
#36791=CARTESIAN_POINT ( 'NONE',  ( 8.581715799613704121, 5.025392983842594141, 6.195064399343296557 ) ) ;
#36793=B_SPLINE_CURVE_WITH_KNOTS ( 'NONE', 3,
 ( #44801, #29420, #22764, #29073, #13335, #28026, #34659, #44465, #24153, #18223, #45486, #7730, #17531, #38861, #50383, #65410, #23808, #33270 ),
 .UNSPECIFIED., .F., .F.,
 ( 4, 2, 2, 2, 2, 2, 2, 2, 4 ),
 ( 0.000000000000000000, 0.1250000000000000278, 0.2500000000000000555, 0.3749999999999999445, 0.4999999999999999445, 0.6249999999999998890, 0.7499999999999998890, 0.8750000000000000000, 1.000000000000000000 ),
 .UNSPECIFIED. ) ;
#36797=CARTESIAN_POINT ( 'NONE',  ( 9.225036466121004253, 2.649952287134117235, 7.500002258928285315 ) ) ;
#36802=EDGE_CURVE ( 'NONE', #42751, #24606, #3156, .T. ) ;
#36804=CARTESIAN_POINT ( 'NONE',  ( 8.754720280412998434, 5.687930027805999877, -7.109876198051000351 ) ) ;
#36807=B_SPLINE_CURVE_WITH_KNOTS ( 'NONE', 3,
 ( #60374, #44658, #35193, #66985, #50919, #39397, #3358, #29616, #40420, #50231, #65950, #23654 ),
 .UNSPECIFIED., .F., .F.,
 ( 4, 2, 2, 2, 2, 4 ),
 ( 0.000000000000000000, 0.2499999999999754641, 0.3749999999999631961, 0.4374999999999594213, 0.4999999999999557021, 1.000000000000000000 ),
 .UNSPECIFIED. ) ;
#36819=ORIENTED_EDGE ( 'NONE', *, *, #36951, .F. ) ;
#36821=CARTESIAN_POINT ( 'NONE',  ( 9.178620280414001797, 2.990001567622999623, -8.695425648791999862 ) ) ;
#36822=VERTEX_POINT ( 'NONE', #37352 ) ;
#36824=CARTESIAN_POINT ( 'NONE',  ( 10.43284001513000092, 3.279325423736999756, -9.029279369994000604 ) ) ;
#36832=ORIENTED_EDGE ( 'NONE', *, *, #49045, .F. ) ;
#36836=CARTESIAN_POINT ( 'NONE',  ( 10.33253786428999987, 2.899999999999999911, 6.571291218949999902 ) ) ;
#36837=CARTESIAN_POINT ( 'NONE',  ( 9.096889158776001238, 2.235961884443999459, -6.794506518623999902 ) ) ;
#36840=EDGE_CURVE ( 'NONE', #46556, #11525, #16391, .T. ) ;
#36841=ADVANCED_FACE ( 'NONE', ( #34875 ), #23920, .F. ) ;
#36844=CARTESIAN_POINT ( 'NONE',  ( 11.09999999999999964, 5.350000000000000533, -7.500000000000000000 ) ) ;
#36846=CARTESIAN_POINT ( 'NONE',  ( 0.1499942179679999987, -2.750000000000000000, 0.000000000000000000 ) ) ;
#36861=EDGE_CURVE ( 'NONE', #4517, #39722, #59730, .T. ) ;
#36865=CARTESIAN_POINT ( 'NONE',  ( 7.935762780894745738, 2.895074738935549341, -6.665507318599334319 ) ) ;
#36873=ORIENTED_EDGE ( 'NONE', *, *, #52271, .F. ) ;
#36876=CARTESIAN_POINT ( 'NONE',  ( 5.440293061358000060, -12.88483958404999896, 2.133988467673999967 ) ) ;
#36878=CARTESIAN_POINT ( 'NONE',  ( 9.317462135714000837, 5.100000000000000533, 6.571291218949999902 ) ) ;
#36897=CARTESIAN_POINT ( 'NONE',  ( 7.183854719589999327, 5.564636229952000690, -7.532446618777999703 ) ) ;
#36899=CARTESIAN_POINT ( 'NONE',  ( 7.115095033390245405, 5.350161709276040511, -7.499994210608702083 ) ) ;
#36910=VECTOR ( 'NONE', #19025, 1000.000000000000114 ) ;
#36915=EDGE_LOOP ( 'NONE', ( #14489, #51470, #69158, #44105 ) ) ;
#36919=CARTESIAN_POINT ( 'NONE',  ( 10.61382428715999993, 3.385080336122999967, 5.849521480782000182 ) ) ;
#36920=CARTESIAN_POINT ( 'NONE',  ( 10.75915165876999957, 5.387277012365999873, -6.278112168454999420 ) ) ;
#36925=CARTESIAN_POINT ( 'NONE',  ( 8.316694475082000437, 2.898380349184999982, 6.611503672649000407 ) ) ;
#36928=EDGE_CURVE ( 'NONE', #18734, #33797, #55158, .T. ) ;
#36929=EDGE_CURVE ( 'NONE', #27423, #44223, #47378, .T. ) ;
#36930=VERTEX_POINT ( 'NONE', #4414 ) ;
#36936=CARTESIAN_POINT ( 'NONE',  ( 5.000000000000000000, 0.000000000000000000, 0.000000000000000000 ) ) ;
#36944=FACE_OUTER_BOUND ( 'NONE', #37706, .T. ) ;
#36945=ORIENTED_EDGE ( 'NONE', *, *, #60976, .F. ) ;
#36947=CARTESIAN_POINT ( 'NONE',  ( 9.608904719592000987, 4.946705552514000459, -6.253848946732999181 ) ) ;
#36951=EDGE_CURVE ( 'NONE', #29419, #13267, #4756, .T. ) ;
#36954=FACE_OUTER_BOUND ( 'NONE', #32560, .T. ) ;
#36955=CARTESIAN_POINT ( 'NONE',  ( 10.61443584123000150, 5.287628373050000441, -7.937241318065001217 ) ) ;
#36961=CARTESIAN_POINT ( 'NONE',  ( 7.239691113742999562, 4.389299166881000858, 9.135259451319999613 ) ) ;
#36974=DIRECTION ( 'NONE',  ( -1.000000000000000000, 0.000000000000000000, 0.000000000000000000 ) ) ;
#36984=CARTESIAN_POINT ( 'NONE',  ( 8.475642219593000348, 5.095085596809999728, 6.286981168432999922 ) ) ;
#36985=VERTEX_POINT ( 'NONE', #9660 ) ;
#36986=CARTESIAN_POINT ( 'NONE',  ( 7.770167205733136129, 2.851533015163007168, 6.786995571359490498 ) ) ;
#36991=CARTESIAN_POINT ( 'NONE',  ( 11.83099708403000072, 9.769906715298992239, -5.688772285757997871 ) ) ;
#36996=DIRECTION ( 'NONE',  ( 0.000000000000000000, -0.1218274111675001353, -0.9925512993736016476 ) ) ;
#37002=DIRECTION ( 'NONE',  ( 0.000000000000000000, 0.000000000000000000, -1.000000000000000000 ) ) ;
#37003=CARTESIAN_POINT ( 'NONE',  ( 10.75911768454999873, 4.477564074640000058, -5.708570851020999370 ) ) ;
#37006=CARTESIAN_POINT ( 'NONE',  ( 7.698447294381004724, 2.921226879009002797, -6.534475276641003916 ) ) ;
#37011=ORIENTED_EDGE ( 'NONE', *, *, #59561, .F. ) ;
#37015=CARTESIAN_POINT ( 'NONE',  ( 10.02991192131000098, 2.506457833269999824, 6.215406506815000398 ) ) ;
#37017=CARTESIAN_POINT ( 'NONE',  ( 10.18908827523999960, 5.907871695079999874, 7.801541097952000570 ) ) ;
#37019=CARTESIAN_POINT ( 'NONE',  ( 9.517835841233001304, 4.883347899767999323, -6.417062834774999835 ) ) ;
#37021=CARTESIAN_POINT ( 'NONE',  ( 11.08630703507021309, 2.236024944707789786, -7.580658295093686050 ) ) ;
#37023=CARTESIAN_POINT ( 'NONE',  ( 8.257250525884806791, 3.704169666136653660, -8.842725691832136192 ) ) ;
#37024=CARTESIAN_POINT ( 'NONE',  ( 10.06843885510000014, 4.148608506723999945, 8.941445591976998841 ) ) ;
#37026=VERTEX_POINT ( 'NONE', #35564 ) ;
#37030=CARTESIAN_POINT ( 'NONE',  ( 9.156894352917975155, 5.179846900956039057, -8.179877273890650002 ) ) ;
#37036=CARTESIAN_POINT ( 'NONE',  ( 9.559179719593000613, 4.038835765825999680, -5.935509327774999733 ) ) ;
#37038=CARTESIAN_POINT ( 'NONE',  ( 10.76685100253999927, 2.832432432432000269, 6.822293592207000934 ) ) ;
#37040=CARTESIAN_POINT ( 'NONE',  ( 10.85069631730999973, 4.478098874537000285, 6.162039661770999821 ) ) ;
#37046=CARTESIAN_POINT ( 'NONE',  ( 9.251926658770999623, 5.159258275969999197, 9.109498396691998678 ) ) ;
#37051=CARTESIAN_POINT ( 'NONE',  ( 2.072248059201999837, -3.125150066150999884, -0.9245224406458000255 ) ) ;
#37052=EDGE_LOOP ( 'NONE', ( #26039, #11962, #67065, #4321 ) ) ;
#37056=CARTESIAN_POINT ( 'NONE',  ( 10.78089701270000056, 5.735299658853000082, 7.801561896854000366 ) ) ;
#37060=B_SPLINE_CURVE_WITH_KNOTS ( 'NONE', 3,
 ( #44236, #7155, #45262, #29185 ),
 .UNSPECIFIED., .F., .F.,
 ( 4, 4 ),
 ( 0.000000000000000000, 0.1252897355259763035 ),
 .UNSPECIFIED. ) ;
#37063=DIRECTION ( 'NONE',  ( -0.7071067811865955344, -0.7011937529517955348, 0.09125415509064935260 ) ) ;
#37070=CYLINDRICAL_SURFACE ( 'NONE', #30190, 1.350000000000000533 ) ;
#37071=ORIENTED_EDGE ( 'NONE', *, *, #28774, .F. ) ;
#37075=CARTESIAN_POINT ( 'NONE',  ( 9.199602729599000384, 2.551394566582000145, 7.536605852160000119 ) ) ;
#37076=CARTESIAN_POINT ( 'NONE',  ( 10.46009300862000124, 2.565654508827999614, -6.975684004278000394 ) ) ;
#37082=CARTESIAN_POINT ( 'NONE',  ( 9.138573341230998182, 2.933833973450999721, 8.496479443567000800 ) ) ;
#37085=CYLINDRICAL_SURFACE ( 'NONE', #33616, 1.350000000000000533 ) ;
#37086=CYLINDRICAL_SURFACE ( 'NONE', #39468, 1.350000000000000533 ) ;
#37087=CARTESIAN_POINT ( 'NONE',  ( 8.606334483814224612, 2.950802682660377485, -6.230750935425441561 ) ) ;
#37089=CARTESIAN_POINT ( 'NONE',  ( 11.12487846393999824, 6.581954511489999327, 5.643507977536000197 ) ) ;
#37090=CARTESIAN_POINT ( 'NONE',  ( 11.14434846828000047, 10.07921384928999942, 5.729912880222999938 ) ) ;
#37103=CARTESIAN_POINT ( 'NONE',  ( 8.970944094206998898, 5.100000000000000533, 6.571291218949999902 ) ) ;
#37108=CARTESIAN_POINT ( 'NONE',  ( 11.09999999999999964, 2.700000000000000178, -6.461133846875999787 ) ) ;
#37109=CARTESIAN_POINT ( 'NONE',  ( 10.62256721958999961, 2.471460423959999986, -8.210789473540000216 ) ) ;
#37110=EDGE_CURVE ( 'NONE', #54335, #53667, #1250, .T. ) ;
#37114=CARTESIAN_POINT ( 'NONE',  ( 8.962848138711493107, 5.333207449751190765, 7.284311848532326827 ) ) ;
#37117=CARTESIAN_POINT ( 'NONE',  ( 0.8334276407239999962, 1.717122193005000019, 2.769960469742999809 ) ) ;
#37129=DIRECTION ( 'NONE',  ( 1.000000000000000000, 0.000000000000000000, 0.000000000000000000 ) ) ;
#37143=CARTESIAN_POINT ( 'NONE',  ( 8.506095280410999493, 2.305580295895999665, -7.860904109308999743 ) ) ;
#37146=CIRCLE ( 'NONE', #59445, 2.099999999999998757 ) ;
#37158=CARTESIAN_POINT ( 'NONE',  ( 9.418385841233000377, 3.251172436837000301, -6.320036569851000152 ) ) ;
#37160=VECTOR ( 'NONE', #44306, 1000.000000000000114 ) ;
#37166=DIRECTION ( 'NONE',  ( 0.9999999999998953060, 4.575885588343982003E-07, -2.007390825282990779E-09 ) ) ;
#37167=EDGE_CURVE ( 'NONE', #55522, #23367, #13896, .T. ) ;
#37179=ORIENTED_EDGE ( 'NONE', *, *, #68958, .F. ) ;
#37181=CARTESIAN_POINT ( 'NONE',  ( 11.13228700150999906, 5.320905268945000266, -4.957687855802999088 ) ) ;
#37183=CARTESIAN_POINT ( 'NONE',  ( 1.280140132540750653, -3.408904368339108260, 0.9161175952574674985 ) ) ;
#37192=AXIS2_PLACEMENT_3D ( 'NONE', #11554, #18546, #60498 ) ;
#37193=ADVANCED_FACE ( 'NONE', ( #11725 ), #59279, .F. ) ;
#37202=CARTESIAN_POINT ( 'NONE',  ( 7.047500695249826919, 4.967648385114367571, -6.408980097745973659 ) ) ;
#37206=CARTESIAN_POINT ( 'NONE',  ( 6.999999999999999112, 9.352249708179474652, -4.701180404399401880 ) ) ;
#37208=CARTESIAN_POINT ( 'NONE',  ( 0.5000220334827000235, 3.499749845413000049, -0.04184518527856000147 ) ) ;
#37214=CARTESIAN_POINT ( 'NONE',  ( 1.623890132540958486, 2.150913519912194261, 2.798833948393636195 ) ) ;
#37219=FACE_OUTER_BOUND ( 'NONE', #16169, .T. ) ;
#37229=DIRECTION ( 'NONE',  ( 0.000000000000000000, -1.000000000000000000, 0.000000000000000000 ) ) ;
#37231=ORIENTED_EDGE ( 'NONE', *, *, #19972, .F. ) ;
#37233=CARTESIAN_POINT ( 'NONE',  ( 7.166135841225999670, 2.502464354543000091, -6.330838737160999763 ) ) ;
#37238=AXIS2_PLACEMENT_3D ( 'NONE', #14885, #68349, #20468 ) ;
#37257=CARTESIAN_POINT ( 'NONE',  ( 9.799251915619999309, 4.057329420971000467, 9.430703183047999261 ) ) ;
#37258=CARTESIAN_POINT ( 'NONE',  ( 10.91060165877000188, 4.702351492776999820, -9.210043641106000933 ) ) ;
#37271=CARTESIAN_POINT ( 'NONE',  ( 10.00637913184999839, 5.119263020957999899, 8.420380450036001108 ) ) ;
#37274=B_SPLINE_CURVE_WITH_KNOTS ( 'NONE', 3,
 ( #68331, #36532, #31637, #11328, #52266, #57856, #65151, #33710, #6083, #22507, #54679, #16915 ),
 .UNSPECIFIED., .F., .F.,
 ( 4, 2, 2, 2, 2, 4 ),
 ( 0.1253171456473068379, 0.2189680742877681552, 0.3126190029282295280, 0.4999208602091519404, 0.6872227174900742419, 0.8745245747709966544 ),
 .UNSPECIFIED. ) ;
#37275=EDGE_CURVE ( 'NONE', #27251, #46140, #21345, .T. ) ;
#37284=CARTESIAN_POINT ( 'NONE',  ( 9.021064158776001207, 4.883347899767999323, -6.417062834774999835 ) ) ;
#37287=ORIENTED_EDGE ( 'NONE', *, *, #12873, .T. ) ;
#37289=CARTESIAN_POINT ( 'NONE',  ( 0.7573593903515000170, -3.617551005558000021, 0.7847820700415000239 ) ) ;
#37291=CARTESIAN_POINT ( 'NONE',  ( 10.99306084123000105, 4.495422912016000083, -6.233618171705999522 ) ) ;
#37292=ORIENTED_EDGE ( 'NONE', *, *, #10872, .T. ) ;
#37297=CARTESIAN_POINT ( 'NONE',  ( 7.629823341228000544, 4.763536573491999881, 5.668879554882000349 ) ) ;
#37300=CARTESIAN_POINT ( 'NONE',  ( 8.096145280407000655, 4.514357753279999663, -8.978030925517998639 ) ) ;
#37307=CARTESIAN_POINT ( 'NONE',  ( 11.09999999999999964, 4.000000000000000000, -7.500000000000000000 ) ) ;
#37311=EDGE_CURVE ( 'NONE', #25355, #14617, #26165, .T. ) ;
#37320=CARTESIAN_POINT ( 'NONE',  ( 7.614801658771000348, 3.326263523254000098, 8.794511546544999447 ) ) ;
#37324=CARTESIAN_POINT ( 'NONE',  ( 11.01654498872999888, 6.706008375310999803, -5.523030698055999999 ) ) ;
#37337=VERTEX_POINT ( 'NONE', #28166 ) ;
#37341=EDGE_CURVE ( 'NONE', #51168, #7076, #24295, .T. ) ;
#37342=CARTESIAN_POINT ( 'NONE',  ( 10.05205635875000070, 2.669891600604999748, -8.791543746052999708 ) ) ;
#37347=ORIENTED_EDGE ( 'NONE', *, *, #15752, .T. ) ;
#37352=CARTESIAN_POINT ( 'NONE',  ( 7.871384581343000342, 5.129340811002999878, 6.740051537885999977 ) ) ;
#37353=AXIS2_PLACEMENT_3D ( 'NONE', #26232, #64906, #15046 ) ;
#37358=CARTESIAN_POINT ( 'NONE',  ( 8.349704787027532049, 2.649832477958418586, -7.761626529551069353 ) ) ;
#37359=CARTESIAN_POINT ( 'NONE',  ( 9.447841622600000377, 5.447457912891000120, 7.431328695644999982 ) ) ;
#37361=ORIENTED_EDGE ( 'NONE', *, *, #39670, .T. ) ;
#37362=CARTESIAN_POINT ( 'NONE',  ( 9.517835841233001304, 4.883347899767999323, -6.417062834774999835 ) ) ;
#37365=CARTESIAN_POINT ( 'NONE',  ( 9.365090231804463983, 2.650133164351947013, -7.500005474590564880 ) ) ;
#37367=CARTESIAN_POINT ( 'NONE',  ( 10.63652412174386264, 4.781907488123494865, 4.773914205728686966 ) ) ;
#37374=CARTESIAN_POINT ( 'NONE',  ( 9.550320280412000429, 2.370176859044999862, -6.912649125838000508 ) ) ;
#37377=ORIENTED_EDGE ( 'NONE', *, *, #12810, .T. ) ;
#37378=CARTESIAN_POINT ( 'NONE',  ( 11.09425120759000016, 2.431871068503000277, 7.769513029648000391 ) ) ;
#37383=ORIENTED_EDGE ( 'NONE', *, *, #20347, .T. ) ;
#37398=CARTESIAN_POINT ( 'NONE',  ( 9.360279719594000625, 3.031907308384000022, -8.729608011560001657 ) ) ;
#37404=VERTEX_POINT ( 'NONE', #13133 ) ;
#37412=CARTESIAN_POINT ( 'NONE',  ( 10.47212119989999835, 2.640756834784999896, -8.505248851866998194 ) ) ;
#37413=CARTESIAN_POINT ( 'NONE',  ( 8.251334741087001490, 4.957169262993001091, 6.172567036706003485 ) ) ;
#37416=CARTESIAN_POINT ( 'NONE',  ( 9.074999999999999289, 4.417172942406000224, 8.783926296998000538 ) ) ;
#37418=CARTESIAN_POINT ( 'NONE',  ( 8.085170280410000743, 2.431401017850999935, 7.958393275880999873 ) ) ;
#37419=VERTEX_POINT ( 'NONE', #29212 ) ;
#37425=CARTESIAN_POINT ( 'NONE',  ( 10.95123291824999967, 9.911369087126999489, 5.636315692926999965 ) ) ;
#37440=CARTESIAN_POINT ( 'NONE',  ( 9.606444982449859893, 5.179832995385928562, -8.179900027810633745 ) ) ;
#37444=CARTESIAN_POINT ( 'NONE',  ( 8.432510841230001830, 5.430400319332999715, 7.210801214872999410 ) ) ;
#37446=CARTESIAN_POINT ( 'NONE',  ( 7.924470805432005882, 3.443171588504001068, -6.303962341916999890 ) ) ;
#37447=CARTESIAN_POINT ( 'NONE',  ( 10.07762665876999897, 2.169012810937000157, -7.244984731085000185 ) ) ;
#37453=CARTESIAN_POINT ( 'NONE',  ( 1.119519337369000000, -0.3298644081521999727, -3.242294882329999961 ) ) ;
#37456=CARTESIAN_POINT ( 'NONE',  ( 7.766851002543999627, 2.832432432432000269, 6.822293592207000934 ) ) ;
#37465=CARTESIAN_POINT ( 'NONE',  ( 8.023148997453999343, 5.167567567567999731, -6.822293592207000934 ) ) ;
#37469=EDGE_CURVE ( 'NONE', #9641, #67407, #11308, .T. ) ;
#37470=FACE_OUTER_BOUND ( 'NONE', #37052, .T. ) ;
#37474=DIRECTION ( 'NONE',  ( -0.7071042364840377514, 0.08614528851969455170, 0.7018422814366376272 ) ) ;
#37475=ADVANCED_FACE ( 'NONE', ( #25666 ), #41062, .F. ) ;
#37479=CARTESIAN_POINT ( 'NONE',  ( 8.465229719592999302, 2.567871051582000241, -6.869011921437000012 ) ) ;
#37485=ORIENTED_EDGE ( 'NONE', *, *, #44458, .T. ) ;
#37495=CARTESIAN_POINT ( 'NONE',  ( 9.120035841232999374, 5.288433695693000480, -8.041290150997999930 ) ) ;
#37500=CARTESIAN_POINT ( 'NONE',  ( 0.2212347920160371018, 2.507835299313069477, -2.070680120134882785 ) ) ;
#37509=ORIENTED_EDGE ( 'NONE', *, *, #60920, .F. ) ;
#37514=CARTESIAN_POINT ( 'NONE',  ( 9.743314158772999889, 5.149303692842000402, -5.987168472229000393 ) ) ;
#37517=ORIENTED_EDGE ( 'NONE', *, *, #24482, .T. ) ;
#37518=ORIENTED_EDGE ( 'NONE', *, *, #57825, .T. ) ;
#37519=CARTESIAN_POINT ( 'NONE',  ( 8.921135841230999119, 3.292387953886000140, -6.294868737226000377 ) ) ;
#37520=EDGE_CURVE ( 'NONE', #66492, #46708, #43016, .T. ) ;
#37521=CARTESIAN_POINT ( 'NONE',  ( 10.16000000000000014, 4.496968146123999865, -8.755198255949000696 ) ) ;
#37523=CYLINDRICAL_SURFACE ( 'NONE', #20145, 2.000000000000000000 ) ;
#37524=CARTESIAN_POINT ( 'NONE',  ( 0.1499942179680000265, 2.402872127494068533, -1.384928887584814028 ) ) ;
#37525=CARTESIAN_POINT ( 'NONE',  ( 11.09999999999999964, 5.299999999999999822, 6.469505845987999493 ) ) ;
#37528=CARTESIAN_POINT ( 'NONE',  ( 8.344265712141698543, 4.916725855472337869, -6.188913847335090423 ) ) ;
#37530=B_SPLINE_CURVE_WITH_KNOTS ( 'NONE', 3,
 ( #15240, #49036, #63115, #32958 ),
 .UNSPECIFIED., .F., .F.,
 ( 4, 4 ),
 ( 0.000000000000000000, 1.000000000000000000 ),
 .UNSPECIFIED. ) ;
#37541=CARTESIAN_POINT ( 'NONE',  ( 7.000000000000000000, 8.307879248642999315, -4.307879248643000203 ) ) ;
#37542=CARTESIAN_POINT ( 'NONE',  ( 0.1499942179680000542, -2.199046806507067853, -1.689975037551103121 ) ) ;
#37548=CARTESIAN_POINT ( 'NONE',  ( 10.19837725606034162, 4.679950664087191292, -8.679651447172831880 ) ) ;
#37549=ORIENTED_EDGE ( 'NONE', *, *, #65257, .F. ) ;
#37551=EDGE_CURVE ( 'NONE', #23998, #34256, #6356, .T. ) ;
#37559=ORIENTED_EDGE ( 'NONE', *, *, #6394, .F. ) ;
#37565=CARTESIAN_POINT ( 'NONE',  ( 9.120514158775000269, 5.306366356490000769, -7.996450761531000317 ) ) ;
#37568=CARTESIAN_POINT ( 'NONE',  ( 6.967235841227999771, 4.499022151374000522, -9.333214642871000777 ) ) ;
#37570=CARTESIAN_POINT ( 'NONE',  ( 7.881896300820000256, 5.128252728555000139, 6.737017011364999419 ) ) ;
#37583=EDGE_CURVE ( 'NONE', #56175, #25126, #43894, .T. ) ;
#37593=ORIENTED_EDGE ( 'NONE', *, *, #24191, .F. ) ;
#37594=CARTESIAN_POINT ( 'NONE',  ( 10.39106065309000115, 4.025321035224999733, 9.261125884460000179 ) ) ;
#37595=CARTESIAN_POINT ( 'NONE',  ( 10.72128915877000033, 4.673511966357999370, -5.778393480304000462 ) ) ;
#37610=CARTESIAN_POINT ( 'NONE',  ( 10.59344747867000081, 5.297752619853000944, 8.474195539311001113 ) ) ;
#37620=CARTESIAN_POINT ( 'NONE',  ( 9.269689158774999882, 3.135494838036999798, -8.598037907310999373 ) ) ;
#37624=AXIS2_PLACEMENT_3D ( 'NONE', #55325, #17927, #44845 ) ;
#37628=CARTESIAN_POINT ( 'NONE',  ( 11.14451084122999980, 5.035416949823999566, -8.381520599479999944 ) ) ;
#37634=AXIS2_PLACEMENT_3D ( 'NONE', #62530, #14649, #45778 ) ;
#37635=CARTESIAN_POINT ( 'NONE',  ( 7.795982780410000146, 3.164805384346000228, 9.104735843897000080 ) ) ;
#37638=EDGE_CURVE ( 'NONE', #26116, #19641, #30515, .T. ) ;
#37640=B_SPLINE_CURVE_WITH_KNOTS ( 'NONE', 3,
 ( #59464, #26637, #47954, #32905 ),
 .UNSPECIFIED., .F., .F.,
 ( 4, 4 ),
 ( 0.000000000000000000, 1.000000000000000000 ),
 .UNSPECIFIED. ) ;
#37641=CARTESIAN_POINT ( 'NONE',  ( 7.060779719589000081, 3.391196421714000042, -9.121921547671998809 ) ) ;
#37643=AXIS2_PLACEMENT_3D ( 'NONE', #46499, #67803, #41248 ) ;
#37650=FACE_OUTER_BOUND ( 'NONE', #59053, .T. ) ;
#37655=CARTESIAN_POINT ( 'NONE',  ( 10.63263472587000180, 7.502444384430999591, 6.008454772957000145 ) ) ;
#37661=CARTESIAN_POINT ( 'NONE',  ( 9.272295280408998863, 3.705846972803000128, 9.096435887808000942 ) ) ;
#37663=ADVANCED_FACE ( 'NONE', ( #17242 ), #1165, .T. ) ;
#37664=CARTESIAN_POINT ( 'NONE',  ( 9.129428851719998406, 5.099284414202999827, 6.151604790022999758 ) ) ;
#37666=CARTESIAN_POINT ( 'NONE',  ( 10.96506373917000055, 5.561809752472999691, -4.905726767165999647 ) ) ;
#37667=EDGE_LOOP ( 'NONE', ( #41837, #35820, #19610, #9695 ) ) ;
#37670=DIRECTION ( 'NONE',  ( 0.5000000000000169864, 0.000000000000000000, -0.8660254037844288266 ) ) ;
#37671=PLANE ( 'NONE',  #53873 ) ;
#37672=DIRECTION ( 'NONE',  ( -1.000000000000000000, 0.000000000000000000, -1.776356839426000147E-14 ) ) ;
#37674=B_SPLINE_CURVE_WITH_KNOTS ( 'NONE', 3,
 ( #66263, #28180, #34123, #23966 ),
 .UNSPECIFIED., .F., .F.,
 ( 4, 4 ),
 ( 0.000000000000000000, 1.000000000000000000 ),
 .UNSPECIFIED. ) ;
#37680=ORIENTED_EDGE ( 'NONE', *, *, #36951, .T. ) ;
#37684=CARTESIAN_POINT ( 'NONE',  ( 10.43284001513000092, 3.279325423736999756, -9.029279369994000604 ) ) ;
#37688=CARTESIAN_POINT ( 'NONE',  ( 7.859795284898003942, 2.854589328742001886, -6.788356039251000063 ) ) ;
#37689=CARTESIAN_POINT ( 'NONE',  ( 10.50285691784999997, 5.158890929072000198, 8.369954994793999958 ) ) ;
#37693=CARTESIAN_POINT ( 'NONE',  ( 9.566963020987998334, 5.215925787220999865, 6.177726425586999248 ) ) ;
#37698=CARTESIAN_POINT ( 'NONE',  ( 11.12958489392000061, 8.838800255109999782, -6.730293042198999487 ) ) ;
#37703=CARTESIAN_POINT ( 'NONE',  ( 10.15000066238999921, -1.190159082397999942E-13, -1.213918169242000045E-13 ) ) ;
#37706=EDGE_LOOP ( 'NONE', ( #35100, #22672, #31124, #25467 ) ) ;
#37707=DIRECTION ( 'NONE',  ( -0.7071063750894808209, 0.7071071872833809557, -1.205032604263965641E-09 ) ) ;
#37714=CARTESIAN_POINT ( 'NONE',  ( 9.362885841227999606, 3.677414437776999723, 9.250745771096999803 ) ) ;
#37715=CARTESIAN_POINT ( 'NONE',  ( 9.699495280410998177, 5.048004622677000341, -6.120508709481000231 ) ) ;
#37717=CARTESIAN_POINT ( 'NONE',  ( 10.63445696039368116, 3.217964742311511195, 4.772905834338354580 ) ) ;
#37719=CARTESIAN_POINT ( 'NONE',  ( 10.98286939055999945, 3.998514186275999638, 9.091062412789998604 ) ) ;
#37733=CARTESIAN_POINT ( 'NONE',  ( 1.547746615352999955, -3.258362327980000028, 0.06604197684371000687 ) ) ;
#37734=ORIENTED_EDGE ( 'NONE', *, *, #49582, .F. ) ;
#37739=ORIENTED_EDGE ( 'NONE', *, *, #66088, .T. ) ;
#37740=CARTESIAN_POINT ( 'NONE',  ( 8.912754719595000097, 2.481540185810000132, -7.878707153279001396 ) ) ;
#37743=ORIENTED_EDGE ( 'NONE', *, *, #41271, .T. ) ;
#37744=CARTESIAN_POINT ( 'NONE',  ( 7.947155777501817120, 4.876130771725635249, -6.371895583161996335 ) ) ;
#37746=VERTEX_POINT ( 'NONE', #40630 ) ;
#37753=CARTESIAN_POINT ( 'NONE',  ( 10.19255830160000009, 2.560287027313000063, 7.664549200117999561 ) ) ;
#37754=CARTESIAN_POINT ( 'NONE',  ( 10.32702465212000043, 5.663794543395000325, -6.682030833630000721 ) ) ;
#37761=CARTESIAN_POINT ( 'NONE',  ( 9.395323341230000125, 5.146726419831999522, 6.597424767138000412 ) ) ;
#37765=CARTESIAN_POINT ( 'NONE',  ( 9.254613120524085801, 2.734600818827677582, 7.018933991638915515 ) ) ;
#37769=CARTESIAN_POINT ( 'NONE',  ( 11.12373268272000004, 6.329904650298000313, 5.418930548134000880 ) ) ;
#37782=ADVANCED_FACE ( 'NONE', ( #3905 ), #41666, .F. ) ;
#37784=CARTESIAN_POINT ( 'NONE',  ( 0.1538438179258999894, 2.601420761213999899, -2.147952162500999851 ) ) ;
#37785=CARTESIAN_POINT ( 'NONE',  ( 9.679376605108515719, 4.176514373757539644, -8.850130121363157798 ) ) ;
#37790=CARTESIAN_POINT ( 'NONE',  ( 8.339994183033994091, 2.871570486036998382, -6.342248726812004911 ) ) ;
#37791=CARTESIAN_POINT ( 'NONE',  ( 10.08211611373999972, 4.728047954991999369, -8.793974144431000894 ) ) ;
#37793=CARTESIAN_POINT ( 'NONE',  ( 9.777068864297932649, 2.899999999999999911, -6.444141223371950389 ) ) ;
#37795=FACE_OUTER_BOUND ( 'NONE', #25911, .T. ) ;
#37802=B_SPLINE_CURVE_WITH_KNOTS ( 'NONE', 3,
 ( #14182, #57161, #46687, #14863, #20447, #19766, #41774, #51915, #56483, #3336, #36530, #51574, #67991, #45990, #25694, #14529, #41091, #47372 ),
 .UNSPECIFIED., .F., .F.,
 ( 4, 2, 2, 2, 2, 2, 2, 2, 4 ),
 ( 0.000000000000000000, 0.1250000000000000278, 0.2500000000000000000, 0.3749999999999999445, 0.4999999999999999445, 0.6249999999999998890, 0.7499999999999998890, 0.8750000000000000000, 1.000000000000000000 ),
 .UNSPECIFIED. ) ;
#37806=LINE ( 'NONE', #59127, #67871 ) ;
#37811=DIRECTION ( 'NONE',  ( 1.000000000000000000, 0.000000000000000000, 0.000000000000000000 ) ) ;
#37813=EDGE_CURVE ( 'NONE', #14861, #28055, #33957, .T. ) ;
#37817=FACE_OUTER_BOUND ( 'NONE', #3327, .T. ) ;
#37824=CARTESIAN_POINT ( 'NONE',  ( 9.541460841232000334, 2.824732249080000202, -8.992748220058999209 ) ) ;
#37843=ORIENTED_EDGE ( 'NONE', *, *, #52477, .T. ) ;
#37844=CARTESIAN_POINT ( 'NONE',  ( 10.28774346735000123, 5.077605961126000267, -5.991341245382999503 ) ) ;
#37845=SURFACE_SIDE_STYLE ('',( #42750 ) ) ;
#37856=CARTESIAN_POINT ( 'NONE',  ( 7.137771682458000200, 5.278582711742999756, -7.933273873238999130 ) ) ;
#37861=CARTESIAN_POINT ( 'NONE',  ( 9.892489158770999325, 5.099602161831000124, -9.049221499261999924 ) ) ;
#37866=ORIENTED_EDGE ( 'NONE', *, *, #62391, .T. ) ;
#37880=ORIENTED_EDGE ( 'NONE', *, *, #37813, .F. ) ;
#37888=EDGE_CURVE ( 'NONE', #30450, #58602, #54567, .T. ) ;
#37898=CARTESIAN_POINT ( 'NONE',  ( 1.030140132541691678, 3.408904368339106483, -0.9161175952574748260 ) ) ;
#37909=CARTESIAN_POINT ( 'NONE',  ( 9.099999886593998610, 3.268496584495999908E-13, 3.613587358477999789E-14 ) ) ;
#37914=CARTESIAN_POINT ( 'NONE',  ( 9.717214158771000143, 3.990126737362999609, -8.809457313313998839 ) ) ;
#37917=CARTESIAN_POINT ( 'NONE',  ( 7.523070280405000254, 2.267583043933999676, -7.494013172964999470 ) ) ;
#37920=CARTESIAN_POINT ( 'NONE',  ( 9.453817378629960189, 5.259207081053330235, 7.986245092988616179 ) ) ;
#37925=ORIENTED_EDGE ( 'NONE', *, *, #24475, .T. ) ;
#37934=CARTESIAN_POINT ( 'NONE',  ( 7.100000000000000533, 5.221516520829000640, -8.074802043613001246 ) ) ;
#37938=ORIENTED_EDGE ( 'NONE', *, *, #41348, .T. ) ;
#37939=CARTESIAN_POINT ( 'NONE',  ( 9.910633732652998518, 2.107262079134000210, 7.885285091859000062 ) ) ;
#37940=CARTESIAN_POINT ( 'NONE',  ( 10.19121415877000203, 3.990707652596999555, -5.651362387566000400 ) ) ;
#37957=VECTOR ( 'NONE', #46444, 1000.000000000000000 ) ;
#37966=VERTEX_POINT ( 'NONE', #40896 ) ;
#37968=CARTESIAN_POINT ( 'NONE',  ( 8.573539158775000502, 5.361622798585000460, -7.185294144754000634 ) ) ;
#37971=CARTESIAN_POINT ( 'NONE',  ( 10.98768472569999943, 5.449702578894000560, 4.945212061318999375 ) ) ;
#37972=CARTESIAN_POINT ( 'NONE',  ( 0.3460379451994000100, -2.198759671591000053, -2.775001775783000113 ) ) ;
#37974=CARTESIAN_POINT ( 'NONE',  ( 2.313974293799999860, -3.372637136287000015, -1.659426359180999899 ) ) ;
#37976=DIRECTION ( 'NONE',  ( 0.000000000000000000, -0.7158784314710767704, 0.6982249432342778617 ) ) ;
#37977=CARTESIAN_POINT ( 'NONE',  ( 8.150000662387999029, 3.037570195374000164E-13, -3.945735770681999509E-14 ) ) ;
#37980=CARTESIAN_POINT ( 'NONE',  ( 7.577017219590000074, 5.480308727866000318, 8.192324747680999053 ) ) ;
#37983=CARTESIAN_POINT ( 'NONE',  ( 7.756929719584999994, 3.458959908335999867, -5.854223596299999777 ) ) ;
#37987=CARTESIAN_POINT ( 'NONE',  ( 10.98768472567999943, 5.449702577258999980, -4.945212061305999107 ) ) ;
#37992=CARTESIAN_POINT ( 'NONE',  ( 8.312776266199000119, 10.52971825582000065, -4.244445611735000234 ) ) ;
#37996=CARTESIAN_POINT ( 'NONE',  ( 8.298515680831000552, 8.052744916463998592, 4.948539300261999507 ) ) ;
#38001=VERTEX_POINT ( 'NONE', #9076 ) ;
#38002=CARTESIAN_POINT ( 'NONE',  ( 8.604017219593000476, 5.165497731316000873, 8.645531386060000045 ) ) ;
#38003=ORIENTED_EDGE ( 'NONE', *, *, #41840, .F. ) ;
#38004=VECTOR ( 'NONE', #7364, 1000.000000000000114 ) ;
#38005=CARTESIAN_POINT ( 'NONE',  ( 8.630000000000000782, 4.924138593003999809, -8.484107647018999998 ) ) ;
#38007=FACE_OUTER_BOUND ( 'NONE', #39759, .T. ) ;
#38008=EDGE_LOOP ( 'NONE', ( #20048, #37549, #35112, #41736, #935, #56849, #25626, #66963 ) ) ;
#38022=CARTESIAN_POINT ( 'NONE',  ( 9.544414158773999901, 2.173570076733999823, -8.023168429484000441 ) ) ;
#38023=CARTESIAN_POINT ( 'NONE',  ( 10.31499646082999888, 5.458376174241999834, -8.355105941236999456 ) ) ;
#38028=VERTEX_POINT ( 'NONE', #18548 ) ;
#38031=CARTESIAN_POINT ( 'NONE',  ( 11.25041981190000051, 5.730782764036999488, 8.122675980938000251 ) ) ;
#38039=CARTESIAN_POINT ( 'NONE',  ( 10.18658456763778375, 5.723604601771135059, 7.204491886445339333 ) ) ;
#38045=CARTESIAN_POINT ( 'NONE',  ( 8.771960841230001193, 3.061731693614000438, -8.535706278603999664 ) ) ;
#38054=CARTESIAN_POINT ( 'NONE',  ( 7.149100552923999707, 4.351669901925999895, 8.977196921526999773 ) ) ;
#38055=CARTESIAN_POINT ( 'NONE',  ( 9.450870280412999591, 2.928319778732999978, -8.861178115809998701 ) ) ;
#38057=CARTESIAN_POINT ( 'NONE',  ( 2.352367082289130717, 1.876785584549146568, 2.663032597268895518 ) ) ;
#38059=CARTESIAN_POINT ( 'NONE',  ( 10.37026939687000038, 5.571553923009999743, 7.748385725654999945 ) ) ;
#38063=CARTESIAN_POINT ( 'NONE',  ( 7.895830451470996714, 3.177662910779999628, 6.240430379278997464 ) ) ;
#38070=CARTESIAN_POINT ( 'NONE',  ( 8.472537864290000442, 2.899999999999999911, -6.571291218949999902 ) ) ;
#38074=CARTESIAN_POINT ( 'NONE',  ( 8.056015159639001055, 3.481518869265999072, 6.232552614174998951 ) ) ;
#38076=ORIENTED_EDGE ( 'NONE', *, *, #31487, .F. ) ;
#38077=CARTESIAN_POINT ( 'NONE',  ( 9.260829719593999698, 4.861259245430999520, -8.806664389576001284 ) ) ;
#38081=CARTESIAN_POINT ( 'NONE',  ( 7.959937255769798270, 5.013283352723129305, -6.497370493178895146 ) ) ;
#38093=CARTESIAN_POINT ( 'NONE',  ( 10.71983649979000042, 3.571741329336999726, -5.696148467328000287 ) ) ;
#38098=VECTOR ( 'NONE', #53846, 999.9999999999998863 ) ;
#38101=CARTESIAN_POINT ( 'NONE',  ( 9.176357780411999343, 2.935741164366000522, 6.259844213126999790 ) ) ;
#38106=LINE ( 'NONE', #32532, #38098 ) ;
#38108=CARTESIAN_POINT ( 'NONE',  ( 11.07071178722999960, 6.643972308597000165, 5.583263443185999542 ) ) ;
#38109=CARTESIAN_POINT ( 'NONE',  ( 11.12552327284000064, 8.121114117777999297, 6.768012205397000436 ) ) ;
#38112=EDGE_CURVE ( 'NONE', #9405, #46731, #61347, .T. ) ;
#38113=ORIENTED_EDGE ( 'NONE', *, *, #50157, .F. ) ;
#38117=CARTESIAN_POINT ( 'NONE',  ( 10.23809632363000155, 2.752447932331000047, 6.820051270595000048 ) ) ;
#38119=EDGE_CURVE ( 'NONE', #12504, #42732, #51311, .T. ) ;
#38122=CARTESIAN_POINT ( 'NONE',  ( 9.138573341230998182, 2.933833973450999721, 8.496479443567000800 ) ) ;
#38123=CARTESIAN_POINT ( 'NONE',  ( 9.629022744239000176, 5.794335169544999609, 7.414871903737999759 ) ) ;
#38125=CARTESIAN_POINT ( 'NONE',  ( 9.934999999999998721, 4.640430492595999823, -9.117542781427999898 ) ) ;
#38128=CARTESIAN_POINT ( 'NONE',  ( 10.33453278041000090, 3.295703187163999459, -6.149878749787999865 ) ) ;
#38129=CARTESIAN_POINT ( 'NONE',  ( 9.587263606520032511, 3.377808641629922892, 8.716806737539613437 ) ) ;
#38130=CARTESIAN_POINT ( 'NONE',  ( 7.969753415490000492, 5.131577060784002775, 6.757500301899002970 ) ) ;
#38139=AXIS2_PLACEMENT_3D ( 'NONE', #46855, #36013, #57329 ) ;
#38150=CARTESIAN_POINT ( 'NONE',  ( 10.23809632363000155, 2.752447932331000047, 6.820051270595000048 ) ) ;
#38160=CARTESIAN_POINT ( 'NONE',  ( 7.416780799524962831, 2.408868269339266455, 8.205667337080191359 ) ) ;
#38165=ORIENTED_EDGE ( 'NONE', *, *, #52309, .T. ) ;
#38178=CARTESIAN_POINT ( 'NONE',  ( 9.667010841233000917, 4.769103072373000352, -8.666849124598000387 ) ) ;
#38180=CARTESIAN_POINT ( 'NONE',  ( 0.3857633700769134144, 0.6253109423643958831, 3.191549458069821821 ) ) ;
#38182=( NAMED_UNIT ( * ) PLANE_ANGLE_UNIT ( ) SI_UNIT ( $, .RADIAN. ) );
#38195=CARTESIAN_POINT ( 'NONE',  ( 10.93769855012999948, 2.936883479403999964, 4.920828759365000415 ) ) ;
#38202=CARTESIAN_POINT ( 'NONE',  ( 8.458179719589999479, 5.332332124071999857, -8.487089944253000340 ) ) ;
#38203=CARTESIAN_POINT ( 'NONE',  ( 10.52314899745999988, 5.167567567567999731, -6.822293592207000934 ) ) ;
#38216=CARTESIAN_POINT ( 'NONE',  ( 8.336034600740228839, 4.707624567763986079, -6.071688517621553594 ) ) ;
#38217=CARTESIAN_POINT ( 'NONE',  ( 10.91080643070814205, 2.803404389955949760, -6.850777194058569997 ) ) ;
#38224=CARTESIAN_POINT ( 'NONE',  ( 11.09999999999999964, 5.556627878592999004, -5.124965741051999757 ) ) ;
#38230=AXIS2_PLACEMENT_3D ( 'NONE', #6678, #65048, #1443 ) ;
#38248=VECTOR ( 'NONE', #66189, 999.9999999999998863 ) ;
#38253=CARTESIAN_POINT ( 'NONE',  ( 11.09999868801999945, 0.5000013103249000279, -9.776630274038000223 ) ) ;
#38257=CARTESIAN_POINT ( 'NONE',  ( 0.000000000000000000, 2.899969545325999931, -0.3811992978302039536 ) ) ;
#38260=CARTESIAN_POINT ( 'NONE',  ( 8.061185841224999038, 2.494419548310999879, -8.658783402411998509 ) ) ;
#38262=EDGE_CURVE ( 'NONE', #5496, #68419, #16265, .T. ) ;
#38263=CARTESIAN_POINT ( 'NONE',  ( 9.525000000000000355, 4.417172942406000224, 8.783926296998000538 ) ) ;
#38264=ORIENTED_EDGE ( 'NONE', *, *, #66773, .T. ) ;
#38277=CARTESIAN_POINT ( 'NONE',  ( 9.393077698596744796, 2.713274643879884263, -7.026852155855150883 ) ) ;
#38281=ORIENTED_EDGE ( 'NONE', *, *, #31262, .T. ) ;
#38282=DIRECTION ( 'NONE',  ( 1.000000000000000000, 0.000000000000000000, 0.000000000000000000 ) ) ;
#38290=DIRECTION ( 'NONE',  ( 0.000000000000000000, 1.000000000000000000, 0.000000000000000000 ) ) ;
#38293=CARTESIAN_POINT ( 'NONE',  ( 10.07770645819999977, 4.622041375574999833, 5.671348593713000596 ) ) ;
#38299=DIRECTION ( 'NONE',  ( -1.000000000000000000, 0.000000000000000000, 0.000000000000000000 ) ) ;
#38301=CARTESIAN_POINT ( 'NONE',  ( 9.716851002543000604, 2.832432432432000269, 6.822293592207000934 ) ) ;
#38306=CARTESIAN_POINT ( 'NONE',  ( 8.457129882803000598, 5.100036551512999949, -6.571411952062999440 ) ) ;
#38308=CARTESIAN_POINT ( 'NONE',  ( 6.999999691988000095, -12.36734761319999798, -2.759114534468000368 ) ) ;
#38309=EDGE_CURVE ( 'NONE', #38790, #38001, #23831, .T. ) ;
#38313=CARTESIAN_POINT ( 'NONE',  ( 8.275189158773001097, 3.061731693614000438, -8.535706278603999664 ) ) ;
#38314=CARTESIAN_POINT ( 'NONE',  ( 11.09999965054999826, -2.398081733189999864E-14, -12.24999851416000141 ) ) ;
#38316=CARTESIAN_POINT ( 'NONE',  ( 0.5761782687131999925, -3.296907118028000294, 0.7152224222591000435 ) ) ;
#38318=CARTESIAN_POINT ( 'NONE',  ( 11.18237334122999904, 4.516636732814999888, -8.757876389238999693 ) ) ;
#38321=CARTESIAN_POINT ( 'NONE',  ( 8.999999001754000361, 0.000000000000000000, 0.000000000000000000 ) ) ;
#38324=CARTESIAN_POINT ( 'NONE',  ( 7.448642219589999947, 4.628941086829000184, 5.991667691044999522 ) ) ;
#38325=ORIENTED_EDGE ( 'NONE', *, *, #10392, .F. ) ;
#38327=B_SPLINE_CURVE_WITH_KNOTS ( 'NONE', 3,
 ( #61630, #13746, #66871, #35416 ),
 .UNSPECIFIED., .F., .F.,
 ( 4, 4 ),
 ( 0.000000000000000000, 1.000000000000000000 ),
 .UNSPECIFIED. ) ;
#38328=CIRCLE ( 'NONE', #8199, 2.000000000000000888 ) ;
#38329=CARTESIAN_POINT ( 'NONE',  ( 7.996695280407001505, 5.564823112884000444, -7.478368060284999785 ) ) ;
#38331=CARTESIAN_POINT ( 'NONE',  ( 10.52323372634000087, 3.325642821414999784, 5.689987891230000372 ) ) ;
#38333=ORIENTED_EDGE ( 'NONE', *, *, #7398, .F. ) ;
#38340=ORIENTED_EDGE ( 'NONE', *, *, #29066, .T. ) ;
#38344=CARTESIAN_POINT ( 'NONE',  ( 8.200000998245998929, 0.000000000000000000, 0.000000000000000000 ) ) ;
#38346=EDGE_CURVE ( 'NONE', #7896, #27999, #57122, .T. ) ;
#38348=ORIENTED_EDGE ( 'NONE', *, *, #9080, .T. ) ;
#38349=CARTESIAN_POINT ( 'NONE',  ( 8.705989158774000813, 2.542862824481000317, 7.419808961972999661 ) ) ;
#38350=EDGE_CURVE ( 'NONE', #53307, #14947, #65414, .T. ) ;
#38352=VERTEX_POINT ( 'NONE', #33774 ) ;
#38356=CARTESIAN_POINT ( 'NONE',  ( 11.07074946250000025, 5.433303208544999485, -5.078292924949999509 ) ) ;
#38357=VERTEX_POINT ( 'NONE', #56119 ) ;
#38361=CARTESIAN_POINT ( 'NONE',  ( 7.441372165042849041, 4.549423936828223880, -9.274025057497155444 ) ) ;
#38365=DIRECTION ( 'NONE',  ( 0.8660254037844288266, 0.000000000000000000, -0.5000000000000169864 ) ) ;
#38367=ORIENTED_EDGE ( 'NONE', *, *, #35845, .F. ) ;
#38372=CARTESIAN_POINT ( 'NONE',  ( 9.883629719592001095, 5.656948148960999845, -6.994239053114000626 ) ) ;
#38373=CARTESIAN_POINT ( 'NONE',  ( 10.68055531501999944, 2.768167480619000198, -6.114404645958000373 ) ) ;
#38380=CARTESIAN_POINT ( 'NONE',  ( 10.40227026081000083, 2.765684886876999649, 9.035354958280999327 ) ) ;
#38382=CARTESIAN_POINT ( 'NONE',  ( 2.123890132542666453, 2.150913519912194261, 2.798833948393636195 ) ) ;
#38387=CARTESIAN_POINT ( 'NONE',  ( 7.100000000000070699, 4.845481125806140099, -8.600290376098520539 ) ) ;
#38393=CARTESIAN_POINT ( 'NONE',  ( 8.622785841227999626, 5.189036231907000030, -8.048606212067999977 ) ) ;
#38401=CARTESIAN_POINT ( 'NONE',  ( 8.181107780410998842, 5.485785046334999748, 8.532070739720001740 ) ) ;
#38403=CARTESIAN_POINT ( 'NONE',  ( 9.898395280408998076, 3.987760651117999711, -9.123263301387000368 ) ) ;
#38407=CARTESIAN_POINT ( 'NONE',  ( 10.11260611051000069, 3.359887741436999864, 5.859127722154000573 ) ) ;
#38411=CARTESIAN_POINT ( 'NONE',  ( 8.434803823919004628, 2.901237182992001173, 6.624660446101000133 ) ) ;
#38413=VERTEX_POINT ( 'NONE', #38895 ) ;
#38420=ORIENTED_EDGE ( 'NONE', *, *, #23940, .T. ) ;
#38421=CARTESIAN_POINT ( 'NONE',  ( 6.949999692291999764, -2.604139126561000230E-12, 1.310063169058000104E-14 ) ) ;
#38423=CARTESIAN_POINT ( 'NONE',  ( 8.160036350658002036, 2.891230335795000883, 6.361714733157999291 ) ) ;
#38427=CARTESIAN_POINT ( 'NONE',  ( 8.672989158774999652, 4.728328492779000136, -8.692725459657999920 ) ) ;
#38430=EDGE_CURVE ( 'NONE', #30974, #66075, #411, .T. ) ;
#38434=CARTESIAN_POINT ( 'NONE',  ( 9.106448366594660726, 5.179987832526970593, -8.180032552820186709 ) ) ;
#38435=AXIS2_PLACEMENT_3D ( 'NONE', #57556, #20503, #62459 ) ;
#38444=CARTESIAN_POINT ( 'NONE',  ( 11.04497253829999970, 2.754551879881000254, -5.177000083688999332 ) ) ;
#38451=CARTESIAN_POINT ( 'NONE',  ( 8.417489158772999858, 2.029098103856999735, 7.726995416028000108 ) ) ;
#38457=LINE ( 'NONE', #65363, #47250 ) ;
#38459=ADVANCED_FACE ( 'NONE', ( #40234 ), #45818, .T. ) ;
#38463=CARTESIAN_POINT ( 'NONE',  ( 11.07076162495999938, 7.299628065904999019, 6.238550388720000228 ) ) ;
#38466=DIRECTION ( 'NONE',  ( -1.000000000000000000, 0.000000000000000000, 0.000000000000000000 ) ) ;
#38471=CARTESIAN_POINT ( 'NONE',  ( 8.322761924339483031, 2.900588934367011706, -6.581379904120886692 ) ) ;
#38474=CARTESIAN_POINT ( 'NONE',  ( 8.817635841231000526, 3.894644548817000285, 6.044465307984999924 ) ) ;
#38475=CARTESIAN_POINT ( 'NONE',  ( 9.215291255903000689, 4.861981595026999337, 8.938817176893000038 ) ) ;
#38478=DIRECTION ( 'NONE',  ( -1.000000000000000000, 0.000000000000000000, -9.258974054407000394E-14 ) ) ;
#38482=CARTESIAN_POINT ( 'NONE',  ( 8.086080172061008042, 4.921420473137001927, 6.235316328396007357 ) ) ;
#38485=CARTESIAN_POINT ( 'NONE',  ( 10.97499895057999986, -2.398081733189999864E-14, 0.000000000000000000 ) ) ;
#38486=ORIENTED_EDGE ( 'NONE', *, *, #62610, .T. ) ;
#38488=CARTESIAN_POINT ( 'NONE',  ( 2.200310191360999923, 2.483819732826999971, -1.905290611529000033 ) ) ;
#38493=CARTESIAN_POINT ( 'NONE',  ( 7.975339216757242333, 5.350090185752605976, 7.499980949462685231 ) ) ;
#38496=ORIENTED_EDGE ( 'NONE', *, *, #66910, .F. ) ;
#38503=PLANE ( 'NONE',  #19835 ) ;
#38510=CARTESIAN_POINT ( 'NONE',  ( 0.4687253537224814193, 1.074401066710667818, -3.341895325573862596 ) ) ;
#38513=B_SPLINE_CURVE_WITH_KNOTS ( 'NONE', 3,
 ( #35919, #61800, #46414, #34899, #67038, #4433, #30010, #25081, #56558, #8664, #3408, #19149, #62478, #19499, #25425, #52339, #4089, #62817 ),
 .UNSPECIFIED., .F., .F.,
 ( 4, 2, 2, 2, 2, 2, 2, 2, 4 ),
 ( 0.000000000000000000, 0.1250000000000000000, 0.2500000000000000000, 0.3750000000000000000, 0.5000000000000000000, 0.6250000000000000000, 0.7500000000000000000, 0.8750000000000000000, 1.000000000000000000 ),
 .UNSPECIFIED. ) ;
#38516=CARTESIAN_POINT ( 'NONE',  ( 9.044210841233001119, 2.773858540272000184, -8.951250717848999727 ) ) ;
#38517=ORIENTED_EDGE ( 'NONE', *, *, #1914, .F. ) ;
#38520=VERTEX_POINT ( 'NONE', #2817 ) ;
#38531=ORIENTED_EDGE ( 'NONE', *, *, #33626, .T. ) ;
#38532=CARTESIAN_POINT ( 'NONE',  ( 9.020585841232000135, 4.920236664407999783, -6.448229650796999834 ) ) ;
#38534=CARTESIAN_POINT ( 'NONE',  ( 9.856851002545999663, 2.832432432432000269, -6.822293592207000934 ) ) ;
#38536=CARTESIAN_POINT ( 'NONE',  ( 10.93769906941999892, 2.936877991120999898, -4.920829195977000303 ) ) ;
#38547=CARTESIAN_POINT ( 'NONE',  ( 10.97867121346000019, 2.873849435084999904, 4.940815226079000588 ) ) ;
#38548=CARTESIAN_POINT ( 'NONE',  ( 10.83325146359777591, 5.014643093291043741, -4.869878762730592392 ) ) ;
#38551=CARTESIAN_POINT ( 'NONE',  ( 9.924495280410999598, 4.946705552514000459, -6.253848946732999181 ) ) ;
#38560=CARTESIAN_POINT ( 'NONE',  ( 9.099999999999999645, 0.000000000000000000, 0.000000000000000000 ) ) ;
#38564=CARTESIAN_POINT ( 'NONE',  ( 0.000000000000000000, 0.000000000000000000, 0.000000000000000000 ) ) ;
#38566=EDGE_LOOP ( 'NONE', ( #60886, #53289, #59525, #51537 ) ) ;
#38579=LINE ( 'NONE', #59904, #7537 ) ;
#38581=B_SPLINE_SURFACE_WITH_KNOTS ( 'NONE', 3, 3, ( 
 ( #52464, #4564, #9462, #8451, #3534, #8791, #51437, #29796, #46197, #67508, #19627, #40948, #57026, #9126, #25208, #53156, #27626, #48602, #707, #58739, #21671, #14, #63973, #26597, #43009, #6279, #37082, #36742, #356, #5593, #37761, #53840, #10500, #59427, #41980 ),
 ( #15415, #20654, #59086, #10846, #21337, #10165, #42666, #32188, #54182, #31840, #32525, #37418, #68883, #52815, #64665, #5937, #48949, #27280, #53503, #16432, #31495, #16090, #26937, #58397, #4908, #43365, #26250, #16769, #38101, #5258, #47577, #21001, #48250, #64313, #22018 ),
 ( #63287, #47918, #42335, #63637, #58062, #32868, #15755, #11188, #11524, #7677, #1739, #61164, #55921, #33215, #23057, #2095, #34608, #12237, #8025, #54537, #55226, #39842, #29362, #1056, #6983, #13283, #22368, #11876, #44750, #29022, #50330, #23415, #12929, #33560, #27973 ),
 ( #22710, #60816, #66053, #54881, #65359, #43707, #23756, #28310, #65002, #2429, #45090, #39148, #18172, #49633, #44408, #65708, #39494, #17118, #17478, #38451, #49983, #7326, #34255, #55578, #59774, #38804, #66397, #18520, #6635, #60472, #49284, #1394, #44055, #28668, #60128 ) ),
 .UNSPECIFIED., .F., .F., .F.,
 ( 4, 4 ),
 ( 4, 1, 1, 1, 1, 1, 1, 1, 1, 1, 1, 1, 1, 1, 1, 1, 1, 1, 1, 1, 1, 1, 1, 1, 1, 1, 1, 1, 1, 1, 1, 1, 4 ),
 ( -0.1039370721279000015, 1.103937072127999963 ),
 ( -0.02000000000000000042, 0.01250000000000000069, 0.04499999999999999833, 0.07749999999999999944, 0.1100000000000000006, 0.1424999999999999878, 0.1749999999999999889, 0.2074999999999999900, 0.2399999999999999911, 0.2725000000000000200, 0.3049999999999999933, 0.3375000000000000222, 0.3699999999999999956, 0.4025000000000000244, 0.4349999999999999978, 0.4675000000000000266, 0.5000000000000000000, 0.5324999999999999734, 0.5649999999999999467, 0.5975000000000000311, 0.6300000000000000044, 0.6624999999999999778, 0.6949999999999999512, 0.7275000000000000355, 0.7600000000000000089, 0.7924999999999999822, 0.8249999999999999556, 0.8575000000000000400, 0.8900000000000000133, 0.9224999999999999867, 0.9549999999999999600, 0.9875000000000000444, 1.020000000000000018 ),
 .UNSPECIFIED. ) ;
#38584=CARTESIAN_POINT ( 'NONE',  ( 9.472537864290000442, 2.899999999999999911, -6.571291218949999902 ) ) ;
#38587=CARTESIAN_POINT ( 'NONE',  ( 2.059804692936264114, 2.284309548437588600, -2.477449380090549269 ) ) ;
#38589=ORIENTED_EDGE ( 'NONE', *, *, #52748, .T. ) ;
#38595=CARTESIAN_POINT ( 'NONE',  ( 3.500000000000000000, -1.789730407083999886, 2.652709005895000249 ) ) ;
#38601=DIRECTION ( 'NONE',  ( 0.000000000000000000, -0.9478160162686030121, -0.3188178152248009600 ) ) ;
#38606=VECTOR ( 'NONE', #44049, 1000.000000000000000 ) ;
#38607=CARTESIAN_POINT ( 'NONE',  ( 8.275189158773001097, 3.061731693614000438, -8.535706278603999664 ) ) ;
#38611=CARTESIAN_POINT ( 'NONE',  ( 7.066685841226999720, 2.417988323708999854, -8.552044326954000297 ) ) ;
#38619=DIRECTION ( 'NONE',  ( 0.000000000000000000, -0.9565994702956990281, 0.2914059941558995726 ) ) ;
#38626=CARTESIAN_POINT ( 'NONE',  ( 8.025716582962996171, 5.094285164475001793, -6.419293649061996732 ) ) ;
#38627=DIRECTION ( 'NONE',  ( -1.000000000000000000, 0.000000000000000000, 0.000000000000000000 ) ) ;
#38633=CARTESIAN_POINT ( 'NONE',  ( 10.33453278041000090, 3.295703187163999459, -6.149878749787999865 ) ) ;
#38639=AXIS2_PLACEMENT_3D ( 'NONE', #46476, #35978, #39949 ) ;
#38641=ORIENTED_EDGE ( 'NONE', *, *, #32928, .F. ) ;
#38643=CARTESIAN_POINT ( 'NONE',  ( 8.450464158772000189, 3.789127741898000057, -9.388182174781999123 ) ) ;
#38647=FACE_OUTER_BOUND ( 'NONE', #59410, .T. ) ;
#38654=AXIS2_PLACEMENT_3D ( 'NONE', #66867, #25249, #40990 ) ;
#38658=ADVANCED_FACE ( 'NONE', ( #40914 ), #13382, .F. ) ;
#38663=ORIENTED_EDGE ( 'NONE', *, *, #40024, .F. ) ;
#38665=CARTESIAN_POINT ( 'NONE',  ( 3.458495577646333974, 3.039910566627586963, -1.793659031961971628 ) ) ;
#38666=CARTESIAN_POINT ( 'NONE',  ( 8.323770280408998801, 5.332332124071999857, -8.487089944253000340 ) ) ;
#38668=DIRECTION ( 'NONE',  ( -1.000000000000000000, 0.000000000000000000, 0.000000000000000000 ) ) ;
#38670=CARTESIAN_POINT ( 'NONE',  ( 0.6584425577435999433, -2.301202007355999779, -2.466905145517999998 ) ) ;
#38671=CARTESIAN_POINT ( 'NONE',  ( 9.502457028859783605, 2.587963025190172850, 6.404785931707032809 ) ) ;
#38672=CARTESIAN_POINT ( 'NONE',  ( 2.161381769351999882, 2.835781239812999566, -1.921535772062000103 ) ) ;
#38673=ORIENTED_EDGE ( 'NONE', *, *, #19311, .F. ) ;
#38674=B_SPLINE_CURVE_WITH_KNOTS ( 'NONE', 3,
 ( #60160, #37793, #32898, #27657 ),
 .UNSPECIFIED., .F., .F.,
 ( 4, 4 ),
 ( 0.000000000000000000, 1.000000000000000000 ),
 .UNSPECIFIED. ) ;
#38676=CARTESIAN_POINT ( 'NONE',  ( 6.916399741278000057, 12.19468928278000064, -3.104275424020000340 ) ) ;
#38679=CARTESIAN_POINT ( 'NONE',  ( 8.116920280410999666, 5.773189794777000117, 7.141495931231999883 ) ) ;
#38682=CARTESIAN_POINT ( 'NONE',  ( 7.350270280410000190, 3.562914451704999763, -5.997303864335000512 ) ) ;
#38684=CARTESIAN_POINT ( 'NONE',  ( 10.35616100078999935, 2.777276096020000029, 8.995275123087999702 ) ) ;
#38692=DIRECTION ( 'NONE',  ( 0.000000000000000000, -0.2461538461537955136, 0.9692307692307821076 ) ) ;
#38695=EDGE_LOOP ( 'NONE', ( #11346, #30135, #62065, #38853 ) ) ;
#38702=CARTESIAN_POINT ( 'NONE',  ( 8.064114158772998309, 4.228291488957999888, 8.941375734143997889 ) ) ;
#38712=CARTESIAN_POINT ( 'NONE',  ( 0.4529763571839853786, 3.676114825633475335E-06, -3.452897576335808072 ) ) ;
#38721=VERTEX_POINT ( 'NONE', #31128 ) ;
#38723=CARTESIAN_POINT ( 'NONE',  ( 9.336654719594999818, 5.095038542659000136, -6.157541456184000062 ) ) ;
#38724=CARTESIAN_POINT ( 'NONE',  ( 3.502409213219000339, -3.069775387992999871, 0.006882399294532000333 ) ) ;
#38727=CARTESIAN_POINT ( 'NONE',  ( 9.573148997458000409, 5.167567567567999731, -6.822293592207000934 ) ) ;
#38730=CARTESIAN_POINT ( 'NONE',  ( 1.885432296257667062, -1.713969392196469155, -3.070236115647939634 ) ) ;
#38731=CARTESIAN_POINT ( 'NONE',  ( 10.89874804681000064, 2.834828962328999502, 9.088465460431999432 ) ) ;
#38732=CARTESIAN_POINT ( 'NONE',  ( 2.228056799209332972, -2.150913519912213800, 2.798833948393621540 ) ) ;
#38736=CYLINDRICAL_SURFACE ( 'NONE', #49224, 0.4999999999999998335 ) ;
#38738=EDGE_CURVE ( 'NONE', #35994, #55227, #10315, .T. ) ;
#38754=CARTESIAN_POINT ( 'NONE',  ( 7.769579719591000355, 2.431401017850999935, 7.958393275880999873 ) ) ;
#38755=CARTESIAN_POINT ( 'NONE',  ( 9.541460841232000334, 2.824732249080000202, -8.992748220058999209 ) ) ;
#38757=CARTESIAN_POINT ( 'NONE',  ( 3.232623315315109824, 2.781099406263673579, -1.696921006577742030 ) ) ;
#38759=CARTESIAN_POINT ( 'NONE',  ( 10.16829701902000060, 4.567214950372999738, 5.832525041908999341 ) ) ;
#38764=CARTESIAN_POINT ( 'NONE',  ( 7.411012926802005296, 3.233242541571998085, 6.481873309613996881 ) ) ;
#38767=EDGE_CURVE ( 'NONE', #11746, #57153, #67021, .T. ) ;
#38774=VERTEX_POINT ( 'NONE', #46421 ) ;
#38778=CARTESIAN_POINT ( 'NONE',  ( 8.205377021103002377, 3.106081841748002059, 6.107037662485001128 ) ) ;
#38780=CARTESIAN_POINT ( 'NONE',  ( 9.012204719595001023, 3.161445734422999809, -6.178649910536000434 ) ) ;
#38784=CARTESIAN_POINT ( 'NONE',  ( 7.946914507420710372, 4.862230276086360270, -6.362913330584241578 ) ) ;
#38790=VERTEX_POINT ( 'NONE', #20877 ) ;
#38793=ADVANCED_FACE ( 'NONE', ( #19849 ), #40823, .F. ) ;
#38796=CARTESIAN_POINT ( 'NONE',  ( 10.13061872827999998, 2.189311095934999951, -7.101639631284999865 ) ) ;
#38804=CARTESIAN_POINT ( 'NONE',  ( 8.802614158774000330, 3.975069902178000270, 9.483774112875002160 ) ) ;
#38810=CARTESIAN_POINT ( 'NONE',  ( 10.81905590578999998, 2.899999999999999911, -6.571291218949999902 ) ) ;
#38811=CARTESIAN_POINT ( 'NONE',  ( 9.285195242305000818, 5.269680202247999823, 8.747831873285999649 ) ) ;
#38813=AXIS2_PLACEMENT_3D ( 'NONE', #62146, #13242, #3071 ) ;
#38822=ORIENTED_EDGE ( 'NONE', *, *, #41609, .F. ) ;
#38824=CARTESIAN_POINT ( 'NONE',  ( 8.689260841231000398, 2.550241116032999855, 7.666973618349000041 ) ) ;
#38825=CARTESIAN_POINT ( 'NONE',  ( 9.719613305057999142, 5.967773797872000685, 7.406643507784999692 ) ) ;
#38827=ORIENTED_EDGE ( 'NONE', *, *, #37275, .F. ) ;
#38828=CARTESIAN_POINT ( 'NONE',  ( 9.793039158772000263, 5.817107086401000160, -6.945352709928000579 ) ) ;
#38830=AXIS2_PLACEMENT_3D ( 'NONE', #2682, #45343, #67669 ) ;
#38833=CARTESIAN_POINT ( 'NONE',  ( 9.624831031535665105, 2.894183647070226240, 8.301356454186311851 ) ) ;
#38838=DIRECTION ( 'NONE',  ( 0.000000000000000000, 0.9565994702956989171, 0.2914059941558995170 ) ) ;
#38839=ORIENTED_EDGE ( 'NONE', *, *, #20347, .F. ) ;
#38840=VECTOR ( 'NONE', #39908, 1000.000000000000114 ) ;
#38842=CARTESIAN_POINT ( 'NONE',  ( 1.739384680100000136, 3.214278412021000175, -0.5382386926684999962 ) ) ;
#38843=LINE ( 'NONE', #53875, #50122 ) ;
#38850=CARTESIAN_POINT ( 'NONE',  ( 11.04796807867000119, 2.753385297824999967, 5.093099052209000277 ) ) ;
#38853=ORIENTED_EDGE ( 'NONE', *, *, #33227, .F. ) ;
#38854=CARTESIAN_POINT ( 'NONE',  ( 7.479583333330875661, 3.823285413235573582, -6.150000000000000355 ) ) ;
#38855=ADVANCED_FACE ( 'NONE', ( #57584 ), #17217, .T. ) ;
#38857=CARTESIAN_POINT ( 'NONE',  ( 9.814910518647794291, 2.650130971540564317, -7.499994893876710478 ) ) ;
#38860=CARTESIAN_POINT ( 'NONE',  ( 1.419020781218000016, 0.7707009544374999743, -3.678912518181000291 ) ) ;
#38861=CARTESIAN_POINT ( 'NONE',  ( 1.948890132539667031, 2.798833948393634863, -2.150913519912196925 ) ) ;
#38871=VERTEX_POINT ( 'NONE', #29593 ) ;
#38876=ORIENTED_EDGE ( 'NONE', *, *, #3466, .T. ) ;
#38880=CARTESIAN_POINT ( 'NONE',  ( 9.442843574488000158, 2.691255504502000129, 6.269523028052000235 ) ) ;
#38881=CARTESIAN_POINT ( 'NONE',  ( 8.508401286604998504, 5.100000004859538194, -6.571371713575075546 ) ) ;
#38884=EDGE_CURVE ( 'NONE', #15849, #15877, #23692, .T. ) ;
#38887=ORIENTED_EDGE ( 'NONE', *, *, #34333, .T. ) ;
#38889=ORIENTED_EDGE ( 'NONE', *, *, #59986, .F. ) ;
#38890=CYLINDRICAL_SURFACE ( 'NONE', #35915, 0.5000000000000002220 ) ;
#38891=B_SPLINE_CURVE_WITH_KNOTS ( 'NONE', 3,
 ( #25882, #41617, #26580, #31822, #68173 ),
 .UNSPECIFIED., .F., .F.,
 ( 4, 1, 4 ),
 ( 0.000000000000000000, 0.5000000000000000000, 1.000000000000000000 ),
 .UNSPECIFIED. ) ;
#38895=CARTESIAN_POINT ( 'NONE',  ( 0.1499942179679999987, 2.750000000000000000, 0.000000000000000000 ) ) ;
#38904=CARTESIAN_POINT ( 'NONE',  ( 7.254771682458000193, 3.668692617901999853, -8.939602259005999585 ) ) ;
#38908=CARTESIAN_POINT ( 'NONE',  ( 10.21398584123000042, 3.990126737362999609, -8.809457313313998839 ) ) ;
#38909=CYLINDRICAL_SURFACE ( 'NONE', #41393, 12.50000000000000000 ) ;
#38911=VECTOR ( 'NONE', #62602, 1000.000000000000114 ) ;
#38916=PLANE ( 'NONE',  #34690 ) ;
#38919=EDGE_CURVE ( 'NONE', #40232, #4735, #37802, .T. ) ;
#38931=CARTESIAN_POINT ( 'NONE',  ( 11.09999803709000155, -1.199999999999999956, 9.776630298829998011 ) ) ;
#38934=EDGE_CURVE ( 'NONE', #38871, #23293, #32001, .T. ) ;
#38936=CARTESIAN_POINT ( 'NONE',  ( 11.10000000009000054, 2.699999999911000259, 6.571291220400000022 ) ) ;
#38939=CARTESIAN_POINT ( 'NONE',  ( 6.999999999999999112, 9.785203231686947944, -4.607313921344089458 ) ) ;
#38947=CIRCLE ( 'NONE', #12147, 11.84999999999999964 ) ;
#38948=DIRECTION ( 'NONE',  ( 1.000000000000000000, 0.000000000000000000, 0.000000000000000000 ) ) ;
#38951=LINE ( 'NONE', #23203, #53372 ) ;
#38955=CARTESIAN_POINT ( 'NONE',  ( 4.900006121741999010, 2.000000000000000000, 0.000000000000000000 ) ) ;
#38956=CARTESIAN_POINT ( 'NONE',  ( 6.999999999999999112, 9.047814540315521015, 4.692211904642501707 ) ) ;
#38964=CARTESIAN_POINT ( 'NONE',  ( 9.269689158774999882, 3.135494838036999798, -8.598037907310999373 ) ) ;
#38969=ORIENTED_EDGE ( 'NONE', *, *, #22077, .F. ) ;
#38970=CARTESIAN_POINT ( 'NONE',  ( 8.343110571751518378, 3.605921234441439971, -6.059113279906364724 ) ) ;
#38973=ORIENTED_EDGE ( 'NONE', *, *, #37110, .T. ) ;
#38974=CARTESIAN_POINT ( 'NONE',  ( 10.61721774768000159, 5.045603402166999985, -6.386910706193999587 ) ) ;
#38976=ORIENTED_EDGE ( 'NONE', *, *, #49392, .F. ) ;
#38981=PLANE ( 'NONE',  #46350 ) ;
#38986=CARTESIAN_POINT ( 'NONE',  ( 11.02445190299000011, 3.404087387974999768, 5.822483872269000216 ) ) ;
#38987=CARTESIAN_POINT ( 'NONE',  ( 10.62256721958999961, 2.471460423959999986, -8.210789473540000216 ) ) ;
#38997=CARTESIAN_POINT ( 'NONE',  ( 9.237204719595000668, 3.071719032003000116, -6.037263251225000182 ) ) ;
#39001=PLANE ( 'NONE',  #1554 ) ;
#39007=DIRECTION ( 'NONE',  ( 0.000000000000000000, 0.9916377111174247139, -0.1290528957048031888 ) ) ;
#39015=CARTESIAN_POINT ( 'NONE',  ( 4.149992563292000725, -2.000000000000000000, 0.000000000000000000 ) ) ;
#39016=VERTEX_POINT ( 'NONE', #31986 ) ;
#39019=CARTESIAN_POINT ( 'NONE',  ( 9.699495280410998177, 5.048004622677000341, -6.120508709481000231 ) ) ;
#39023=B_SPLINE_CURVE_WITH_KNOTS ( 'NONE', 3,
 ( #40745, #62069, #35512, #8933, #3670, #9961, #47028, #31298, #52959, #41776, #5056, #42470, #16580, #42128, #64118, #69031, #52608, #15206 ),
 .UNSPECIFIED., .F., .F.,
 ( 4, 2, 2, 2, 2, 2, 2, 2, 4 ),
 ( 0.000000000000000000, 0.1250000000000000000, 0.2500000000000000000, 0.3750000000000000000, 0.5000000000000000000, 0.6250000000000000000, 0.7500000000000000000, 0.8750000000000000000, 1.000000000000000000 ),
 .UNSPECIFIED. ) ;
#39027=CARTESIAN_POINT ( 'NONE',  ( 3.548931641198000086, 2.181374122857000053, -2.586569627374999847 ) ) ;
#39032=CARTESIAN_POINT ( 'NONE',  ( 8.181107780410998842, 5.485785046334999748, 8.532070739720001740 ) ) ;
#39035=CARTESIAN_POINT ( 'NONE',  ( 8.634260841228998729, 5.171553746019000641, -8.261796965435999951 ) ) ;
#39039=ORIENTED_EDGE ( 'NONE', *, *, #27025, .T. ) ;
#39040=CARTESIAN_POINT ( 'NONE',  ( 10.98768472567999943, 5.449702577258999980, -4.945212061305999107 ) ) ;
#39041=CARTESIAN_POINT ( 'NONE',  ( 10.06489140842196406, 5.349900232312646331, -7.500006335289779003 ) ) ;
#39049=CARTESIAN_POINT ( 'NONE',  ( 7.441339158769000761, 3.563552687850000122, -6.172381771908999504 ) ) ;
#39058=CARTESIAN_POINT ( 'NONE',  ( 10.90000000296000060, 2.899999999990999999, 5.160242730682999657 ) ) ;
#39059=CARTESIAN_POINT ( 'NONE',  ( 10.90000000162999960, 2.899999999992999733, -5.160242739096000619 ) ) ;
#39061=PLANE ( 'NONE',  #49790 ) ;
#39068=ORIENTED_EDGE ( 'NONE', *, *, #54658, .F. ) ;
#39070=CARTESIAN_POINT ( 'NONE',  ( 8.367589158771000513, 5.461114003844000031, -8.582501063019000398 ) ) ;
#39071=CARTESIAN_POINT ( 'NONE',  ( 3.257664066220000265, 1.608864567386000033, -2.971833076323999734 ) ) ;
#39077=ORIENTED_EDGE ( 'NONE', *, *, #53066, .F. ) ;
#39080=CARTESIAN_POINT ( 'NONE',  ( 11.06923869026000062, 5.425682056982999768, 8.012911262916999178 ) ) ;
#39083=CARTESIAN_POINT ( 'NONE',  ( 11.03333333333435640, 2.969278270712281564, 8.594189652917812339 ) ) ;
#39086=CARTESIAN_POINT ( 'NONE',  ( 10.30896519935103761, 4.355941342076152800, 9.241073271048676929 ) ) ;
#39089=CARTESIAN_POINT ( 'NONE',  ( 8.114525141030208388, 5.047092373262178633, -6.489789622603527874 ) ) ;
#39096=ORIENTED_EDGE ( 'NONE', *, *, #1822, .F. ) ;
#39098=CARTESIAN_POINT ( 'NONE',  ( 7.924357780410000274, 2.432118421226999949, 6.597517552098000060 ) ) ;
#39102=CARTESIAN_POINT ( 'NONE',  ( 10.79701415876999882, 5.792870175253000298, -7.049262931951000510 ) ) ;
#39104=CARTESIAN_POINT ( 'NONE',  ( 10.33536974457000035, 5.153692264686000613, 8.830864265869999841 ) ) ;
#39109=EDGE_LOOP ( 'NONE', ( #44384, #35791, #13961 ) ) ;
#39124=CARTESIAN_POINT ( 'NONE',  ( 9.591185841232000797, 2.173570076733999823, -8.023168429484000441 ) ) ;
#39130=EDGE_LOOP ( 'NONE', ( #42250, #28939, #31597 ) ) ;
#39137=CARTESIAN_POINT ( 'NONE',  ( 10.40558702164999971, 5.599341344818000721, -8.437759619346000051 ) ) ;
#39144=DIRECTION ( 'NONE',  ( -0.8660254037844288266, 4.668797665416159739E-13, 0.5000000000000169864 ) ) ;
#39148=CARTESIAN_POINT ( 'NONE',  ( 7.903989158771000056, 2.095715612964000218, 8.056490963156001328 ) ) ;
#39153=CARTESIAN_POINT ( 'NONE',  ( 10.51655086620999846, 4.930662802525000110, 8.573584269714999095 ) ) ;
#39158=CARTESIAN_POINT ( 'NONE',  ( 10.77462860031000069, 5.575476001419000127, 8.682676628339999425 ) ) ;
#39164=CARTESIAN_POINT ( 'NONE',  ( 9.472537864290000442, 2.899999999999999911, -6.571291218949999902 ) ) ;
#39166=B_SPLINE_SURFACE_WITH_KNOTS ( 'NONE', 3, 3, ( 
 ( #65661, #18469, #23366, #28267, #44361, #45042, #28622, #44706, #17783, #39102, #29313, #12532, #24050, #60426, #13576, #66347, #50626, #45728, #33863, #34897, #39795, #67036, #2727, #60767, #56213, #45385, #8322, #66003, #18126, #34561, #12882, #50967, #7628, #61118, #55872 ),
 ( #7979, #66695, #3065, #24398, #51309, #8997, #3406, #26115, #41503, #36258, #62474, #31028, #15282, #30340, #47443, #56898, #14257, #62815, #63505, #4431, #30007, #68398, #3743, #67372, #46067, #68060, #25078, #8660, #20866, #4087, #51646, #46412, #19497, #40814, #9678 ),
 ( #25769, #52337, #47098, #67713, #20175, #4773, #20521, #35242, #35916, #19839, #41847, #46757, #14596, #51981, #41169, #57230, #14934, #35584, #42204, #63153, #24741, #56556, #9330, #62138, #30675, #36605, #57931, #25423, #68749, #57575, #52679, #10028, #31367, #42883, #54403 ),
 ( #5476, #16303, #6503, #43924, #31709, #64190, #38318, #37628, #26812, #27152, #27493, #37291, #232, #58962, #10371, #27848, #15624, #6152, #48473, #63848, #43576, #36955, #11066, #59646, #32059, #48818, #53030, #32400, #58269, #5126, #53715, #5811, #43224, #11745, #33087 ) ),
 .UNSPECIFIED., .F., .F., .F.,
 ( 4, 4 ),
 ( 4, 1, 1, 1, 1, 1, 1, 1, 1, 1, 1, 1, 1, 1, 1, 1, 1, 1, 1, 1, 1, 1, 1, 1, 1, 1, 1, 1, 1, 1, 1, 1, 4 ),
 ( -0.1039370721279000015, 1.103937072127999963 ),
 ( 0.2233333333344000027, 0.2480800653604999795, 0.2728267973865999840, 0.2975735294126999886, 0.3223202614387999931, 0.3470669934649999733, 0.3718137254910999778, 0.3965604575171999824, 0.4213071895433000424, 0.4460539215694000470, 0.4708006535954999960, 0.4955473856216000006, 0.5202941176476999496, 0.5450408496738000652, 0.5697875816999000698, 0.5945343137260000743, 0.6192810457521999989, 0.6440277777783000035, 0.6687745098044000081, 0.6935212418305000126, 0.7182679738566000172, 0.7430147058827000217, 0.7677614379088000263, 0.7925081699349000308, 0.8172549019609999243, 0.8420016339870999289, 0.8667483660132000445, 0.8914950980394000801, 0.9162418300655000847, 0.9409885620915999782, 0.9657352941176999828, 0.9904820261437999873, 1.015228758169999912 ),
 .UNSPECIFIED. ) ;
#39169=CARTESIAN_POINT ( 'NONE',  ( 7.443295280410000103, 4.698356649019999942, 8.789431186081998248 ) ) ;
#39170=CARTESIAN_POINT ( 'NONE',  ( 10.83668832355999889, 4.288537082977999404, 9.448742031664000507 ) ) ;
#39173=CARTESIAN_POINT ( 'NONE',  ( 9.784179719593000257, 4.042991257420999851, -5.768106221333000327 ) ) ;
#39180=EDGE_LOOP ( 'NONE', ( #4048, #56009, #11099, #15829 ) ) ;
#39181=CARTESIAN_POINT ( 'NONE',  ( 1.262565185690999847, 3.233448155534000001, 0.4075532224664999981 ) ) ;
#39189=DIRECTION ( 'NONE',  ( 0.000000000000000000, 1.000000000000000000, 0.000000000000000000 ) ) ;
#39192=EDGE_LOOP ( 'NONE', ( #15498, #25640, #1, #32417, #22369, #40571, #53004, #44726, #68472, #52686, #47892, #60830 ) ) ;
#39194=CARTESIAN_POINT ( 'NONE',  ( 7.469166666664250442, 3.646640356114970505, -6.185136886497774711 ) ) ;
#39195=CARTESIAN_POINT ( 'NONE',  ( 9.536859343794805710, 5.286513823918975952, -7.027110704272522490 ) ) ;
#39198=CARTESIAN_POINT ( 'NONE',  ( 0.9422012868096000249, 1.794790469053999971, -3.302590565797000277 ) ) ;
#39200=CARTESIAN_POINT ( 'NONE',  ( 10.61503919148293740, 5.349978903665603802, -7.499997722305280945 ) ) ;
#39203=DIRECTION ( 'NONE',  ( 1.000000000000000000, 0.000000000000000000, 0.000000000000000000 ) ) ;
#39205=VECTOR ( 'NONE', #54470, 1000.000000000000000 ) ;
#39212=CARTESIAN_POINT ( 'NONE',  ( 8.745860841232000027, 4.178200486578000472, -5.608493638783999202 ) ) ;
#39220=CARTESIAN_POINT ( 'NONE',  ( 9.566963020987998334, 5.215925787220999865, 6.177726425586999248 ) ) ;
#39226=CARTESIAN_POINT ( 'NONE',  ( 4.000000000000000000, -1.082895748633089683, -1.878475312369199957 ) ) ;
#39227=EDGE_CURVE ( 'NONE', #25280, #67407, #53655, .T. ) ;
#39232=CARTESIAN_POINT ( 'NONE',  ( 10.71434555259480348, 3.092585117345866497, -4.811875879314510662 ) ) ;
#39239=ORIENTED_EDGE ( 'NONE', *, *, #22070, .F. ) ;
#39240=CARTESIAN_POINT ( 'NONE',  ( 7.849513827001898036, 2.927712334411324946, -6.623875161447396742 ) ) ;
#39242=ORIENTED_EDGE ( 'NONE', *, *, #13448, .T. ) ;
#39245=EDGE_CURVE ( 'NONE', #60041, #8802, #49571, .T. ) ;
#39246=B_SPLINE_CURVE_WITH_KNOTS ( 'NONE', 3,
 ( #48991, #43755, #1792, #7032 ),
 .UNSPECIFIED., .F., .F.,
 ( 4, 4 ),
 ( 0.000000000000000000, 1.000000000000000000 ),
 .UNSPECIFIED. ) ;
#39249=CARTESIAN_POINT ( 'NONE',  ( 8.938854719593997800, 5.597201461420000967, -8.171008079894999554 ) ) ;
#39254=CYLINDRICAL_SURFACE ( 'NONE', #12512, 0.5000000000000002220 ) ;
#39258=CARTESIAN_POINT ( 'NONE',  ( 1.167640132542000275, -1.762666431298160141, 3.058252359239895579 ) ) ;
#39260=B_SPLINE_CURVE_WITH_KNOTS ( 'NONE', 3,
 ( #15788, #68225, #20344, #10200, #14765, #67889, #57397, #63323, #3571, #4949, #47613, #58434, #24904, #19665, #62309, #14426, #35743, #57062 ),
 .UNSPECIFIED., .F., .F.,
 ( 4, 2, 2, 2, 2, 2, 2, 2, 4 ),
 ( 0.000000000000000000, 0.1250000000000000555, 0.2500000000000001110, 0.3750000000000001665, 0.5000000000000002220, 0.6250000000000001110, 0.7500000000000001110, 0.8750000000000000000, 1.000000000000000000 ),
 .UNSPECIFIED. ) ;
#39275=ORIENTED_EDGE ( 'NONE', *, *, #63540, .F. ) ;
#39282=B_SPLINE_CURVE_WITH_KNOTS ( 'NONE', 3,
 ( #42280, #19915, #56972, #62551, #25502, #20254, #26195, #4503, #62215, #41923 ),
 .UNSPECIFIED., .F., .F.,
 ( 4, 2, 2, 2, 4 ),
 ( 0.1253970409990855239, 0.3126921946255971640, 0.4999873482521087764, 0.6872825018786201667, 0.8745776555051315571 ),
 .UNSPECIFIED. ) ;
#39285=LINE ( 'NONE', #49772, #59950 ) ;
#39287=LINE ( 'NONE', #64447, #17038 ) ;
#39294=CARTESIAN_POINT ( 'NONE',  ( 7.000000000000000888, 8.702830230118003385, 4.583331007515480060 ) ) ;
#39302=CARTESIAN_POINT ( 'NONE',  ( 9.260829719593999698, 4.861259245430999520, -8.806664389576001284 ) ) ;
#39312=CARTESIAN_POINT ( 'NONE',  ( 9.925639158771000226, 4.357364160690000432, -9.282962013144999247 ) ) ;
#39314=AXIS2_PLACEMENT_3D ( 'NONE', #16107, #48266, #47593 ) ;
#39315=CARTESIAN_POINT ( 'NONE',  ( 10.17309652395999997, 4.709165316578000748, -8.664874001714000684 ) ) ;
#39327=CARTESIAN_POINT ( 'NONE',  ( 11.09178278040999999, 4.578541652803000517, -8.908598806528001290 ) ) ;
#39336=EDGE_LOOP ( 'NONE', ( #29034, #9112, #59869, #7223 ) ) ;
#39338=CARTESIAN_POINT ( 'NONE',  ( 9.295789158775001226, 5.835196551504000517, -7.008466539623000813 ) ) ;
#39350=CARTESIAN_POINT ( 'NONE',  ( 7.398321641533604165, 3.320456282957297223, -6.320831307949290157 ) ) ;
#39355=ORIENTED_EDGE ( 'NONE', *, *, #21267, .F. ) ;
#39358=CARTESIAN_POINT ( 'NONE',  ( 8.233179719589999834, 5.203550244299999683, -8.391678825488000371 ) ) ;
#39359=CYLINDRICAL_SURFACE ( 'NONE', #2969, 1.350000000000000533 ) ;
#39362=DIRECTION ( 'NONE',  ( 1.000000000000000000, 0.000000000000000000, 0.000000000000000000 ) ) ;
#39364=CARTESIAN_POINT ( 'NONE',  ( 2.404564854619000158, -3.223169239229000116, -1.585884214500000056 ) ) ;
#39365=PRODUCT_DEFINITION ( 'UNKNOWN', '', #63066, #20607 ) ;
#39366=ORIENTED_EDGE ( 'NONE', *, *, #65837, .T. ) ;
#39368=DIRECTION ( 'NONE',  ( 0.000000000000000000, 0.000000000000000000, -1.000000000000000000 ) ) ;
#39370=CARTESIAN_POINT ( 'NONE',  ( 8.502045280412000139, 3.869396554003000421, 5.695652484872999466 ) ) ;
#39373=CARTESIAN_POINT ( 'NONE',  ( 7.739210841226999982, 3.554387346680000004, -8.824570035521999145 ) ) ;
#39375=CARTESIAN_POINT ( 'NONE',  ( 9.160535748954998780, 2.900115872948000106, -6.152093930328999427 ) ) ;
#39376=CARTESIAN_POINT ( 'NONE',  ( 10.74207053302655446, 3.170338597610619757, -8.579608023176378495 ) ) ;
#39378=ORIENTED_EDGE ( 'NONE', *, *, #67301, .T. ) ;
#39380=VERTEX_POINT ( 'NONE', #6612 ) ;
#39385=CARTESIAN_POINT ( 'NONE',  ( 10.93606915609024810, 9.383178346453151519, -6.183004993341985056 ) ) ;
#39387=CARTESIAN_POINT ( 'NONE',  ( 8.137489158770998543, 5.171553746019000641, -8.261796965435999951 ) ) ;
#39393=B_SPLINE_CURVE_WITH_KNOTS ( 'NONE', 3,
 ( #30295, #15580, #41121, #9633, #14554, #35872, #30630, #51599, #51940, #4038, #25376, #57882, #9983, #4727, #46713, #52631, #68356, #68016, #20134, #41462, #25721, #26071 ),
 .UNSPECIFIED., .F., .F.,
 ( 4, 2, 2, 2, 2, 2, 2, 2, 2, 2, 4 ),
 ( 0.000000000000000000, 0.1249999999999995559, 0.2499999999999991118, 0.3124999999999991673, 0.3749999999999992228, 0.4999999999999993339, 0.6249999999999994449, 0.7499999999999995559, 0.8124999999999996669, 0.8749999999999997780, 1.000000000000000000 ),
 .UNSPECIFIED. ) ;
#39395=B_SPLINE_CURVE_WITH_KNOTS ( 'NONE', 3,
 ( #68965, #57784, #31235, #52542, #47307, #68612, #20731 ),
 .UNSPECIFIED., .F., .F.,
 ( 4, 1, 1, 1, 4 ),
 ( 0.000000000000000000, 0.2500000590475000006, 0.5000000002693999468, 0.7499999414914000351, 1.000000000000000000 ),
 .UNSPECIFIED. ) ;
#39397=CARTESIAN_POINT ( 'NONE',  ( 10.99691776498582207, 5.205777403464205477, 6.655421476746652409 ) ) ;
#39400=ORIENTED_EDGE ( 'NONE', *, *, #37888, .T. ) ;
#39402=CARTESIAN_POINT ( 'NONE',  ( 0.3738300074506999970, -3.373808768376999723, -1.182108054635000026E-09 ) ) ;
#39413=CARTESIAN_POINT ( 'NONE',  ( 9.734454719592999794, 3.021734963141999852, -6.070209284876999511 ) ) ;
#39414=CARTESIAN_POINT ( 'NONE',  ( 2.747903870626000167, 3.209484249071000050, -0.1891215843542000119 ) ) ;
#39421=ORIENTED_EDGE ( 'NONE', *, *, #62643, .F. ) ;
#39422=CYLINDRICAL_SURFACE ( 'NONE', #60359, 0.5000000000000002220 ) ;
#39424=CARTESIAN_POINT ( 'NONE',  ( 8.404999999999999361, 5.190914425723000214, -8.768195054477999406 ) ) ;
#39427=CARTESIAN_POINT ( 'NONE',  ( 11.09166666666771839, 2.528771982359670822, 6.972956482935108724 ) ) ;
#39429=CARTESIAN_POINT ( 'NONE',  ( 7.100000000000000533, 5.326087788487999575, -7.247035225330000330 ) ) ;
#39432=CARTESIAN_POINT ( 'NONE',  ( 0.8233524344999001432, -2.161873583226317397, -2.781123199319127437 ) ) ;
#39433=CARTESIAN_POINT ( 'NONE',  ( 10.76588584123000025, 3.166544027818999574, -8.574484964885998650 ) ) ;
#39443=CARTESIAN_POINT ( 'NONE',  ( 8.192489158772998437, 2.550241116032999855, 7.666973618349000041 ) ) ;
#39444=CARTESIAN_POINT ( 'NONE',  ( 8.447510841229000533, 4.933589693325000525, -9.154576215408999573 ) ) ;
#39450=CARTESIAN_POINT ( 'NONE',  ( 10.52323372634000087, 3.325642821414999784, 5.689987891230000372 ) ) ;
#39457=CARTESIAN_POINT ( 'NONE',  ( 1.448890132540874953, 2.798833948393634863, -2.150913519912196925 ) ) ;
#39468=AXIS2_PLACEMENT_3D ( 'NONE', #47580, #53507, #15758 ) ;
#39470=CARTESIAN_POINT ( 'NONE',  ( 9.401145280412999128, 3.927090956378999742, -9.230892435423001530 ) ) ;
#39494=CARTESIAN_POINT ( 'NONE',  ( 8.224926658773000554, 5.629399530851999955, 8.631829656822000985 ) ) ;
#39498=CARTESIAN_POINT ( 'NONE',  ( 7.474999999999999645, 5.349999999999999645, 7.500000000000000000 ) ) ;
#39499=CARTESIAN_POINT ( 'NONE',  ( 10.21237770872999917, 4.072568038926999812, -8.861829932786999819 ) ) ;
#39503=CARTESIAN_POINT ( 'NONE',  ( 10.00138108374000012, 3.855364958793999985, 5.709478909302000638 ) ) ;
#39511=AXIS2_PLACEMENT_3D ( 'NONE', #60276, #66199, #7471 ) ;
#39514=AXIS2_PLACEMENT_3D ( 'NONE', #22787, #54254, #28047 ) ;
#39515=CARTESIAN_POINT ( 'NONE',  ( 8.406107780410998487, 5.342170561818999630, 8.432311822615000452 ) ) ;
#39516=CARTESIAN_POINT ( 'NONE',  ( 9.409314688805999083, 2.634692233435000031, 8.920311306029999443 ) ) ;
#39519=CARTESIAN_POINT ( 'NONE',  ( 10.01622971959000097, 4.325866256860000369, -9.125812605905000652 ) ) ;
#39529=CARTESIAN_POINT ( 'NONE',  ( 2.163748887004999677, -2.164574875407999865, -2.655056891479000036 ) ) ;
#39543=CARTESIAN_POINT ( 'NONE',  ( 10.87376707297999978, 5.064086065370999812, 5.106852026787000121 ) ) ;
#39546=CARTESIAN_POINT ( 'NONE',  ( 0.6084276407238999873, 1.980426728703999828, 3.194707851357999839 ) ) ;
#39547=EDGE_LOOP ( 'NONE', ( #15065, #22088, #35436, #32949 ) ) ;
#39548=CARTESIAN_POINT ( 'NONE',  ( 10.69839231854705908, 4.679932939043758289, -8.679767489842406647 ) ) ;
#39550=CARTESIAN_POINT ( 'NONE',  ( 10.73931450027999901, 2.763002390638999994, 6.801034082888999244 ) ) ;
#39558=CARTESIAN_POINT ( 'NONE',  ( 8.086348386990133363, 4.224401473857131606, 5.771886138180387427 ) ) ;
#39565=CARTESIAN_POINT ( 'NONE',  ( 4.149992563291999836, 1.747525841223985354, -1.007210908820209472 ) ) ;
#39566=CIRCLE ( 'NONE', #11646, 1.900000000000000577 ) ;
#39568=CARTESIAN_POINT ( 'NONE',  ( 9.719613305057999142, 5.967773797872000685, 7.406643507784999692 ) ) ;
#39569=CARTESIAN_POINT ( 'NONE',  ( 10.29094007826000023, 2.903522982536999919, -8.310916170934000036 ) ) ;
#39570=CARTESIAN_POINT ( 'NONE',  ( 11.10000000001000053, 7.524088986311000760, -6.497786318682999607 ) ) ;
#39575=ORIENTED_EDGE ( 'NONE', *, *, #50328, .F. ) ;
#39580=CARTESIAN_POINT ( 'NONE',  ( 11.04422294928000170, 7.351868426856999150, 6.139941188252000082 ) ) ;
#39584=ORIENTED_EDGE ( 'NONE', *, *, #19365, .T. ) ;
#39592=CARTESIAN_POINT ( 'NONE',  ( 8.513406929461279304, 3.194994825692138996, 5.997290436226018429 ) ) ;
#39595=CARTESIAN_POINT ( 'NONE',  ( 9.386379719595000282, 5.673443217382001080, -7.051790060464000476 ) ) ;
#39597=CARTESIAN_POINT ( 'NONE',  ( 11.12455582848000013, 7.801067643070999758, -6.682512661172999913 ) ) ;
#39599=DIRECTION ( 'NONE',  ( 0.000000000000000000, -0.8648648648648720183, 0.5020047465136825426 ) ) ;
#39603=CARTESIAN_POINT ( 'NONE',  ( 1.209306799208499816, -3.058252359239909790, 1.762666431298136382 ) ) ;
#39610=ORIENTED_EDGE ( 'NONE', *, *, #61399, .T. ) ;
#39616=EDGE_CURVE ( 'NONE', #54068, #13653, #49366, .T. ) ;
#39617=B_SPLINE_CURVE_WITH_KNOTS ( 'NONE', 3,
 ( #52149, #53538, #20004, #42701 ),
 .UNSPECIFIED., .F., .F.,
 ( 4, 4 ),
 ( 0.000000000000000000, 1.000000000000000000 ),
 .UNSPECIFIED. ) ;
#39633=CARTESIAN_POINT ( 'NONE',  ( 10.52052890781999928, 2.899999999999999911, 6.152188490330000370 ) ) ;
#39637=CARTESIAN_POINT ( 'NONE',  ( 8.279780186038228962, 3.802829437883106234, 6.095677095145819457 ) ) ;
#39641=CARTESIAN_POINT ( 'NONE',  ( 11.09999999999999964, 5.340540480602000706, -6.721892539640999864 ) ) ;
#39646=ORIENTED_EDGE ( 'NONE', *, *, #49304, .F. ) ;
#39648=CARTESIAN_POINT ( 'NONE',  ( 2.623890132543956977, 2.150913519912194261, 2.798833948393636195 ) ) ;
#39649=CARTESIAN_POINT ( 'NONE',  ( 9.839810841229999383, 5.817107086401000160, -6.945352709928000579 ) ) ;
#39657=CARTESIAN_POINT ( 'NONE',  ( 10.09999999999999964, 0.000000000000000000, -11.84999999999999964 ) ) ;
#39658=FACE_OUTER_BOUND ( 'NONE', #67096, .T. ) ;
#39660=CARTESIAN_POINT ( 'NONE',  ( 10.21237770872999917, 4.072568038926999812, -8.861829932786999819 ) ) ;
#39661=ORIENTED_EDGE ( 'NONE', *, *, #22785, .T. ) ;
#39664=VECTOR ( 'NONE', #48290, 1000.000000000000000 ) ;
#39665=EDGE_CURVE ( 'NONE', #3005, #43316, #29951, .T. ) ;
#39670=EDGE_CURVE ( 'NONE', #35486, #26545, #33807, .T. ) ;
#39675=CARTESIAN_POINT ( 'NONE',  ( 10.13035471959000056, 2.409325917207000511, -8.058043919563999680 ) ) ;
#39676=DIRECTION ( 'NONE',  ( 1.069977439982493646E-11, 1.000000000000000000, -6.186023915333288444E-12 ) ) ;
#39686=CARTESIAN_POINT ( 'NONE',  ( 8.997439158776000312, 2.773858540272000184, -8.951250717848999727 ) ) ;
#39697=CARTESIAN_POINT ( 'NONE',  ( 7.356653345687266032, 2.795129470416956696, -6.794966557345468061 ) ) ;
#39705=CARTESIAN_POINT ( 'NONE',  ( 8.953620280414000376, 2.881930053949999682, -8.823338183322999129 ) ) ;
#39709=DIRECTION ( 'NONE',  ( 1.000000000000000000, 0.000000000000000000, 0.000000000000000000 ) ) ;
#39713=VECTOR ( 'NONE', #49743, 1000.000000000000000 ) ;
#39715=CARTESIAN_POINT ( 'NONE',  ( 2.113699819910999977, 1.185225022173999943, -3.001128720719000054 ) ) ;
#39720=CARTESIAN_POINT ( 'NONE',  ( 8.256676658772999389, 2.876288091423999660, 6.568897128359000526 ) ) ;
#39722=VERTEX_POINT ( 'NONE', #2669 ) ;
#39724=CARTESIAN_POINT ( 'NONE',  ( 10.91724622068368866, 9.661695380177112824, 5.909120167440196525 ) ) ;
#39725=EDGE_CURVE ( 'NONE', #46011, #53731, #12497, .T. ) ;
#39732=ORIENTED_EDGE ( 'NONE', *, *, #19083, .F. ) ;
#39738=CARTESIAN_POINT ( 'NONE',  ( 10.96710728122044287, 8.735833061596222748, -6.507096358675760861 ) ) ;
#39739=DIRECTION ( 'NONE',  ( 0.000000000000000000, 0.000000000000000000, -1.000000000000000000 ) ) ;
#39744=CARTESIAN_POINT ( 'NONE',  ( 7.871551658771999804, 4.780986922229000236, 6.267222470044999660 ) ) ;
#39754=CARTESIAN_POINT ( 'NONE',  ( 11.08757144985999865, 2.712428550139000194, 6.571291218949999902 ) ) ;
#39759=EDGE_LOOP ( 'NONE', ( #34652, #29496, #56856, #48679 ) ) ;
#39762=CARTESIAN_POINT ( 'NONE',  ( 0.1499942179680000265, 2.402872127494067644, 1.384928887584814916 ) ) ;
#39764=CARTESIAN_POINT ( 'NONE',  ( 8.988579719593998263, 4.902869380824999901, -8.978557145469999057 ) ) ;
#39765=CARTESIAN_POINT ( 'NONE',  ( 3.460492249740999782, -2.775615920636000045, 1.622391736872000001 ) ) ;
#39772=CARTESIAN_POINT ( 'NONE',  ( 9.137543006348998631, 2.995704926864999784, 8.544754656710999541 ) ) ;
#39775=CARTESIAN_POINT ( 'NONE',  ( 10.90833333333429067, 5.360760283597206133, 7.292330520109749692 ) ) ;
#39777=CARTESIAN_POINT ( 'NONE',  ( 10.96262032192263902, 2.824326349884676013, -6.677398119062115889 ) ) ;
#39781=CARTESIAN_POINT ( 'NONE',  ( 8.082873386424997975, 5.111739203374999541, -6.679001318365999751 ) ) ;
#39782=CARTESIAN_POINT ( 'NONE',  ( 10.53871084122999946, 5.103389446345000025, -6.705205355781999721 ) ) ;
#39785=EDGE_CURVE ( 'NONE', #51086, #31394, #59398, .T. ) ;
#39786=ADVANCED_FACE ( 'NONE', ( #44652 ), #27256, .T. ) ;
#39790=ORIENTED_EDGE ( 'NONE', *, *, #47453, .T. ) ;
#39791=CARTESIAN_POINT ( 'NONE',  ( 8.475642219593000348, 5.095085596809999728, 6.286981168432999922 ) ) ;
#39792=CIRCLE ( 'NONE', #48723, 2.000000000000000000 ) ;
#39795=CARTESIAN_POINT ( 'NONE',  ( 10.38052665877000003, 5.283793195606000026, -8.830196380017000024 ) ) ;
#39796=ORIENTED_EDGE ( 'NONE', *, *, #22162, .T. ) ;
#39797=CARTESIAN_POINT ( 'NONE',  ( 9.409415556003999370, 2.113395950889999764, 7.914199712930999553 ) ) ;
#39801=CARTESIAN_POINT ( 'NONE',  ( 8.056015159639001055, 3.481518869265999072, 6.232552614174998951 ) ) ;
#39802=ORIENTED_EDGE ( 'NONE', *, *, #41513, .F. ) ;
#39803=FACE_OUTER_BOUND ( 'NONE', #50913, .T. ) ;
#39814=ORIENTED_EDGE ( 'NONE', *, *, #25647, .T. ) ;
#39819=B_SPLINE_CURVE_WITH_KNOTS ( 'NONE', 3,
 ( #33041, #49455, #17302, #55053 ),
 .UNSPECIFIED., .F., .F.,
 ( 4, 4 ),
 ( 0.000000000000000000, 1.000000000000000000 ),
 .UNSPECIFIED. ) ;
#39820=CARTESIAN_POINT ( 'NONE',  ( 9.541460841232000334, 2.824732249080000202, -8.992748220058999209 ) ) ;
#39822=DIRECTION ( 'NONE',  ( 1.000000000000000000, 0.000000000000000000, 0.000000000000000000 ) ) ;
#39827=CARTESIAN_POINT ( 'NONE',  ( 9.164680296029999340, 2.899999999999999911, -6.162130047625999474 ) ) ;
#39830=CARTESIAN_POINT ( 'NONE',  ( 7.934990594362998806, 3.391823837616000148, -6.294741454024999960 ) ) ;
#39831=EDGE_LOOP ( 'NONE', ( #57168, #4370, #22657, #192 ) ) ;
#39842=CARTESIAN_POINT ( 'NONE',  ( 8.636454719592999041, 3.869396554003000421, 5.695652484872999466 ) ) ;
#39847=CARTESIAN_POINT ( 'NONE',  ( 10.09453415443000068, 5.362844031509000686, -7.550030311027999375 ) ) ;
#39853=CARTESIAN_POINT ( 'NONE',  ( 10.12550053024000007, 5.788811067708000024, 7.335561454339999621 ) ) ;
#39860=CARTESIAN_POINT ( 'NONE',  ( 9.813360311708999362, 5.349397258738000538, 6.657026394682000081 ) ) ;
#39861=B_SPLINE_CURVE_WITH_KNOTS ( 'NONE', 3,
 ( #21428, #5697, #807, #38203 ),
 .UNSPECIFIED., .F., .F.,
 ( 4, 4 ),
 ( 0.8745855536721935941, 1.000000000000000000 ),
 .UNSPECIFIED. ) ;
#39866=CARTESIAN_POINT ( 'NONE',  ( 8.995176658772999545, 2.707986230053999854, 5.994446745591000436 ) ) ;
#39867=CARTESIAN_POINT ( 'NONE',  ( 10.65550720192000078, 4.237674045823999869, 9.105219676299999065 ) ) ;
#39871=CARTESIAN_POINT ( 'NONE',  ( 9.386379719595000282, 5.673443217382001080, -7.051790060464000476 ) ) ;
#39877=CARTESIAN_POINT ( 'NONE',  ( 3.250973465878000290, -3.500000000000000000, 0.000000000000000000 ) ) ;
#39880=ORIENTED_EDGE ( 'NONE', *, *, #36173, .T. ) ;
#39882=CARTESIAN_POINT ( 'NONE',  ( 1.639247443156000017, -2.867416142353000463, -1.874231387797000048 ) ) ;
#39883=CARTESIAN_POINT ( 'NONE',  ( 9.099999999999999645, 0.000000000000000000, 0.000000000000000000 ) ) ;
#39892=CARTESIAN_POINT ( 'NONE',  ( 8.534482780410998615, 3.011620138462000273, 8.801434747080000065 ) ) ;
#39893=CARTESIAN_POINT ( 'NONE',  ( 11.04497253870000151, 5.245448120407000481, 5.177000073770999578 ) ) ;
#39895=CIRCLE ( 'NONE', #10828, 12.24999851416000141 ) ;
#39897=CARTESIAN_POINT ( 'NONE',  ( 1.504838003975000005, -2.867416142353000463, -1.874231387797000048 ) ) ;
#39901=CARTESIAN_POINT ( 'NONE',  ( 11.09999999999999964, 2.899999999999999911, 4.467422426380999845 ) ) ;
#39902=CARTESIAN_POINT ( 'NONE',  ( 11.27765994926999937, 3.273804980682999854, 6.368305648407000419 ) ) ;
#39905=LINE ( 'NONE', #18919, #65038 ) ;
#39908=DIRECTION ( 'NONE',  ( -0.8660254037844288266, -3.264431060564110057E-14, 0.5000000000000169864 ) ) ;
#39910=CARTESIAN_POINT ( 'NONE',  ( 7.810465616207683759, 4.327298288918835389, 9.232443200123778837 ) ) ;
#39911=VERTEX_POINT ( 'NONE', #63363 ) ;
#39912=CIRCLE ( 'NONE', #22020, 12.50000000000000178 ) ;
#39920=CARTESIAN_POINT ( 'NONE',  ( 10.02991192131000098, 2.506457833269999824, 6.215406506815000398 ) ) ;
#39921=CARTESIAN_POINT ( 'NONE',  ( 10.05525296965999971, 5.223856410664000194, -6.898317050646999959 ) ) ;
#39930=CARTESIAN_POINT ( 'NONE',  ( 9.819055905797000605, 2.899999999999999911, -6.571291218949999902 ) ) ;
#39936=EDGE_CURVE ( 'NONE', #11746, #31922, #24604, .T. ) ;
#39938=EDGE_LOOP ( 'NONE', ( #66603, #63119, #62170, #47730, #50215, #40144, #49881, #50570 ) ) ;
#39942=DIRECTION ( 'NONE',  ( 0.000000000000000000, -0.7071067811865475727, -0.7071067811865475727 ) ) ;
#39945=DIRECTION ( 'NONE',  ( 1.000000000000000000, 0.000000000000000000, 0.000000000000000000 ) ) ;
#39948=CARTESIAN_POINT ( 'NONE',  ( 9.384624721950221016, 2.899999999999999911, 6.445686799063069294 ) ) ;
#39949=DIRECTION ( 'NONE',  ( 0.000000000000000000, 0.000000000000000000, -1.000000000000000000 ) ) ;
#39950=CARTESIAN_POINT ( 'NONE',  ( 0.1866496906522999988, 2.306917309723999665, 2.681989686974000087 ) ) ;
#39954=B_SPLINE_CURVE_WITH_KNOTS ( 'NONE', 3,
 ( #4623, #40322, #3258, #24926 ),
 .UNSPECIFIED., .F., .F.,
 ( 4, 4 ),
 ( 0.000000000000000000, 0.1253171456473068379 ),
 .UNSPECIFIED. ) ;
#39958=FACE_OUTER_BOUND ( 'NONE', #27606, .T. ) ;
#39963=EDGE_LOOP ( 'NONE', ( #678, #34789, #33826, #25528, #27869, #63927, #30477, #45742 ) ) ;
#39965=EDGE_CURVE ( 'NONE', #20104, #15326, #34483, .T. ) ;
#39981=CARTESIAN_POINT ( 'NONE',  ( 7.000000000000000000, 7.356634010774431687, 3.356634010774432575 ) ) ;
#39984=CYLINDRICAL_SURFACE ( 'NONE', #10786, 1.350000000000000533 ) ;
#39992=CARTESIAN_POINT ( 'NONE',  ( 9.758079719591000512, 4.905765359186999852, -8.776126235875999271 ) ) ;
#39994=VERTEX_POINT ( 'NONE', #46621 ) ;
#39998=CARTESIAN_POINT ( 'NONE',  ( 8.497376085219444874, 4.829144488946226055, 8.579037299257318949 ) ) ;
#40001=CARTESIAN_POINT ( 'NONE',  ( 9.161379719595000637, 5.511689883260999956, -7.095113581311000672 ) ) ;
#40008=B_SPLINE_CURVE_WITH_KNOTS ( 'NONE', 3,
 ( #60171, #12276, #7023, #65746 ),
 .UNSPECIFIED., .F., .F.,
 ( 4, 4 ),
 ( 0.000000000000000000, 1.000000000000000000 ),
 .UNSPECIFIED. ) ;
#40012=VECTOR ( 'NONE', #21139, 1000.000000000000000 ) ;
#40013=CARTESIAN_POINT ( 'NONE',  ( 10.48734600210000067, 4.351287276768000645, -6.182257940481999725 ) ) ;
#40015=ORIENTED_EDGE ( 'NONE', *, *, #67162, .F. ) ;
#40024=EDGE_CURVE ( 'NONE', #53988, #58219, #40676, .T. ) ;
#40026=EDGE_LOOP ( 'NONE', ( #58040, #14456, #51779, #5049 ) ) ;
#40028=CARTESIAN_POINT ( 'NONE',  ( 10.67529528041000120, 3.066676902634999813, -8.703232886886000941 ) ) ;
#40029=CARTESIAN_POINT ( 'NONE',  ( 10.21685100254000034, 2.832432432432000269, 6.822293592207000934 ) ) ;
#40034=CARTESIAN_POINT ( 'NONE',  ( 7.847544949947995008, 5.056324060593960112, 6.597935295888344598 ) ) ;
#40037=CARTESIAN_POINT ( 'NONE',  ( 9.485829719593997567, 4.953415418491999844, -8.946479654552000227 ) ) ;
#40038=CARTESIAN_POINT ( 'NONE',  ( 0.000000000000000000, 5.100000000000000533, 7.500000000000000000 ) ) ;
#40047=CARTESIAN_POINT ( 'NONE',  ( 10.46166951222540753, 5.351570712698046961, 7.263306442112579475 ) ) ;
#40056=ORIENTED_EDGE ( 'NONE', *, *, #14606, .T. ) ;
#40057=DIRECTION ( 'NONE',  ( 1.000000000000000000, 0.000000000000000000, 0.000000000000000000 ) ) ;
#40058=CARTESIAN_POINT ( 'NONE',  ( 7.936034956448000166, 3.387779868797000216, -6.294138482426000714 ) ) ;
#40059=CARTESIAN_POINT ( 'NONE',  ( 8.795585841232000490, 5.251032986819000214, -6.070151079272999795 ) ) ;
#40063=ADVANCED_FACE ( 'NONE', ( #51177 ), #46034, .T. ) ;
#40065=CARTESIAN_POINT ( 'NONE',  ( 3.172249383735999739, -0.9192862011598000871, 3.644624677705999627 ) ) ;
#40066=ORIENTED_EDGE ( 'NONE', *, *, #9483, .T. ) ;
#40071=CARTESIAN_POINT ( 'NONE',  ( 7.422239158771000156, 5.361039412362000434, 6.973453640356000349 ) ) ;
#40073=ORIENTED_EDGE ( 'NONE', *, *, #54615, .T. ) ;
#40075=CARTESIAN_POINT ( 'NONE',  ( 7.689485841227000407, 4.413443707129999893, -8.834960942136000028 ) ) ;
#40088=CARTESIAN_POINT ( 'NONE',  ( 10.98926421552158317, 7.704176194080371687, -6.385256007597936545 ) ) ;
#40099=FACE_OUTER_BOUND ( 'NONE', #64236, .T. ) ;
#40100=CARTESIAN_POINT ( 'NONE',  ( 10.90987534547535098, 2.900005126128452737, 5.097495377258621119 ) ) ;
#40101=CARTESIAN_POINT ( 'NONE',  ( 6.881640499830017355, 5.514763025938938412, -8.366926484462830160 ) ) ;
#40113=CARTESIAN_POINT ( 'NONE',  ( 9.974220280410998285, 5.496789211521000418, -7.043125396300999874 ) ) ;
#40114=CARTESIAN_POINT ( 'NONE',  ( 3.048079248832999966, -2.851054910039999779, 1.814310612331999861 ) ) ;
#40120=CARTESIAN_POINT ( 'NONE',  ( 9.972850246170999355, 5.044468801812000081, 6.258104779495000436 ) ) ;
#40123=DIRECTION ( 'NONE',  ( -0.8660254037844288266, 0.000000000000000000, 0.5000000000000169864 ) ) ;
#40124=B_SPLINE_CURVE_WITH_KNOTS ( 'NONE', 3,
 ( #62022, #9215, #41387, #14817 ),
 .UNSPECIFIED., .F., .F.,
 ( 4, 4 ),
 ( 0.000000000000000000, 1.000000000000000000 ),
 .UNSPECIFIED. ) ;
#40125=CARTESIAN_POINT ( 'NONE',  ( 11.11845610223999969, 5.767025078915000158, 7.178418469370999588 ) ) ;
#40126=CARTESIAN_POINT ( 'NONE',  ( 9.211683426218488790, 2.668681544687872886, 7.727204560920537979 ) ) ;
#40132=CARTESIAN_POINT ( 'NONE',  ( 8.109941913477543451, 5.060294156615178451, -6.518531832221441391 ) ) ;
#40140=CARTESIAN_POINT ( 'NONE',  ( 8.449239158774000558, 5.458692773671000253, 7.456452194274000078 ) ) ;
#40141=CARTESIAN_POINT ( 'NONE',  ( 0.7886440402156557061, -3.499437203200495894, 0.5186531736757357125 ) ) ;
#40144=ORIENTED_EDGE ( 'NONE', *, *, #38309, .T. ) ;
#40145=CARTESIAN_POINT ( 'NONE',  ( 8.649445371194000032, 5.100000000000000533, -6.459601070175000181 ) ) ;
#40150=CARTESIAN_POINT ( 'NONE',  ( 9.947288403111267385, 2.899999999999999911, 6.305985889562331970 ) ) ;
#40158=ORIENTED_EDGE ( 'NONE', *, *, #33791, .T. ) ;
#40166=CARTESIAN_POINT ( 'NONE',  ( 8.953620280414000376, 2.881930053949999682, -8.823338183322999129 ) ) ;
#40173=CARTESIAN_POINT ( 'NONE',  ( 7.572781938258273726, 4.464961194226365393, 8.785435224012646316 ) ) ;
#40181=CARTESIAN_POINT ( 'NONE',  ( 6.799999999999923439, 5.456597484868973780, -8.185422748483164312 ) ) ;
#40186=CARTESIAN_POINT ( 'NONE',  ( 7.856038276909000473, 2.869044596334999753, -6.744487387516000076 ) ) ;
#40190=EDGE_CURVE ( 'NONE', #37746, #5733, #48676, .T. ) ;
#40194=CARTESIAN_POINT ( 'NONE',  ( 8.058915628308520596, 4.678948124125482444, 8.679023822939951671 ) ) ;
#40195=CARTESIAN_POINT ( 'NONE',  ( 10.88015784977000067, 2.793131772868000073, -6.864962922767000819 ) ) ;
#40200=CARTESIAN_POINT ( 'NONE',  ( 8.050967101794888947, 5.350251359469498702, -7.263554191733096133 ) ) ;
#40204=CARTESIAN_POINT ( 'NONE',  ( 9.388624299788999039, 4.079402096444999515, 9.259357173634999327 ) ) ;
#40205=EDGE_CURVE ( 'NONE', #36985, #15157, #65021, .T. ) ;
#40210=CARTESIAN_POINT ( 'NONE',  ( 8.315517219592001297, 5.485785046334999748, 8.532070739720001740 ) ) ;
#40211=CARTESIAN_POINT ( 'NONE',  ( 9.385781899350000401, 4.980865465981000106, 6.433345686594999613 ) ) ;
#40214=CARTESIAN_POINT ( 'NONE',  ( 9.883629719592001095, 5.656948148960999845, -6.994239053114000626 ) ) ;
#40218=CARTESIAN_POINT ( 'NONE',  ( 3.271725677054833525, -3.409621058607596567, -0.9125531287176791295 ) ) ;
#40222=EDGE_LOOP ( 'NONE', ( #58466, #4230, #19075, #38003, #66198, #15493 ) ) ;
#40223=CARTESIAN_POINT ( 'NONE',  ( 2.381491312999000076, 2.737733327009000295, -2.100062873276000275 ) ) ;
#40232=VERTEX_POINT ( 'NONE', #2172 ) ;
#40233=CARTESIAN_POINT ( 'NONE',  ( 9.138573341230998182, 2.933833973450999721, 8.496479443567000800 ) ) ;
#40234=FACE_OUTER_BOUND ( 'NONE', #60377, .T. ) ;
#40237=CARTESIAN_POINT ( 'NONE',  ( 0.6624568971868999290, 2.744051942617999895, -1.815777288092999875 ) ) ;
#40238=ORIENTED_EDGE ( 'NONE', *, *, #32070, .T. ) ;
#40241=CARTESIAN_POINT ( 'NONE',  ( 10.70441484796999987, 3.444517850837000239, 6.009055070331999815 ) ) ;
#40248=CARTESIAN_POINT ( 'NONE',  ( 8.421727527370212130, 2.365161250210713995, 8.132627738500831427 ) ) ;
#40253=ORIENTED_EDGE ( 'NONE', *, *, #9966, .T. ) ;
#40258=CARTESIAN_POINT ( 'NONE',  ( 11.05639637898999972, 5.030226177531999632, 6.028288223959999748 ) ) ;
#40259=CARTESIAN_POINT ( 'NONE',  ( 9.741003491525001223, 3.588532719919999892, -8.800216240366001585 ) ) ;
#40260=CARTESIAN_POINT ( 'NONE',  ( 8.630000000000000782, 4.924138593003999809, -8.484107647018999998 ) ) ;
#40267=ADVANCED_FACE ( 'NONE', ( #33294, #7060 ), #60895, .T. ) ;
#40268=B_SPLINE_CURVE_WITH_KNOTS ( 'NONE', 3,
 ( #65784, #13013, #34341, #23141, #59505, #11604, #17908, #55657, #39226, #50066, #55308, #23835 ),
 .UNSPECIFIED., .F., .F.,
 ( 4, 2, 2, 2, 2, 4 ),
 ( 0.000000000000000000, 0.06249999999999998612, 0.1249999999999999722, 0.2500000000000000000, 0.3750000000000000000, 0.5000000000000000000 ),
 .UNSPECIFIED. ) ;
#40281=VERTEX_POINT ( 'NONE', #15234 ) ;
#40287=CARTESIAN_POINT ( 'NONE',  ( 8.615121458427411838, 5.349954800205006578, -7.499992720895565235 ) ) ;
#40288=CARTESIAN_POINT ( 'NONE',  ( 0.2194555633787999838, -2.757152670777000214, 2.469952924947999673 ) ) ;
#40289=CARTESIAN_POINT ( 'NONE',  ( 8.154130060498527399, 2.684642961096642022, 7.853228170896760396 ) ) ;
#40300=CARTESIAN_POINT ( 'NONE',  ( 4.550000802215999229, 3.641531520771000148E-13, 3.197442310919999608E-14 ) ) ;
#40316=CARTESIAN_POINT ( 'NONE',  ( 7.722357335211003537, 2.834201928695000650, 6.826641520477001457 ) ) ;
#40318=CARTESIAN_POINT ( 'NONE',  ( 0.8738901325418791943, -2.150913519912200922, -2.798833948393631754 ) ) ;
#40322=CARTESIAN_POINT ( 'NONE',  ( 10.75304154458061312, 2.714670728013289569, 7.026954893539028468 ) ) ;
#40324=CARTESIAN_POINT ( 'NONE',  ( 2.811390132544666187, -3.500000000000000888, -0.4581489286485119217 ) ) ;
#40325=FACE_OUTER_BOUND ( 'NONE', #8655, .T. ) ;
#40333=CARTESIAN_POINT ( 'NONE',  ( 8.605545280412000508, 3.122811675949999977, -6.006064052396999919 ) ) ;
#40343=ORIENTED_EDGE ( 'NONE', *, *, #33706, .T. ) ;
#40344=CARTESIAN_POINT ( 'NONE',  ( 9.976690600124999975, 4.172224310749999887, -6.147156451669999910 ) ) ;
#40345=CARTESIAN_POINT ( 'NONE',  ( 0.000000000000000000, 0.000000000000000000, 0.000000000000000000 ) ) ;
#40357=CARTESIAN_POINT ( 'NONE',  ( 11.09999999999999964, 0.5000000000000000000, -5.124965750789000296 ) ) ;
#40365=ORIENTED_EDGE ( 'NONE', *, *, #54536, .T. ) ;
#40367=CARTESIAN_POINT ( 'NONE',  ( 8.681370280410998674, 2.949305648881000330, -8.659807625323999503 ) ) ;
#40368=CARTESIAN_POINT ( 'NONE',  ( 9.286567869848370904, 4.827162169466027386, 9.039452245500738670 ) ) ;
#40374=CARTESIAN_POINT ( 'NONE',  ( 2.360701334807637330, 2.284289129262892626, -2.477459195523546764 ) ) ;
#40382=CARTESIAN_POINT ( 'NONE',  ( 8.615121458427411838, 5.349954800205006578, -7.499992720895565235 ) ) ;
#40383=CARTESIAN_POINT ( 'NONE',  ( 9.975298369746390392, 5.350379160513678123, 7.499985214262784083 ) ) ;
#40386=CARTESIAN_POINT ( 'NONE',  ( 7.890669420221000152, 4.660296061153999858, 6.322498784873999078 ) ) ;
#40394=CARTESIAN_POINT ( 'NONE',  ( 8.705989158774000813, 2.542862824481000317, 7.419808961972999661 ) ) ;
#40399=CARTESIAN_POINT ( 'NONE',  ( 10.92037236908235620, 9.620066740324960008, 5.957247158094110873 ) ) ;
#40400=CARTESIAN_POINT ( 'NONE',  ( 10.61705858902311306, 5.079493225103655973, -8.329679463145396312 ) ) ;
#40401=CARTESIAN_POINT ( 'NONE',  ( 1.553056799207125138, 2.798833948393625537, 2.150913519912209360 ) ) ;
#40411=CARTESIAN_POINT ( 'NONE',  ( 10.98384919964044570, 8.157961774527716869, -6.541894492409994655 ) ) ;
#40413=CARTESIAN_POINT ( 'NONE',  ( 7.099999886593999499, -1.865174681369999698E-13, 1.040815226917999900E-13 ) ) ;
#40417=CARTESIAN_POINT ( 'NONE',  ( 2.178056799207042538, -2.150913519912214245, 2.798833948393621984 ) ) ;
#40420=CARTESIAN_POINT ( 'NONE',  ( 10.99214179192066254, 5.203944559837983874, 6.668820502926433136 ) ) ;
#40423=CARTESIAN_POINT ( 'NONE',  ( 11.09999999999999964, 4.000000000000000000, 7.500000000000000000 ) ) ;
#40425=CARTESIAN_POINT ( 'NONE',  ( 3.500000000000000000, 3.499738125128000199, -0.04281419768536000314 ) ) ;
#40427=CARTESIAN_POINT ( 'NONE',  ( 3.021806799210415839, 3.408904368339103375, 0.9161175952574877046 ) ) ;
#40433=CARTESIAN_POINT ( 'NONE',  ( 9.924742128742000347, 5.060458431729999873, 8.686130311522999747 ) ) ;
#40435=CARTESIAN_POINT ( 'NONE',  ( 9.915635841230999503, 3.210851187372000037, -6.346613542714999667 ) ) ;
#40437=CARTESIAN_POINT ( 'NONE',  ( 2.516671991354999527, 3.690792505019000025, -0.3576329073664999969 ) ) ;
#40445=CARTESIAN_POINT ( 'NONE',  ( 9.696080515601000371, 2.554416243104999928, 7.600685069647000525 ) ) ;
#40448=CARTESIAN_POINT ( 'NONE',  ( 11.14698693981000055, 5.129806801114000336, 5.886034047559999927 ) ) ;
#40456=CARTESIAN_POINT ( 'NONE',  ( 0.7600208369539874775, -3.500000000000000000, -0.3979241631804403267 ) ) ;
#40461=CARTESIAN_POINT ( 'NONE',  ( 5.000030787343000327, -1.679270695423617177, -1.290525307673965782 ) ) ;
#40467=CARTESIAN_POINT ( 'NONE',  ( 3.500000000000000000, -2.946081722130999836, 0.9972449351501998516 ) ) ;
#40470=CARTESIAN_POINT ( 'NONE',  ( 8.610944094208999644, 5.100000000000000533, -6.571291218949999902 ) ) ;
#40475=CARTESIAN_POINT ( 'NONE',  ( 10.98768472638000127, 7.408460511344000743, 6.159405790617999976 ) ) ;
#40485=ORIENTED_EDGE ( 'NONE', *, *, #66687, .F. ) ;
#40493=CARTESIAN_POINT ( 'NONE',  ( 8.415504719592000527, 2.469361196073999842, -7.826019481986000059 ) ) ;
#40498=CARTESIAN_POINT ( 'NONE',  ( 8.528448341230999930, 2.472348777564000066, 6.234194744024999402 ) ) ;
#40501=CARTESIAN_POINT ( 'NONE',  ( 7.742593052214973959, 2.625666041398489359, 7.178124245676486659 ) ) ;
#40521=CARTESIAN_POINT ( 'NONE',  ( 8.079724940884538853, 4.352763894256345800, 8.815588961478567853 ) ) ;
#40522=CARTESIAN_POINT ( 'NONE',  ( 9.675534850247000662, 4.656736118461000551, -8.653212384786000300 ) ) ;
#40524=CARTESIAN_POINT ( 'NONE',  ( 27.64127793187000037, 4.599999999999999645, -4.505338571134999803 ) ) ;
#40526=CARTESIAN_POINT ( 'NONE',  ( 8.350387243830999395, 4.599999999999999645, -6.632262360512000576 ) ) ;
#40527=CARTESIAN_POINT ( 'NONE',  ( 9.600491906670001185, 5.206545077004999911, 8.585111878242999595 ) ) ;
#40530=ORIENTED_EDGE ( 'NONE', *, *, #28539, .T. ) ;
#40533=CARTESIAN_POINT ( 'NONE',  ( 10.57224177473000104, 4.020426023752999178, 8.920668579831000145 ) ) ;
#40539=CARTESIAN_POINT ( 'NONE',  ( 9.278329719590999503, 5.791553967443999973, 7.752111263209999770 ) ) ;
#40541=CARTESIAN_POINT ( 'NONE',  ( 10.71756692516999898, 3.040224182812999665, 8.808452309630000698 ) ) ;
#40544=CARTESIAN_POINT ( 'NONE',  ( 10.21398584123000042, 3.990126737362999609, -8.809457313313998839 ) ) ;
#40548=CARTESIAN_POINT ( 'NONE',  ( 3.302853993820082490, -2.804141251808610402, -2.143609296475933679 ) ) ;
#40553=CARTESIAN_POINT ( 'NONE',  ( 1.634474105091999974, -2.924745949230000086, 2.085595834630999956 ) ) ;
#40555=AXIS2_PLACEMENT_3D ( 'NONE', #68984, #62700, #63730 ) ;
#40557=LINE ( 'NONE', #56643, #64429 ) ;
#40559=CARTESIAN_POINT ( 'NONE',  ( 10.18240541510999897, 2.607737086676999994, 7.783408568367999436 ) ) ;
#40564=EDGE_LOOP ( 'NONE', ( #44382, #54582, #25603, #32672 ) ) ;
#40565=CARTESIAN_POINT ( 'NONE',  ( 7.866204719590000671, 4.580608786027000612, 9.213365309690999538 ) ) ;
#40566=ADVANCED_FACE ( 'NONE', ( #44459 ), #28218, .F. ) ;
#40570=CARTESIAN_POINT ( 'NONE',  ( 1.886293599501000173, -2.100427248507999778, 2.706108474410000131 ) ) ;
#40571=ORIENTED_EDGE ( 'NONE', *, *, #37311, .T. ) ;
#40572=CARTESIAN_POINT ( 'NONE',  ( 0.8095474569573147816, 3.020249054117508436, 1.336761677555526218 ) ) ;
#40573=B_SPLINE_CURVE_WITH_KNOTS ( 'NONE', 3,
 ( #8313, #3058, #30333, #25417 ),
 .UNSPECIFIED., .F., .F.,
 ( 4, 4 ),
 ( 0.6083653520376346435, 1.000000000000000000 ),
 .UNSPECIFIED. ) ;
#40576=CARTESIAN_POINT ( 'NONE',  ( 9.332933391271998502, 5.100349772922000646, 8.693467186193998941 ) ) ;
#40584=EDGE_CURVE ( 'NONE', #19975, #53136, #64401, .T. ) ;
#40585=CARTESIAN_POINT ( 'NONE',  ( 7.866984495661538013, 3.121299587659922103, 9.063503846007870735 ) ) ;
#40591=ORIENTED_EDGE ( 'NONE', *, *, #8194, .T. ) ;
#40596=CARTESIAN_POINT ( 'NONE',  ( 9.910790522921001156, 3.869345236050000025, 5.882548872612999524 ) ) ;
#40597=CARTESIAN_POINT ( 'NONE',  ( 10.91943903453000075, 3.268382602297999817, -6.413946631105000407 ) ) ;
#40608=CARTESIAN_POINT ( 'NONE',  ( 5.000030787343002103, 2.099962892531005654, -0.2748844998327801270 ) ) ;
#40619=CARTESIAN_POINT ( 'NONE',  ( 8.486008579191000933, 3.399999999999999911, 5.976611076844000614 ) ) ;
#40622=CARTESIAN_POINT ( 'NONE',  ( 8.070721554491719019, 3.646115526505103510, 8.813957122113052378 ) ) ;
#40623=CARTESIAN_POINT ( 'NONE',  ( 5.000000000000000000, 0.2999999999999999889, -9.776630298829998011 ) ) ;
#40626=CARTESIAN_POINT ( 'NONE',  ( 8.436987556243993325, 2.901283824935000144, -6.624026488670998525 ) ) ;
#40630=CARTESIAN_POINT ( 'NONE',  ( 10.98768472569999943, 5.449702578894000560, 4.945212061318999375 ) ) ;
#40637=CARTESIAN_POINT ( 'NONE',  ( 11.09999999999999964, 4.000000000000000000, -7.500000000000000000 ) ) ;
#40649=CARTESIAN_POINT ( 'NONE',  ( 2.511390132542666631, 3.499999999999998224, 0.4581489286485194157 ) ) ;
#40651=FACE_OUTER_BOUND ( 'NONE', #4002, .T. ) ;
#40654=CARTESIAN_POINT ( 'NONE',  ( 9.050809142811473862, 5.350259454271556692, -7.263208790141661986 ) ) ;
#40661=CARTESIAN_POINT ( 'NONE',  ( 2.842640132544666631, -3.058252359239902685, -1.762666431298148595 ) ) ;
#40662=CARTESIAN_POINT ( 'NONE',  ( 9.021064158776001207, 4.883347899767999323, -6.417062834774999835 ) ) ;
#40663=CARTESIAN_POINT ( 'NONE',  ( 8.679055905797000037, 2.899999999999999911, 6.571291218949999902 ) ) ;
#40667=ORIENTED_EDGE ( 'NONE', *, *, #68106, .T. ) ;
#40669=CARTESIAN_POINT ( 'NONE',  ( 8.591232269961365020, 3.293719616469499289, 8.705632950218131327 ) ) ;
#40671=CARTESIAN_POINT ( 'NONE',  ( 8.514954719592999766, 3.207599814920999659, -6.150466394809999571 ) ) ;
#40676=LINE ( 'NONE', #57435, #10286 ) ;
#40678=ORIENTED_EDGE ( 'NONE', *, *, #58006, .T. ) ;
#40681=CARTESIAN_POINT ( 'NONE',  ( 9.038304719595000591, 3.867331042029999999, -9.227339949050001877 ) ) ;
#40682=EDGE_LOOP ( 'NONE', ( #8927, #49104, #38333, #65521 ) ) ;
#40684=CARTESIAN_POINT ( 'NONE',  ( 10.68055531501999944, 2.768167480619000198, -6.114404645958000373 ) ) ;
#40690=CARTESIAN_POINT ( 'NONE',  ( 8.551536913492149949, 3.201507455693337612, 5.984856406915247007 ) ) ;
#40693=CARTESIAN_POINT ( 'NONE',  ( 11.14451084122999980, 5.035416949823999566, -8.381520599479999944 ) ) ;
#40694=CIRCLE ( 'NONE', #13910, 3.200000000000000178 ) ;
#40706=CARTESIAN_POINT ( 'NONE',  ( 10.19741084123000086, 4.262870449202000422, -8.811513791423999820 ) ) ;
#40707=DIRECTION ( 'NONE',  ( -1.000000000000000000, 0.000000000000000000, 0.000000000000000000 ) ) ;
#40711=DIRECTION ( 'NONE',  ( 0.000000000000000000, -0.9916377111174247139, 0.1290528957048031888 ) ) ;
#40712=AXIS2_PLACEMENT_3D ( 'NONE', #28115, #49426, #1539 ) ;
#40714=CARTESIAN_POINT ( 'NONE',  ( 7.785640454728832260, 3.765028847004302293, 6.163541840524195514 ) ) ;
#40723=CARTESIAN_POINT ( 'NONE',  ( 9.839810841229999383, 5.817107086401000160, -6.945352709928000579 ) ) ;
#40724=EDGE_CURVE ( 'NONE', #24902, #43188, #37146, .T. ) ;
#40733=CARTESIAN_POINT ( 'NONE',  ( 3.587066914515000260, -2.899936811858999874, -1.487130161374000004 ) ) ;
#40738=CARTESIAN_POINT ( 'NONE',  ( 8.513426658773999733, 5.040787533781999841, 8.522957620707000359 ) ) ;
#40740=ORIENTED_EDGE ( 'NONE', *, *, #26798, .F. ) ;
#40745=CARTESIAN_POINT ( 'NONE',  ( 7.856851002541000106, 2.832432432432000269, -6.822293592207000934 ) ) ;
#40751=CARTESIAN_POINT ( 'NONE',  ( 9.110944094209999733, 5.100000000000000533, -6.571291218949999902 ) ) ;
#40753=VECTOR ( 'NONE', #36426, 1000.000000000000114 ) ;
#40758=CARTESIAN_POINT ( 'NONE',  ( 6.745189158770999782, 3.508889101792000087, -8.808374944720000599 ) ) ;
#40759=CARTESIAN_POINT ( 'NONE',  ( 8.350387243830999395, 3.399999999999999911, 6.632262360512000576 ) ) ;
#40762=CARTESIAN_POINT ( 'NONE',  ( 2.250973465874000379, -3.500000000000000000, 0.000000000000000000 ) ) ;
#40777=ORIENTED_EDGE ( 'NONE', *, *, #60224, .T. ) ;
#40778=CARTESIAN_POINT ( 'NONE',  ( 10.81579666500999970, 5.374569445151000657, 6.698728322222000209 ) ) ;
#40781=CARTESIAN_POINT ( 'NONE',  ( 8.789679719592999874, 4.162493982103000256, -5.775210092227999858 ) ) ;
#40782=CARTESIAN_POINT ( 'NONE',  ( 2.935841626129000126, 1.641030631418000096, -3.325153953193000333 ) ) ;
#40787=EDGE_CURVE ( 'NONE', #5467, #63876, #12549, .T. ) ;
#40788=ORIENTED_EDGE ( 'NONE', *, *, #4327, .F. ) ;
#40791=CARTESIAN_POINT ( 'NONE',  ( 10.59536758177122096, 2.228958812539000522, -7.375678105216161740 ) ) ;
#40793=CARTESIAN_POINT ( 'NONE',  ( 10.81746213571000048, 5.100000000000000533, 6.571291218949999902 ) ) ;
#40794=CARTESIAN_POINT ( 'NONE',  ( 9.228133567168001150, 2.875367362387999837, 8.669940206484001877 ) ) ;
#40807=CARTESIAN_POINT ( 'NONE',  ( 4.000000000000000000, 0.5625597044909160793, -2.094005558844440618 ) ) ;
#40808=CARTESIAN_POINT ( 'NONE',  ( 10.40685100253999984, 2.832432432432000269, -6.822293592207000934 ) ) ;
#40811=CARTESIAN_POINT ( 'NONE',  ( 7.743176658771999676, 2.735218126362000124, 6.771983639047999937 ) ) ;
#40814=CARTESIAN_POINT ( 'NONE',  ( 9.991525552923999243, 4.805950298207000593, -8.932431532051998246 ) ) ;
#40820=CARTESIAN_POINT ( 'NONE',  ( 8.221179504219003675, 3.443168248977001245, 6.131664885159996636 ) ) ;
#40823=CYLINDRICAL_SURFACE ( 'NONE', #12797, 2.000000000000000000 ) ;
#40830=B_SPLINE_CURVE_WITH_KNOTS ( 'NONE', 3,
 ( #29922, #20095, #2981, #45648, #66954, #19061, #62730, #25337, #61711, #19407, #51560, #3325, #25680, #46675, #35833, #46329, #24657, #51901 ),
 .UNSPECIFIED., .F., .F.,
 ( 4, 2, 2, 2, 2, 2, 2, 2, 4 ),
 ( 0.000000000000000000, 0.1249999999999999722, 0.2499999999999999445, 0.3749999999999998890, 0.4999999999999998890, 0.6249999999999998890, 0.7499999999999998890, 0.8750000000000000000, 1.000000000000000000 ),
 .UNSPECIFIED. ) ;
#40842=CARTESIAN_POINT ( 'NONE',  ( 7.950760841228999176, 2.095715612964000218, 8.056490963156001328 ) ) ;
#40843=EDGE_LOOP ( 'NONE', ( #25825, #51480, #34031, #63007, #53997, #45795, #52629 ) ) ;
#40844=B_SPLINE_CURVE_WITH_KNOTS ( 'NONE', 3,
 ( #54585, #49331, #44109, #44462 ),
 .UNSPECIFIED., .F., .F.,
 ( 4, 4 ),
 ( 0.000000000000000000, 1.000000000000000000 ),
 .UNSPECIFIED. ) ;
#40851=VECTOR ( 'NONE', #57615, 999.9999999999998863 ) ;
#40860=B_SPLINE_CURVE_WITH_KNOTS ( 'NONE', 3,
 ( #68283, #46641, #51530, #35464 ),
 .UNSPECIFIED., .F., .F.,
 ( 4, 4 ),
 ( 0.000000000000000000, 1.000000000000000000 ),
 .UNSPECIFIED. ) ;
#40861=DIRECTION ( 'NONE',  ( 0.000000000000000000, 0.000000000000000000, -1.000000000000000000 ) ) ;
#40864=CARTESIAN_POINT ( 'NONE',  ( 7.099999886593999499, 1.243449787579999883E-13, -1.714758320200999846E-13 ) ) ;
#40868=CARTESIAN_POINT ( 'NONE',  ( 10.61721774768000159, 5.045603402166999985, -6.386910706193999587 ) ) ;
#40873=CARTESIAN_POINT ( 'NONE',  ( 10.96580581817999978, 4.930645553951000792, 6.170542400361000546 ) ) ;
#40877=ADVANCED_FACE ( 'NONE', ( #54032 ), #43556, .T. ) ;
#40881=CARTESIAN_POINT ( 'NONE',  ( 11.18706938844999854, 3.186790175674999670, 6.232702730851999995 ) ) ;
#40886=AXIS2_PLACEMENT_3D ( 'NONE', #10220, #47288, #64718 ) ;
#40887=CARTESIAN_POINT ( 'NONE',  ( 8.610051658774001027, 5.329437560656000272, 6.027391099688998999 ) ) ;
#40888=CARTESIAN_POINT ( 'NONE',  ( 10.87021720923999979, 2.226038107033000202, 7.782753921296999167 ) ) ;
#40890=EDGE_LOOP ( 'NONE', ( #66065, #58345, #31747, #31087 ) ) ;
#40891=CARTESIAN_POINT ( 'NONE',  ( 8.789679719592999874, 4.162493982103000256, -5.775210092227999858 ) ) ;
#40896=CARTESIAN_POINT ( 'NONE',  ( 8.216851002544000693, 2.832432432432000269, 6.822293592207000934 ) ) ;
#40900=AXIS2_PLACEMENT_3D ( 'NONE', #48293, #65748, #6320 ) ;
#40901=CARTESIAN_POINT ( 'NONE',  ( 0.9621534748591999975, 2.512752844666000129, -2.494243791339000094 ) ) ;
#40903=CARTESIAN_POINT ( 'NONE',  ( 9.686609873374599999, 5.723279044498072565, 7.204524705702328724 ) ) ;
#40909=CARTESIAN_POINT ( 'NONE',  ( 9.970944094204998720, 5.100000000000000533, 6.571291218949999902 ) ) ;
#40912=CARTESIAN_POINT ( 'NONE',  ( 9.395323341230000125, 5.146726419831999522, 6.597424767138000412 ) ) ;
#40914=FACE_OUTER_BOUND ( 'NONE', #24418, .T. ) ;
#40917=CARTESIAN_POINT ( 'NONE',  ( 0.9326546106848000450, -3.242811033061999915, 1.104080751309999942 ) ) ;
#40919=DIRECTION ( 'NONE',  ( 0.000000000000000000, 1.000000000000000000, 0.000000000000000000 ) ) ;
#40922=CARTESIAN_POINT ( 'NONE',  ( 11.18484176840999922, 2.599663474744000169, 7.740674686800000259 ) ) ;
#40929=CARTESIAN_POINT ( 'NONE',  ( 7.586311969103031849, 4.230699495907120244, 5.772666978407863247 ) ) ;
#40935=CARTESIAN_POINT ( 'NONE',  ( 9.049999337612000261, 3.268496584495999908E-13, 3.612668863294000056E-14 ) ) ;
#40940=CARTESIAN_POINT ( 'NONE',  ( 9.352253013669001191, 2.817757427878999632, 6.388459691516000127 ) ) ;
#40941=CARTESIAN_POINT ( 'NONE',  ( 10.81362367151999848, 3.876947539724999725, -9.022206283674000460 ) ) ;
#40946=CARTESIAN_POINT ( 'NONE',  ( 5.500000000000000000, 6.217248937900999058E-14, 3.708144902247999495E-14 ) ) ;
#40948=CARTESIAN_POINT ( 'NONE',  ( 8.175760841228999709, 2.599243720295000060, 7.909344432242998657 ) ) ;
#40955=CARTESIAN_POINT ( 'NONE',  ( 7.608454017953003579, 10.31012780980999999, 5.117594110825002041 ) ) ;
#40963=EDGE_CURVE ( 'NONE', #20386, #3072, #8109, .T. ) ;
#40971=CARTESIAN_POINT ( 'NONE',  ( -0.04643246160058000366, -1.644388561977000007, -3.014063655381999940 ) ) ;
#40977=CARTESIAN_POINT ( 'NONE',  ( 10.41838915877000105, 4.531912033713999755, -9.270484952459998595 ) ) ;
#40984=AXIS2_PLACEMENT_3D ( 'NONE', #62791, #14912, #27737 ) ;
#40990=DIRECTION ( 'NONE',  ( 0.000000000000000000, 0.000000000000000000, -1.000000000000000000 ) ) ;
#40991=CARTESIAN_POINT ( 'NONE',  ( 8.186600515489956820, 2.905260986775225707, 6.578663288309482660 ) ) ;
#40996=DIRECTION ( 'NONE',  ( 1.000000000000000000, 0.000000000000000000, 0.000000000000000000 ) ) ;
#41000=CARTESIAN_POINT ( 'NONE',  ( 11.09999999999999964, 10.03015638309000046, -5.726993439934999763 ) ) ;
#41003=CIRCLE ( 'NONE', #62267, 3.200000000000000178 ) ;
#41011=CARTESIAN_POINT ( 'NONE',  ( 2.396856900172125382, 0.9112004763889646197, -3.396138185504796070 ) ) ;
#41012=CARTESIAN_POINT ( 'NONE',  ( 9.369139158774000720, 2.685250982074999904, -7.026194612421999608 ) ) ;
#41013=CARTESIAN_POINT ( 'NONE',  ( 8.721802827889733933, 2.874603711573444187, 6.749639981083119800 ) ) ;
#41015=CARTESIAN_POINT ( 'NONE',  ( 4.000000000000000000, -1.719428477288966750, 1.321180510578594536 ) ) ;
#41021=CARTESIAN_POINT ( 'NONE',  ( 10.15596191468078224, 2.820845708124703144, -6.216775022417006191 ) ) ;
#41028=CARTESIAN_POINT ( 'NONE',  ( 9.585279719593998493, 2.928319778732999978, -8.861178115809998701 ) ) ;
#41029=ORIENTED_EDGE ( 'NONE', *, *, #60447, .F. ) ;
#41030=AXIS2_PLACEMENT_3D ( 'NONE', #25257, #35078, #24228 ) ;
#41031=CARTESIAN_POINT ( 'NONE',  ( 10.04002816746000093, 2.348904337896000172, -7.136750921008999882 ) ) ;
#41032=ORIENTED_EDGE ( 'NONE', *, *, #44643, .T. ) ;
#41038=CARTESIAN_POINT ( 'NONE',  ( 8.433148997460000018, 5.167567567567999731, 6.822293592207000934 ) ) ;
#41040=CARTESIAN_POINT ( 'NONE',  ( 9.856463691914767011, 5.100000000000000533, 6.665341197415451724 ) ) ;
#41043=CARTESIAN_POINT ( 'NONE',  ( 8.972537864292000620, 2.899999999999999911, -6.571291218949999902 ) ) ;
#41048=CARTESIAN_POINT ( 'NONE',  ( 9.160535748954998780, 2.900115872948000106, -6.152093930328999427 ) ) ;
#41050=CARTESIAN_POINT ( 'NONE',  ( 7.831595309934897386, 4.878214714082836245, 6.417939907564524482 ) ) ;
#41054=CARTESIAN_POINT ( 'NONE',  ( 9.915635841230999503, 3.210851187372000037, -6.346613542714999667 ) ) ;
#41055=DIRECTION ( 'NONE',  ( 0.000000000000000000, -0.2461538461537955136, -0.9692307692307821076 ) ) ;
#41058=CARTESIAN_POINT ( 'NONE',  ( 7.860744422257667452, 4.181951828900120738, 6.138447713083068358 ) ) ;
#41062=CYLINDRICAL_SURFACE ( 'NONE', #34011, 1.350000000000000533 ) ;
#41063=CARTESIAN_POINT ( 'NONE',  ( 7.800894426331000275, 3.218815461055000160, 6.398977422524000147 ) ) ;
#41064=ORIENTED_EDGE ( 'NONE', *, *, #31530, .F. ) ;
#41069=CARTESIAN_POINT ( 'NONE',  ( 10.90000000000000036, 0.2999999999999999889, -4.902439024389999567 ) ) ;
#41072=CARTESIAN_POINT ( 'NONE',  ( 8.447510841229000533, 4.933589693325000525, -9.154576215408999573 ) ) ;
#41079=CARTESIAN_POINT ( 'NONE',  ( 0.1625046544502119494, 1.591888665051217622, -2.763666953839243323 ) ) ;
#41085=CARTESIAN_POINT ( 'NONE',  ( 8.703529634540137394, 5.100000000000000533, -6.308756105309840656 ) ) ;
#41091=CARTESIAN_POINT ( 'NONE',  ( 0.5107036710124341905, 3.504666613735739400, 0.4180694620915118564 ) ) ;
#41094=AXIS2_PLACEMENT_3D ( 'NONE', #46420, #61127, #34569 ) ;
#41096=ORIENTED_EDGE ( 'NONE', *, *, #14797, .F. ) ;
#41098=B_SPLINE_CURVE_WITH_KNOTS ( 'NONE', 3,
 ( #33, #38471, #11207, #11542, #43026, #58755, #16449, #54196, #16790, #6649, #59791, #48621 ),
 .UNSPECIFIED., .F., .F.,
 ( 4, 2, 2, 2, 2, 4 ),
 ( 0.000000000000000000, 0.2500000000000179856, 0.3750000000000235922, 0.4375000000000248135, 0.5000000000000259792, 1.000000000000000000 ),
 .UNSPECIFIED. ) ;
#41104=EDGE_CURVE ( 'NONE', #57460, #27251, #5961, .T. ) ;
#41106=CARTESIAN_POINT ( 'NONE',  ( -0.000000000000000000, 0.7585797238574916168, -2.824612379753442148 ) ) ;
#41107=CARTESIAN_POINT ( 'NONE',  ( 0.000000000000000000, 0.000000000000000000, 0.000000000000000000 ) ) ;
#41108=CARTESIAN_POINT ( 'NONE',  ( 7.970595280405999183, 2.627120679234999923, -8.556648795244999661 ) ) ;
#41116=CARTESIAN_POINT ( 'NONE',  ( 9.143998948451265818, 2.899999999999999911, 6.465127702479446015 ) ) ;
#41117=B_SPLINE_CURVE_WITH_KNOTS ( 'NONE', 3,
 ( #68304, #47691, #31609, #58511 ),
 .UNSPECIFIED., .F., .F.,
 ( 4, 4 ),
 ( 0.000000000000000000, 1.000000000000000000 ),
 .UNSPECIFIED. ) ;
#41118=CARTESIAN_POINT ( 'NONE',  ( 10.76685100253999927, 2.832432432432000269, 6.822293592207000934 ) ) ;
#41120=PRODUCT_DEFINITION_SHAPE ( 'NONE', 'NONE',  #39365 ) ;
#41121=CARTESIAN_POINT ( 'NONE',  ( 10.66153368166920679, 5.571142525177961602, 6.679759109773798720 ) ) ;
#41124=CARTESIAN_POINT ( 'NONE',  ( 8.356851002541000994, 2.832432432432000269, -6.822293592207000934 ) ) ;
#41128=ADVANCED_FACE ( 'NONE', ( #33591 ), #59491, .F. ) ;
#41133=CARTESIAN_POINT ( 'NONE',  ( 9.569805421428000614, 4.064052243276000453, 8.919241792616000808 ) ) ;
#41135=CARTESIAN_POINT ( 'NONE',  ( 8.491329719591000469, 4.851303550474000303, -9.008742670124000540 ) ) ;
#41137=CARTESIAN_POINT ( 'NONE',  ( 3.103509480039000401, 2.020192966679000168, 3.109413244175000202 ) ) ;
#41145=CARTESIAN_POINT ( 'NONE',  ( 10.54648703831772316, 2.506660384375831718, -8.410204393717869209 ) ) ;
#41147=FACE_OUTER_BOUND ( 'NONE', #60755, .T. ) ;
#41148=CARTESIAN_POINT ( 'NONE',  ( 10.12550053024000007, 5.788811067708000024, 7.335561454339999621 ) ) ;
#41152=ADVANCED_FACE ( 'NONE', ( #59456 ), #64693, .F. ) ;
#41155=AXIS2_PLACEMENT_3D ( 'NONE', #53323, #59592, #5423 ) ;
#41169=CARTESIAN_POINT ( 'NONE',  ( 10.78888278041000071, 2.675726696512000125, -6.748227692827999391 ) ) ;
#41183=CARTESIAN_POINT ( 'NONE',  ( 7.000002934099999408, 1.243449787579999883E-13, -1.714942011622999690E-13 ) ) ;
#41190=CARTESIAN_POINT ( 'NONE',  ( 2.498890132543458709, 2.798833948393634419, -2.150913519912196925 ) ) ;
#41196=CARTESIAN_POINT ( 'NONE',  ( 7.694010841228000608, 5.850290547079999293, 6.784176679236000318 ) ) ;
#41201=ORIENTED_EDGE ( 'NONE', *, *, #53455, .F. ) ;
#41205=CARTESIAN_POINT ( 'NONE',  ( 11.27712163255998412, 9.461969908151001363, -6.800304254993005948 ) ) ;
#41218=CARTESIAN_POINT ( 'NONE',  ( 9.988718791410999387, 2.842026940133999702, -6.504333051298999635 ) ) ;
#41222=CARTESIAN_POINT ( 'NONE',  ( 9.124700695083998170, 4.778663323155000420, 8.799742559280000265 ) ) ;
#41227=CARTESIAN_POINT ( 'NONE',  ( 9.834151567923001380, 5.173929249342999803, 8.813048229486998508 ) ) ;
#41229=CARTESIAN_POINT ( 'NONE',  ( 9.617285841233000454, 5.306366356490000769, -7.996450761531000317 ) ) ;
#41230=CARTESIAN_POINT ( 'NONE',  ( 10.96416317549000041, 7.893339070327000329, -6.439103628860999962 ) ) ;
#41235=CARTESIAN_POINT ( 'NONE',  ( 9.538432183420001209, 5.620896541217999420, 7.423100299691999915 ) ) ;
#41238=CARTESIAN_POINT ( 'NONE',  ( 9.128895280414001334, 3.880154689736000417, -9.060377011187000562 ) ) ;
#41239=CARTESIAN_POINT ( 'NONE',  ( -2.444943969992999916E-05, -2.899969545325999931, 0.000000000000000000 ) ) ;
#41245=CARTESIAN_POINT ( 'NONE',  ( 1.915792463674000023, 0.7707009544374999743, -3.678912518181000291 ) ) ;
#41247=CARTESIAN_POINT ( 'NONE',  ( 9.152446624286001864, 2.899999999999999911, -6.169193161299999950 ) ) ;
#41248=DIRECTION ( 'NONE',  ( 0.000000000000000000, 0.000000000000000000, -1.000000000000000000 ) ) ;
#41250=CARTESIAN_POINT ( 'NONE',  ( 10.38314899745999931, 5.167567567567999731, 6.822293592207000934 ) ) ;
#41256=CARTESIAN_POINT ( 'NONE',  ( 7.764232780408999446, 4.628941086829000184, 5.991667691044999522 ) ) ;
#41259=VECTOR ( 'NONE', #54670, 1000.000000000000114 ) ;
#41262=CARTESIAN_POINT ( 'NONE',  ( 1.748021089240999970, -0.2184777168079999887, 3.585542759708000293 ) ) ;
#41264=CARTESIAN_POINT ( 'NONE',  ( 1.143321103043043463, -0.3342943453538773646, -3.285837508824063224 ) ) ;
#41266=CARTESIAN_POINT ( 'NONE',  ( 9.595493858556999101, 3.928424745541000185, 5.531312048131000303 ) ) ;
#41267=CARTESIAN_POINT ( 'NONE',  ( 10.76010575649000067, 4.535386075958999896, 6.001721352166000223 ) ) ;
#41271=EDGE_CURVE ( 'NONE', #4517, #7244, #52652, .T. ) ;
#41287=CARTESIAN_POINT ( 'NONE',  ( 9.414312736919001168, 3.941041961981000430, 5.878350450964999752 ) ) ;
#41288=CARTESIAN_POINT ( 'NONE',  ( 10.31499646082999888, 5.458376174241999834, -8.355105941236999456 ) ) ;
#41296=ORIENTED_EDGE ( 'NONE', *, *, #1037, .T. ) ;
#41300=DIRECTION ( 'NONE',  ( 1.000000000000000000, 0.000000000000000000, 0.000000000000000000 ) ) ;
#41307=DIRECTION ( 'NONE',  ( 1.000000000000000000, 0.000000000000000000, 0.000000000000000000 ) ) ;
#41312=FACE_OUTER_BOUND ( 'NONE', #12580, .T. ) ;
#41318=CARTESIAN_POINT ( 'NONE',  ( 10.98768472639999949, 2.860903110339000133, 4.945212061661000469 ) ) ;
#41319=EDGE_CURVE ( 'NONE', #50139, #6099, #39282, .T. ) ;
#41321=DIRECTION ( 'NONE',  ( 0.000000000000000000, -0.8648648648648720183, 0.5020047465136825426 ) ) ;
#41324=CARTESIAN_POINT ( 'NONE',  ( 10.24394221959000184, 3.220342255699999878, -6.005413528376000620 ) ) ;
#41326=DIRECTION ( 'NONE',  ( 0.9999999999999682476, 2.518941077746920288E-07, -2.686336010433915230E-09 ) ) ;
#41329=ORIENTED_EDGE ( 'NONE', *, *, #12873, .F. ) ;
#41338=CARTESIAN_POINT ( 'NONE',  ( 8.159770655660624428, 3.206342737484559002, 6.208500430850088847 ) ) ;
#41346=CARTESIAN_POINT ( 'NONE',  ( 2.584306799209334038, 1.762666431298138825, 3.058252359239908014 ) ) ;
#41348=EDGE_CURVE ( 'NONE', #15832, #67676, #48318, .T. ) ;
#41352=CARTESIAN_POINT ( 'NONE',  ( 9.573148997458000409, 5.167567567567999731, -6.822293592207000934 ) ) ;
#41362=ORIENTED_EDGE ( 'NONE', *, *, #14440, .F. ) ;
#41373=ORIENTED_EDGE ( 'NONE', *, *, #16001, .T. ) ;
#41374=CARTESIAN_POINT ( 'NONE',  ( 5.000000000000000000, 0.8000000000000000444, -3.149999999999999911 ) ) ;
#41375=CARTESIAN_POINT ( 'NONE',  ( 9.137754719594999742, 2.319062457810000311, -7.919229449146000022 ) ) ;
#41376=ORIENTED_EDGE ( 'NONE', *, *, #50407, .T. ) ;
#41378=CARTESIAN_POINT ( 'NONE',  ( 11.15192953222999961, 2.359300361215999953, -6.636686939130999718 ) ) ;
#41383=CARTESIAN_POINT ( 'NONE',  ( 11.09999938828999966, -12.24999938819000000, -1.815295647579999972E-09 ) ) ;
#41386=ORIENTED_EDGE ( 'NONE', *, *, #23270, .T. ) ;
#41387=CARTESIAN_POINT ( 'NONE',  ( 10.22422653164065487, 2.899999999999999911, -6.304440313833538312 ) ) ;
#41389=CARTESIAN_POINT ( 'NONE',  ( 5.500000000000000000, 0.000000000000000000, 0.000000000000000000 ) ) ;
#41393=AXIS2_PLACEMENT_3D ( 'NONE', #29119, #11628, #7780 ) ;
#41400=CARTESIAN_POINT ( 'NONE',  ( 9.178620280414001797, 2.990001567622999623, -8.695425648791999862 ) ) ;
#41402=CARTESIAN_POINT ( 'NONE',  ( 4.650001657043312697, -2.000000000000000000, -2.821984759847882640E-09 ) ) ;
#41408=CARTESIAN_POINT ( 'NONE',  ( 8.852883527364793892, 3.390765634497458159, 9.167735097122442056 ) ) ;
#41409=CARTESIAN_POINT ( 'NONE',  ( 11.00000000000000000, 5.200000000000000178, -5.865766984179000332 ) ) ;
#41417=CARTESIAN_POINT ( 'NONE',  ( 8.646410841231000788, 2.261390688294000029, -6.733978371730000134 ) ) ;
#41419=CARTESIAN_POINT ( 'NONE',  ( 7.969586219655325543, 2.977443839350291555, -6.507548348051052756 ) ) ;
#41420=LINE ( 'NONE', #67631, #35608 ) ;
#41423=CARTESIAN_POINT ( 'NONE',  ( 2.728791824580000025, 2.059424881456000112, -2.525877225825000405 ) ) ;
#41427=CARTESIAN_POINT ( 'NONE',  ( 8.757697342472001267, 2.899999999999999911, -6.397101765418000241 ) ) ;
#41429=CARTESIAN_POINT ( 'NONE',  ( 1.759306799208166350, -3.058252359239909346, 1.762666431298136605 ) ) ;
#41430=ORIENTED_EDGE ( 'NONE', *, *, #2048, .F. ) ;
#41435=EDGE_CURVE ( 'NONE', #3245, #5981, #17617, .T. ) ;
#41438=CARTESIAN_POINT ( 'NONE',  ( 7.790487273278715818, 2.917542662690631339, 6.652519583927194446 ) ) ;
#41442=EDGE_LOOP ( 'NONE', ( #42200, #3705, #20113, #32768, #17710, #26813, #62885, #54894, #35206, #9569, #63454, #17598 ) ) ;
#41447=CARTESIAN_POINT ( 'NONE',  ( 8.591652855523911114, 2.244927656352591505, -7.464460470874615616 ) ) ;
#41448=CARTESIAN_POINT ( 'NONE',  ( 9.074999999999999289, 4.417172942406000224, 8.783926296998000538 ) ) ;
#41449=VECTOR ( 'NONE', #49031, 1000.000000000000000 ) ;
#41450=CARTESIAN_POINT ( 'NONE',  ( 6.844639158771000709, 2.603491674958000157, -7.446887986542999549 ) ) ;
#41454=CARTESIAN_POINT ( 'NONE',  ( 2.021806799206416372, 3.408904368339103375, 0.9161175952574877046 ) ) ;
#41457=ORIENTED_EDGE ( 'NONE', *, *, #43653, .F. ) ;
#41461=ORIENTED_EDGE ( 'NONE', *, *, #8276, .T. ) ;
#41462=CARTESIAN_POINT ( 'NONE',  ( 10.98194940877535863, 2.363165821928819188, 6.818563111302845314 ) ) ;
#41463=ADVANCED_FACE ( 'NONE', ( #14249 ), #57926, .T. ) ;
#41473=CARTESIAN_POINT ( 'NONE',  ( 10.25888757983999966, 4.512388525173999909, 5.993701490107000929 ) ) ;
#41474=CARTESIAN_POINT ( 'NONE',  ( 11.04384236319999957, 5.374507068257000419, 5.035088906224999938 ) ) ;
#41476=CARTESIAN_POINT ( 'NONE',  ( 3.683590334856999604, -3.383589507348999881, 0.007585966762053000974 ) ) ;
#41479=FACE_OUTER_BOUND ( 'NONE', #32936, .T. ) ;
#41485=CARTESIAN_POINT ( 'NONE',  ( 9.215291255903000689, 4.861981595026999337, 8.938817176893000038 ) ) ;
#41492=AXIS2_PLACEMENT_3D ( 'NONE', #34656, #3502, #24840 ) ;
#41500=CARTESIAN_POINT ( 'NONE',  ( 0.3621912743483999830, 0.6171034757514999303, 3.149659041885999766 ) ) ;
#41503=CARTESIAN_POINT ( 'NONE',  ( 10.92546721959000067, 5.641524285727999910, -7.883474821562000301 ) ) ;
#41504=ORIENTED_EDGE ( 'NONE', *, *, #5813, .T. ) ;
#41509=CARTESIAN_POINT ( 'NONE',  ( 7.437260841228000352, 2.216873702600000051, 8.370081218683999680 ) ) ;
#41510=ORIENTED_EDGE ( 'NONE', *, *, #6525, .T. ) ;
#41513=EDGE_CURVE ( 'NONE', #33524, #17499, #46131, .T. ) ;
#41514=CARTESIAN_POINT ( 'NONE',  ( 8.395639158770999089, 4.988620887051999908, -9.026201633254999024 ) ) ;
#41520=ORIENTED_EDGE ( 'NONE', *, *, #19754, .F. ) ;
#41532=AXIS2_PLACEMENT_3D ( 'NONE', #40413, #66640, #34841 ) ;
#41535=VERTEX_POINT ( 'NONE', #31360 ) ;
#41541=CARTESIAN_POINT ( 'NONE',  ( 2.479064736456999540, 3.399126080497508973, -0.9633645835951678560 ) ) ;
#41549=EDGE_LOOP ( 'NONE', ( #5156, #29044, #66336, #16958 ) ) ;
#41555=CARTESIAN_POINT ( 'NONE',  ( 10.62924593896999959, 3.609487840896999700, -5.855139066690000504 ) ) ;
#41560=CARTESIAN_POINT ( 'NONE',  ( 10.74609776273999984, 4.263105564403999459, 9.276980853981999786 ) ) ;
#41562=CARTESIAN_POINT ( 'NONE',  ( 9.094793214210151078, 2.227663154009282831, -7.390522279650845405 ) ) ;
#41566=CARTESIAN_POINT ( 'NONE',  ( 10.30047009227000032, 4.027768540959000276, 9.431354536774000152 ) ) ;
#41569=CARTESIAN_POINT ( 'NONE',  ( 11.01765929220000118, 7.436533042258000492, -6.255518063588999311 ) ) ;
#41572=EDGE_CURVE ( 'NONE', #57358, #23058, #8991, .T. ) ;
#41575=CARTESIAN_POINT ( 'NONE',  ( 10.37873747135000002, 4.882725050998000249, 6.350806206758999650 ) ) ;
#41577=ORIENTED_EDGE ( 'NONE', *, *, #16966, .T. ) ;
#41578=CARTESIAN_POINT ( 'NONE',  ( 8.541054719591000932, 3.807713920470999991, -9.221758713517999695 ) ) ;
#41579=CARTESIAN_POINT ( 'NONE',  ( -0.000000000000000000, -1.460960874861672476, 2.533832635912068643 ) ) ;
#41581=CARTESIAN_POINT ( 'NONE',  ( 9.167308658909917085, 5.079249101950133571, -8.329436424852559639 ) ) ;
#41586=CARTESIAN_POINT ( 'NONE',  ( 1.534336868148000077, 3.729267013836000011, 0.4700476753697999666 ) ) ;
#41587=CARTESIAN_POINT ( 'NONE',  ( 7.629823341228000544, 4.763536573491999881, 5.668879554882000349 ) ) ;
#41589=CARTESIAN_POINT ( 'NONE',  ( 9.792620004638278530, 4.710589479228226573, 9.124905218709104204 ) ) ;
#41590=LINE ( 'NONE', #15367, #58857 ) ;
#41599=CARTESIAN_POINT ( 'NONE',  ( 8.443892219592001425, 2.905861847853000057, 8.940690431604000565 ) ) ;
#41608=DIRECTION ( 'NONE',  ( 0.000000000000000000, 1.000000000000000000, 0.000000000000000000 ) ) ;
#41609=EDGE_CURVE ( 'NONE', #18530, #16538, #10707, .T. ) ;
#41611=CARTESIAN_POINT ( 'NONE',  ( 9.533434135307000901, 2.564753581125000181, 6.150586364588000343 ) ) ;
#41612=CARTESIAN_POINT ( 'NONE',  ( 10.57892463485000079, 4.649960478797999563, 5.681084732956000138 ) ) ;
#41617=CARTESIAN_POINT ( 'NONE',  ( 11.00270877634999955, 2.832878561424999830, -4.969257129766999626 ) ) ;
#41624=CARTESIAN_POINT ( 'NONE',  ( 8.214872450534432602, 2.885034184131826329, 6.708591157435166430 ) ) ;
#41627=CARTESIAN_POINT ( 'NONE',  ( 10.34520858566999912, 2.724123081339000052, 6.497325124886000225 ) ) ;
#41628=CARTESIAN_POINT ( 'NONE',  ( 10.78637067803999905, 5.666041748529999644, -7.787005432561999285 ) ) ;
#41641=CARTESIAN_POINT ( 'NONE',  ( 8.857252140395999618, 8.766943526461002278, 6.126566717276006102 ) ) ;
#41652=VECTOR ( 'NONE', #19779, 999.9999999999998863 ) ;
#41654=EDGE_CURVE ( 'NONE', #35162, #37966, #59642, .T. ) ;
#41656=CARTESIAN_POINT ( 'NONE',  ( 0.6474295521082999993, 2.420060471650000267, -2.350339292168000416 ) ) ;
#41657=CARTESIAN_POINT ( 'NONE',  ( 7.945608795480783471, 5.314576234847344871, 7.853946780411420470 ) ) ;
#41662=DIRECTION ( 'NONE',  ( -0.7071068341558115478, 0.000000000000000000, -0.7071067282172794899 ) ) ;
#41663=CARTESIAN_POINT ( 'NONE',  ( 10.34266415877000078, 5.750490533313000086, -8.094415907623000450 ) ) ;
#41666=CYLINDRICAL_SURFACE ( 'NONE', #66328, 1.500000000000000000 ) ;
#41694=CARTESIAN_POINT ( 'NONE',  ( 2.427569202129625126, 2.124261041935756378, -2.802062795322278532 ) ) ;
#41696=CARTESIAN_POINT ( 'NONE',  ( 9.012204719595001023, 3.161445734422999809, -6.178649910536000434 ) ) ;
#41701=B_SPLINE_CURVE_WITH_KNOTS ( 'NONE', 3,
 ( #69181, #17071, #58695, #32144 ),
 .UNSPECIFIED., .F., .F.,
 ( 4, 4 ),
 ( 0.000000000000000000, 1.000000000000000000 ),
 .UNSPECIFIED. ) ;
#41708=CARTESIAN_POINT ( 'NONE',  ( 9.243110841233001196, 4.112741311853999271, -5.603466076760000192 ) ) ;
#41709=CARTESIAN_POINT ( 'NONE',  ( 9.709999999999999076, 4.496968146123999865, -8.755198255949000696 ) ) ;
#41710=FACE_OUTER_BOUND ( 'NONE', #14760, .T. ) ;
#41711=DIRECTION ( 'NONE',  ( 1.000000000000000000, 0.000000000000000000, 2.662749306050999794E-14 ) ) ;
#41714=ORIENTED_EDGE ( 'NONE', *, *, #20144, .F. ) ;
#41716=CARTESIAN_POINT ( 'NONE',  ( 9.535554719593998030, 3.927090956378999742, -9.230892435423001530 ) ) ;
#41717=ORIENTED_EDGE ( 'NONE', *, *, #6943, .F. ) ;
#41718=CARTESIAN_POINT ( 'NONE',  ( 9.922184613163000932, 3.489926301007000298, -9.111807643819000546 ) ) ;
#41727=CARTESIAN_POINT ( 'NONE',  ( 8.716308103597052437, 4.026268495047269802, -5.729473523615199682 ) ) ;
#41736=ORIENTED_EDGE ( 'NONE', *, *, #44866, .T. ) ;
#41738=CARTESIAN_POINT ( 'NONE',  ( 9.626145280412998773, 3.934138271021000222, -9.063586117809000697 ) ) ;
#41739=CARTESIAN_POINT ( 'NONE',  ( 10.66052890781999984, 2.899999999999999911, -6.152188490330000370 ) ) ;
#41740=ADVANCED_FACE ( 'NONE', ( #32053 ), #6147, .T. ) ;
#41744=CARTESIAN_POINT ( 'NONE',  ( 11.05851190073833301, 5.258511900738333189, 6.537362761296000357 ) ) ;
#41755=CARTESIAN_POINT ( 'NONE',  ( 7.945227163831277473, 5.100007011413144831, 6.648088212574772449 ) ) ;
#41761=CARTESIAN_POINT ( 'NONE',  ( 7.965310626361219448, 2.964115357972241238, -6.528796737864926314 ) ) ;
#41765=CARTESIAN_POINT ( 'NONE',  ( 3.019656859288000206, -2.470837861336999897, -2.372715509949999912 ) ) ;
#41766=ORIENTED_EDGE ( 'NONE', *, *, #17050, .F. ) ;
#41770=CARTESIAN_POINT ( 'NONE',  ( 3.500000000000000000, 1.113524292603000010, -3.231029921506000324 ) ) ;
#41771=CARTESIAN_POINT ( 'NONE',  ( 10.29214449041363366, 3.170483834885991836, -8.579383242754643035 ) ) ;
#41774=CARTESIAN_POINT ( 'NONE',  ( 0.6675864513507200337, -1.750409042682265159, 3.065373999385508252 ) ) ;
#41776=CARTESIAN_POINT ( 'NONE',  ( 7.698725635631044284, 3.848229261580326188, -8.856856640736939568 ) ) ;
#41778=ORIENTED_EDGE ( 'NONE', *, *, #42234, .F. ) ;
#41788=CARTESIAN_POINT ( 'NONE',  ( 7.976241301082664492, 3.766713024421330047, -6.157346639817824041 ) ) ;
#41789=CARTESIAN_POINT ( 'NONE',  ( 6.935229719590999764, 2.436157974829999961, -7.440523950196999969 ) ) ;
#41793=VERTEX_POINT ( 'NONE', #38314 ) ;
#41798=CARTESIAN_POINT ( 'NONE',  ( 9.051550650638001017, 2.899999999999999911, 6.227445478845999638 ) ) ;
#41799=VECTOR ( 'NONE', #42846, 1000.000000000000000 ) ;
#41805=AXIS2_PLACEMENT_3D ( 'NONE', #22173, #32676, #5062 ) ;
#41807=DIRECTION ( 'NONE',  ( 1.000000000000000000, 0.000000000000000000, 0.000000000000000000 ) ) ;
#41810=ORIENTED_EDGE ( 'NONE', *, *, #39670, .F. ) ;
#41812=EDGE_LOOP ( 'NONE', ( #43522, #63440, #27528, #38663, #23394 ) ) ;
#41813=CARTESIAN_POINT ( 'NONE',  ( 11.09647882763000126, 3.099775370665000196, 6.097099813297999660 ) ) ;
#41814=CARTESIAN_POINT ( 'NONE',  ( 7.000000000000000000, 0.8000000000000000444, 3.149999999999999911 ) ) ;
#41815=CARTESIAN_POINT ( 'NONE',  ( 9.120035841232999374, 5.288433695693000480, -8.041290150997999930 ) ) ;
#41816=CARTESIAN_POINT ( 'NONE',  ( 2.684339845264999802, -1.577989888572000066, 3.355529501073999832 ) ) ;
#41823=CARTESIAN_POINT ( 'NONE',  ( 11.09999987043000047, 10.03015713885000082, 5.726993666320999488 ) ) ;
#41827=CARTESIAN_POINT ( 'NONE',  ( 10.34520858566999912, 2.724123081339000052, 6.497325124886000225 ) ) ;
#41837=ORIENTED_EDGE ( 'NONE', *, *, #15796, .F. ) ;
#41839=DIRECTION ( 'NONE',  ( 0.000000000000000000, -1.000000000000000000, 0.000000000000000000 ) ) ;
#41840=EDGE_CURVE ( 'NONE', #57343, #23533, #31861, .T. ) ;
#41841=CARTESIAN_POINT ( 'NONE',  ( 5.000030787343001215, -2.045306479342562156, -0.5496608443529855670 ) ) ;
#41847=CARTESIAN_POINT ( 'NONE',  ( 10.94033278040999946, 5.142729166069000435, -6.493505370358000128 ) ) ;
#41850=CARTESIAN_POINT ( 'NONE',  ( 8.610875063856999745, 4.757997781751000410, 5.934102420827000124 ) ) ;
#41853=CARTESIAN_POINT ( 'NONE',  ( 8.592635841230999105, 3.856772556595000179, 5.521246073317000125 ) ) ;
#41860=ORIENTED_EDGE ( 'NONE', *, *, #34550, .T. ) ;
#41863=EDGE_LOOP ( 'NONE', ( #18039, #18874, #33828, #5270 ) ) ;
#41864=CARTESIAN_POINT ( 'NONE',  ( 10.98768472639999949, 0.3876847264043000174, 4.945212061661000469 ) ) ;
#41866=EDGE_LOOP ( 'NONE', ( #265, #10615, #30544, #53337, #62812 ) ) ;
#41875=CARTESIAN_POINT ( 'NONE',  ( 7.758198341228000672, 5.797099724369999763, 8.340484548805999765 ) ) ;
#41876=ORIENTED_EDGE ( 'NONE', *, *, #25647, .F. ) ;
#41884=CARTESIAN_POINT ( 'NONE',  ( 11.32777510966000634, 9.448502962084004864, -6.821781130533998372 ) ) ;
#41888=B_SPLINE_CURVE_WITH_KNOTS ( 'NONE', 3,
 ( #36925, #20839, #5097, #42851 ),
 .UNSPECIFIED., .F., .F.,
 ( 4, 4 ),
 ( 0.000000000000000000, 1.000000000000000000 ),
 .UNSPECIFIED. ) ;
#41896=CARTESIAN_POINT ( 'NONE',  ( 9.858847045824999711, 2.668090821818000169, -7.206973500459000093 ) ) ;
#41901=CARTESIAN_POINT ( 'NONE',  ( 10.68403803949000164, 5.436614310638000269, 8.578436083822998270 ) ) ;
#41907=EDGE_CURVE ( 'NONE', #4028, #20987, #37674, .T. ) ;
#41909=CARTESIAN_POINT ( 'NONE',  ( 11.11504246380000005, 3.456610836627000083, 5.970339330302000036 ) ) ;
#41915=CARTESIAN_POINT ( 'NONE',  ( 10.98988709139175945, 3.461087363048998444, -9.181105347514801451 ) ) ;
#41920=CARTESIAN_POINT ( 'NONE',  ( 8.681370280410998674, 2.949305648881000330, -8.659807625323999503 ) ) ;
#41921=CARTESIAN_POINT ( 'NONE',  ( -0.000000000000000000, -2.824745580908275766, 0.7586348975822421181 ) ) ;
#41923=CARTESIAN_POINT ( 'NONE',  ( 9.174642513462172744, 2.649442673323004538, 7.499981897072118819 ) ) ;
#41924=CARTESIAN_POINT ( 'NONE',  ( 3.385862838527417207, 0.4349489234253638981, -3.502725854251790505 ) ) ;
#41929=VECTOR ( 'NONE', #18518, 1000.000000000000000 ) ;
#41931=ADVANCED_FACE ( 'NONE', ( #60338 ), #39359, .F. ) ;
#41932=CARTESIAN_POINT ( 'NONE',  ( 8.335885841230000537, 4.310355144869000732, 9.459505265942000918 ) ) ;
#41933=CARTESIAN_POINT ( 'NONE',  ( 9.369139158774000720, 2.685250982074999904, -7.026194612421999608 ) ) ;
#41936=VERTEX_POINT ( 'NONE', #2639 ) ;
#41943=CARTESIAN_POINT ( 'NONE',  ( 8.572267219592999865, 2.606995215518000286, 6.345762205468999717 ) ) ;
#41953=CARTESIAN_POINT ( 'NONE',  ( 10.34021053755999908, 4.202028620710000162, 9.459600235481000041 ) ) ;
#41954=CARTESIAN_POINT ( 'NONE',  ( 10.46754281781999829, 2.318340407652000223, 6.549777679168999001 ) ) ;
#41961=CARTESIAN_POINT ( 'NONE',  ( 3.300973465876999580, -3.500000000000000000, 0.000000000000000000 ) ) ;
#41972=CARTESIAN_POINT ( 'NONE',  ( 10.81315553411000074, 3.756074350075000012, 6.071610008629000355 ) ) ;
#41974=CARTESIAN_POINT ( 'NONE',  ( 10.61721774768000159, 5.045603402166999985, -6.386910706193999587 ) ) ;
#41975=CARTESIAN_POINT ( 'NONE',  ( 9.615109647822677630, 5.349900357012234764, -7.499993490198826329 ) ) ;
#41980=CARTESIAN_POINT ( 'NONE',  ( 9.587885841227999251, 3.762712042852999872, 8.787816121229999666 ) ) ;
#41983=CARTESIAN_POINT ( 'NONE',  ( 7.325000000000000178, 4.000000000000000000, 9.239711431703000244 ) ) ;
#41984=CARTESIAN_POINT ( 'NONE',  ( 6.999999691988000095, 12.36734761319999798, 2.759114534468000368 ) ) ;
#41987=CARTESIAN_POINT ( 'NONE',  ( 10.93008194863999449, 9.554106281501004716, 6.653031737998000850 ) ) ;
#42001=AXIS2_PLACEMENT_3D ( 'NONE', #31468, #30778, #62918 ) ;
#42006=B_SPLINE_CURVE_WITH_KNOTS ( 'NONE', 3,
 ( #50923, #17739, #55482, #40100, #39058 ),
 .UNSPECIFIED., .F., .F.,
 ( 4, 1, 4 ),
 ( 0.000000000000000000, 0.2283573561321438072, 1.000000000000000000 ),
 .UNSPECIFIED. ) ;
#42007=CARTESIAN_POINT ( 'NONE',  ( 7.726448341228000061, 2.630487280353000390, 6.995957894972000268 ) ) ;
#42013=CARTESIAN_POINT ( 'NONE',  ( 10.78888278041000071, 2.675726696512000125, -6.748227692827999391 ) ) ;
#42027=DIRECTION ( 'NONE',  ( 0.000000000000000000, -1.000000000000000000, 0.000000000000000000 ) ) ;
#42038=CARTESIAN_POINT ( 'NONE',  ( 5.500000000000000000, 12.43893545635000031, -2.828937028792000152 ) ) ;
#42045=CARTESIAN_POINT ( 'NONE',  ( 9.161379719595000637, 5.511689883260999956, -7.095113581311000672 ) ) ;
#42051=ORIENTED_EDGE ( 'NONE', *, *, #32656, .F. ) ;
#42053=CARTESIAN_POINT ( 'NONE',  ( 9.541460841232000334, 2.824732249080000202, -8.992748220058999209 ) ) ;
#42054=ADVANCED_FACE ( 'NONE', ( #3159 ), #45399, .F. ) ;
#42055=DIRECTION ( 'NONE',  ( 0.8843050081471317547, -0.1786786086946064722, 0.4313682966571153465 ) ) ;
#42056=EDGE_CURVE ( 'NONE', #51187, #10058, #65009, .T. ) ;
#42062=CARTESIAN_POINT ( 'NONE',  ( 8.013507625983999461, 4.606065150774999672, -6.249409674000999892 ) ) ;
#42063=CARTESIAN_POINT ( 'NONE',  ( 9.675870280412999236, 3.031907308384000022, -8.729608011560001657 ) ) ;
#42065=CARTESIAN_POINT ( 'NONE',  ( 10.82565186280000091, 5.331165376905000031, -8.542144899688000947 ) ) ;
#42080=CARTESIAN_POINT ( 'NONE',  ( 10.03280471959000231, 3.987760651117999711, -9.123263301387000368 ) ) ;
#42084=EDGE_LOOP ( 'NONE', ( #38641, #41504, #24610, #539, #3066, #35580, #14319, #52282, #31944, #20464, #27159, #68367, #55034, #20831, #36526, #19078, #1375 ) ) ;
#42087=CARTESIAN_POINT ( 'NONE',  ( 10.86079988039000099, 5.063207163126000943, -5.172914090247000551 ) ) ;
#42089=CARTESIAN_POINT ( 'NONE',  ( 10.09645344438251691, 5.267621374772807563, -8.036571084497403206 ) ) ;
#42090=CARTESIAN_POINT ( 'NONE',  ( 1.217640132540999787, -1.762666431298159475, 3.058252359239895135 ) ) ;
#42109=CARTESIAN_POINT ( 'NONE',  ( 7.972192870573465484, 2.986178616227031846, -6.494259741701720046 ) ) ;
#42111=DIRECTION ( 'NONE',  ( 1.000000000000000000, 0.000000000000000000, 0.000000000000000000 ) ) ;
#42120=CARTESIAN_POINT ( 'NONE',  ( 10.36503728015293646, 2.650011783304074164, -7.500002219258057323 ) ) ;
#42128=CARTESIAN_POINT ( 'NONE',  ( 7.625781557060339999, 4.984822363484057384, -8.445605089947335387 ) ) ;
#42132=B_SPLINE_CURVE_WITH_KNOTS ( 'NONE', 3,
 ( #57195, #52299, #19803, #4396, #20485, #63811, #20141, #42165, #47063, #9297 ),
 .UNSPECIFIED., .F., .F.,
 ( 4, 2, 2, 2, 4 ),
 ( 0.000000000000000000, 0.2500000000000001110, 0.5000000000000001110, 0.7500000000000001110, 1.000000000000000000 ),
 .UNSPECIFIED. ) ;
#42137=DIRECTION ( 'NONE',  ( 0.000000000000000000, 0.000000000000000000, -1.000000000000000000 ) ) ;
#42138=EDGE_CURVE ( 'NONE', #58126, #46140, #30011, .T. ) ;
#42140=CARTESIAN_POINT ( 'NONE',  ( 8.482014052312178976, 3.633347688910150808, -9.218057214805476463 ) ) ;
#42142=CARTESIAN_POINT ( 'NONE',  ( 6.596014158771000169, 5.307493345713999666, -7.572367724995999971 ) ) ;
#42144=CARTESIAN_POINT ( 'NONE',  ( 11.09999803709000155, -1.407105940352999962, 11.46396214177000061 ) ) ;
#42146=CARTESIAN_POINT ( 'NONE',  ( 8.455992358796999397, 2.899999999999999911, -6.571291218954000257 ) ) ;
#42150=CARTESIAN_POINT ( 'NONE',  ( 10.81772273141334750, 5.100000000000000533, -6.253511885790826952 ) ) ;
#42151=DIRECTION ( 'NONE',  ( -1.000000000000000000, 0.000000000000000000, 0.000000000000000000 ) ) ;
#42152=ORIENTED_EDGE ( 'NONE', *, *, #57307, .T. ) ;
#42156=CARTESIAN_POINT ( 'NONE',  ( 3.500000000000000444, 0.4524638778880175072, 3.273161885834219298 ) ) ;
#42159=CARTESIAN_POINT ( 'NONE',  ( 8.769668397160224060, 4.137335898486747432, -5.812840004581696363 ) ) ;
#42164=VERTEX_POINT ( 'NONE', #34564 ) ;
#42165=CARTESIAN_POINT ( 'NONE',  ( 3.326208585479333735, -3.365580714188050937, -1.109430098042168744 ) ) ;
#42167=CARTESIAN_POINT ( 'NONE',  ( 10.22398792753999963, 5.507894434963000130, 6.589802269404000157 ) ) ;
#42170=DIRECTION ( 'NONE',  ( 0.000000000000000000, -1.000000000000000000, 0.000000000000000000 ) ) ;
#42173=CARTESIAN_POINT ( 'NONE',  ( 7.000000000000000888, 6.725378844700938608, -3.045375366903437797 ) ) ;
#42182=CARTESIAN_POINT ( 'NONE',  ( 10.75109581085999899, 2.822145500011000063, 6.655897464539000552 ) ) ;
#42187=EDGE_CURVE ( 'NONE', #47380, #8792, #68063, .T. ) ;
#42197=CARTESIAN_POINT ( 'NONE',  ( 9.758079719591000512, 4.905765359186999852, -8.776126235875999271 ) ) ;
#42199=CARTESIAN_POINT ( 'NONE',  ( 11.09999952335000195, -1.407106647395000021, 11.46396798199000067 ) ) ;
#42200=ORIENTED_EDGE ( 'NONE', *, *, #3074, .T. ) ;
#42204=CARTESIAN_POINT ( 'NONE',  ( 10.63743278041000018, 3.721476136598000028, -8.997092462634000753 ) ) ;
#42205=ORIENTED_EDGE ( 'NONE', *, *, #15720, .T. ) ;
#42207=AXIS2_PLACEMENT_3D ( 'NONE', #24843, #29764, #13673 ) ;
#42208=CARTESIAN_POINT ( 'NONE',  ( 8.613182395985113260, 4.653584300239311133, 5.903187239484920745 ) ) ;
#42211=CARTESIAN_POINT ( 'NONE',  ( 8.143323341229999457, 5.061727314042999915, 5.824077473724000420 ) ) ;
#42214=CARTESIAN_POINT ( 'NONE',  ( 6.821014158771999014, 5.777496342847000754, -7.598381660561000395 ) ) ;
#42219=LINE ( 'NONE', #53392, #31721 ) ;
#42225=CARTESIAN_POINT ( 'NONE',  ( 8.596685841231000325, 2.141799395716999843, -7.895788736628000848 ) ) ;
#42233=CARTESIAN_POINT ( 'NONE',  ( 7.058509992104999853, 4.314040636970999820, 8.819134391732999845 ) ) ;
#42234=EDGE_CURVE ( 'NONE', #22269, #37337, #50927, .T. ) ;
#42235=ORIENTED_EDGE ( 'NONE', *, *, #29731, .T. ) ;
#42236=CARTESIAN_POINT ( 'NONE',  ( 3.500000000000000444, -3.140247483149941399, 0.3442837550748506503 ) ) ;
#42249=ORIENTED_EDGE ( 'NONE', *, *, #3685, .T. ) ;
#42250=ORIENTED_EDGE ( 'NONE', *, *, #7970, .T. ) ;
#42252=AXIS2_PLACEMENT_3D ( 'NONE', #7386, #45495, #1455 ) ;
#42256=CARTESIAN_POINT ( 'NONE',  ( 10.79839886931999970, 5.269366011605000288, -6.148705891248999578 ) ) ;
#42259=CARTESIAN_POINT ( 'NONE',  ( 7.920378813398999185, 2.912874113511002783, -6.463705393502997332 ) ) ;
#42261=CARTESIAN_POINT ( 'NONE',  ( 10.81315553411000074, 3.756074350075000012, 6.071610008629000355 ) ) ;
#42264=ORIENTED_EDGE ( 'NONE', *, *, #11585, .T. ) ;
#42267=CARTESIAN_POINT ( 'NONE',  ( 9.966324641169999055, 2.303991951421000106, 6.575630951545000435 ) ) ;
#42273=CARTESIAN_POINT ( 'NONE',  ( 8.303477656456466960, 3.015375792701138646, -8.459897655016847651 ) ) ;
#42277=ORIENTED_EDGE ( 'NONE', *, *, #9596, .T. ) ;
#42280=CARTESIAN_POINT ( 'NONE',  ( 8.924662153698969647, 5.350575487761837223, 7.500021879703680838 ) ) ;
#42285=ORIENTED_EDGE ( 'NONE', *, *, #54256, .T. ) ;
#42288=CONICAL_SURFACE ( 'NONE', #12140, 3.249989426617000188, 0.7853950157668545540 ) ;
#42290=CARTESIAN_POINT ( 'NONE',  ( 9.857857008493319029, 3.288333712785679541, 9.125423578030003924 ) ) ;
#42294=B_SPLINE_CURVE_WITH_KNOTS ( 'NONE', 3,
 ( #6901, #43978, #2015, #55148 ),
 .UNSPECIFIED., .F., .F.,
 ( 4, 4 ),
 ( 0.000000000000000000, 1.000000000000000000 ),
 .UNSPECIFIED. ) ;
#42295=CARTESIAN_POINT ( 'NONE',  ( 9.590596677641999079, 2.445964682955000136, 7.841184989245001624 ) ) ;
#42302=CARTESIAN_POINT ( 'NONE',  ( 8.700642219592999993, 5.212261578733999201, 6.157186134061999994 ) ) ;
#42306=CYLINDRICAL_SURFACE ( 'NONE', #38139, 1.500000000000001110 ) ;
#42307=CARTESIAN_POINT ( 'NONE',  ( 1.595428564794000081, -2.727979478513999911, -1.783091295463999915 ) ) ;
#42311=CARTESIAN_POINT ( 'NONE',  ( 11.05935155529000014, 2.480238120735000162, 6.610075178640000715 ) ) ;
#42319=ADVANCED_FACE ( 'NONE', ( #9000 ), #10031, .T. ) ;
#42329=CARTESIAN_POINT ( 'NONE',  ( 10.02799997617999850, 3.452028386838999818, -6.074524158096999749 ) ) ;
#42330=CARTESIAN_POINT ( 'NONE',  ( 7.927339924271998406, 4.618926574321004175, 6.298803404070997480 ) ) ;
#42333=CARTESIAN_POINT ( 'NONE',  ( 9.008372914924125396, 5.237369076955197045, 8.039691865988411124 ) ) ;
#42335=CARTESIAN_POINT ( 'NONE',  ( 7.416892219589999335, 3.448180532882000104, 9.222462917385000125 ) ) ;
#42339=CARTESIAN_POINT ( 'NONE',  ( 11.09999999999999964, 2.700000000000000178, -6.461133846875999787 ) ) ;
#42343=CARTESIAN_POINT ( 'NONE',  ( 11.86854277327999085, 9.759924522331001384, 5.704691307148000767 ) ) ;
#42345=CARTESIAN_POINT ( 'NONE',  ( 11.14445611883999909, 10.08446449122000033, 5.720378117617999969 ) ) ;
#42347=DIRECTION ( 'NONE',  ( 0.000000000000000000, -0.2461538461537955136, 0.9692307692307821076 ) ) ;
#42356=CARTESIAN_POINT ( 'NONE',  ( 0.6557558238970999653, -0.7435038563603999506, -3.122230671987999973 ) ) ;
#42361=CARTESIAN_POINT ( 'NONE',  ( 8.224593659958996383, 3.074059020428998146, -6.140725432342995838 ) ) ;
#42362=CARTESIAN_POINT ( 'NONE',  ( 10.73615471958999912, 3.078044734341000233, -6.088740491863000592 ) ) ;
#42366=CARTESIAN_POINT ( 'NONE',  ( 8.973567925431344960, 5.349887660206418261, 7.470588186270433972 ) ) ;
#42375=CARTESIAN_POINT ( 'NONE',  ( 8.199995020667000034, 2.894508905068999827, 6.645190348705000360 ) ) ;
#42380=CARTESIAN_POINT ( 'NONE',  ( 10.93769853197999886, 5.063116524846000388, -4.920828787216999345 ) ) ;
#42390=CARTESIAN_POINT ( 'NONE',  ( 11.09999987043000047, 10.03015713885000082, 5.726993666320999488 ) ) ;
#42393=EDGE_LOOP ( 'NONE', ( #14501, #49803, #49254, #25700, #15215, #34799, #29576, #66382, #15636, #15223, #53258, #17691 ) ) ;
#42394=CARTESIAN_POINT ( 'NONE',  ( 8.555820280412000045, 2.414630869937000046, -6.801495146585999407 ) ) ;
#42396=ORIENTED_EDGE ( 'NONE', *, *, #38346, .T. ) ;
#42397=CARTESIAN_POINT ( 'NONE',  ( 7.900104261408000816, 3.351183067932000270, -6.316134894229000096 ) ) ;
#42401=CARTESIAN_POINT ( 'NONE',  ( 9.093935841232999806, 2.156584729807999867, -7.959751745006000689 ) ) ;
#42405=DIRECTION ( 'NONE',  ( 0.000000000000000000, 1.000000000000000000, 0.000000000000000000 ) ) ;
#42408=CARTESIAN_POINT ( 'NONE',  ( 10.16426084122999995, 4.808846957865000604, -8.639578604182998944 ) ) ;
#42410=VECTOR ( 'NONE', #52869, 1000.000000000000114 ) ;
#42412=ORIENTED_EDGE ( 'NONE', *, *, #20514, .F. ) ;
#42415=ADVANCED_FACE ( 'NONE', ( #65233 ), #11895, .T. ) ;
#42422=LINE ( 'NONE', #42761, #2852 ) ;
#42423=LINE ( 'NONE', #36836, #66254 ) ;
#42424=CARTESIAN_POINT ( 'NONE',  ( 8.848264158775000610, 5.751585344281000545, -8.235867044345999588 ) ) ;
#42429=CARTESIAN_POINT ( 'NONE',  ( 10.95289953139000083, 5.154333551509999722, -5.174586382582000432 ) ) ;
#42430=CARTESIAN_POINT ( 'NONE',  ( 10.12812406805898036, 4.965061169224918025, -8.480932067564513233 ) ) ;
#42432=CARTESIAN_POINT ( 'NONE',  ( 0.1499942179680000265, 0.3599680999394012093, -2.749953718116143531 ) ) ;
#42442=EDGE_CURVE ( 'NONE', #13783, #45966, #43193, .T. ) ;
#42450=DIRECTION ( 'NONE',  ( 0.000000000000000000, 1.000000000000000000, 0.000000000000000000 ) ) ;
#42454=CARTESIAN_POINT ( 'NONE',  ( 6.999999999999999112, 9.045785485369089329, -4.691862879246641249 ) ) ;
#42456=FACE_OUTER_BOUND ( 'NONE', #9668, .T. ) ;
#42462=CARTESIAN_POINT ( 'NONE',  ( 3.500000000000000444, 0.1535256407529738132, 3.288177470438649053 ) ) ;
#42470=CARTESIAN_POINT ( 'NONE',  ( 7.662253596345666828, 4.464690838466052192, -8.784472088508959331 ) ) ;
#42480=ORIENTED_EDGE ( 'NONE', *, *, #7092, .F. ) ;
#42481=CARTESIAN_POINT ( 'NONE',  ( 4.074968078372999791, 0.000000000000000000, 0.000000000000000000 ) ) ;
#42482=CARTESIAN_POINT ( 'NONE',  ( 7.315310841225000082, 5.563598295091999546, -6.420781807775999717 ) ) ;
#42484=CARTESIAN_POINT ( 'NONE',  ( 7.292138728207834930, 3.170712126231089112, -8.579042257717643949 ) ) ;
#42491=B_SPLINE_CURVE_WITH_KNOTS ( 'NONE', 3,
 ( #14043, #35372, #3874, #57357 ),
 .UNSPECIFIED., .F., .F.,
 ( 4, 4 ),
 ( 0.000000000000000000, 1.000000000000000000 ),
 .UNSPECIFIED. ) ;
#42496=EDGE_CURVE ( 'NONE', #56231, #47849, #898, .T. ) ;
#42502=ORIENTED_EDGE ( 'NONE', *, *, #12479, .T. ) ;
#42505=CARTESIAN_POINT ( 'NONE',  ( 9.576488281553999116, 4.593976206186999534, 5.662041230125000268 ) ) ;
#42506=CARTESIAN_POINT ( 'NONE',  ( 10.49411415877000131, 2.866942652264999669, -8.960728730887002058 ) ) ;
#42508=CYLINDRICAL_SURFACE ( 'NONE', #34494, 1.999999999999999556 ) ;
#42519=CARTESIAN_POINT ( 'NONE',  ( 10.06843885510000014, 4.148608506723999945, 8.941445591976998841 ) ) ;
#42525=EDGE_CURVE ( 'NONE', #44634, #22260, #68362, .T. ) ;
#42531=CARTESIAN_POINT ( 'NONE',  ( 8.623264158775000965, 5.288433695693000480, -8.041290150997999930 ) ) ;
#42535=CARTESIAN_POINT ( 'NONE',  ( 10.99284065376417452, 6.341348534417104332, 5.182868225897757419 ) ) ;
#42537=CARTESIAN_POINT ( 'NONE',  ( 0.1565305517722999917, 1.141789477572999978, -2.999605631121999849 ) ) ;
#42539=CARTESIAN_POINT ( 'NONE',  ( 2.838475737650000053, -2.711141585093999939, -2.603476249589999458 ) ) ;
#42549=CARTESIAN_POINT ( 'NONE',  ( 8.204454719587999989, 2.564091104321999826, -6.530737592441999695 ) ) ;
#42555=VERTEX_POINT ( 'NONE', #43579 ) ;
#42559=CARTESIAN_POINT ( 'NONE',  ( 7.974113208588001100, 4.561154361229000642, -6.272154006859000930 ) ) ;
#42560=ORIENTED_EDGE ( 'NONE', *, *, #62365, .T. ) ;
#42562=CARTESIAN_POINT ( 'NONE',  ( 9.961715168003999921, 7.673027129248000122, 5.716196767530000500 ) ) ;
#42567=CARTESIAN_POINT ( 'NONE',  ( 8.373670280412000011, 2.202812441249000219, 7.706988150133999405 ) ) ;
#42569=CARTESIAN_POINT ( 'NONE',  ( 7.768029383457135673, 2.842467889454252994, 6.805004285200667802 ) ) ;
#42571=CARTESIAN_POINT ( 'NONE',  ( 10.96871661479000082, 5.813363305173999684, -4.931850597599000352 ) ) ;
#42575=CARTESIAN_POINT ( 'NONE',  ( 6.343015658241001553, 8.380865186898988739, -3.925761800723999606 ) ) ;
#42583=ORIENTED_EDGE ( 'NONE', *, *, #16186, .T. ) ;
#42585=ORIENTED_EDGE ( 'NONE', *, *, #45620, .T. ) ;
#42589=CARTESIAN_POINT ( 'NONE',  ( 4.900006121741999010, 0.5234957687185628483, 1.947945353336630436 ) ) ;
#42590=CARTESIAN_POINT ( 'NONE',  ( 9.856715971886000460, 4.814120192353000149, -8.929574926876000518 ) ) ;
#42597=CARTESIAN_POINT ( 'NONE',  ( 9.028931733733378096, 2.726262640825360961, -8.739372639417585020 ) ) ;
#42598=CARTESIAN_POINT ( 'NONE',  ( 9.719613305057999142, 5.967773797872000685, 7.406643507784999692 ) ) ;
#42600=CARTESIAN_POINT ( 'NONE',  ( 2.280140132542667342, -3.408904368339108260, 0.9161175952574674985 ) ) ;
#42602=CARTESIAN_POINT ( 'NONE',  ( 5.477523075960999854, 12.82224764859999766, -2.276049205301000189 ) ) ;
#42603=CARTESIAN_POINT ( 'NONE',  ( 11.13257108636000048, 9.198727620182998166, -6.595251064759999338 ) ) ;
#42611=CARTESIAN_POINT ( 'NONE',  ( 9.418385841233000377, 3.251172436837000301, -6.320036569851000152 ) ) ;
#42616=CARTESIAN_POINT ( 'NONE',  ( 9.115118560745049336, 5.349923934101355805, -7.499992884230159973 ) ) ;
#42622=CARTESIAN_POINT ( 'NONE',  ( 8.316054719590999511, 3.826300099041999747, -9.055335252254000267 ) ) ;
#42626=CARTESIAN_POINT ( 'NONE',  ( 9.479214860607999782, 4.071727169861000029, 9.089299483126000112 ) ) ;
#42638=CARTESIAN_POINT ( 'NONE',  ( 2.247081873818999931, 2.483819732826999971, -1.905290611529000033 ) ) ;
#42644=EDGE_LOOP ( 'NONE', ( #32082, #30231, #60084, #30358 ) ) ;
#42645=CARTESIAN_POINT ( 'NONE',  ( 9.021064158776001207, 4.883347899767999323, -6.417062834774999835 ) ) ;
#42657=CIRCLE ( 'NONE', #61672, 12.39999890530000037 ) ;
#42659=CARTESIAN_POINT ( 'NONE',  ( 10.38153063908000107, 2.772139908660999907, -8.408082511401000048 ) ) ;
#42663=ADVANCED_FACE ( 'NONE', ( #7208 ), #56569, .F. ) ;
#42666=CARTESIAN_POINT ( 'NONE',  ( 7.764232780408999446, 4.628941086829000184, 5.991667691044999522 ) ) ;
#42671=CARTESIAN_POINT ( 'NONE',  ( 8.617856957858560207, 2.961633343650540873, -6.199064870269592298 ) ) ;
#42673=CARTESIAN_POINT ( 'NONE',  ( 10.97046361309999973, 6.148683856984000329, 5.033387594187999525 ) ) ;
#42687=CARTESIAN_POINT ( 'NONE',  ( 0.04415809921860000542, -1.568133397559999809, -2.874292603119999789 ) ) ;
#42692=CARTESIAN_POINT ( 'NONE',  ( 8.175760841228999709, 2.599243720295000060, 7.909344432242998657 ) ) ;
#42694=CARTESIAN_POINT ( 'NONE',  ( 7.612465007326000510, 3.179383379803001564, -6.407107007521996245 ) ) ;
#42696=EDGE_CURVE ( 'NONE', #24788, #5489, #63237, .T. ) ;
#42697=CARTESIAN_POINT ( 'NONE',  ( 10.66042971959000063, 2.315663237570999566, -7.431702255173999738 ) ) ;
#42701=CARTESIAN_POINT ( 'NONE',  ( 8.757697342472001267, 2.899999999999999911, -6.397101765418000241 ) ) ;
#42704=CARTESIAN_POINT ( 'NONE',  ( 1.071837387928000096, -2.100966486736999705, -2.491430570518000209 ) ) ;
#42705=CARTESIAN_POINT ( 'NONE',  ( 9.020964430773000586, 2.907392932634000005, 6.146188468825999784 ) ) ;
#42706=VECTOR ( 'NONE', #8297, 1000.000000000000227 ) ;
#42730=CARTESIAN_POINT ( 'NONE',  ( 8.804445280412998898, 5.597201461420000967, -8.171008079894999554 ) ) ;
#42732=VERTEX_POINT ( 'NONE', #7898 ) ;
#42733=AXIS2_PLACEMENT_3D ( 'NONE', #20515, #10366, #41839 ) ;
#42734=CARTESIAN_POINT ( 'NONE',  ( 7.924773910468002391, 3.741844367409119521, -6.158492087791373137 ) ) ;
#42736=VERTEX_POINT ( 'NONE', #2646 ) ;
#42746=CARTESIAN_POINT ( 'NONE',  ( 9.468110841233000841, 4.082930418187999955, -6.104944817728999773 ) ) ;
#42748=AXIS2_PLACEMENT_3D ( 'NONE', #1466, #11950, #11256 ) ;
#42750=SURFACE_STYLE_FILL_AREA ( #27361 ) ;
#42751=VERTEX_POINT ( 'NONE', #29235 ) ;
#42758=EDGE_LOOP ( 'NONE', ( #11643, #46811, #40015, #66829 ) ) ;
#42761=CARTESIAN_POINT ( 'NONE',  ( 11.09999999999999964, 2.700688487044999864, -5.124965750789000296 ) ) ;
#42764=CARTESIAN_POINT ( 'NONE',  ( 9.734454719592999794, 3.021734963141999852, -6.070209284876999511 ) ) ;
#42767=ORIENTED_EDGE ( 'NONE', *, *, #3527, .T. ) ;
#42769=CARTESIAN_POINT ( 'NONE',  ( 11.09999999999999964, 5.299999999999999822, 6.469505845987999493 ) ) ;
#42779=CARTESIAN_POINT ( 'NONE',  ( 8.348093183609000434, 4.599999999999999645, -6.056236567608999977 ) ) ;
#42782=CONICAL_SURFACE ( 'NONE', #12644, 2.050045943449999797, 0.7853981633972997312 ) ;
#42792=CARTESIAN_POINT ( 'NONE',  ( 6.816501042874381078, 2.788803157567000035, -8.345558963038001821 ) ) ;
#42798=CONICAL_SURFACE ( 'NONE', #50646, 2.824973347946000413, 0.7853886971611369061 ) ;
#42803=CARTESIAN_POINT ( 'NONE',  ( 7.100000000000000533, 4.000000000000000000, 8.849999999999999645 ) ) ;
#42819=CARTESIAN_POINT ( 'NONE',  ( 8.623264158775000965, 5.288433695693000480, -8.041290150997999930 ) ) ;
#42823=CARTESIAN_POINT ( 'NONE',  ( 6.917510841229000285, 5.477119873501999692, -8.694708770948999188 ) ) ;
#42825=CARTESIAN_POINT ( 'NONE',  ( 7.344182448917417005, 2.650014028440602409, -7.853118540549031579 ) ) ;
#42829=CARTESIAN_POINT ( 'NONE',  ( 8.350387243830999395, 5.100000000000000533, -6.632262360512000576 ) ) ;
#42833=ORIENTED_EDGE ( 'NONE', *, *, #29564, .T. ) ;
#42839=CARTESIAN_POINT ( 'NONE',  ( 7.108747422739984501, 5.156822660709760697, -8.212378574850216495 ) ) ;
#42845=CARTESIAN_POINT ( 'NONE',  ( 10.02201554968999986, 3.298015135926000152, 5.700522662207000657 ) ) ;
#42846=DIRECTION ( 'NONE',  ( -1.000000000000000000, 0.000000000000000000, 9.258974054462001038E-14 ) ) ;
#42850=DIRECTION ( 'NONE',  ( 1.000000000000000000, 0.000000000000000000, 0.000000000000000000 ) ) ;
#42851=CARTESIAN_POINT ( 'NONE',  ( 8.379867906096000851, 2.923743482149999906, 6.439439799146000176 ) ) ;
#42860=ADVANCED_FACE ( 'NONE', ( #9747 ), #68126, .F. ) ;
#42862=CARTESIAN_POINT ( 'NONE',  ( 9.034110134264999203, 4.695345051283999815, 8.660667941667000491 ) ) ;
#42873=ORIENTED_EDGE ( 'NONE', *, *, #28058, .F. ) ;
#42875=CARTESIAN_POINT ( 'NONE',  ( 9.468589158772999781, 4.034680274230000308, -6.102912434217000026 ) ) ;
#42877=CARTESIAN_POINT ( 'NONE',  ( 0.9681103717476999826, 3.205765437135000173, -1.404659375816999844 ) ) ;
#42878=ORIENTED_EDGE ( 'NONE', *, *, #43256, .T. ) ;
#42880=CARTESIAN_POINT ( 'NONE',  ( 0.6995747022588000297, -0.7815069638253000495, -3.281818906455000295 ) ) ;
#42881=ADVANCED_FACE ( 'NONE', ( #60156 ), #36720, .T. ) ;
#42883=CARTESIAN_POINT ( 'NONE',  ( 10.08211611373999972, 4.728047954991999369, -8.793974144431000894 ) ) ;
#42889=CARTESIAN_POINT ( 'NONE',  ( 7.731795280408999993, 4.580608786027000612, 9.213365309690999538 ) ) ;
#42892=CARTESIAN_POINT ( 'NONE',  ( 7.359129719585999929, 5.425783499582999880, -6.515903575897000088 ) ) ;
#42897=CARTESIAN_POINT ( 'NONE',  ( 2.990556799210291938, 3.500000000000001776, -0.4581489286485044832 ) ) ;
#42899=ORIENTED_EDGE ( 'NONE', *, *, #12273, .T. ) ;
#42900=CARTESIAN_POINT ( 'NONE',  ( 8.158337970077000990E-06, -2.999989272562999965, 0.000000000000000000 ) ) ;
#42901=CARTESIAN_POINT ( 'NONE',  ( 9.944763587296000296, 10.12538011034999919, -5.137399309246999834 ) ) ;
#42912=CARTESIAN_POINT ( 'NONE',  ( 8.758795280412000395, 3.977267228909999730, 9.308925224542001331 ) ) ;
#42914=CARTESIAN_POINT ( 'NONE',  ( 10.07314899745999881, 5.167567567567999731, -6.822293592207000934 ) ) ;
#42916=CARTESIAN_POINT ( 'NONE',  ( 11.01665240710999960, 6.699956017084000237, -5.516881093594999896 ) ) ;
#42934=CARTESIAN_POINT ( 'NONE',  ( 10.40558702164999971, 5.599341344818000721, -8.437759619346000051 ) ) ;
#42936=FACE_OUTER_BOUND ( 'NONE', #50627, .T. ) ;
#42937=CARTESIAN_POINT ( 'NONE',  ( 8.200215151753006637, 2.889589711576002085, -6.692116421364998402 ) ) ;
#42938=CARTESIAN_POINT ( 'NONE',  ( 9.820199962102000413, 3.883325513302000154, 6.055618835924000187 ) ) ;
#42940=CARTESIAN_POINT ( 'NONE',  ( 1.800973465875000068, -3.500000000000000000, 0.000000000000000000 ) ) ;
#42941=CARTESIAN_POINT ( 'NONE',  ( 9.228133567168001150, 2.875367362387999837, 8.669940206484001877 ) ) ;
#42942=CARTESIAN_POINT ( 'NONE',  ( 2.217640132542666453, -1.762666431298159475, 3.058252359239895135 ) ) ;
#42944=CARTESIAN_POINT ( 'NONE',  ( 5.399998535875000449, 12.98068687585000092, -1.765643277144999912 ) ) ;
#42946=CARTESIAN_POINT ( 'NONE',  ( 11.05748560607000108, 9.481327459506999844, -6.305849355301000436 ) ) ;
#42948=CARTESIAN_POINT ( 'NONE',  ( 11.09999999999999964, 2.274006712557999688, -7.281956340829000673 ) ) ;
#42949=AXIS2_PLACEMENT_3D ( 'NONE', #43442, #4639, #47990 ) ;
#42951=CARTESIAN_POINT ( 'NONE',  ( 10.56491664109999995, 4.212242527248999835, 8.933458498617000032 ) ) ;
#42957=CARTESIAN_POINT ( 'NONE',  ( 10.83581759971949587, 5.012714476637088801, 4.871130536448504245 ) ) ;
#42960=ORIENTED_EDGE ( 'NONE', *, *, #7970, .F. ) ;
#42962=CARTESIAN_POINT ( 'NONE',  ( 7.795982780410000146, 3.164805384346000228, 9.104735843897000080 ) ) ;
#42964=CARTESIAN_POINT ( 'NONE',  ( 8.903895280414001689, 3.867331042029999999, -9.227339949050001877 ) ) ;
#42968=CARTESIAN_POINT ( 'NONE',  ( 9.388624299788999039, 4.079402096444999515, 9.259357173634999327 ) ) ;
#42974=CARTESIAN_POINT ( 'NONE',  ( 7.968176658772001097, 2.280568568659000483, 6.510284508622999233 ) ) ;
#42979=CARTESIAN_POINT ( 'NONE',  ( 1.166291019826000142, -0.3298644081521999727, -3.242294882329999961 ) ) ;
#42980=EDGE_LOOP ( 'NONE', ( #27856, #52262, #21538, #58281, #9298, #29630, #17004, #24304, #3400, #64428, #53371, #918, #62848, #44599 ) ) ;
#42986=CARTESIAN_POINT ( 'NONE',  ( 8.175739158770999992, 4.686731264770999772, -8.717075579553000608 ) ) ;
#42989=CARTESIAN_POINT ( 'NONE',  ( 9.116868839903307986, 5.079248981113716255, -8.329446991275979428 ) ) ;
#42991=ORIENTED_EDGE ( 'NONE', *, *, #7004, .F. ) ;
#42994=ORIENTED_EDGE ( 'NONE', *, *, #58227, .T. ) ;
#42998=CARTESIAN_POINT ( 'NONE',  ( 9.323722176100000425, 3.947350570199999797, 6.051869652381999920 ) ) ;
#42999=CARTESIAN_POINT ( 'NONE',  ( 10.90760153359000029, 2.969978076949999934, -4.934359432739999995 ) ) ;
#43000=CARTESIAN_POINT ( 'NONE',  ( 8.335548698406999080, 5.102342278510997531, 6.653323484791000553 ) ) ;
#43003=ADVANCED_FACE ( 'NONE', ( #300 ), #21963, .T. ) ;
#43007=EDGE_CURVE ( 'NONE', #59855, #44325, #6225, .T. ) ;
#43009=CARTESIAN_POINT ( 'NONE',  ( 9.010198341230998054, 5.040787533781999841, 8.522957620707000359 ) ) ;
#43015=CARTESIAN_POINT ( 'NONE',  ( 10.96255546505999945, 6.761651470398000185, 5.456355616689999799 ) ) ;
#43016=B_SPLINE_CURVE_WITH_KNOTS ( 'NONE', 3,
 ( #57470, #52577, #36499, #9232, #40714, #51546, #9577, #14499 ),
 .UNSPECIFIED., .F., .F.,
 ( 4, 2, 2, 4 ),
 ( 0.000000000000000000, 0.2500000000000000000, 0.5000000000000000000, 1.000000000000000000 ),
 .UNSPECIFIED. ) ;
#43017=CARTESIAN_POINT ( 'NONE',  ( 11.13997082032999941, 9.835715680716001330, 6.100895928452999328 ) ) ;
#43019=CARTESIAN_POINT ( 'NONE',  ( -15.86200481174999943, 2.399999999999999911, -6.571291218949999902 ) ) ;
#43020=AXIS2_PLACEMENT_3D ( 'NONE', #45614, #7164, #39676 ) ;
#43026=CARTESIAN_POINT ( 'NONE',  ( 8.300444773060121406, 2.921714170698993751, -6.487055555563432385 ) ) ;
#43031=CARTESIAN_POINT ( 'NONE',  ( 0.3678308122907000266, 2.092960143115000005, 2.433246087927000367 ) ) ;
#43032=CARTESIAN_POINT ( 'NONE',  ( 8.745593092018999926, 5.100000000000000533, 6.404090157675000228 ) ) ;
#43037=CARTESIAN_POINT ( 'NONE',  ( 7.572352458090005456, 3.472372354340000911, -6.527657354165006254 ) ) ;
#43045=CARTESIAN_POINT ( 'NONE',  ( 7.773264469372000107, 2.859518616742000141, 6.768376720750000075 ) ) ;
#43046=EDGE_CURVE ( 'NONE', #10323, #54361, #26652, .T. ) ;
#43047=CARTESIAN_POINT ( 'NONE',  ( 11.09999999999999964, 4.000000000000000000, -7.500000000000000000 ) ) ;
#43051=CARTESIAN_POINT ( 'NONE',  ( 11.13228700200999910, 2.679094735942999961, 4.957687805034000306 ) ) ;
#43053=ORIENTED_EDGE ( 'NONE', *, *, #1099, .T. ) ;
#43055=CARTESIAN_POINT ( 'NONE',  ( 8.571413182547999554, 4.599999999999999645, 5.927302706106000407 ) ) ;
#43068=CARTESIAN_POINT ( 'NONE',  ( 7.349539055719287006, 3.476414806253772749, 9.161239507722385156 ) ) ;
#43074=ORIENTED_EDGE ( 'NONE', *, *, #32405, .T. ) ;
#43088=ADVANCED_FACE ( 'NONE', ( #48810 ), #6346, .T. ) ;
#43089=CARTESIAN_POINT ( 'NONE',  ( 8.621524209948821849, 3.647212272540921951, 8.851469415033248467 ) ) ;
#43103=ORIENTED_EDGE ( 'NONE', *, *, #18280, .F. ) ;
#43106=ADVANCED_FACE ( 'NONE', ( #43569 ), #53480, .T. ) ;
#43109=CARTESIAN_POINT ( 'NONE',  ( 9.047164158776000775, 2.156584729807999867, -7.959751745006000689 ) ) ;
#43114=CARTESIAN_POINT ( 'NONE',  ( 10.87371169224999967, 5.064035864983999602, -5.107130734103000336 ) ) ;
#43131=ADVANCED_FACE ( 'NONE', ( #35493 ), #9587, .F. ) ;
#43135=VECTOR ( 'NONE', #62230, 1000.000000000000114 ) ;
#43138=FACE_OUTER_BOUND ( 'NONE', #2163, .T. ) ;
#43139=EDGE_LOOP ( 'NONE', ( #5333, #10501, #6905, #20748, #17202 ) ) ;
#43146=CARTESIAN_POINT ( 'NONE',  ( 10.76537527815838580, 5.100000000000000533, 6.445686799303629755 ) ) ;
#43158=CARTESIAN_POINT ( 'NONE',  ( 7.307500000000000107, 0.2999999999999999889, -3.149999999999999911 ) ) ;
#43160=CARTESIAN_POINT ( 'NONE',  ( 8.474089158773999486, 4.131080973160000447, -6.108642999115999395 ) ) ;
#43163=CARTESIAN_POINT ( 'NONE',  ( 7.563935841224999734, 2.455281733534999677, -8.606072783617999988 ) ) ;
#43165=CARTESIAN_POINT ( 'NONE',  ( 9.424850063658244181, 5.349972463430670899, 7.500009360578276052 ) ) ;
#43166=ORIENTED_EDGE ( 'NONE', *, *, #62529, .F. ) ;
#43175=LINE ( 'NONE', #16602, #7443 ) ;
#43176=ORIENTED_EDGE ( 'NONE', *, *, #9597, .F. ) ;
#43181=CARTESIAN_POINT ( 'NONE',  ( 8.229591223330004368, 5.116109178766001797, -6.360512773592004621 ) ) ;
#43183=CARTESIAN_POINT ( 'NONE',  ( 7.189449102910221434, 4.002238097908506376, -8.883099350742211797 ) ) ;
#43185=CIRCLE ( 'NONE', #16375, 3.200000000000000178 ) ;
#43188=VERTEX_POINT ( 'NONE', #3653 ) ;
#43189=CARTESIAN_POINT ( 'NONE',  ( 9.889842476439000052, 4.052276433608000161, 9.260531940735001299 ) ) ;
#43190=CARTESIAN_POINT ( 'NONE',  ( 10.83253786428999987, 2.899999999999999911, 6.571291218949999902 ) ) ;
#43191=EDGE_CURVE ( 'NONE', #55845, #12182, #758, .T. ) ;
#43193=CIRCLE ( 'NONE', #35374, 12.50000000000000000 ) ;
#43195=CARTESIAN_POINT ( 'NONE',  ( 9.216851002545999094, 2.832432432432000269, 6.822293592207000934 ) ) ;
#43201=VECTOR ( 'NONE', #58803, 1000.000000000000000 ) ;
#43204=DIRECTION ( 'NONE',  ( 0.000000000000000000, 0.000000000000000000, 1.000000000000000000 ) ) ;
#43207=CARTESIAN_POINT ( 'NONE',  ( 10.40726830891999910, 3.797905842462999892, 5.889914049998000500 ) ) ;
#43208=CARTESIAN_POINT ( 'NONE',  ( 10.98768472639999949, 0.3876847264043000174, 4.945212061661000469 ) ) ;
#43213=DIRECTION ( 'NONE',  ( -1.000000000000000000, 0.000000000000000000, 0.000000000000000000 ) ) ;
#43222=CARTESIAN_POINT ( 'NONE',  ( 0.6256366850171000138, -2.634961698279000064, 2.360490016663000290 ) ) ;
#43224=CARTESIAN_POINT ( 'NONE',  ( 10.19794834123000093, 4.262170647947000290, -8.834315641189999013 ) ) ;
#43233=CARTESIAN_POINT ( 'NONE',  ( 8.218892219592001780, 3.011620138462000273, 8.801434747080000065 ) ) ;
#43236=CARTESIAN_POINT ( 'NONE',  ( 8.576820280409998887, 4.814347755891000169, -8.757164289523000633 ) ) ;
#43245=CARTESIAN_POINT ( 'NONE',  ( 6.983162019845000401, 12.13278763737000077, 3.076796177952999756 ) ) ;
#43247=ORIENTED_EDGE ( 'NONE', *, *, #52838, .T. ) ;
#43249=FACE_OUTER_BOUND ( 'NONE', #1491, .T. ) ;
#43251=DIRECTION ( 'NONE',  ( 0.000000000000000000, -1.000000000000000000, 0.000000000000000000 ) ) ;
#43252=DIRECTION ( 'NONE',  ( -1.000000000000000000, 0.000000000000000000, 0.000000000000000000 ) ) ;
#43255=CARTESIAN_POINT ( 'NONE',  ( 7.705392219590000202, 3.245534453799999941, 8.949623695221001540 ) ) ;
#43256=EDGE_CURVE ( 'NONE', #28703, #68545, #39912, .T. ) ;
#43259=LINE ( 'NONE', #49531, #10565 ) ;
#43262=CARTESIAN_POINT ( 'NONE',  ( 11.07243245105999918, 6.098035042109999360, -5.197348905474999725 ) ) ;
#43277=CARTESIAN_POINT ( 'NONE',  ( 9.925639158771000226, 4.357364160690000432, -9.282962013144999247 ) ) ;
#43278=CARTESIAN_POINT ( 'NONE',  ( 10.52343057594999998, 3.209665745824000105, -9.177097971982000502 ) ) ;
#43280=CARTESIAN_POINT ( 'NONE',  ( 8.924662153698969647, 5.350575487761837223, 7.500021879703680838 ) ) ;
#43282=CARTESIAN_POINT ( 'NONE',  ( 9.068197172117432814, 5.125396288428779812, -6.749639981086953178 ) ) ;
#43289=CARTESIAN_POINT ( 'NONE',  ( 11.18051582549000145, 5.340073783367000892, 8.416152717850000187 ) ) ;
#43290=CARTESIAN_POINT ( 'NONE',  ( 2.248890132542666898, -2.798833948393641080, 2.150913519912190708 ) ) ;
#43292=CARTESIAN_POINT ( 'NONE',  ( 5.500000000000000000, 2.451372438371999805E-13, 6.461498003317998333E-14 ) ) ;
#43293=AXIS2_PLACEMENT_3D ( 'NONE', #60352, #12461, #44638 ) ;
#43294=CARTESIAN_POINT ( 'NONE',  ( 10.99074018437999989, 9.115166694568001660, -6.428052138438000718 ) ) ;
#43295=CARTESIAN_POINT ( 'NONE',  ( 10.78327292636594237, 5.333380840314849713, -6.342316951424320060 ) ) ;
#43298=CIRCLE ( 'NONE', #63342, 12.39999890530000037 ) ;
#43299=LINE ( 'NONE', #64607, #7602 ) ;
#43302=CARTESIAN_POINT ( 'NONE',  ( 11.00000000000000000, 5.200000000000000178, 5.865766984179000332 ) ) ;
#43308=B_SPLINE_CURVE_WITH_KNOTS ( 'NONE', 3,
 ( #26299, #27329, #26987, #31546, #21050, #63337, #15465, #36791, #58112, #48303, #47966, #59136 ),
 .UNSPECIFIED., .F., .F.,
 ( 4, 2, 2, 2, 2, 4 ),
 ( 0.000000000000000000, 0.2499999999999965583, 0.3749999999999968914, 0.4374999999999996669, 0.5000000000000025535, 1.000000000000000000 ),
 .UNSPECIFIED. ) ;
#43311=CARTESIAN_POINT ( 'NONE',  ( 7.218295280410000458, 4.773081973066999772, 8.927402469597002010 ) ) ;
#43312=CARTESIAN_POINT ( 'NONE',  ( 9.459729719592999686, 2.527713920559999661, -6.969421869128999525 ) ) ;
#43314=CARTESIAN_POINT ( 'NONE',  ( 2.520034936199110120, -3.248084742043254813, 0.2529824396494559924 ) ) ;
#43315=ADVANCED_FACE ( 'NONE', ( #31965 ), #61112, .T. ) ;
#43316=VERTEX_POINT ( 'NONE', #52587 ) ;
#43318=CARTESIAN_POINT ( 'NONE',  ( 9.722769750889000306, 5.493785011855999656, 6.566826815556000341 ) ) ;
#43335=CARTESIAN_POINT ( 'NONE',  ( 8.162581873609997984, 3.457979189883997329, 6.166988478103001547 ) ) ;
#43336=VECTOR ( 'NONE', #23102, 1000.000000000000000 ) ;
#43339=CARTESIAN_POINT ( 'NONE',  ( 9.658629719592001450, 5.496789211521000418, -7.043125396300999874 ) ) ;
#43344=EDGE_CURVE ( 'NONE', #14597, #32433, #40557, .T. ) ;
#43346=CARTESIAN_POINT ( 'NONE',  ( 7.948155326409716892, 4.903496817485942572, -6.391515375827595768 ) ) ;
#43356=CARTESIAN_POINT ( 'NONE',  ( 9.447841622600000377, 5.447457912891000120, 7.431328695644999982 ) ) ;
#43357=CARTESIAN_POINT ( 'NONE',  ( 10.96087378956999991, 2.844615129876999937, -5.099797510035999792 ) ) ;
#43358=CARTESIAN_POINT ( 'NONE',  ( 7.969753415490000492, 5.131577060784002775, 6.757500301899002970 ) ) ;
#43359=CARTESIAN_POINT ( 'NONE',  ( 11.09999999999999964, 5.350000000000000533, 7.500000000000000000 ) ) ;
#43365=CARTESIAN_POINT ( 'NONE',  ( 8.983795280412000039, 3.979464555644999901, 9.134076336209998814 ) ) ;
#43371=EDGE_CURVE ( 'NONE', #33656, #14617, #64151, .T. ) ;
#43373=CARTESIAN_POINT ( 'NONE',  ( 11.01665246377999985, 6.699949187588000399, 5.516876281257999892 ) ) ;
#43374=CARTESIAN_POINT ( 'NONE',  ( 11.14285950365999867, 10.00557278198999889, 5.861225909637999720 ) ) ;
#43380=CARTESIAN_POINT ( 'NONE',  ( 10.07102359808000003, 4.042170458878000083, 8.920189456109998360 ) ) ;
#43385=CARTESIAN_POINT ( 'NONE',  ( 9.112170280412000167, 2.368264398678999516, 7.410200237937000445 ) ) ;
#43387=CONICAL_SURFACE ( 'NONE', #47880, 11.45000314237999994, 0.7853984362573629419 ) ;
#43391=CARTESIAN_POINT ( 'NONE',  ( 8.231600168468999001, 3.072304018142998139, -6.138007231110007567 ) ) ;
#43392=CARTESIAN_POINT ( 'NONE',  ( 10.99306084123000105, 4.495422912016000083, -6.233618171705999522 ) ) ;
#43394=CARTESIAN_POINT ( 'NONE',  ( 7.927339924271998406, 4.618926574321004175, 6.298803404070997480 ) ) ;
#43408=DIRECTION ( 'NONE',  ( 0.000000000000000000, -1.000000000000000000, 0.000000000000000000 ) ) ;
#43411=EDGE_CURVE ( 'NONE', #7557, #15849, #29842, .T. ) ;
#43415=CARTESIAN_POINT ( 'NONE',  ( 10.61503919148293740, 5.349978903665603802, -7.499997722305280945 ) ) ;
#43424=CARTESIAN_POINT ( 'NONE',  ( 9.793536308085231568, 2.899999999999999911, 6.665341197415458829 ) ) ;
#43428=CARTESIAN_POINT ( 'NONE',  ( 7.407491200529044306, 2.500879239676554011, 8.383868204678638136 ) ) ;
#43442=CARTESIAN_POINT ( 'NONE',  ( 11.09999999999999964, 4.000000000000000000, 7.500000000000000000 ) ) ;
#43444=CARTESIAN_POINT ( 'NONE',  ( 9.219485841232998524, 3.892978337449999771, -8.893414073324001023 ) ) ;
#43445=ORIENTED_EDGE ( 'NONE', *, *, #61008, .T. ) ;
#43457=EDGE_CURVE ( 'NONE', #8013, #22744, #41590, .T. ) ;
#43458=CARTESIAN_POINT ( 'NONE',  ( 7.849215480312374815, 2.936390630773842769, -6.610087627805777188 ) ) ;
#43460=VERTEX_POINT ( 'NONE', #25165 ) ;
#43465=CARTESIAN_POINT ( 'NONE',  ( 9.925639158771000226, 4.357364160690000432, -9.282962013144999247 ) ) ;
#43478=CARTESIAN_POINT ( 'NONE',  ( 8.450126246929182017, 5.099734361584643771, -6.554153617478260863 ) ) ;
#43489=ADVANCED_FACE ( 'NONE', ( #3826 ), #35415, .T. ) ;
#43498=DIRECTION ( 'NONE',  ( 0.000000000000000000, 0.000000000000000000, -1.000000000000000000 ) ) ;
#43499=CARTESIAN_POINT ( 'NONE',  ( 0.9676401325417666177, 1.762666431298152148, -3.058252359239900908 ) ) ;
#43500=ORIENTED_EDGE ( 'NONE', *, *, #53066, .T. ) ;
#43515=CARTESIAN_POINT ( 'NONE',  ( 9.468589158772999781, 4.034680274230000308, -6.102912434217000026 ) ) ;
#43516=ORIENTED_EDGE ( 'NONE', *, *, #48296, .F. ) ;
#43519=CARTESIAN_POINT ( 'NONE',  ( 8.309810841226997979, 5.485324155719999872, -6.315380258366999122 ) ) ;
#43521=CARTESIAN_POINT ( 'NONE',  ( 7.250503751640505534, 3.823235083025295467, -8.849529909115084081 ) ) ;
#43522=ORIENTED_EDGE ( 'NONE', *, *, #1654, .F. ) ;
#43525=LINE ( 'NONE', #42829, #43934 ) ;
#43529=ORIENTED_EDGE ( 'NONE', *, *, #39936, .F. ) ;
#43533=CARTESIAN_POINT ( 'NONE',  ( 8.115647571493003198, 4.568121236579997024, -6.191716341584998951 ) ) ;
#43539=CARTESIAN_POINT ( 'NONE',  ( 10.80168826891999956, 3.998196217194999846, 9.431555066626000183 ) ) ;
#43549=CARTESIAN_POINT ( 'NONE',  ( 10.91307008594999850, 2.096286256021000050, 7.827189715349000210 ) ) ;
#43551=B_SPLINE_CURVE_WITH_KNOTS ( 'NONE', 3,
 ( #39059, #55136, #7583, #17383 ),
 .UNSPECIFIED., .F., .F.,
 ( 4, 4 ),
 ( 0.000000000000000000, 1.000000000000000000 ),
 .UNSPECIFIED. ) ;
#43556=CYLINDRICAL_SURFACE ( 'NONE', #50526, 0.5000000000000002220 ) ;
#43557=AXIS2_PLACEMENT_3D ( 'NONE', #48147, #58983, #47814 ) ;
#43564=CARTESIAN_POINT ( 'NONE',  ( 0.1103081484368000076, -1.521127753326000143, -2.712944034833999929 ) ) ;
#43569=FACE_OUTER_BOUND ( 'NONE', #10063, .T. ) ;
#43570=EDGE_CURVE ( 'NONE', #3005, #49517, #29215, .T. ) ;
#43573=CARTESIAN_POINT ( 'NONE',  ( 10.99335825054266103, 5.917683583687179727, 4.994028698803151478 ) ) ;
#43574=CARTESIAN_POINT ( 'NONE',  ( 0.5928308122907000044, 2.413895893032000028, 2.806361486493000434 ) ) ;
#43576=CARTESIAN_POINT ( 'NONE',  ( 10.65229834123000074, 4.944334466443999432, -8.478467788338001299 ) ) ;
#43579=CARTESIAN_POINT ( 'NONE',  ( 8.615121458427411838, 5.349954800205006578, -7.499992720895565235 ) ) ;
#43582=CARTESIAN_POINT ( 'NONE',  ( 9.079732780410999737, 5.421534627450999899, 6.381126373995999579 ) ) ;
#43585=CARTESIAN_POINT ( 'NONE',  ( 7.011054719589999706, 4.455038580940000159, -9.171635993214000138 ) ) ;
#43589=CARTESIAN_POINT ( 'NONE',  ( 10.72520610419000064, 5.521650664120000940, 6.612990918765000004 ) ) ;
#43595=EDGE_CURVE ( 'NONE', #26293, #60334, #32481, .T. ) ;
#43596=CARTESIAN_POINT ( 'NONE',  ( 11.10000000000000142, 2.718803219220815137, -8.524899190229213275 ) ) ;
#43600=VERTEX_POINT ( 'NONE', #26894 ) ;
#43604=DIRECTION ( 'NONE',  ( -1.000000000000000000, 0.000000000000000000, 0.000000000000000000 ) ) ;
#43606=ORIENTED_EDGE ( 'NONE', *, *, #4010, .T. ) ;
#43607=CARTESIAN_POINT ( 'NONE',  ( 8.309482780410998970, 2.905861847853000057, 8.940690431604000565 ) ) ;
#43611=ORIENTED_EDGE ( 'NONE', *, *, #55681, .F. ) ;
#43615=CARTESIAN_POINT ( 'NONE',  ( 11.01654511052000096, 5.423852610492999382, -4.991940169492999679 ) ) ;
#43616=ORIENTED_EDGE ( 'NONE', *, *, #44643, .F. ) ;
#43617=B_SPLINE_SURFACE_WITH_KNOTS ( 'NONE', 3, 3, ( 
 ( #3592, #56757, #45580, #29516, #20031, #57085, #66886, #13077, #41012, #62334, #51166, #35431, #61646, #56407, #50469, #40662, #67225, #51839, #14451, #8509, #67915, #9185, #19691, #55724, #50819, #61994, #30191, #7824, #24592, #29161, #8854, #56056, #19338, #61306, #23900 ),
 ( #51497, #30525, #39992, #45236, #13427, #3936, #25274, #66541, #24243, #18660, #18998, #29858, #45913, #15131, #42045, #20373, #57423, #41696, #63351, #52185, #15479, #52879, #26999, #52530, #5320, #10225, #63002, #25621, #37479, #26662, #21737, #47978, #4978, #58460, #4285 ),
 ( #20718, #21397, #36451, #47640, #48315, #31559, #26311, #68597, #57770, #21063, #9881, #420, #80, #30871, #62669, #31223, #68253, #4627, #36107, #5658, #25965, #14788, #15813, #42730, #36804, #53563, #10567, #31905, #42394, #37143, #58124, #68950, #47294, #9528, #63700 ),
 ( #53219, #64034, #16155, #58805, #10910, #32254, #46948, #28382, #22083, #11249, #37824, #6696, #17544, #1807, #2159, #1116, #17895, #59488, #7047, #32587, #38516, #1459, #22774, #48663, #33630, #44125, #39212, #60538, #49345, #7390, #54598, #6343, #49698, #43771, #65423 ) ),
 .UNSPECIFIED., .F., .F., .F.,
 ( 4, 4 ),
 ( 4, 1, 1, 1, 1, 1, 1, 1, 1, 1, 1, 1, 1, 1, 1, 1, 1, 1, 1, 1, 1, 1, 1, 1, 1, 1, 1, 1, 1, 1, 1, 1, 4 ),
 ( -0.1039370721279000015, 1.103937072127999963 ),
 ( -0.02000000000000000042, 0.01250000000000000069, 0.04499999999999999833, 0.07749999999999999944, 0.1100000000000000006, 0.1424999999999999878, 0.1749999999999999889, 0.2074999999999999900, 0.2399999999999999911, 0.2725000000000000200, 0.3049999999999999933, 0.3375000000000000222, 0.3699999999999999956, 0.4025000000000000244, 0.4349999999999999978, 0.4675000000000000266, 0.5000000000000000000, 0.5324999999999999734, 0.5649999999999999467, 0.5975000000000000311, 0.6300000000000000044, 0.6624999999999999778, 0.6949999999999999512, 0.7275000000000000355, 0.7600000000000000089, 0.7924999999999999822, 0.8249999999999999556, 0.8575000000000000400, 0.8900000000000000133, 0.9224999999999999867, 0.9549999999999999600, 0.9875000000000000444, 1.020000000000000018 ),
 .UNSPECIFIED. ) ;
#43630=CARTESIAN_POINT ( 'NONE',  ( 9.196339158776000389, 4.112741311853999271, -5.603466076760000192 ) ) ;
#43631=CARTESIAN_POINT ( 'NONE',  ( 10.01277517397999972, 3.440623091551000101, -9.267603345544999982 ) ) ;
#43636=ORIENTED_EDGE ( 'NONE', *, *, #33542, .T. ) ;
#43638=CARTESIAN_POINT ( 'NONE',  ( 10.46432998405999903, 2.042755206296999582, 7.723699495214000343 ) ) ;
#43639=CARTESIAN_POINT ( 'NONE',  ( 10.90000000000000036, 2.832432432432000269, -6.822293592207000934 ) ) ;
#43644=CARTESIAN_POINT ( 'NONE',  ( 10.47213937496879232, 2.299779464567346388, 7.025414528928831892 ) ) ;
#43647=VECTOR ( 'NONE', #10616, 1000.000000000000000 ) ;
#43650=CARTESIAN_POINT ( 'NONE',  ( 9.269210841233000764, 3.098073081301000009, -8.567513114264999174 ) ) ;
#43653=EDGE_CURVE ( 'NONE', #51187, #42164, #41701, .T. ) ;
#43659=CARTESIAN_POINT ( 'NONE',  ( 7.346670280409000497, 2.374037589774999901, 8.293392681990997772 ) ) ;
#43660=CARTESIAN_POINT ( 'NONE',  ( 8.713854719593998155, 5.442817578555000146, -8.106149115450000053 ) ) ;
#43664=CARTESIAN_POINT ( 'NONE',  ( 10.46085995768999943, 5.403395036974999677, 7.721808039505000387 ) ) ;
#43677=FACE_OUTER_BOUND ( 'NONE', #49805, .T. ) ;
#43680=CARTESIAN_POINT ( 'NONE',  ( 8.493443684196000376, 2.902502839086001263, 6.607649189245996091 ) ) ;
#43683=CARTESIAN_POINT ( 'NONE',  ( 9.170239158775000732, 4.769103072373000352, -8.666849124598000387 ) ) ;
#43690=CYLINDRICAL_SURFACE ( 'NONE', #36269, 0.5000000000000002220 ) ;
#43695=ORIENTED_EDGE ( 'NONE', *, *, #56990, .F. ) ;
#43696=CARTESIAN_POINT ( 'NONE',  ( 7.000000000000000000, 10.80467228076000019, -3.475853456584999890 ) ) ;
#43707=CARTESIAN_POINT ( 'NONE',  ( 7.518864158771000561, 3.206360348473000332, 5.681727837477000165 ) ) ;
#43711=CARTESIAN_POINT ( 'NONE',  ( 0.7509734658760000015, -3.500000000000000000, 0.000000000000000000 ) ) ;
#43715=CARTESIAN_POINT ( 'NONE',  ( 11.07071174448999962, 5.425085858506999870, 5.078388370519999917 ) ) ;
#43717=CARTESIAN_POINT ( 'NONE',  ( 11.07143661373999954, 7.542210745176000763, 6.453318764178000322 ) ) ;
#43727=CARTESIAN_POINT ( 'NONE',  ( 9.523698341228998387, 4.852728889087999598, 8.683917172082999514 ) ) ;
#43728=LINE ( 'NONE', #50352, #24912 ) ;
#43731=CARTESIAN_POINT ( 'NONE',  ( 9.073148997461000675, 5.167567567567999731, -6.822293592207000934 ) ) ;
#43737=CARTESIAN_POINT ( 'NONE',  ( 7.800985831153996131, 4.602212482482000766, 6.372454311207003563 ) ) ;
#43743=CARTESIAN_POINT ( 'NONE',  ( 0.8763362521023999596, 3.132555770593000055, 1.386468609675000074 ) ) ;
#43745=CARTESIAN_POINT ( 'NONE',  ( 8.241912900173000267, 4.599999999999999645, 6.117539782833000928 ) ) ;
#43748=VECTOR ( 'NONE', #35681, 1000.000000000000000 ) ;
#43751=LINE ( 'NONE', #17521, #16521 ) ;
#43754=CARTESIAN_POINT ( 'NONE',  ( 10.84999882987999875, -12.50000000000000000, 0.000000000000000000 ) ) ;
#43755=CARTESIAN_POINT ( 'NONE',  ( 9.709204462303732797, 2.899999999999999911, 6.662590550607019324 ) ) ;
#43756=CARTESIAN_POINT ( 'NONE',  ( 1.032791847629000115, 1.715249283262000102, -3.156226979448999881 ) ) ;
#43760=CARTESIAN_POINT ( 'NONE',  ( 11.07345995138000028, 3.998673170817999889, 8.920816085870999501 ) ) ;
#43762=AXIS2_PLACEMENT_3D ( 'NONE', #27360, #49028, #1135 ) ;
#43769=CARTESIAN_POINT ( 'NONE',  ( 9.411508750485571895, 5.333019778067357386, 7.282918306495822947 ) ) ;
#43771=CARTESIAN_POINT ( 'NONE',  ( 8.414360841228999632, 5.461114003844000031, -8.582501063019000398 ) ) ;
#43784=CARTESIAN_POINT ( 'NONE',  ( 11.09999999999999964, 4.000000000000000000, -7.500000000000000000 ) ) ;
#43786=CARTESIAN_POINT ( 'NONE',  ( 10.19741084123000086, 4.262870449202000422, -8.811513791423999820 ) ) ;
#43795=ADVANCED_FACE ( 'NONE', ( #45041 ), #61117, .T. ) ;
#43797=EDGE_CURVE ( 'NONE', #44976, #14053, #19964, .T. ) ;
#43799=CARTESIAN_POINT ( 'NONE',  ( 7.848633776075367940, 2.977326305471488244, -6.549596320077490041 ) ) ;
#43803=CARTESIAN_POINT ( 'NONE',  ( 10.94535373587000038, 2.924507478818999751, 4.924562996314999275 ) ) ;
#43804=CARTESIAN_POINT ( 'NONE',  ( 10.65445404527255135, 4.823605068675146157, -4.782660509889021583 ) ) ;
#43807=VECTOR ( 'NONE', #13717, 1000.000000000000000 ) ;
#43808=CARTESIAN_POINT ( 'NONE',  ( 8.532195280408998883, 5.331510020787000315, -8.114341808290998159 ) ) ;
#43809=CARTESIAN_POINT ( 'NONE',  ( 4.149992563292000725, -2.000000000000000000, 0.000000000000000000 ) ) ;
#43812=ORIENTED_EDGE ( 'NONE', *, *, #16966, .F. ) ;
#43818=CARTESIAN_POINT ( 'NONE',  ( 1.042640132542499654, 3.058252359239899132, 1.762666431298154146 ) ) ;
#43841=ADVANCED_FACE ( 'NONE', ( #36954 ), #23128, .T. ) ;
#43845=ORIENTED_EDGE ( 'NONE', *, *, #29818, .T. ) ;
#43850=CARTESIAN_POINT ( 'NONE',  ( 7.000000000000000888, 9.166793235311024191, 4.705382354989500193 ) ) ;
#43853=CARTESIAN_POINT ( 'NONE',  ( 5.000000000000000000, 0.2999999999999999889, 2.733587386567000177 ) ) ;
#43858=CARTESIAN_POINT ( 'NONE',  ( 8.971339158776000744, 4.082930418187999955, -6.104944817728999773 ) ) ;
#43860=CARTESIAN_POINT ( 'NONE',  ( 8.793536308084599185, 2.899999999999999911, 6.665341197421785324 ) ) ;
#43861=CARTESIAN_POINT ( 'NONE',  ( 8.160635841226000053, 2.425297598239999797, -6.437049665397999831 ) ) ;
#43867=DIRECTION ( 'NONE',  ( 0.000000000000000000, 0.7158784314710769925, -0.6982249432342777506 ) ) ;
#43868=EDGE_LOOP ( 'NONE', ( #625, #16421, #13346, #46426, #50943, #14374, #1458, #62523, #24145, #56604, #44026, #67966, #24584, #50254, #4980 ) ) ;
#43869=FACE_OUTER_BOUND ( 'NONE', #15406, .T. ) ;
#43870=DIRECTION ( 'NONE',  ( 0.000000000000000000, -1.000000000000000000, 0.000000000000000000 ) ) ;
#43877=DIRECTION ( 'NONE',  ( -1.000000000000000000, 0.000000000000000000, 0.000000000000000000 ) ) ;
#43886=CARTESIAN_POINT ( 'NONE',  ( 10.24394221959000184, 3.220342255699999878, -6.005413528376000620 ) ) ;
#43887=CARTESIAN_POINT ( 'NONE',  ( 11.09999999999999964, 7.281355457699000056, 6.286510842043999681 ) ) ;
#43894=B_SPLINE_CURVE_WITH_KNOTS ( 'NONE', 3,
 ( #59197, #16204, #48364, #26710, #21444, #21788 ),
 .UNSPECIFIED., .F., .F.,
 ( 4, 2, 4 ),
 ( 0.000000000000000000, 0.5000000000000000000, 1.000000000000000000 ),
 .UNSPECIFIED. ) ;
#43897=CARTESIAN_POINT ( 'NONE',  ( 9.942214158770999788, 3.986577607995999806, -9.280166295424001177 ) ) ;
#43918=CARTESIAN_POINT ( 'NONE',  ( 8.456370280410999030, 2.836879604150999601, -8.783908972046001296 ) ) ;
#43921=CARTESIAN_POINT ( 'NONE',  ( 1.004152257442999963, 3.426971461775999650, -0.8894074146212000986 ) ) ;
#43923=CARTESIAN_POINT ( 'NONE',  ( 9.392382111846503179, 2.695375482096328490, 8.670063079933681749 ) ) ;
#43924=CARTESIAN_POINT ( 'NONE',  ( 11.29596084123000210, 2.828872990872000059, -8.191118698770999629 ) ) ;
#43929=EDGE_CURVE ( 'NONE', #5573, #54836, #48305, .T. ) ;
#43931=CARTESIAN_POINT ( 'NONE',  ( 9.250899447075999760, 4.135077451221000011, 9.175524215473998879 ) ) ;
#43932=ORIENTED_EDGE ( 'NONE', *, *, #15720, .F. ) ;
#43934=VECTOR ( 'NONE', #28132, 1000.000000000000114 ) ;
#43935=CARTESIAN_POINT ( 'NONE',  ( 7.499445280409000603, 5.564636229952000690, -7.532446618777999703 ) ) ;
#43937=CARTESIAN_POINT ( 'NONE',  ( 11.11504246380000005, 3.456610836627000083, 5.970339330302000036 ) ) ;
#43941=CARTESIAN_POINT ( 'NONE',  ( 11.10000000009000054, 2.699999999911000259, 6.571291220400000022 ) ) ;
#43944=CARTESIAN_POINT ( 'NONE',  ( 10.90000000296000060, 2.899999999990999999, 5.160242730682999657 ) ) ;
#43951=CARTESIAN_POINT ( 'NONE',  ( 8.216851002544000693, 2.832432432432000269, 6.822293592207000934 ) ) ;
#43953=ORIENTED_EDGE ( 'NONE', *, *, #23439, .T. ) ;
#43954=CARTESIAN_POINT ( 'NONE',  ( 7.743176658771999676, 2.735218126362000124, 6.771983639047999937 ) ) ;
#43956=DIRECTION ( 'NONE',  ( 1.000000000000000000, 0.000000000000000000, 0.000000000000000000 ) ) ;
#43963=CARTESIAN_POINT ( 'NONE',  ( 7.789447165042808763, 5.491073919830230743, -6.392873027944447450 ) ) ;
#43964=CARTESIAN_POINT ( 'NONE',  ( 9.129428851719998406, 5.099284414202999827, 6.151604790022999758 ) ) ;
#43970=EDGE_CURVE ( 'NONE', #10927, #35290, #13293, .T. ) ;
#43975=CARTESIAN_POINT ( 'NONE',  ( 8.500189158773000742, 2.724453559418999582, -8.908010318766001134 ) ) ;
#43976=CARTESIAN_POINT ( 'NONE',  ( 2.265629263920999836, 1.834942145265999969, -2.713944450215000082 ) ) ;
#43978=CARTESIAN_POINT ( 'NONE',  ( 10.77706886429733402, 2.899999999999999911, -6.444141223373583749 ) ) ;
#43982=CARTESIAN_POINT ( 'NONE',  ( 1.839363843321667691, -3.114462284487641508, -1.632227178342313012 ) ) ;
#43983=VECTOR ( 'NONE', #36495, 1000.000000000000114 ) ;
#43984=CARTESIAN_POINT ( 'NONE',  ( 10.37373942323999998, 2.215265813302000009, 7.703982730183001060 ) ) ;
#43987=CARTESIAN_POINT ( 'NONE',  ( 4.500000000000000000, 13.10000000000000142, -1.604287306883032847E-15 ) ) ;
#43988=CARTESIAN_POINT ( 'NONE',  ( 5.399998535875000449, 12.99045401563999924, -1.690592933733000125 ) ) ;
#43991=CARTESIAN_POINT ( 'NONE',  ( 10.45582195740702325, 2.255160618932426697, 7.383274727460120701 ) ) ;
#44004=CARTESIAN_POINT ( 'NONE',  ( 7.256079719589999755, 2.531201476950000195, 8.216704145297999418 ) ) ;
#44005=AXIS2_PLACEMENT_3D ( 'NONE', #45324, #8254, #61051 ) ;
#44006=CARTESIAN_POINT ( 'NONE',  ( 9.939260841229000221, 5.099602161831000124, -9.049221499261999924 ) ) ;
#44008=CARTESIAN_POINT ( 'NONE',  ( 3.023038497928110413, -3.255317685661237803, 0.1302360752436395042 ) ) ;
#44009=ORIENTED_EDGE ( 'NONE', *, *, #22248, .T. ) ;
#44010=CARTESIAN_POINT ( 'NONE',  ( 10.96876099447000108, 2.333339469804000199, 6.524055942683999021 ) ) ;
#44015=CARTESIAN_POINT ( 'NONE',  ( 8.205377021103002377, 3.106081841748002059, 6.107037662485001128 ) ) ;
#44026=ORIENTED_EDGE ( 'NONE', *, *, #63133, .F. ) ;
#44031=EDGE_LOOP ( 'NONE', ( #43166, #43636, #48741, #42878, #33992 ) ) ;
#44033=CARTESIAN_POINT ( 'NONE',  ( 8.962479719595000560, 2.546924812613000189, -6.918870225297999887 ) ) ;
#44047=CARTESIAN_POINT ( 'NONE',  ( 10.95282897429000002, 2.845676247909999734, -5.175250098289999379 ) ) ;
#44049=DIRECTION ( 'NONE',  ( 1.000000000000000000, 0.000000000000000000, 0.000000000000000000 ) ) ;
#44050=CARTESIAN_POINT ( 'NONE',  ( 8.061933748689000367, 4.603465626214999773, -6.221450782568999749 ) ) ;
#44055=CARTESIAN_POINT ( 'NONE',  ( 9.251926658770999623, 5.159258275969999197, 9.109498396691998678 ) ) ;
#44061=CARTESIAN_POINT ( 'NONE',  ( 7.303793052280064479, 3.233246055057100943, 6.357929222382162848 ) ) ;
#44066=CARTESIAN_POINT ( 'NONE',  ( 11.12440625316000009, 5.543025011711000261, 5.163735498011999603 ) ) ;
#44074=EDGE_CURVE ( 'NONE', #6099, #46556, #20436, .T. ) ;
#44075=B_SPLINE_CURVE_WITH_KNOTS ( 'NONE', 3,
 ( #30321, #8642, #12863, #34877, #56196, #55511, #39777, #35226, #8304, #66677, #34543, #19127, #61097, #46393 ),
 .UNSPECIFIED., .F., .F.,
 ( 4, 2, 2, 1, 1, 2, 2, 4 ),
 ( 0.000000000000000000, 0.2500000000001028067, 0.3750000000001583178, 0.4375000000001811329, 0.4687500000001925127, 0.4843750000001808553, 0.5000000000001691980, 1.000000000000000000 ),
 .UNSPECIFIED. ) ;
#44077=CARTESIAN_POINT ( 'NONE',  ( 4.149992563292000725, 2.000000000000000000, 0.000000000000000000 ) ) ;
#44078=EDGE_CURVE ( 'NONE', #57550, #41936, #1928, .T. ) ;
#44081=CARTESIAN_POINT ( 'NONE',  ( 9.497295280408998508, 3.734279507827999556, 8.942126004519000304 ) ) ;
#44084=ORIENTED_EDGE ( 'NONE', *, *, #8223, .F. ) ;
#44085=CARTESIAN_POINT ( 'NONE',  ( 8.047385841228999581, 4.468366666325000125, 8.882140983065999862 ) ) ;
#44095=CARTESIAN_POINT ( 'NONE',  ( 1.114745999307000135, -3.300563260077000294, -0.9171157435373999967 ) ) ;
#44102=CARTESIAN_POINT ( 'NONE',  ( 10.98417233644999946, 2.893962206862000119, 4.881461471176000266 ) ) ;
#44105=ORIENTED_EDGE ( 'NONE', *, *, #43411, .F. ) ;
#44106=CARTESIAN_POINT ( 'NONE',  ( 7.604583333330377393, 5.349999999999999645, -7.323285413235573138 ) ) ;
#44107=CARTESIAN_POINT ( 'NONE',  ( 9.564884880418375701, 5.349923162331274185, -7.500006638304977713 ) ) ;
#44109=CARTESIAN_POINT ( 'NONE',  ( 10.51835931249053324, 5.126777126165764642, -6.752018918838221140 ) ) ;
#44110=CARTESIAN_POINT ( 'NONE',  ( 1.705112477863000020, -2.304706330186000240, 2.969293668968000066 ) ) ;
#44114=CARTESIAN_POINT ( 'NONE',  ( 9.514114512910998300, 4.887632373702999189, 8.462748516415999234 ) ) ;
#44117=EDGE_CURVE ( 'NONE', #57932, #22650, #35757, .T. ) ;
#44125=CARTESIAN_POINT ( 'NONE',  ( 8.795585841232000490, 5.251032986819000214, -6.070151079272999795 ) ) ;
#44133=CARTESIAN_POINT ( 'NONE',  ( 11.20904666305999875, 5.937823941418000295, 7.147334722859000067 ) ) ;
#44138=CARTESIAN_POINT ( 'NONE',  ( 11.08380555355736163, 3.999999927305438963, -9.033895164528459532 ) ) ;
#44139=VERTEX_POINT ( 'NONE', #40386 ) ;
#44142=EDGE_CURVE ( 'NONE', #9965, #57932, #40830, .T. ) ;
#44144=FACE_OUTER_BOUND ( 'NONE', #68955, .T. ) ;
#44146=EDGE_CURVE ( 'NONE', #6099, #27955, #59149, .T. ) ;
#44147=ORIENTED_EDGE ( 'NONE', *, *, #66482, .F. ) ;
#44148=CARTESIAN_POINT ( 'NONE',  ( 10.90000000000000036, 2.778483479159999714, -6.925197956411000000 ) ) ;
#44154=CARTESIAN_POINT ( 'NONE',  ( 7.850354840490529895, 2.911893064861816427, -6.650750720717241826 ) ) ;
#44156=ORIENTED_EDGE ( 'NONE', *, *, #12756, .F. ) ;
#44162=CARTESIAN_POINT ( 'NONE',  ( 9.684729719592999331, 2.370176859044999862, -6.912649125838000508 ) ) ;
#44191=B_SPLINE_SURFACE_WITH_KNOTS ( 'NONE', 3, 3, ( 
 ( #580, #49155, #11400, #26463, #21889, #53375, #54055, #64529, #16648, #37974, #21547, #58611, #32737, #15961, #1267, #926, #47795, #22583, #48126, #21206, #42539, #22238, #64876, #69103, #10712, #16988, #13495, #40065, #18733, #23286, #34816, #28893, #28186, #44964, #55791 ),
 ( #12104, #44628, #61377, #18047, #55099, #7541, #7895, #17703, #49852, #39364, #59994, #8237, #65230, #29232, #50203, #44279, #23972, #24315, #65920, #56128, #12448, #50543, #33434, #60684, #17343, #54750, #12801, #34129, #23624, #29584, #50887, #2304, #2982, #66268, #39027 ),
 ( #39715, #18390, #38672, #2643, #6849, #1962, #49501, #1613, #55446, #61033, #22929, #65579, #60342, #33783, #13152, #45306, #7205, #34480, #28541, #66613, #41765, #3658, #35499, #20438, #9248, #14172, #56820, #9594, #8920, #67290, #29923, #9949, #45980, #62057, #15194 ),
 ( #31286, #14517, #19408, #30257, #56473, #8575, #20097, #3326, #14854, #4689, #30938, #57152, #41423, #36517, #52594, #25682, #35834, #57842, #24996, #57488, #52254, #63068, #51561, #24658, #51229, #30590, #46676, #4350, #67980, #36176, #40733, #62398, #46331, #47015, #45649 ) ),
 .UNSPECIFIED., .F., .F., .F.,
 ( 4, 4 ),
 ( 4, 1, 1, 1, 1, 1, 1, 1, 1, 1, 1, 1, 1, 1, 1, 1, 1, 1, 1, 1, 1, 1, 1, 1, 1, 1, 1, 1, 1, 1, 1, 1, 4 ),
 ( -0.1039370721279000015, 1.103937072127999963 ),
 ( -0.01999999999998999800, 0.01250000000001000137, 0.04500000000000999728, 0.07750000000001000533, 0.1100000000000000006, 0.1424999999999999878, 0.1749999999999999889, 0.2074999999999999900, 0.2399999999999999911, 0.2725000000000000200, 0.3049999999999999933, 0.3375000000000000222, 0.3699999999999999956, 0.4025000000000000244, 0.4349999999999999978, 0.4675000000000000266, 0.5000000000000000000, 0.5324999999999999734, 0.5649999999999999467, 0.5975000000000000311, 0.6300000000000000044, 0.6624999999999999778, 0.6949999999999999512, 0.7275000000000000355, 0.7600000000000000089, 0.7924999999999000622, 0.8249999999999000355, 0.8574999999999000089, 0.8899999999999000933, 0.9224999999999000666, 0.9549999999999000400, 0.9874999999999000133, 1.020000000000000018 ),
 .UNSPECIFIED. ) ;
#44192=CARTESIAN_POINT ( 'NONE',  ( 7.000000000000000000, 10.32086050633190766, -4.256250858473547893 ) ) ;
#44197=CARTESIAN_POINT ( 'NONE',  ( 9.406851002546000373, 2.832432432432000269, -6.822293592207000934 ) ) ;
#44206=CARTESIAN_POINT ( 'NONE',  ( 2.327754220767750404, -2.003492624900453212, -2.889646723249190696 ) ) ;
#44210=VERTEX_POINT ( 'NONE', #20781 ) ;
#44215=CARTESIAN_POINT ( 'NONE',  ( 7.307500000000000107, 0.2999999999999999889, 3.149999999999999911 ) ) ;
#44217=CIRCLE ( 'NONE', #14064, 1.500000000000001110 ) ;
#44218=FACE_OUTER_BOUND ( 'NONE', #65996, .T. ) ;
#44223=VERTEX_POINT ( 'NONE', #53287 ) ;
#44224=CARTESIAN_POINT ( 'NONE',  ( 8.299720885770000223, 3.399999999999999911, -6.084164326786999588 ) ) ;
#44226=B_SPLINE_CURVE_WITH_KNOTS ( 'NONE', 3,
 ( #65049, #32572, #53884, #38857 ),
 .UNSPECIFIED., .F., .F.,
 ( 4, 4 ),
 ( 0.000000000000000000, 0.1254233535197428473 ),
 .UNSPECIFIED. ) ;
#44230=CARTESIAN_POINT ( 'NONE',  ( 10.44806481732999792, 3.684980864017000091, -6.173120265414000052 ) ) ;
#44236=CARTESIAN_POINT ( 'NONE',  ( 8.266851002545999805, 2.832432432432000269, 6.822293592207000934 ) ) ;
#44241=ORIENTED_EDGE ( 'NONE', *, *, #25050, .T. ) ;
#44242=FACE_OUTER_BOUND ( 'NONE', #25180, .T. ) ;
#44243=CARTESIAN_POINT ( 'NONE',  ( 10.71315778041000044, 2.619207518211999819, -8.142085279690999045 ) ) ;
#44255=CARTESIAN_POINT ( 'NONE',  ( 8.748814158775001459, 5.251032986819000214, -6.070151079272999795 ) ) ;
#44259=LINE ( 'NONE', #17678, #65170 ) ;
#44265=CIRCLE ( 'NONE', #4052, 3.200000000000000178 ) ;
#44270=CARTESIAN_POINT ( 'NONE',  ( 4.149992563291998948, -1.599290730647371594, 1.229060429538527011 ) ) ;
#44272=CARTESIAN_POINT ( 'NONE',  ( 10.89419229449708659, 5.254378413735692810, 6.992145683900290898 ) ) ;
#44273=CARTESIAN_POINT ( 'NONE',  ( 9.897084615057014645, 5.285910559402416276, 7.026781793019058142 ) ) ;
#44274=CARTESIAN_POINT ( 'NONE',  ( 9.749220280410998640, 5.656948148960999845, -6.994239053114000626 ) ) ;
#44277=CARTESIAN_POINT ( 'NONE',  ( 0.5516986677755000290, 3.485378829570000114, 1.246872170512999922 ) ) ;
#44279=CARTESIAN_POINT ( 'NONE',  ( 2.690656551265000029, 2.202451855867999964, 2.837790456605000067 ) ) ;
#44284=CARTESIAN_POINT ( 'NONE',  ( 6.950054030189999565, -13.87069231928999891, 4.225386915259999654 ) ) ;
#44286=CARTESIAN_POINT ( 'NONE',  ( 7.293864158771000028, 3.416213390569000197, 6.162512717529000206 ) ) ;
#44289=EDGE_CURVE ( 'NONE', #64753, #30347, #14091, .T. ) ;
#44291=CARTESIAN_POINT ( 'NONE',  ( 10.92585229548211423, 9.545762865684249476, 6.039706820605043269 ) ) ;
#44296=CYLINDRICAL_SURFACE ( 'NONE', #36665, 0.5000000000000000000 ) ;
#44298=CARTESIAN_POINT ( 'NONE',  ( 10.03687746070841058, 5.286620459901869573, -7.027007559937229253 ) ) ;
#44300=CARTESIAN_POINT ( 'NONE',  ( 0.09997256829956273350, 2.799974420760032334, 1.315025725132122498E-09 ) ) ;
#44302=AXIS2_PLACEMENT_3D ( 'NONE', #11352, #22531, #43870 ) ;
#44306=DIRECTION ( 'NONE',  ( -0.7071067811865086039, -0.6115519423577077118, 0.3549707337212042457 ) ) ;
#44311=CARTESIAN_POINT ( 'NONE',  ( 7.935739158771999868, 5.430400319332999715, 7.210801214872999410 ) ) ;
#44315=ORIENTED_EDGE ( 'NONE', *, *, #53449, .F. ) ;
#44316=DIRECTION ( 'NONE',  ( 0.000000000000000000, -1.000000000000000000, 0.000000000000000000 ) ) ;
#44319=CARTESIAN_POINT ( 'NONE',  ( 5.000030787342999439, 0.5496608443529871213, 2.045306479342561268 ) ) ;
#44325=VERTEX_POINT ( 'NONE', #66184 ) ;
#44327=CARTESIAN_POINT ( 'NONE',  ( 9.395239158775000377, 5.045571591548999812, -9.086294919530001124 ) ) ;
#44328=CARTESIAN_POINT ( 'NONE',  ( 3.383414956651999983, 2.956519816798000022, 1.636834048316999857 ) ) ;
#44331=CARTESIAN_POINT ( 'NONE',  ( 3.500000000000000000, 1.140396268832999827, -3.309002319436000317 ) ) ;
#44335=EDGE_CURVE ( 'NONE', #866, #67604, #54949, .T. ) ;
#44336=DIRECTION ( 'NONE',  ( -1.000000000000000000, 3.552713679026999935E-14, -3.552713679026999935E-14 ) ) ;
#44338=CARTESIAN_POINT ( 'NONE',  ( 9.939321360490000146, 2.638097915594000309, 6.328629954376999933 ) ) ;
#44341=B_SPLINE_CURVE_WITH_KNOTS ( 'NONE', 3,
 ( #49118, #28501, #34089, #44926 ),
 .UNSPECIFIED., .F., .F.,
 ( 4, 4 ),
 ( 0.000000000000000000, 1.000000000000000000 ),
 .UNSPECIFIED. ) ;
#44342=CARTESIAN_POINT ( 'NONE',  ( 9.208681878221188555, 2.678902866167812924, 7.777850098883442698 ) ) ;
#44344=CARTESIAN_POINT ( 'NONE',  ( 7.100000000000176392, 3.045734354883735229, -8.506847764030522896 ) ) ;
#44358=CARTESIAN_POINT ( 'NONE',  ( 7.239691113742999562, 4.389299166881000858, 9.135259451319999613 ) ) ;
#44359=CARTESIAN_POINT ( 'NONE',  ( 8.845310841232000953, 5.851083642416999631, -7.072167224702999633 ) ) ;
#44361=CARTESIAN_POINT ( 'NONE',  ( 10.98632665877000036, 3.015084670878999784, -9.064442106213000727 ) ) ;
#44362=EDGE_LOOP ( 'NONE', ( #45944, #58430, #48603, #13664, #64739 ) ) ;
#44363=CARTESIAN_POINT ( 'NONE',  ( 10.46754281781999829, 2.318340407652000223, 6.549777679168999001 ) ) ;
#44371=EDGE_CURVE ( 'NONE', #36055, #39994, #60762, .T. ) ;
#44372=EDGE_CURVE ( 'NONE', #23807, #58927, #10728, .T. ) ;
#44382=ORIENTED_EDGE ( 'NONE', *, *, #45315, .F. ) ;
#44383=DIRECTION ( 'NONE',  ( 0.000000000000000000, -0.9916377111174248249, -0.1290528957048031888 ) ) ;
#44384=ORIENTED_EDGE ( 'NONE', *, *, #31262, .F. ) ;
#44385=CARTESIAN_POINT ( 'NONE',  ( 9.699495280410998177, 5.048004622677000341, -6.120508709481000231 ) ) ;
#44387=CARTESIAN_POINT ( 'NONE',  ( 8.262341161841696646, 5.029723662799696626, 6.384309865549246510 ) ) ;
#44391=DIRECTION ( 'NONE',  ( 1.000000000000000000, 0.000000000000000000, 0.000000000000000000 ) ) ;
#44400=CARTESIAN_POINT ( 'NONE',  ( 11.13224000329999974, 2.679518535232000342, -4.955559702528000265 ) ) ;
#44408=CARTESIAN_POINT ( 'NONE',  ( 8.096551658772000337, 5.061727314042999915, 5.824077473724000420 ) ) ;
#44412=DIRECTION ( 'NONE',  ( 0.000000000000000000, 1.000000000000000000, 0.000000000000000000 ) ) ;
#44417=CARTESIAN_POINT ( 'NONE',  ( 11.25041981190000051, 5.730782764036999488, 8.122675980938000251 ) ) ;
#44418=AXIS2_PLACEMENT_3D ( 'NONE', #44454, #7371, #54926 ) ;
#44421=CARTESIAN_POINT ( 'NONE',  ( 2.202983345419999850, 2.610295513370000098, -1.876847361837999939 ) ) ;
#44430=CARTESIAN_POINT ( 'NONE',  ( 9.459510841229999301, 5.445214367171999470, 7.703373622193999459 ) ) ;
#44431=CARTESIAN_POINT ( 'NONE',  ( 8.674830025576062198, 2.649890579813255709, 7.499988935010339475 ) ) ;
#44438=CARTESIAN_POINT ( 'NONE',  ( 9.537173706499306292, 4.215401811041960656, 8.849618031277225683 ) ) ;
#44443=EDGE_LOOP ( 'NONE', ( #62399, #1321, #48668, #18155 ) ) ;
#44444=CARTESIAN_POINT ( 'NONE',  ( 1.405611034014000227, -1.124102084663000101, 3.059032707631999859 ) ) ;
#44449=CARTESIAN_POINT ( 'NONE',  ( 10.02314899745999988, 5.167567567567999731, -6.822293592207000934 ) ) ;
#44452=CARTESIAN_POINT ( 'NONE',  ( 10.98148522610999933, 2.884794181589999784, 4.906648103019000118 ) ) ;
#44454=CARTESIAN_POINT ( 'NONE',  ( -15.86200481174999943, 2.399999999999999911, -6.571291218949999902 ) ) ;
#44458=EDGE_CURVE ( 'NONE', #55115, #69034, #48255, .T. ) ;
#44459=FACE_OUTER_BOUND ( 'NONE', #53603, .T. ) ;
#44462=CARTESIAN_POINT ( 'NONE',  ( 10.52314899745999988, 5.167567567567999731, -6.822293592207000934 ) ) ;
#44465=CARTESIAN_POINT ( 'NONE',  ( 1.855140132539666586, -0.9161175952574772685, -3.408904368339104707 ) ) ;
#44469=CONICAL_SURFACE ( 'NONE', #64533, 2.824973347946000413, 0.7853886971611369061 ) ;
#44476=VERTEX_POINT ( 'NONE', #67555 ) ;
#44477=CARTESIAN_POINT ( 'NONE',  ( 7.366448187504803791, 3.134553601932692946, 9.009082482539499281 ) ) ;
#44480=CARTESIAN_POINT ( 'NONE',  ( 7.793464139059000040, 3.207866775510000323, 6.406745604615000644 ) ) ;
#44486=CARTESIAN_POINT ( 'NONE',  ( 10.89874804681000064, 2.834828962328999502, 9.088465460431999432 ) ) ;
#44495=ORIENTED_EDGE ( 'NONE', *, *, #42056, .T. ) ;
#44496=CARTESIAN_POINT ( 'NONE',  ( 10.68942872663553523, 3.124652943151730700, -4.799721330066085478 ) ) ;
#44498=FACE_OUTER_BOUND ( 'NONE', #66274, .T. ) ;
#44503=DIRECTION ( 'NONE',  ( -7.209535665603963368E-10, -0.7071067809378975833, -0.7071067814351975622 ) ) ;
#44506=CARTESIAN_POINT ( 'NONE',  ( 6.794909439180999655, 5.172411450403999744, -8.246583185469999577 ) ) ;
#44511=CARTESIAN_POINT ( 'NONE',  ( 9.825045280412000537, 3.116293075258000478, -6.208411413796000033 ) ) ;
#44516=CARTESIAN_POINT ( 'NONE',  ( 8.294122261300687526, 2.649609490281852331, -7.853149655434442877 ) ) ;
#44518=CARTESIAN_POINT ( 'NONE',  ( 10.90000668870999867, -1.199999999999999956, -9.776630298829998011 ) ) ;
#44521=CARTESIAN_POINT ( 'NONE',  ( 1.000973465875999890, 3.500000000000000000, 0.000000000000000000 ) ) ;
#44527=DIRECTION ( 'NONE',  ( 1.000000000000000000, 0.000000000000000000, 0.000000000000000000 ) ) ;
#44550=VECTOR ( 'NONE', #29920, 1000.000000000000000 ) ;
#44551=CARTESIAN_POINT ( 'NONE',  ( 8.455992358796999397, 5.100000000000000533, 6.571291218954000257 ) ) ;
#44553=VERTEX_POINT ( 'NONE', #755 ) ;
#44559=CARTESIAN_POINT ( 'NONE',  ( 7.000000000000000888, 10.53694504865381631, 4.009111100864517496 ) ) ;
#44568=CARTESIAN_POINT ( 'NONE',  ( 8.854170280414001226, 4.902869380824999901, -8.978557145469999057 ) ) ;
#44574=CARTESIAN_POINT ( 'NONE',  ( 8.374870900372675564, 4.397654444569530696, -6.040776445627388469 ) ) ;
#44578=CARTESIAN_POINT ( 'NONE',  ( 10.30296826955000000, 4.081263352980999848, -9.025008366823000117 ) ) ;
#44579=ORIENTED_EDGE ( 'NONE', *, *, #6394, .T. ) ;
#44582=CARTESIAN_POINT ( 'NONE',  ( 10.99338701711599242, 6.091027238782714903, -5.064515391775427311 ) ) ;
#44583=DIRECTION ( 'NONE',  ( 0.000000000000000000, 1.000000000000000000, 0.000000000000000000 ) ) ;
#44585=B_SPLINE_CURVE_WITH_KNOTS ( 'NONE', 3,
 ( #26056, #31647, #58210, #62078, #4023, #41447, #57867, #14197, #9270, #35522, #15568, #56844, #42140, #20459, #57511, #62756, #25706, #8942 ),
 .UNSPECIFIED., .F., .F.,
 ( 4, 2, 2, 2, 2, 2, 2, 2, 4 ),
 ( 0.000000000000000000, 0.1250000000000000000, 0.2500000000000000000, 0.3750000000000000000, 0.5000000000000000000, 0.6250000000000000000, 0.7500000000000000000, 0.8750000000000000000, 1.000000000000000000 ),
 .UNSPECIFIED. ) ;
#44590=CARTESIAN_POINT ( 'NONE',  ( 11.16750778041000025, 3.188704589882000118, -8.788663768996000769 ) ) ;
#44599=ORIENTED_EDGE ( 'NONE', *, *, #6692, .T. ) ;
#44601=CARTESIAN_POINT ( 'NONE',  ( 8.889129719593999113, 5.687930027805999877, -7.109876198051000351 ) ) ;
#44609=CARTESIAN_POINT ( 'NONE',  ( 8.766851002546001581, 2.832432432432000269, 6.822293592207000934 ) ) ;
#44612=CARTESIAN_POINT ( 'NONE',  ( 8.668369459057998938, 3.037916315484999963, -6.050520490110999461 ) ) ;
#44615=CARTESIAN_POINT ( 'NONE',  ( 6.999999691988000095, 11.00717859340000082, -1.432487142323000118 ) ) ;
#44616=CARTESIAN_POINT ( 'NONE',  ( 4.149992563291999836, 0.2617923565147971532, 1.999946284944288388 ) ) ;
#44620=CARTESIAN_POINT ( 'NONE',  ( 8.903895280414001689, 3.867331042029999999, -9.227339949050001877 ) ) ;
#44625=EDGE_CURVE ( 'NONE', #7311, #63350, #15817, .T. ) ;
#44628=CARTESIAN_POINT ( 'NONE',  ( 2.039003242238999647, 1.871422929480999864, -2.898831499164999936 ) ) ;
#44629=VERTEX_POINT ( 'NONE', #21724 ) ;
#44633=CARTESIAN_POINT ( 'NONE',  ( 9.181704719590001673, 3.734279507827999556, 8.942126004519000304 ) ) ;
#44634=VERTEX_POINT ( 'NONE', #20706 ) ;
#44636=CARTESIAN_POINT ( 'NONE',  ( 10.94393950981584496, 9.248375527724082446, 6.280586408606567694 ) ) ;
#44638=DIRECTION ( 'NONE',  ( 1.000000000000000000, 0.000000000000000000, 0.000000000000000000 ) ) ;
#44643=EDGE_CURVE ( 'NONE', #23998, #26809, #43308, .T. ) ;
#44648=CARTESIAN_POINT ( 'NONE',  ( 10.94661356027324750, 9.196282120471490629, -6.312081210087247207 ) ) ;
#44651=CARTESIAN_POINT ( 'NONE',  ( 8.378939858970831267, 5.131721239846337212, 6.760536747085705400 ) ) ;
#44652=FACE_OUTER_BOUND ( 'NONE', #35574, .T. ) ;
#44656=CARTESIAN_POINT ( 'NONE',  ( 8.256676658772999389, 2.876288091423999660, 6.568897128359000526 ) ) ;
#44658=CARTESIAN_POINT ( 'NONE',  ( 11.02644139764960229, 5.226441397652185294, 6.590108525923451310 ) ) ;
#44659=CARTESIAN_POINT ( 'NONE',  ( 8.379867906096000851, 2.923743482149999906, 6.439439799146000176 ) ) ;
#44664=CARTESIAN_POINT ( 'NONE',  ( 5.000030787343002103, -1.834918991542628941, 1.057581170753189248 ) ) ;
#44671=CIRCLE ( 'NONE', #29051, 2.000000000000000888 ) ;
#44673=FACE_OUTER_BOUND ( 'NONE', #16655, .T. ) ;
#44674=CARTESIAN_POINT ( 'NONE',  ( 2.503158723626000004, -1.438123771530000150, 3.058110052863999950 ) ) ;
#44677=CARTESIAN_POINT ( 'NONE',  ( 8.163776391448005043, 3.396249911995000481, -6.162465440825001473 ) ) ;
#44685=CARTESIAN_POINT ( 'NONE',  ( 10.34520858566999912, 2.724123081339000052, 6.497325124886000225 ) ) ;
#44688=CARTESIAN_POINT ( 'NONE',  ( 10.99166666666766723, 4.098468854244242010, 8.958105619230160244 ) ) ;
#44693=CARTESIAN_POINT ( 'NONE',  ( 0.7509734658760000015, -3.500000000000000000, 0.000000000000000000 ) ) ;
#44694=CARTESIAN_POINT ( 'NONE',  ( 10.56170778040999991, 5.057487376164999660, -8.595710652231000282 ) ) ;
#44698=CARTESIAN_POINT ( 'NONE',  ( 7.000000000000000000, 0.3230303992915000144, 3.000000000000000000 ) ) ;
#44703=CARTESIAN_POINT ( 'NONE',  ( 7.999926658772999133, 5.198556077301000222, 8.332552905512999430 ) ) ;
#44706=CARTESIAN_POINT ( 'NONE',  ( 10.87273915876999908, 5.407616985330000681, -8.698399706473999515 ) ) ;
#44708=CARTESIAN_POINT ( 'NONE',  ( 10.35616100078999935, 2.777276096020000029, 8.995275123087999702 ) ) ;
#44714=CARTESIAN_POINT ( 'NONE',  ( 11.09999999999999964, 5.299769311822999818, 5.136744346970999686 ) ) ;
#44718=DIRECTION ( 'NONE',  ( 1.000000000000000000, 0.000000000000000000, 0.000000000000000000 ) ) ;
#44724=ADVANCED_FACE ( 'NONE', ( #49336 ), #38503, .T. ) ;
#44726=ORIENTED_EDGE ( 'NONE', *, *, #40963, .F. ) ;
#44727=CARTESIAN_POINT ( 'NONE',  ( 9.053070280414001303, 2.391443348526999912, -6.856688371964000162 ) ) ;
#44734=EDGE_LOOP ( 'NONE', ( #19427, #26413, #51654, #47755 ) ) ;
#44744=CARTESIAN_POINT ( 'NONE',  ( 8.457129882803000598, 5.100036551512999949, -6.571411952062999440 ) ) ;
#44750=CARTESIAN_POINT ( 'NONE',  ( 9.085767219592000288, 2.821863697211000055, 6.127145479358000024 ) ) ;
#44754=CARTESIAN_POINT ( 'NONE',  ( 10.48734600210000067, 4.351287276768000645, -6.182257940481999725 ) ) ;
#44755=AXIS2_PLACEMENT_3D ( 'NONE', #50341, #30064, #8035 ) ;
#44757=CARTESIAN_POINT ( 'NONE',  ( 10.96255537160999971, 5.431623798070999598, 4.905442062451000673 ) ) ;
#44758=CARTESIAN_POINT ( 'NONE',  ( 10.52638970730999901, 2.451081172664000274, 6.282749363171999946 ) ) ;
#44759=ADVANCED_FACE ( 'NONE', ( #59828 ), #28410, .F. ) ;
#44767=CARTESIAN_POINT ( 'NONE',  ( 9.681187238460999822, 2.612249048987000055, 7.804677627401999551 ) ) ;
#44772=CARTESIAN_POINT ( 'NONE',  ( 8.149357780409999918, 2.583668273793999770, 6.684750595573999199 ) ) ;
#44773=CARTESIAN_POINT ( 'NONE',  ( 11.20904666305999875, 5.937823941418000295, 7.147334722859000067 ) ) ;
#44776=CARTESIAN_POINT ( 'NONE',  ( 8.897989158775001073, 4.990139824845000405, -9.121472988377998803 ) ) ;
#44778=EDGE_CURVE ( 'NONE', #58012, #55873, #11591, .T. ) ;
#44781=DIRECTION ( 'NONE',  ( 1.000000000000000000, 0.000000000000000000, 0.000000000000000000 ) ) ;
#44785=CARTESIAN_POINT ( 'NONE',  ( 1.453292983455000131, -2.653487697479000040, 1.892165331686999963 ) ) ;
#44794=ORIENTED_EDGE ( 'NONE', *, *, #33625, .T. ) ;
#44796=CARTESIAN_POINT ( 'NONE',  ( 11.04798050665000098, 5.246683672049000435, 5.092742987927000975 ) ) ;
#44798=CARTESIAN_POINT ( 'NONE',  ( 9.564884880418375701, 5.349923162331274185, -7.500006638304977713 ) ) ;
#44799=CARTESIAN_POINT ( 'NONE',  ( 1.975310191361000056, 2.864690124100000013, -2.197449004149000462 ) ) ;
#44801=CARTESIAN_POINT ( 'NONE',  ( 1.750973465873000068, -3.500000000000000000, 0.000000000000000000 ) ) ;
#44804=CARTESIAN_POINT ( 'NONE',  ( 10.40516904918000129, 5.216391323504000255, 6.765759859247999941 ) ) ;
#44808=CARTESIAN_POINT ( 'NONE',  ( 6.999999691988000095, 1.243449787579999883E-13, -1.714942017578999994E-13 ) ) ;
#44809=EDGE_CURVE ( 'NONE', #31174, #26452, #51597, .T. ) ;
#44814=CARTESIAN_POINT ( 'NONE',  ( 7.916096965541012942, 2.414406326178271112, 8.226579130988907806 ) ) ;
#44824=CARTESIAN_POINT ( 'NONE',  ( 9.595493858556999101, 3.928424745541000185, 5.531312048131000303 ) ) ;
#44831=VERTEX_POINT ( 'NONE', #24327 ) ;
#44832=CARTESIAN_POINT ( 'NONE',  ( 0.7106019637973529646, 2.186897047493125523, -2.353682317170576965 ) ) ;
#44834=DIRECTION ( 'NONE',  ( 1.000000000000000000, 0.000000000000000000, 0.000000000000000000 ) ) ;
#44836=CARTESIAN_POINT ( 'NONE',  ( 5.000030787343000327, 1.290525307673961120, -1.679270695423620952 ) ) ;
#44841=CARTESIAN_POINT ( 'NONE',  ( 10.12947109217999930, 5.100000000000000533, 6.152188490330000370 ) ) ;
#44843=EDGE_CURVE ( 'NONE', #46708, #44139, #36622, .T. ) ;
#44845=DIRECTION ( 'NONE',  ( 0.000000000000000000, -1.000000000000000000, 0.000000000000000000 ) ) ;
#44849=CARTESIAN_POINT ( 'NONE',  ( 8.739954719592999410, 3.122811675949999977, -6.006064052396999919 ) ) ;
#44851=CARTESIAN_POINT ( 'NONE',  ( 10.96581858901999951, 7.643649345463000344, -6.313571852796998840 ) ) ;
#44852=DIRECTION ( 'NONE',  ( 1.000000000000000000, 0.000000000000000000, 0.000000000000000000 ) ) ;
#44866=EDGE_CURVE ( 'NONE', #48780, #26681, #64090, .T. ) ;
#44868=VECTOR ( 'NONE', #30817, 1000.000000000000000 ) ;
#44879=CARTESIAN_POINT ( 'NONE',  ( 7.000000000000000000, 10.55012386388540335, -4.027521431284991849 ) ) ;
#44898=ORIENTED_EDGE ( 'NONE', *, *, #15398, .T. ) ;
#44900=CARTESIAN_POINT ( 'NONE',  ( 2.561390132543708287, 3.499999999999999112, 0.4581489286485193602 ) ) ;
#44901=CARTESIAN_POINT ( 'NONE',  ( 9.972410841228999345, 4.357364160690000432, -9.282962013144999247 ) ) ;
#44910=CARTESIAN_POINT ( 'NONE',  ( 7.100000000000000533, 5.221516520829000640, -8.074802043613001246 ) ) ;
#44911=VERTEX_POINT ( 'NONE', #54760 ) ;
#44913=CARTESIAN_POINT ( 'NONE',  ( 9.949437606643998677, 2.508497579857000392, -7.171862210735000076 ) ) ;
#44924=ADVANCED_FACE ( 'NONE', ( #49511 ), #29245, .F. ) ;
#44926=CARTESIAN_POINT ( 'NONE',  ( 9.433148997456999751, 5.167567567567999731, 6.822293592207000934 ) ) ;
#44927=CARTESIAN_POINT ( 'NONE',  ( 10.50897971959000010, 4.485029564998000318, -9.114435267298000909 ) ) ;
#44929=ADVANCED_FACE ( 'NONE', ( #50555 ), #22064, .F. ) ;
#44936=VERTEX_POINT ( 'NONE', #2314 ) ;
#44938=CARTESIAN_POINT ( 'NONE',  ( 9.196339158776000389, 4.112741311853999271, -5.603466076760000192 ) ) ;
#44952=CARTESIAN_POINT ( 'NONE',  ( 11.10000000000000142, 5.421946730020413163, 6.652676983765400287 ) ) ;
#44957=CARTESIAN_POINT ( 'NONE',  ( 8.856793857978997764, 5.100000000000000533, -6.339888365514000590 ) ) ;
#44958=CARTESIAN_POINT ( 'NONE',  ( 9.649770280412001355, 4.042991257420999851, -5.768106221333000327 ) ) ;
#44964=CARTESIAN_POINT ( 'NONE',  ( 3.442447097232000264, 1.741959211826000109, -3.162405688284999794 ) ) ;
#44972=CARTESIAN_POINT ( 'NONE',  ( 8.385635841226999787, 2.841678116489999795, -6.718113446527000931 ) ) ;
#44974=CARTESIAN_POINT ( 'NONE',  ( 10.60664092702282346, 5.179495029648225390, -8.179803431736248243 ) ) ;
#44976=VERTEX_POINT ( 'NONE', #49862 ) ;
#44983=EDGE_CURVE ( 'NONE', #15150, #7244, #25718, .T. ) ;
#44985=CARTESIAN_POINT ( 'NONE',  ( 10.94064497426557558, 9.306490196098094358, -6.239143843092519681 ) ) ;
#44987=CARTESIAN_POINT ( 'NONE',  ( 7.292164158769000259, 2.863733890340999899, -8.313606627241000524 ) ) ;
#44991=CARTESIAN_POINT ( 'NONE',  ( 9.587288403116620117, 2.899999999999999911, -6.305985889556955826 ) ) ;
#44998=DIRECTION ( 'NONE',  ( 0.000000000000000000, 1.000000000000000000, 0.000000000000000000 ) ) ;
#45010=CARTESIAN_POINT ( 'NONE',  ( 9.825045280412000537, 3.116293075258000478, -6.208411413796000033 ) ) ;
#45012=CARTESIAN_POINT ( 'NONE',  ( 2.412568162807000149, -1.368190713007999992, 2.909400328758999787 ) ) ;
#45015=CARTESIAN_POINT ( 'NONE',  ( 7.798085185677998687, 3.459333709783000366, -6.382131374430003667 ) ) ;
#45017=ORIENTED_EDGE ( 'NONE', *, *, #37583, .T. ) ;
#45019=CARTESIAN_POINT ( 'NONE',  ( 10.15293113568789352, 5.100000000000000533, -6.444141223401127938 ) ) ;
#45022=CARTESIAN_POINT ( 'NONE',  ( 9.218008530890955399, 2.655297806746307554, 7.619097669105685533 ) ) ;
#45024=EDGE_CURVE ( 'NONE', #49108, #33013, #59891, .T. ) ;
#45029=CARTESIAN_POINT ( 'NONE',  ( 0.8685892898898377457, -0.3281013245661921207, -3.507234403409725587 ) ) ;
#45030=CARTESIAN_POINT ( 'NONE',  ( 10.23581084123000018, 3.621841509808999771, -8.806208131805998818 ) ) ;
#45031=ORIENTED_EDGE ( 'NONE', *, *, #303, .T. ) ;
#45039=CARTESIAN_POINT ( 'NONE',  ( 8.513426658773999733, 5.040787533781999841, 8.522957620707000359 ) ) ;
#45041=FACE_OUTER_BOUND ( 'NONE', #63501, .T. ) ;
#45042=CARTESIAN_POINT ( 'NONE',  ( 10.94846415877000112, 3.841064079579000090, -9.341816855317999213 ) ) ;
#45044=CARTESIAN_POINT ( 'NONE',  ( 9.298033738970000073, 4.087077023028999001, 9.429414864145000408 ) ) ;
#45048=CARTESIAN_POINT ( 'NONE',  ( 7.453125355210004521, 3.231590054310000237, 6.459270056246999125 ) ) ;
#45049=VERTEX_POINT ( 'NONE', #3337 ) ;
#45062=AXIS2_PLACEMENT_3D ( 'NONE', #23927, #19978, #46889 ) ;
#45065=EDGE_CURVE ( 'NONE', #14617, #3072, #59225, .T. ) ;
#45067=CARTESIAN_POINT ( 'NONE',  ( 8.456370280410999030, 2.836879604150999601, -8.783908972046001296 ) ) ;
#45069=CARTESIAN_POINT ( 'NONE',  ( 8.237102957402385073, 4.936199535989180376, 6.266989881494448689 ) ) ;
#45075=CARTESIAN_POINT ( 'NONE',  ( 9.226510893196484986, 2.899999999999999911, -6.310481362401603178 ) ) ;
#45083=DIRECTION ( 'NONE',  ( 0.8843050080896639464, -0.1786785916254929885, 0.4313683038451824325 ) ) ;
#45084=CARTESIAN_POINT ( 'NONE',  ( 7.621422090919002912, 4.588776658069999570, 6.481258258681996232 ) ) ;
#45088=CARTESIAN_POINT ( 'NONE',  ( 8.716851002545999094, 2.832432432432000269, 6.822293592207000934 ) ) ;
#45090=CARTESIAN_POINT ( 'NONE',  ( 7.839801658770999992, 3.084076314893000159, 9.259847992573000397 ) ) ;
#45094=CARTESIAN_POINT ( 'NONE',  ( 7.413218301918568010, 4.974493527912905222, 6.530297539223000491 ) ) ;
#45096=CARTESIAN_POINT ( 'NONE',  ( 10.17309652395999997, 4.709165316578000748, -8.664874001714000684 ) ) ;
#45099=CARTESIAN_POINT ( 'NONE',  ( 10.71256887705999894, 5.951815279772000089, 7.233043586354999555 ) ) ;
#45105=CARTESIAN_POINT ( 'NONE',  ( 10.20319667131999886, 3.421760346951000287, 6.017732782098999422 ) ) ;
#45111=CARTESIAN_POINT ( 'NONE',  ( 8.545864158774001851, 3.856772556595000179, 5.521246073317000125 ) ) ;
#45112=CARTESIAN_POINT ( 'NONE',  ( 9.566963020987998334, 5.215925787220999865, 6.177726425586999248 ) ) ;
#45124=CARTESIAN_POINT ( 'NONE',  ( 0.8715629140400000807, 2.401393137604999950, -2.383704365015999915 ) ) ;
#45129=CARTESIAN_POINT ( 'NONE',  ( 4.900006121742000786, -2.000000000000001332, -0.2617993877991417473 ) ) ;
#45130=CARTESIAN_POINT ( 'NONE',  ( 6.999999691988000095, -1.865174681369999698E-13, 1.040631529540999901E-13 ) ) ;
#45133=VERTEX_POINT ( 'NONE', #53300 ) ;
#45134=CARTESIAN_POINT ( 'NONE',  ( 9.459510841229999301, 5.445214367171999470, 7.703373622193999459 ) ) ;
#45137=VECTOR ( 'NONE', #55507, 1000.000000000000000 ) ;
#45139=CARTESIAN_POINT ( 'NONE',  ( 0.8420640498653999551, -3.400502393318999950, 1.157769971473999959 ) ) ;
#45141=CARTESIAN_POINT ( 'NONE',  ( 10.65673534980369119, 5.179482957638356311, -8.179835726794676631 ) ) ;
#45143=CARTESIAN_POINT ( 'NONE',  ( 9.444315208305999576, 2.927258006877999641, 8.897018628538001295 ) ) ;
#45149=CYLINDRICAL_SURFACE ( 'NONE', #42252, 11.84999999999999964 ) ;
#45154=CARTESIAN_POINT ( 'NONE',  ( 7.938548115121596638, 2.267677432809916294, 7.755639217155871457 ) ) ;
#45155=AXIS2_PLACEMENT_3D ( 'NONE', #43853, #2917, #2575 ) ;
#45160=VERTEX_POINT ( 'NONE', #16232 ) ;
#45163=AXIS2_PLACEMENT_3D ( 'NONE', #37307, #58982, #27866 ) ;
#45165=DIRECTION ( 'NONE',  ( 1.000000000000000000, 0.000000000000000000, 0.000000000000000000 ) ) ;
#45166=CARTESIAN_POINT ( 'NONE',  ( 10.25165889348999926, 3.418644779562000302, -8.733642166016998942 ) ) ;
#45168=CARTESIAN_POINT ( 'NONE',  ( 9.660528907822998335, 2.899999999999999911, -6.152188490330000370 ) ) ;
#45175=B_SPLINE_CURVE_WITH_KNOTS ( 'NONE', 3,
 ( #49094, #49434, #19699, #2246, #66203, #7833, #23559, #14458, #13084, #56065, #57092, #51173, #39648, #56414, #51504, #35778, #44900, #14114 ),
 .UNSPECIFIED., .F., .F.,
 ( 4, 2, 2, 2, 2, 2, 2, 2, 4 ),
 ( 0.000000000000000000, 0.1250000000000000278, 0.2500000000000000000, 0.3749999999999999445, 0.4999999999999999445, 0.6249999999999998890, 0.7499999999999998890, 0.8750000000000000000, 1.000000000000000000 ),
 .UNSPECIFIED. ) ;
#45176=DIRECTION ( 'NONE',  ( 0.000000000000000000, 1.000000000000000000, 0.000000000000000000 ) ) ;
#45177=PLANE ( 'NONE',  #4603 ) ;
#45185=ORIENTED_EDGE ( 'NONE', *, *, #44142, .T. ) ;
#45186=CARTESIAN_POINT ( 'NONE',  ( 11.04384236319999957, 7.001054304361000291, 5.879104636179000032 ) ) ;
#45192=ADVANCED_FACE ( 'NONE', ( #37219 ), #158, .T. ) ;
#45193=DIRECTION ( 'NONE',  ( 1.000000000000000000, 0.000000000000000000, 0.000000000000000000 ) ) ;
#45195=CARTESIAN_POINT ( 'NONE',  ( 0.5842604209659999492, 3.128647331775999962, -1.414269894618000123 ) ) ;
#45199=CARTESIAN_POINT ( 'NONE',  ( 9.817462135711998883, 5.100000000000000533, 6.571291218949999902 ) ) ;
#45202=CARTESIAN_POINT ( 'NONE',  ( 11.09991415876999987, 2.373387781209999936, -6.776601845694000481 ) ) ;
#45206=B_SPLINE_CURVE_WITH_KNOTS ( 'NONE', 3,
 ( #38195, #43803, #65098, #38547, #67177 ),
 .UNSPECIFIED., .F., .F.,
 ( 4, 1, 4 ),
 ( 0.000000000000000000, 0.5000000000000000000, 1.000000000000000000 ),
 .UNSPECIFIED. ) ;
#45210=CARTESIAN_POINT ( 'NONE',  ( 8.856793857978997764, 5.100000000000000533, -6.339888365514000590 ) ) ;
#45220=CARTESIAN_POINT ( 'NONE',  ( 5.399998535875000449, 6.217248937900999058E-14, -13.10000000000360210 ) ) ;
#45222=CARTESIAN_POINT ( 'NONE',  ( 7.000000000000000888, 7.162101251533245616, 3.226271710805416415 ) ) ;
#45225=DIRECTION ( 'NONE',  ( -1.000000000000000000, 0.000000000000000000, 0.000000000000000000 ) ) ;
#45228=ORIENTED_EDGE ( 'NONE', *, *, #66632, .T. ) ;
#45235=CARTESIAN_POINT ( 'NONE',  ( 4.900006121741999898, 1.947945353336630436, -0.5234957687185638475 ) ) ;
#45236=CARTESIAN_POINT ( 'NONE',  ( 9.708354719591000048, 5.481267232667000222, -8.005061172455999241 ) ) ;
#45238=ORIENTED_EDGE ( 'NONE', *, *, #55793, .T. ) ;
#45239=CARTESIAN_POINT ( 'NONE',  ( 4.000000000000000000, 1.878608423871360289, 1.082950885222729420 ) ) ;
#45244=CARTESIAN_POINT ( 'NONE',  ( 9.310554719594000161, 3.934138271021000222, -9.063586117809000697 ) ) ;
#45253=CARTESIAN_POINT ( 'NONE',  ( 8.599639158772999892, 2.261390688294000029, -6.733978371730000134 ) ) ;
#45256=CARTESIAN_POINT ( 'NONE',  ( 10.56590837162999996, 5.293226105229999590, -7.067087619452999903 ) ) ;
#45261=CIRCLE ( 'NONE', #32967, 12.49999909016000110 ) ;
#45262=CARTESIAN_POINT ( 'NONE',  ( 8.239310352252500635, 2.650829846289728842, 7.263894687833489350 ) ) ;
#45269=CARTESIAN_POINT ( 'NONE',  ( 10.82674528040999995, 3.167160000746000126, -6.225151413000000744 ) ) ;
#45278=ORIENTED_EDGE ( 'NONE', *, *, #61833, .T. ) ;
#45279=CARTESIAN_POINT ( 'NONE',  ( 8.640504719592000171, 2.305580295895999665, -7.860904109308999743 ) ) ;
#45280=EDGE_CURVE ( 'NONE', #53432, #36464, #20582, .T. ) ;
#45286=DIRECTION ( 'NONE',  ( 1.000000000000000000, 0.000000000000000000, 0.000000000000000000 ) ) ;
#45292=CARTESIAN_POINT ( 'NONE',  ( 7.931011803055000975, 3.387313518888000363, -6.297038610257000180 ) ) ;
#45295=CARTESIAN_POINT ( 'NONE',  ( 4.149992563291998948, 0.5234817089163672499, 1.947893036340042849 ) ) ;
#45297=CARTESIAN_POINT ( 'NONE',  ( 11.09999999999999964, 5.299311513382999550, 5.124965750789000296 ) ) ;
#45299=CARTESIAN_POINT ( 'NONE',  ( 8.655270280412999284, 4.162493982103000256, -5.775210092227999858 ) ) ;
#45301=CARTESIAN_POINT ( 'NONE',  ( 9.271640687503564848, 2.873222873816658307, 6.752018918868503583 ) ) ;
#45303=AXIS2_PLACEMENT_3D ( 'NONE', #30837, #52497, #36420 ) ;
#45306=CARTESIAN_POINT ( 'NONE',  ( 2.781247112084000328, 2.100317644827999874, 2.706193714288000152 ) ) ;
#45313=EDGE_LOOP ( 'NONE', ( #51939, #53548, #60275, #27707, #6033, #5361, #48579, #67254, #5529, #54159 ) ) ;
#45315=EDGE_CURVE ( 'NONE', #10058, #13432, #24803, .T. ) ;
#45317=CARTESIAN_POINT ( 'NONE',  ( 8.087285841226000471, 5.397384434738000003, -7.480682713844000631 ) ) ;
#45320=DIRECTION ( 'NONE',  ( 0.000000000000000000, 0.7071067811865474617, 0.7071067811865474617 ) ) ;
#45323=ORIENTED_EDGE ( 'NONE', *, *, #50671, .T. ) ;
#45324=CARTESIAN_POINT ( 'NONE',  ( 0.000000000000000000, 0.000000000000000000, 0.000000000000000000 ) ) ;
#45331=FACE_OUTER_BOUND ( 'NONE', #49179, .T. ) ;
#45333=ORIENTED_EDGE ( 'NONE', *, *, #36440, .F. ) ;
#45343=DIRECTION ( 'NONE',  ( 1.000000000000000000, 0.000000000000000000, 0.000000000000000000 ) ) ;
#45344=CARTESIAN_POINT ( 'NONE',  ( 3.500000000000000888, 2.793279419286928356, 1.985771234201202606 ) ) ;
#45346=PLANE ( 'NONE',  #57759 ) ;
#45353=AXIS2_PLACEMENT_3D ( 'NONE', #8832, #9167, #46588 ) ;
#45354=CARTESIAN_POINT ( 'NONE',  ( 8.532195280408998883, 5.331510020787000315, -8.114341808290998159 ) ) ;
#45355=CARTESIAN_POINT ( 'NONE',  ( 2.580236016716999981, -1.802165296364000024, -2.662471851299000214 ) ) ;
#45360=ORIENTED_EDGE ( 'NONE', *, *, #38262, .T. ) ;
#45362=CARTESIAN_POINT ( 'NONE',  ( 10.40726830891999910, 3.797905842462999892, 5.889914049998000500 ) ) ;
#45365=CARTESIAN_POINT ( 'NONE',  ( 10.68403803949000164, 5.436614310638000269, 8.578436083822998270 ) ) ;
#45366=CARTESIAN_POINT ( 'NONE',  ( 9.074999999999999289, 4.417172942406000224, 8.783926296998000538 ) ) ;
#45374=CARTESIAN_POINT ( 'NONE',  ( 8.093108454043214550, 5.099642902067280659, -6.624168013080805828 ) ) ;
#45379=LINE ( 'NONE', #44698, #33407 ) ;
#45381=ORIENTED_EDGE ( 'NONE', *, *, #27078, .F. ) ;
#45382=CARTESIAN_POINT ( 'NONE',  ( 7.422239158771000156, 5.361039412362000434, 6.973453640356000349 ) ) ;
#45383=CARTESIAN_POINT ( 'NONE',  ( 9.690635841230999858, 2.927176851028000293, -5.932007155957999878 ) ) ;
#45384=CARTESIAN_POINT ( 'NONE',  ( 0.7532955584366096691, -2.936936850608698801, 1.972122296016285858 ) ) ;
#45385=CARTESIAN_POINT ( 'NONE',  ( 10.19121415877000203, 3.990707652596999555, -5.651362387566000400 ) ) ;
#45393=FACE_BOUND ( 'NONE', #52992, .T. ) ;
#45395=EDGE_CURVE ( 'NONE', #51926, #14947, #22042, .T. ) ;
#45399=CONICAL_SURFACE ( 'NONE', #9693, 1.449999999967999553, 0.7853981633972997312 ) ;
#45411=CARTESIAN_POINT ( 'NONE',  ( 8.704995280412999747, 5.140767546012999567, -6.196177269779999719 ) ) ;
#45437=CARTESIAN_POINT ( 'NONE',  ( 10.80159548023000049, 2.805082485475999476, -8.157276499959001725 ) ) ;
#45438=CARTESIAN_POINT ( 'NONE',  ( 8.717034166355354330, 5.096433331277959056, 6.336971952315185064 ) ) ;
#45439=AXIS2_PLACEMENT_3D ( 'NONE', #7151, #66562, #35115 ) ;
#45442=CARTESIAN_POINT ( 'NONE',  ( 11.27110638630999873, 5.469603964121000139, 8.504707115835000053 ) ) ;
#45448=CARTESIAN_POINT ( 'NONE',  ( 9.722769750889000306, 5.493785011855999656, 6.566826815556000341 ) ) ;
#45450=AXIS2_PLACEMENT_3D ( 'NONE', #27151, #21888, #47794 ) ;
#45453=EDGE_CURVE ( 'NONE', #27484, #45997, #1396, .T. ) ;
#45454=EDGE_CURVE ( 'NONE', #26293, #12504, #22311, .T. ) ;
#45455=CARTESIAN_POINT ( 'NONE',  ( 7.866204719590000671, 4.580608786027000612, 9.213365309690999538 ) ) ;
#45456=CARTESIAN_POINT ( 'NONE',  ( 9.075483283097998566, 4.020836891789999257, 8.948690653012000951 ) ) ;
#45459=CARTESIAN_POINT ( 'NONE',  ( 8.450464158772000189, 3.789127741898000057, -9.388182174781999123 ) ) ;
#45467=CARTESIAN_POINT ( 'NONE',  ( 1.057517373740999966, 3.437215509016000148, 1.521310954037999874 ) ) ;
#45477=CARTESIAN_POINT ( 'NONE',  ( 9.331135841230999262, 4.141907758973999876, 6.047574021139999978 ) ) ;
#45480=CARTESIAN_POINT ( 'NONE',  ( 10.25000000000000000, 0.000000000000000000, 0.000000000000000000 ) ) ;
#45484=CARTESIAN_POINT ( 'NONE',  ( 1.843384988122999779, -3.419251011552999930, 1.101167613520000144 ) ) ;
#45485=ORIENTED_EDGE ( 'NONE', *, *, #60477, .T. ) ;
#45486=CARTESIAN_POINT ( 'NONE',  ( 1.896806799206333327, 0.9161175952574848180, -3.408904368339103819 ) ) ;
#45487=ADVANCED_FACE ( 'NONE', ( #65384 ), #22227, .F. ) ;
#45489=CARTESIAN_POINT ( 'NONE',  ( 10.22398792753999963, 5.507894434963000130, 6.589802269404000157 ) ) ;
#45492=CYLINDRICAL_SURFACE ( 'NONE', #18956, 2.750000000000000000 ) ;
#45495=DIRECTION ( 'NONE',  ( -1.000000000000000000, 0.000000000000000000, 0.000000000000000000 ) ) ;
#45498=CARTESIAN_POINT ( 'NONE',  ( 8.068768932173844277, 3.857044016492371163, 5.763189706540536861 ) ) ;
#45506=PLANE ( 'NONE',  #29400 ) ;
#45509=CYLINDRICAL_SURFACE ( 'NONE', #13053, 1.350000000000000533 ) ;
#45523=CARTESIAN_POINT ( 'NONE',  ( 6.865208375034998589, 8.291377142895010266, 4.196513763680004061 ) ) ;
#45536=CONICAL_SURFACE ( 'NONE', #41030, 2.074968475931999734, 0.7853828752794411727 ) ;
#45538=CARTESIAN_POINT ( 'NONE',  ( 8.823496488120920134, 2.820676299976329293, -8.179574529512112946 ) ) ;
#45539=EDGE_CURVE ( 'NONE', #59750, #12624, #9816, .T. ) ;
#45540=EDGE_CURVE ( 'NONE', #9263, #34148, #23374, .T. ) ;
#45541=CARTESIAN_POINT ( 'NONE',  ( 0.3428519969243999932, -2.525007632204000263, -2.706826389191999915 ) ) ;
#45543=CONICAL_SURFACE ( 'NONE', #54461, 1.449999999967999553, 0.7853981633972997312 ) ;
#45555=CIRCLE ( 'NONE', #51134, 1.900000000000001021 ) ;
#45564=ORIENTED_EDGE ( 'NONE', *, *, #1041, .T. ) ;
#45569=CARTESIAN_POINT ( 'NONE',  ( 2.521806799209333150, 3.408904368339103375, 0.9161175952574877046 ) ) ;
#45570=CARTESIAN_POINT ( 'NONE',  ( 5.407309473667999633, 12.95251760905999916, 1.915207572621000054 ) ) ;
#45579=CARTESIAN_POINT ( 'NONE',  ( 3.040556799211332706, 3.500000000000000888, -0.4581489286485045387 ) ) ;
#45580=CARTESIAN_POINT ( 'NONE',  ( 9.667489158770999680, 4.808846957865000604, -8.639578604182998944 ) ) ;
#45583=CARTESIAN_POINT ( 'NONE',  ( 5.000000000000000000, 0.6769230769231000533, -2.665384615385000266 ) ) ;
#45588=EDGE_CURVE ( 'NONE', #50903, #48489, #23059, .T. ) ;
#45589=CARTESIAN_POINT ( 'NONE',  ( 8.754720280412998434, 5.687930027805999877, -7.109876198051000351 ) ) ;
#45599=CARTESIAN_POINT ( 'NONE',  ( 6.649999999999999467, 5.221516520829000640, -8.074802043613001246 ) ) ;
#45601=CARTESIAN_POINT ( 'NONE',  ( 10.69578011722000177, 5.505003832924999507, -7.759263776825999770 ) ) ;
#45602=EDGE_LOOP ( 'NONE', ( #41362, #11270, #51082, #17464, #12903, #42249, #2035 ) ) ;
#45605=DIRECTION ( 'NONE',  ( 1.000000000000000000, 0.000000000000000000, 0.000000000000000000 ) ) ;
#45606=CARTESIAN_POINT ( 'NONE',  ( 11.04230989607018643, 2.757690103929812064, 6.361542621410388065 ) ) ;
#45608=CARTESIAN_POINT ( 'NONE',  ( 8.428197172116266955, 5.125396288426561142, 6.749639981083130458 ) ) ;
#45614=CARTESIAN_POINT ( 'NONE',  ( 8.455992358769000461, 4.599999999999999645, 6.571291218974000259 ) ) ;
#45620=EDGE_CURVE ( 'NONE', #8503, #45133, #59054, .T. ) ;
#45621=ORIENTED_EDGE ( 'NONE', *, *, #10584, .T. ) ;
#45622=ORIENTED_EDGE ( 'NONE', *, *, #66755, .F. ) ;
#45623=CARTESIAN_POINT ( 'NONE',  ( 8.491329719591000469, 4.851303550474000303, -9.008742670124000540 ) ) ;
#45624=DIRECTION ( 'NONE',  ( 0.7071067811866525998, 0.000000000000000000, -0.7071067811864425456 ) ) ;
#45644=CARTESIAN_POINT ( 'NONE',  ( 9.342560841233000346, 5.835196551504000517, -7.008466539623000813 ) ) ;
#45645=EDGE_CURVE ( 'NONE', #47743, #65548, #17792, .T. ) ;
#45648=CARTESIAN_POINT ( 'NONE',  ( 0.3474143384075761842, -2.924575863667731035, 1.686609425636008908 ) ) ;
#45649=CARTESIAN_POINT ( 'NONE',  ( 3.730112762836999885, 1.979060574517999882, -2.346675849479999965 ) ) ;
#45654=CARTESIAN_POINT ( 'NONE',  ( 8.064114158772998309, 4.228291488957999888, 8.941375734143997889 ) ) ;
#45658=CARTESIAN_POINT ( 'NONE',  ( 10.90570892106003065, 9.799753219705101159, 5.723325390456533768 ) ) ;
#45659=CARTESIAN_POINT ( 'NONE',  ( 10.76290585702710523, 2.920651757519677538, -8.329491109684418859 ) ) ;
#45661=CARTESIAN_POINT ( 'NONE',  ( 1.521806799207250149, 3.408904368339103375, 0.9161175952574877046 ) ) ;
#45665=ORIENTED_EDGE ( 'NONE', *, *, #57375, .T. ) ;
#45670=CARTESIAN_POINT ( 'NONE',  ( 10.90000053908999966, 9.856474340180000127, -5.627824942316999923 ) ) ;
#45671=CARTESIAN_POINT ( 'NONE',  ( 9.299999999999998934, 4.537600397704999899, 9.154563893594000135 ) ) ;
#45682=ORIENTED_EDGE ( 'NONE', *, *, #59925, .T. ) ;
#45683=CYLINDRICAL_SURFACE ( 'NONE', #26082, 1.350000000000000533 ) ;
#45685=CARTESIAN_POINT ( 'NONE',  ( 10.71685100253999856, 2.832432432432000269, 6.822293592207000934 ) ) ;
#45693=ORIENTED_EDGE ( 'NONE', *, *, #66910, .T. ) ;
#45694=CARTESIAN_POINT ( 'NONE',  ( 10.20319667131999886, 3.421760346951000287, 6.017732782098999422 ) ) ;
#45695=LINE ( 'NONE', #19113, #66858 ) ;
#45696=CARTESIAN_POINT ( 'NONE',  ( 10.01508584123000034, 4.845406482350000488, -6.387189183984999907 ) ) ;
#45697=CARTESIAN_POINT ( 'NONE',  ( 3.138669809652000264, -2.989695960142000342, 1.902536878218999972 ) ) ;
#45699=CARTESIAN_POINT ( 'NONE',  ( 10.20000030442999872, 12.49999969551000056, -3.568568717444000015E-10 ) ) ;
#45701=EDGE_LOOP ( 'NONE', ( #33975, #53565, #47690, #3788 ) ) ;
#45703=CARTESIAN_POINT ( 'NONE',  ( 10.62697636434999993, 3.142921793056999924, 8.668445734229999644 ) ) ;
#45707=CARTESIAN_POINT ( 'NONE',  ( 10.37373942323999998, 2.215265813302000009, 7.703982730183001060 ) ) ;
#45710=B_SPLINE_CURVE_WITH_KNOTS ( 'NONE', 3,
 ( #23211, #11672, #22166, #53981, #44559, #33011, #28822, #48746, #2238, #65503, #23552, #12378, #66196, #54326, #27777, #49087, #1199, #43850, #38956, #17975, #59919, #39294, #18318, #12028, #60962, #33364, #6777 ),
 .UNSPECIFIED., .F., .F.,
 ( 4, 2, 2, 2, 2, 2, 2, 2, 2, 2, 1, 2, 2, 4 ),
 ( 0.000000000000000000, 0.1249999999999979183, 0.1874999999999976963, 0.2499999999999975020, 0.3124999999999972800, 0.3749999999999970579, 0.4374999999999968914, 0.4999999999999966693, 0.6249999999999976685, 0.7499999999999986677, 0.8124999999999992228, 0.8437499999999992228, 0.8749999999999993339, 1.000000000000000000 ),
 .UNSPECIFIED. ) ;
#45715=CARTESIAN_POINT ( 'NONE',  ( 5.000015393671500163, -2.571712834666313134E-16, -2.099962892531002545 ) ) ;
#45720=ADVANCED_FACE ( 'NONE', ( #19155 ), #18477, .T. ) ;
#45722=CARTESIAN_POINT ( 'NONE',  ( 10.31746213571000048, 5.100000000000000533, 6.571291218949999902 ) ) ;
#45725=CARTESIAN_POINT ( 'NONE',  ( 8.347267219593000220, 2.741641653469999884, 6.457329666915000210 ) ) ;
#45728=CARTESIAN_POINT ( 'NONE',  ( 10.49411415877000131, 2.866942652264999669, -8.960728730887002058 ) ) ;
#45742=ORIENTED_EDGE ( 'NONE', *, *, #31710, .F. ) ;
#45743=CARTESIAN_POINT ( 'NONE',  ( 2.750973465876000557, -3.500000000000000000, 0.000000000000000000 ) ) ;
#45749=CARTESIAN_POINT ( 'NONE',  ( 9.798945280410000791, 5.639765292528999829, -8.059103558718000215 ) ) ;
#45754=CARTESIAN_POINT ( 'NONE',  ( 7.988545280410000338, 3.566637212418000136, 5.743604853744000316 ) ) ;
#45761=B_SPLINE_SURFACE_WITH_KNOTS ( 'NONE', 3, 3, ( 
 ( #25733, #9644, #41133, #3370, #51950, #62443, #30640, #65712, #13878, #46377, #9299, #36226, #17834, #14564, #24708, #67677, #51611, #62781, #57540, #39153, #30992, #60476, #35882, #46724, #52301, #25045, #12584, #35549, #14902, #46030, #4398, #33914, #55231, #57197, #56867 ),
 ( #4049, #29973, #25386, #24362, #8286, #68029, #67337, #8625, #14222, #8964, #40433, #35209, #29631, #50933, #20143, #45694, #41473, #3032, #67002, #30304, #19111, #61759, #56520, #51276, #3706, #19458, #40778, #62102, #19805, #21855, #31673, #4736, #9993, #31331, #47065 ),
 ( #52644, #54014, #15590, #26080, #47409, #57893, #26427, #58576, #68713, #48091, #64494, #43189, #542, #5091, #16614, #10679, #20832, #42167, #53340, #63467, #37594, #16269, #20487, #58928, #36919, #195, #36569, #5442, #48433, #64157, #47758, #6116, #58235, #41813, #52995 ),
 ( #26779, #69068, #63120, #10338, #21174, #11029, #15246, #42505, #68368, #63813, #15924, #37257, #21512, #37939, #59261, #42845, #11364, #32368, #32027, #53682, #32702, #5775, #27118, #59954, #1925, #22543, #888, #33745, #65538, #43539, #6812, #50165, #49460, #17307, #38986 ) ),
 .UNSPECIFIED., .F., .F., .F.,
 ( 4, 4 ),
 ( 4, 1, 1, 1, 1, 1, 1, 1, 1, 1, 1, 1, 1, 1, 1, 1, 1, 1, 1, 1, 1, 1, 1, 1, 1, 1, 1, 1, 1, 1, 1, 1, 4 ),
 ( -0.1039370721279000015, 1.103937072127999963 ),
 ( -0.01735257130020999988, 0.01084535706264999969, 0.03904328542550000031, 0.06724121378835999641, 0.09543914215121999944, 0.1236370705141000004, 0.1518349988768999959, 0.1800329272397999947, 0.2082308556026999935, 0.2364287839655000167, 0.2646267123283999601, 0.2928246406912000110, 0.3210225690540999821, 0.3492204974169000331, 0.3774184257798000042, 0.4056163541427000307, 0.4338142825054999707, 0.4620122108683999973, 0.4902101392311999928, 0.5184080675940999638, 0.5466059959569999904, 0.5748039243197999859, 0.6030018526827000125, 0.6311997810455000080, 0.6593977094084000345, 0.6875956377712000300, 0.7157935661340999456, 0.7439914944969999722, 0.7721894228597999676, 0.8003873512226999942, 0.8285852795854999897, 0.8567832079484000163, 0.8849811363112999318 ),
 .UNSPECIFIED. ) ;
#45773=EDGE_LOOP ( 'NONE', ( #50998, #19728, #47619, #50688, #3519 ) ) ;
#45778=DIRECTION ( 'NONE',  ( 0.000000000000000000, -0.9565994702956989171, 0.2914059941558995170 ) ) ;
#45780=FACE_OUTER_BOUND ( 'NONE', #47812, .T. ) ;
#45781=CARTESIAN_POINT ( 'NONE',  ( 10.22108913916999917, 2.983268757921999637, 8.764704075288999974 ) ) ;
#45786=ADVANCED_FACE ( 'NONE', ( #45393, #39803 ), #12890, .T. ) ;
#45788=CARTESIAN_POINT ( 'NONE',  ( 11.07345995138000028, 3.998673170817999889, 8.920816085870999501 ) ) ;
#45792=CARTESIAN_POINT ( 'NONE',  ( 8.481676658773000810, 2.472348777564000066, 6.234194744024999402 ) ) ;
#45793=CARTESIAN_POINT ( 'NONE',  ( 10.34520858566999912, 2.724123081339000052, 6.497325124886000225 ) ) ;
#45795=ORIENTED_EDGE ( 'NONE', *, *, #59514, .T. ) ;
#45805=CARTESIAN_POINT ( 'NONE',  ( 2.154202210879000212, -0.2286091751511999948, 3.751814989407999956 ) ) ;
#45806=EDGE_CURVE ( 'NONE', #43188, #10178, #45555, .T. ) ;
#45810=CARTESIAN_POINT ( 'NONE',  ( 11.03776785110999903, 5.237767851104999650, 6.571291218949999902 ) ) ;
#45811=CARTESIAN_POINT ( 'NONE',  ( 10.07102359808000003, 4.042170458878000083, 8.920189456109998360 ) ) ;
#45817=CARTESIAN_POINT ( 'NONE',  ( 7.464691113743000095, 4.351669901925999895, 8.977196921526999773 ) ) ;
#45818=CYLINDRICAL_SURFACE ( 'NONE', #66380, 11.84999999999999964 ) ;
#45820=DIRECTION ( 'NONE',  ( 0.4384236320213996119, 0.6355252626312996034, 0.6355252626312996034 ) ) ;
#45821=CARTESIAN_POINT ( 'NONE',  ( 0.7419268129216000096, 3.132555770593000055, 1.386468609675000074 ) ) ;
#45826=CARTESIAN_POINT ( 'NONE',  ( 10.98286939055999945, 3.998514186275999638, 9.091062412789998604 ) ) ;
#45833=CARTESIAN_POINT ( 'NONE',  ( 7.925081587919548198, 2.341303385547595983, 8.036180917343964225 ) ) ;
#45836=CARTESIAN_POINT ( 'NONE',  ( 11.09999999999999964, 2.685305999535000154, 6.664030027596000494 ) ) ;
#45837=EDGE_LOOP ( 'NONE', ( #12204, #65037, #11610, #23818, #50049 ) ) ;
#45844=CARTESIAN_POINT ( 'NONE',  ( 9.815201913989998417, 2.813632032385000148, 8.848857341496000117 ) ) ;
#45854=ORIENTED_EDGE ( 'NONE', *, *, #4016, .T. ) ;
#45856=AXIS2_PLACEMENT_3D ( 'NONE', #32976, #17237, #12341 ) ;
#45864=ORIENTED_EDGE ( 'NONE', *, *, #59514, .F. ) ;
#45874=CARTESIAN_POINT ( 'NONE',  ( 8.656893636725156327, 5.180000428241942068, -8.180009313714272423 ) ) ;
#45875=CARTESIAN_POINT ( 'NONE',  ( 0.5568389912892000027, 2.537743131474000435, -2.464631551651000230 ) ) ;
#45876=CARTESIAN_POINT ( 'NONE',  ( 11.09999999999999964, 2.700683852703999577, 5.124965750789000296 ) ) ;
#45880=DIRECTION ( 'NONE',  ( 0.000000000000000000, 1.000000000000000000, 0.000000000000000000 ) ) ;
#45886=ORIENTED_EDGE ( 'NONE', *, *, #38919, .T. ) ;
#45887=EDGE_CURVE ( 'NONE', #3039, #37419, #26123, .T. ) ;
#45894=CARTESIAN_POINT ( 'NONE',  ( 6.999999691988000095, -12.49999909016000110, 4.774434232535999529E-10 ) ) ;
#45896=B_SPLINE_CURVE_WITH_KNOTS ( 'NONE', 3,
 ( #63131, #67691, #57907, #48708, #52656, #31002, #36581, #31686, #27381, #68726, #52316, #30650, #14575, #19814, #35891, #63482, #4060, #57206 ),
 .UNSPECIFIED., .F., .F.,
 ( 4, 2, 2, 2, 2, 2, 2, 2, 4 ),
 ( 0.000000000000000000, 0.1250000000000000278, 0.2500000000000000000, 0.3749999999999999445, 0.4999999999999999445, 0.6249999999999998890, 0.7499999999999998890, 0.8750000000000000000, 1.000000000000000000 ),
 .UNSPECIFIED. ) ;
#45906=DIRECTION ( 'NONE',  ( 1.000000000000000000, 0.000000000000000000, 0.000000000000000000 ) ) ;
#45908=CARTESIAN_POINT ( 'NONE',  ( -0.000000000000000000, -2.824612379753681513, -0.7585797238568994239 ) ) ;
#45913=CARTESIAN_POINT ( 'NONE',  ( 9.260829719593999698, 4.861259245430999520, -8.806664389576001284 ) ) ;
#45915=EDGE_LOOP ( 'NONE', ( #37559, #44898, #17266, #37517 ) ) ;
#45918=EDGE_LOOP ( 'NONE', ( #47796, #66981, #19671, #3614, #1301, #12392 ) ) ;
#45921=CARTESIAN_POINT ( 'NONE',  ( 8.953620280414000376, 2.881930053949999682, -8.823338183322999129 ) ) ;
#45923=CARTESIAN_POINT ( 'NONE',  ( 10.13819615328233503, 2.541217446078312570, -6.488444088169603496 ) ) ;
#45932=CARTESIAN_POINT ( 'NONE',  ( 8.979720280412999855, 5.524776413195999325, -7.147585171405999915 ) ) ;
#45934=CARTESIAN_POINT ( 'NONE',  ( 10.15787172175999942, 4.213497149090000171, -5.822953133183999874 ) ) ;
#45941=FACE_OUTER_BOUND ( 'NONE', #21567, .T. ) ;
#45943=B_SPLINE_CURVE_WITH_KNOTS ( 'NONE', 3,
 ( #26763, #42150, #15574, #59936 ),
 .UNSPECIFIED., .F., .F.,
 ( 4, 4 ),
 ( 0.000000000000000000, 1.000000000000000000 ),
 .UNSPECIFIED. ) ;
#45944=ORIENTED_EDGE ( 'NONE', *, *, #19083, .T. ) ;
#45946=CARTESIAN_POINT ( 'NONE',  ( 10.50084834123000022, 4.616783736607999344, -6.288082254674000282 ) ) ;
#45951=FACE_OUTER_BOUND ( 'NONE', #26869, .T. ) ;
#45952=AXIS2_PLACEMENT_3D ( 'NONE', #50070, #1826, #45176 ) ;
#45953=CARTESIAN_POINT ( 'NONE',  ( 7.836901522150861332, 4.790146211336424820, 6.377682021994305117 ) ) ;
#45957=CARTESIAN_POINT ( 'NONE',  ( 10.10682028041000002, 4.294368353031000396, -8.968663198664000191 ) ) ;
#45959=CARTESIAN_POINT ( 'NONE',  ( 10.40685100253999984, 2.832432432432000269, -6.822293592207000934 ) ) ;
#45964=CARTESIAN_POINT ( 'NONE',  ( 8.651157662976507012, 5.422415455645571036, 6.482274542572600495 ) ) ;
#45966=VERTEX_POINT ( 'NONE', #58621 ) ;
#45975=CARTESIAN_POINT ( 'NONE',  ( 11.09999999999999964, 0.000000000000000000, 0.000000000000000000 ) ) ;
#45980=CARTESIAN_POINT ( 'NONE',  ( 3.591840252576999681, 0.3470336765304000148, -3.407861879647000158 ) ) ;
#45987=ORIENTED_EDGE ( 'NONE', *, *, #28497, .T. ) ;
#45990=CARTESIAN_POINT ( 'NONE',  ( 0.5525390791026434378, 2.818854795173400429, 2.124449897083314553 ) ) ;
#45992=CARTESIAN_POINT ( 'NONE',  ( 1.698890132539874642, -2.798833948393640192, 2.150913519912191152 ) ) ;
#45997=VERTEX_POINT ( 'NONE', #4439 ) ;
#46004=CARTESIAN_POINT ( 'NONE',  ( 10.94429324618039523, 9.240129021172709400, -6.284308437708901351 ) ) ;
#46007=CARTESIAN_POINT ( 'NONE',  ( 6.794914158771000245, 2.836301549691000012, -8.273864296493000481 ) ) ;
#46008=CARTESIAN_POINT ( 'NONE',  ( 10.20217841747468945, 2.710350078041137145, 7.038638062422410080 ) ) ;
#46011=VERTEX_POINT ( 'NONE', #19764 ) ;
#46023=B_SPLINE_CURVE_WITH_KNOTS ( 'NONE', 3,
 ( #6768, #43146, #1885, #28107 ),
 .UNSPECIFIED., .F., .F.,
 ( 4, 4 ),
 ( 0.000000000000000000, 1.000000000000000000 ),
 .UNSPECIFIED. ) ;
#46026=ORIENTED_EDGE ( 'NONE', *, *, #45540, .T. ) ;
#46030=CARTESIAN_POINT ( 'NONE',  ( 11.07345995138000028, 3.998673170817999889, 8.920816085870999501 ) ) ;
#46033=CARTESIAN_POINT ( 'NONE',  ( 10.12339528040999959, 3.988943694240999704, -8.966360307350999648 ) ) ;
#46034=CONICAL_SURFACE ( 'NONE', #10342, 3.249989426617000188, 0.7853950157668545540 ) ;
#46035=CARTESIAN_POINT ( 'NONE',  ( 3.438845187857999974, 1.765336245502999946, -3.260861573818000458 ) ) ;
#46042=CARTESIAN_POINT ( 'NONE',  ( 9.758140238852000437, 2.901378080241999946, 6.555076849497999625 ) ) ;
#46045=CARTESIAN_POINT ( 'NONE',  ( 9.104014120666999332, 5.045862207587999748, 8.527865280865999154 ) ) ;
#46058=EDGE_LOOP ( 'NONE', ( #42412, #10736, #4574 ) ) ;
#46064=CARTESIAN_POINT ( 'NONE',  ( 9.160308886257000793, 4.122021000979000149, 9.013569734175000292 ) ) ;
#46067=CARTESIAN_POINT ( 'NONE',  ( 10.31966721959000033, 4.764593388688000530, -5.997651217580999727 ) ) ;
#46069=CARTESIAN_POINT ( 'NONE',  ( 10.90000658885999840, -1.382741116750999977, 11.26545724788999969 ) ) ;
#46070=DIRECTION ( 'NONE',  ( -1.000000000000000000, 0.000000000000000000, 0.000000000000000000 ) ) ;
#46076=CARTESIAN_POINT ( 'NONE',  ( 7.169089158768000125, 3.469376689055999829, -5.675721888027999817 ) ) ;
#46094=CARTESIAN_POINT ( 'NONE',  ( 7.475045280409000625, 3.276311362504999991, 5.841989464160999290 ) ) ;
#46115=EDGE_CURVE ( 'NONE', #61556, #60646, #3666, .T. ) ;
#46119=CARTESIAN_POINT ( 'NONE',  ( 10.57793656291999973, 4.393379542724999531, -6.024362243994999311 ) ) ;
#46123=CARTESIAN_POINT ( 'NONE',  ( 10.37373942323999998, 2.215265813302000009, 7.703982730183001060 ) ) ;
#46124=CARTESIAN_POINT ( 'NONE',  ( 8.064958992852089281, 5.350069970865218849, -7.500002487662858819 ) ) ;
#46128=CARTESIAN_POINT ( 'NONE',  ( 10.09181485429000169, 2.440912084162000006, 7.817367409531000177 ) ) ;
#46130=CARTESIAN_POINT ( 'NONE',  ( 9.766460841231999979, 3.135494838036999798, -8.598037907310999373 ) ) ;
#46131=CIRCLE ( 'NONE', #56160, 2.000000000000000888 ) ;
#46136=CARTESIAN_POINT ( 'NONE',  ( 8.417489158772999858, 2.029098103856999735, 7.726995416028000108 ) ) ;
#46137=CARTESIAN_POINT ( 'NONE',  ( 10.84168637167000071, 2.681011538858999899, 6.554754637093000547 ) ) ;
#46139=ADVANCED_FACE ( 'NONE', ( #15551 ), #8928, .T. ) ;
#46140=VERTEX_POINT ( 'NONE', #25006 ) ;
#46141=CARTESIAN_POINT ( 'NONE',  ( 9.865910841232000905, 2.685250982074999904, -7.026194612421999608 ) ) ;
#46145=CARTESIAN_POINT ( 'NONE',  ( 3.354734521762166466, -0.9333907618945200824, -3.403975714020706977 ) ) ;
#46150=CARTESIAN_POINT ( 'NONE',  ( 1.963474413114999928, 2.711246897165000114, -2.603366577799000048 ) ) ;
#46153=CARTESIAN_POINT ( 'NONE',  ( 9.662145996929073277, 5.577690980164239143, 6.690401850488619573 ) ) ;
#46162=CARTESIAN_POINT ( 'NONE',  ( 9.047982780412000992, 2.806082850903000026, 8.615880516515998622 ) ) ;
#46165=B_SPLINE_CURVE_WITH_KNOTS ( 'NONE', 3,
 ( #55880, #67720, #40150, #25085 ),
 .UNSPECIFIED., .F., .F.,
 ( 4, 4 ),
 ( 0.000000000000000000, 1.000000000000000000 ),
 .UNSPECIFIED. ) ;
#46167=CARTESIAN_POINT ( 'NONE',  ( 8.725348536223823004, 2.649439212887079620, 7.500023728975156345 ) ) ;
#46168=CARTESIAN_POINT ( 'NONE',  ( 1.743247751179000105, 3.109069236570999539, 1.438230559479999782 ) ) ;
#46169=ORIENTED_EDGE ( 'NONE', *, *, #51828, .F. ) ;
#46170=CARTESIAN_POINT ( 'NONE',  ( 1.763186445774021838, 3.257444789362515802, -0.5454670069368401375 ) ) ;
#46173=CARTESIAN_POINT ( 'NONE',  ( 9.980433037259000884, 4.047223446241999589, 9.090360698422999874 ) ) ;
#46178=EDGE_CURVE ( 'NONE', #8371, #44325, #27730, .T. ) ;
#46181=CARTESIAN_POINT ( 'NONE',  ( 8.100081893396536614, 4.526455162270248245, 5.827331516791772970 ) ) ;
#46190=CARTESIAN_POINT ( 'NONE',  ( 11.02786554143000153, 5.596226216413000110, 7.209502215883999199 ) ) ;
#46197=CARTESIAN_POINT ( 'NONE',  ( 7.983198341228001205, 5.321913229613000063, 8.118244847118999630 ) ) ;
#46204=EDGE_CURVE ( 'NONE', #55375, #66241, #9257, .T. ) ;
#46210=ORIENTED_EDGE ( 'NONE', *, *, #55359, .T. ) ;
#46214=PLANE ( 'NONE',  #36535 ) ;
#46215=B_SPLINE_CURVE_WITH_KNOTS ( 'NONE', 3,
 ( #45671, #19087, #20119, #41448 ),
 .UNSPECIFIED., .F., .F.,
 ( 4, 4 ),
 ( 0.000000000000000000, 1.000000000000000000 ),
 .UNSPECIFIED. ) ;
#46220=CARTESIAN_POINT ( 'NONE',  ( 0.2605877078939999869, -3.617551005558000021, 0.7847820700415000239 ) ) ;
#46221=CARTESIAN_POINT ( 'NONE',  ( 10.25000000000000000, 0.000000000000000000, 0.000000000000000000 ) ) ;
#46225=DIRECTION ( 'NONE',  ( 1.000000000000000000, 0.000000000000000000, 0.000000000000000000 ) ) ;
#46226=AXIS2_PLACEMENT_3D ( 'NONE', #57053, #46225, #45880 ) ;
#46227=CARTESIAN_POINT ( 'NONE',  ( 10.53197665877000055, 2.323713329709999886, -8.279493667389999700 ) ) ;
#46249=CARTESIAN_POINT ( 'NONE',  ( 2.553056799209334038, 2.798833948393625537, 2.150913519912209360 ) ) ;
#46251=CARTESIAN_POINT ( 'NONE',  ( 5.399999743830999677, 12.99045401563999924, 1.690592933733000125 ) ) ;
#46252=CARTESIAN_POINT ( 'NONE',  ( 8.328793652375997780, 2.897388771918001371, 6.655272502545993341 ) ) ;
#46262=CARTESIAN_POINT ( 'NONE',  ( 2.381500749193374844, 0.2450796643850099432, -3.507702501826547081 ) ) ;
#46266=EDGE_CURVE ( 'NONE', #2928, #12641, #31359, .T. ) ;
#46267=CARTESIAN_POINT ( 'NONE',  ( 4.000000000000000888, -2.094138670346414433, 0.5626148410812730205 ) ) ;
#46273=CARTESIAN_POINT ( 'NONE',  ( 9.803753476949818690, 2.991225470601273528, -8.479526507175020100 ) ) ;
#46278=CARTESIAN_POINT ( 'NONE',  ( 8.856463691917767278, 5.100000000000000533, 6.665341197415465935 ) ) ;
#46280=CARTESIAN_POINT ( 'NONE',  ( 9.725595280412999699, 2.495531372253999791, -7.930944806125000746 ) ) ;
#46282=CARTESIAN_POINT ( 'NONE',  ( 10.39355883036999906, 4.089958667033000594, -9.188186800857998549 ) ) ;
#46291=DIRECTION ( 'NONE',  ( 0.6684585169941805738, 0.6684585169941805738, -0.3260773253629903334 ) ) ;
#46294=CARTESIAN_POINT ( 'NONE',  ( 10.69016084123000176, 4.391264627567999845, -8.802335896973000118 ) ) ;
#46302=CARTESIAN_POINT ( 'NONE',  ( 10.21685100254000034, 2.832432432432000269, 6.822293592207000934 ) ) ;
#46303=EDGE_LOOP ( 'NONE', ( #57510, #61595, #41096, #45031, #60634, #62765, #53615, #64521, #51591, #46947 ) ) ;
#46305=CARTESIAN_POINT ( 'NONE',  ( 9.924495280410999598, 4.946705552514000459, -6.253848946732999181 ) ) ;
#46306=CARTESIAN_POINT ( 'NONE',  ( 5.000000000000000000, 0.8000000000000000444, 3.149999999999999911 ) ) ;
#46311=AXIS2_PLACEMENT_3D ( 'NONE', #2757, #66727, #34240 ) ;
#46316=CARTESIAN_POINT ( 'NONE',  ( 10.02052890782000105, 2.899999999999999911, 6.152188490330000370 ) ) ;
#46321=CARTESIAN_POINT ( 'NONE',  ( 7.890669420221000152, 4.660296061153999858, 6.322498784873999078 ) ) ;
#46322=FACE_OUTER_BOUND ( 'NONE', #39192, .T. ) ;
#46324=CARTESIAN_POINT ( 'NONE',  ( 8.994485841233000656, 3.854507394315999758, -9.394302886912999639 ) ) ;
#46326=CARTESIAN_POINT ( 'NONE',  ( 7.100000000000000533, 5.326087788487999575, -7.247035225330000330 ) ) ;
#46328=B_SPLINE_SURFACE_WITH_KNOTS ( 'NONE', 3, 3, ( 
 ( #50036, #11929, #54934, #17530, #39546, #28369, #49332, #54586, #17169, #11573, #60868, #39198, #59825, #6681, #1446, #60521, #28025, #6327, #12630, #49684, #27678, #38860, #12984, #60181, #22763, #1793, #2144, #44110, #34307, #33959, #48992, #55281, #23463, #44799, #55629 ),
 ( #66103, #7728, #29071, #50381, #12287, #2480, #23806, #45139, #16821, #1103, #22413, #43756, #65051, #35682, #25527, #30436, #8763, #62240, #57330, #4190, #46514, #56657, #8419, #18912, #24151, #2820, #41262, #51067, #45484, #29418, #66449, #24499, #56314, #24841, #56995 ),
 ( #66799, #40237, #8076, #45821, #30104, #50727, #29762, #40917, #67476, #61554, #67132, #36014, #51407, #13671, #34999, #3503, #3170, #9097, #51747, #39897, #3841, #19243, #19597, #55970, #46168, #67817, #14357, #40570, #18570, #61898, #13333, #14012, #35341, #25179, #19941 ),
 ( #62576, #14696, #9432, #34657, #30774, #61217, #52086, #68851, #63609, #5228, #42979, #64286, #53128, #11161, #26566, #68501, #53474, #32496, #37733, #42307, #16403, #16059, #52434, #15034, #68159, #47891, #15725, #20624, #5568, #37051, #31464, #58367, #26909, #42638, #67576 ) ),
 .UNSPECIFIED., .F., .F., .F.,
 ( 4, 4 ),
 ( 4, 1, 1, 1, 1, 1, 1, 1, 1, 1, 1, 1, 1, 1, 1, 1, 1, 1, 1, 1, 1, 1, 1, 1, 1, 1, 1, 1, 1, 1, 1, 1, 4 ),
 ( -0.1039370721279000015, 1.103937072127999963 ),
 ( -0.01999999999996000116, 0.01250000000003000100, 0.04500000000002999517, 0.07750000000003000322, 0.1100000000000000006, 0.1424999999999999878, 0.1749999999999999889, 0.2074999999999999900, 0.2399999999999999911, 0.2725000000000000200, 0.3049999999999999933, 0.3375000000000000222, 0.3699999999999999956, 0.4025000000000000244, 0.4349999999999999978, 0.4675000000000000266, 0.5000000000000000000, 0.5324999999999999734, 0.5649999999999999467, 0.5975000000000000311, 0.6300000000000000044, 0.6624999999999999778, 0.6949999999999999512, 0.7275000000000000355, 0.7600000000000000089, 0.7924999999999999822, 0.8249999999999999556, 0.8575000000000000400, 0.8900000000000000133, 0.9224999999999999867, 0.9549999999999999600, 0.9875000000000000444, 1.020000000000000018 ),
 .UNSPECIFIED. ) ;
#46329=CARTESIAN_POINT ( 'NONE',  ( 0.2285438277137852858, 3.144824486749696835, 0.8442605543570111948 ) ) ;
#46331=CARTESIAN_POINT ( 'NONE',  ( 3.682430813395999980, 0.3301581287572999956, -3.242144429603999622 ) ) ;
#46336=CARTESIAN_POINT ( 'NONE',  ( 9.091114158770999154, 3.762712042852999872, 8.787816121229999666 ) ) ;
#46339=DIRECTION ( 'NONE',  ( 0.000000000000000000, -1.000000000000000000, 0.000000000000000000 ) ) ;
#46342=LINE ( 'NONE', #34828, #12775 ) ;
#46344=ORIENTED_EDGE ( 'NONE', *, *, #44289, .T. ) ;
#46345=EDGE_CURVE ( 'NONE', #28156, #33506, #38951, .T. ) ;
#46350=AXIS2_PLACEMENT_3D ( 'NONE', #55054, #8193, #29542 ) ;
#46354=CYLINDRICAL_SURFACE ( 'NONE', #47248, 3.500000000000000000 ) ;
#46355=CARTESIAN_POINT ( 'NONE',  ( 7.084404719589999289, 4.524560801752999240, -6.025559345696000157 ) ) ;
#46359=CARTESIAN_POINT ( 'NONE',  ( 2.115556799206792071, 0.4581489286485002088, 3.500000000000001776 ) ) ;
#46367=EDGE_CURVE ( 'NONE', #35521, #38774, #22185, .T. ) ;
#46370=CARTESIAN_POINT ( 'NONE',  ( 10.92292960915206201, 5.090154163873960691, -5.014592317151394418 ) ) ;
#46377=CARTESIAN_POINT ( 'NONE',  ( 9.959641781044998865, 5.406625910119999823, 7.700299649248999678 ) ) ;
#46379=CARTESIAN_POINT ( 'NONE',  ( 8.979720280412999855, 5.524776413195999325, -7.147585171405999915 ) ) ;
#46380=CARTESIAN_POINT ( 'NONE',  ( 2.719500174877999665, -3.192447183199000005, -1.538248846112000079 ) ) ;
#46384=CARTESIAN_POINT ( 'NONE',  ( 7.100000000000000533, 5.221516520829000640, -8.074802043613001246 ) ) ;
#46385=EDGE_LOOP ( 'NONE', ( #8222, #52801, #13135 ) ) ;
#46387=CARTESIAN_POINT ( 'NONE',  ( 10.38355189346693663, 5.519214728663544456, -8.419505157002880935 ) ) ;
#46390=CARTESIAN_POINT ( 'NONE',  ( 9.910790522921001156, 3.869345236050000025, 5.882548872612999524 ) ) ;
#46393=CARTESIAN_POINT ( 'NONE',  ( 10.91620964606000044, 2.818413279081999789, -6.814156272943999504 ) ) ;
#46396=EDGE_CURVE ( 'NONE', #7557, #5127, #66535, .T. ) ;
#46406=DIRECTION ( 'NONE',  ( 0.7071067538246033068, -0.5063796871227020935, 0.4935378923296021569 ) ) ;
#46407=CARTESIAN_POINT ( 'NONE',  ( 5.000030787343000327, -1.057581170753189248, -1.834918991542628275 ) ) ;
#46412=CARTESIAN_POINT ( 'NONE',  ( 10.05462971959000029, 3.531217403581000003, -9.119235467071000301 ) ) ;
#46413=ORIENTED_EDGE ( 'NONE', *, *, #25309, .F. ) ;
#46414=CARTESIAN_POINT ( 'NONE',  ( 1.530140132540667164, 3.408904368339106483, -0.9161175952574748260 ) ) ;
#46419=EDGE_LOOP ( 'NONE', ( #36743, #47980, #9433, #43103 ) ) ;
#46420=CARTESIAN_POINT ( 'NONE',  ( 5.000000000000000000, 0.000000000000000000, 0.000000000000000000 ) ) ;
#46421=CARTESIAN_POINT ( 'NONE',  ( -1.222471984994595150E-05, -9.327013418423733093E-16, -2.899969545326207765 ) ) ;
#46426=ORIENTED_EDGE ( 'NONE', *, *, #38350, .T. ) ;
#46431=VECTOR ( 'NONE', #20686, 1000.000000000000000 ) ;
#46434=CARTESIAN_POINT ( 'NONE',  ( 2.342640132542833431, -3.058252359239902685, -1.762666431298148595 ) ) ;
#46444=DIRECTION ( 'NONE',  ( 1.000000000000000000, 0.000000000000000000, 0.000000000000000000 ) ) ;
#46445=VERTEX_POINT ( 'NONE', #18655 ) ;
#46451=CARTESIAN_POINT ( 'NONE',  ( 8.675198109782005673, 10.51530723774999032, -4.257112462104002404 ) ) ;
#46462=CARTESIAN_POINT ( 'NONE',  ( 9.832537864288001472, 2.899999999999999911, 6.571291218949999902 ) ) ;
#46464=CARTESIAN_POINT ( 'NONE',  ( 11.10062015617000064, 3.093053541899000169, -6.153678467293999255 ) ) ;
#46465=CARTESIAN_POINT ( 'NONE',  ( 8.639949174999173920, 5.001557281985752113, 6.108253387157301262 ) ) ;
#46468=CARTESIAN_POINT ( 'NONE',  ( 9.075483283097998566, 4.020836891789999257, 8.948690653012000951 ) ) ;
#46471=CARTESIAN_POINT ( 'NONE',  ( 10.15403136780999915, 5.267988602993999514, 5.992335067371000079 ) ) ;
#46473=CARTESIAN_POINT ( 'NONE',  ( 10.53734212242000012, 2.992816679959000137, 8.731689474572998932 ) ) ;
#46476=CARTESIAN_POINT ( 'NONE',  ( 9.049999337612000261, -3.819167204710999825E-14, 1.447065004412999939E-13 ) ) ;
#46480=CARTESIAN_POINT ( 'NONE',  ( 8.096551658772000337, 5.061727314042999915, 5.824077473724000420 ) ) ;
#46482=CARTESIAN_POINT ( 'NONE',  ( 11.18051582549000145, 5.340073783367000892, 8.416152717850000187 ) ) ;
#46485=CARTESIAN_POINT ( 'NONE',  ( 8.839404719593998649, 5.140767546012999567, -6.196177269779999719 ) ) ;
#46487=EDGE_CURVE ( 'NONE', #57987, #9965, #52523, .T. ) ;
#46495=CARTESIAN_POINT ( 'NONE',  ( 2.158975548941000078, -3.419251011552999930, 1.101167613520000144 ) ) ;
#46498=CARTESIAN_POINT ( 'NONE',  ( 9.694764498856436319, 5.745394236816313338, 7.382991512957417513 ) ) ;
#46499=CARTESIAN_POINT ( 'NONE',  ( 4.550000802215999229, 1.829647544581999737E-13, 0.000000000000000000 ) ) ;
#46508=CARTESIAN_POINT ( 'NONE',  ( 9.202760841230999134, 2.542862824481000317, 7.419808961972999661 ) ) ;
#46514=CARTESIAN_POINT ( 'NONE',  ( 1.461929392595999966, -1.374622313384999961, -3.318774223758000019 ) ) ;
#46516=DIRECTION ( 'NONE',  ( 0.000000000000000000, 0.9565994702956990281, 0.2914059941558995726 ) ) ;
#46519=CARTESIAN_POINT ( 'NONE',  ( 9.813360311708999362, 5.349397258738000538, 6.657026394682000081 ) ) ;
#46525=CIRCLE ( 'NONE', #57686, 11.84999999999999964 ) ;
#46536=CARTESIAN_POINT ( 'NONE',  ( 9.848730799670999403, 2.769737997918999994, 6.441853401936000090 ) ) ;
#46537=CARTESIAN_POINT ( 'NONE',  ( 10.98277660187000215, 2.518725482848000130, -8.314790074023999722 ) ) ;
#46541=EDGE_CURVE ( 'NONE', #23923, #16538, #9670, .T. ) ;
#46542=CIRCLE ( 'NONE', #4093, 12.50000000000000178 ) ;
#46547=B_SPLINE_CURVE_WITH_KNOTS ( 'NONE', 3,
 ( #23346, #33845, #38387, #65984, #65296, #11464, #44344, #65641, #49220, #27215, #17768, #48540, #60410, #48886, #18110, #646, #39429 ),
 .UNSPECIFIED., .F., .F.,
 ( 4, 2, 2, 2, 1, 2, 2, 2, 4 ),
 ( 0.000000000000000000, 0.1250000000000000833, 0.2500000000000001665, 0.3750000000000000555, 0.5000000000000000000, 0.6250000000000000000, 0.7499999999999998890, 0.8750000000000000000, 1.000000000000000000 ),
 .UNSPECIFIED. ) ;
#46551=DIRECTION ( 'NONE',  ( 1.000000000000000000, 0.000000000000000000, 0.000000000000000000 ) ) ;
#46556=VERTEX_POINT ( 'NONE', #36797 ) ;
#46559=VERTEX_POINT ( 'NONE', #56750 ) ;
#46566=CYLINDRICAL_SURFACE ( 'NONE', #52727, 0.4999999999999998335 ) ;
#46586=AXIS2_PLACEMENT_3D ( 'NONE', #34963, #12252, #2113 ) ;
#46588=DIRECTION ( 'NONE',  ( 0.000000000000000000, 1.000000000000000000, 1.348567142399000110E-14 ) ) ;
#46591=EDGE_CURVE ( 'NONE', #7896, #53136, #20026, .T. ) ;
#46609=CARTESIAN_POINT ( 'NONE',  ( 2.853056799211333594, -2.798833948393629534, -2.150913519912204031 ) ) ;
#46618=CARTESIAN_POINT ( 'NONE',  ( 4.149992563291999836, -1.599290730647366932, -1.229060429538532562 ) ) ;
#46619=CARTESIAN_POINT ( 'NONE',  ( 9.940137750233063230, 4.538038001511168318, -9.158081726654419441 ) ) ;
#46621=CARTESIAN_POINT ( 'NONE',  ( 7.000000000000000000, 6.255435840762999966, 3.000000000000000000 ) ) ;
#46625=CARTESIAN_POINT ( 'NONE',  ( 9.485829719593997567, 4.953415418491999844, -8.946479654552000227 ) ) ;
#46628=CARTESIAN_POINT ( 'NONE',  ( 10.36630583688000051, 5.852743870412999705, -7.568014644338999730 ) ) ;
#46635=B_SPLINE_CURVE_WITH_KNOTS ( 'NONE', 3,
 ( #38308, #22916, #17332, #53704, #33423, #54740 ),
 .UNSPECIFIED., .F., .F.,
 ( 4, 1, 1, 4 ),
 ( 0.0003621572724173774968, 0.3333333333333000081, 0.6666666666667000474, 1.000000000000000000 ),
 .UNSPECIFIED. ) ;
#46640=CARTESIAN_POINT ( 'NONE',  ( 8.020125753392001400, 4.498951069075999953, -6.245588651729999441 ) ) ;
#46641=CARTESIAN_POINT ( 'NONE',  ( 7.249999999999997335, 4.000000000000000000, 9.109807621135335154 ) ) ;
#46643=CYLINDRICAL_SURFACE ( 'NONE', #40555, 1.999999999999999556 ) ;
#46650=CARTESIAN_POINT ( 'NONE',  ( 9.318935841232999451, 2.644017913812000131, -7.838184857420000817 ) ) ;
#46652=CARTESIAN_POINT ( 'NONE',  ( 1.092640132541500053, 3.058252359239899132, 1.762666431298155034 ) ) ;
#46660=CARTESIAN_POINT ( 'NONE',  ( 0.5181103717477000270, 3.205765437135000173, -1.404659375816999844 ) ) ;
#46667=CYLINDRICAL_SURFACE ( 'NONE', #32117, 13.10000000000000142 ) ;
#46671=DIRECTION ( 'NONE',  ( 0.000000000000000000, -1.000000000000000000, 0.000000000000000000 ) ) ;
#46675=CARTESIAN_POINT ( 'NONE',  ( 0.2483555794960837226, 2.598197151148166739, 1.995642445486431438 ) ) ;
#46676=CARTESIAN_POINT ( 'NONE',  ( 3.396339116751999843, 1.123978401994000009, 3.059078227285999763 ) ) ;
#46682=CARTESIAN_POINT ( 'NONE',  ( 3.499577856771284079, 0.2302043132029295003, -3.403026834754980356 ) ) ;
#46683=CARTESIAN_POINT ( 'NONE',  ( 1.634306799207666749, 1.762666431298139713, 3.058252359239908458 ) ) ;
#46687=CARTESIAN_POINT ( 'NONE',  ( 0.7303395634860353480, -3.408546583648842887, 0.9194981686915635333 ) ) ;
#46688=CARTESIAN_POINT ( 'NONE',  ( 10.91281046558188628, 5.099996679677031963, 5.078864286215828194 ) ) ;
#46690=VECTOR ( 'NONE', #49944, 1000.000000000000114 ) ;
#46696=CARTESIAN_POINT ( 'NONE',  ( 8.814947692958833514, 2.650138447187985413, -7.499997389691697158 ) ) ;
#46697=DIRECTION ( 'NONE',  ( 0.4384236320213994453, 0.6355252626312996034, -0.6355252626312994924 ) ) ;
#46700=CARTESIAN_POINT ( 'NONE',  ( 7.702599060372073758, 2.713167639879611848, 7.025738298870125575 ) ) ;
#46701=CARTESIAN_POINT ( 'NONE',  ( 7.821420280405000369, 5.418947913204000599, -8.493927145653000110 ) ) ;
#46704=VERTEX_POINT ( 'NONE', #11580 ) ;
#46707=FACE_OUTER_BOUND ( 'NONE', #1130, .T. ) ;
#46708=VERTEX_POINT ( 'NONE', #16831 ) ;
#46712=EDGE_LOOP ( 'NONE', ( #63974, #60589, #33036, #31481 ) ) ;
#46713=CARTESIAN_POINT ( 'NONE',  ( 10.90184547699885087, 2.543465510515977357, 8.509880136748577684 ) ) ;
#46717=CARTESIAN_POINT ( 'NONE',  ( 3.011390132543707576, 3.499999999999998224, 0.4581489286485194157 ) ) ;
#46724=CARTESIAN_POINT ( 'NONE',  ( 10.73931450027999901, 2.763002390638999994, 6.801034082888999244 ) ) ;
#46725=DIRECTION ( 'NONE',  ( 1.000000000000000000, 0.000000000000000000, 0.000000000000000000 ) ) ;
#46726=CARTESIAN_POINT ( 'NONE',  ( 8.672510841228998402, 4.686731264770999772, -8.717075579553000608 ) ) ;
#46727=CARTESIAN_POINT ( 'NONE',  ( 3.222503736606999958, -3.132127790629000152, -1.657619983915999740 ) ) ;
#46731=VERTEX_POINT ( 'NONE', #64717 ) ;
#46733=CARTESIAN_POINT ( 'NONE',  ( 9.383148997457999130, 5.167567567567999731, 6.822293592207000934 ) ) ;
#46737=CARTESIAN_POINT ( 'NONE',  ( 9.380783851237000093, 2.204242311415999911, 7.545378292079000460 ) ) ;
#46750=CARTESIAN_POINT ( 'NONE',  ( 3.999999999999999112, 1.082950885222931925, -1.878608423871279465 ) ) ;
#46753=CIRCLE ( 'NONE', #24449, 0.5000000000000002220 ) ;
#46754=CARTESIAN_POINT ( 'NONE',  ( 0.6089841414396000019, -0.7435038563603999506, -3.122230671987999973 ) ) ;
#46757=CARTESIAN_POINT ( 'NONE',  ( 10.90247028041000021, 4.554785930130000438, -6.081876607904999510 ) ) ;
#46763=CARTESIAN_POINT ( 'NONE',  ( 7.565635841228000480, 3.206360348473000332, 5.681727837477000165 ) ) ;
#46766=CARTESIAN_POINT ( 'NONE',  ( 7.318264158767999739, 5.899473592675000155, -7.539390303202999633 ) ) ;
#46770=CARTESIAN_POINT ( 'NONE',  ( 2.761390132542709264, -3.499999999999999556, -0.4581489286485119772 ) ) ;
#46777=CIRCLE ( 'NONE', #6435, 1.550000000000000488 ) ;
#46782=CARTESIAN_POINT ( 'NONE',  ( 7.795982780410000146, 3.164805384346000228, 9.104735843897000080 ) ) ;
#46783=ORIENTED_EDGE ( 'NONE', *, *, #22917, .T. ) ;
#46784=DIRECTION ( 'NONE',  ( 1.000000000000000000, 0.000000000000000000, 0.000000000000000000 ) ) ;
#46787=ORIENTED_EDGE ( 'NONE', *, *, #11585, .F. ) ;
#46791=CARTESIAN_POINT ( 'NONE',  ( 10.44065171787999802, 8.381973494822000603, -6.833921068867995885 ) ) ;
#46794=LINE ( 'NONE', #31403, #40851 ) ;
#46806=CARTESIAN_POINT ( 'NONE',  ( 10.53865537815000053, 3.647234352455999584, -6.014129666051999834 ) ) ;
#46810=CARTESIAN_POINT ( 'NONE',  ( 9.290193290418001126, 2.377818438998999806, 7.540992072119000689 ) ) ;
#46811=ORIENTED_EDGE ( 'NONE', *, *, #29031, .T. ) ;
#46812=CARTESIAN_POINT ( 'NONE',  ( 8.979535623375799247, 3.684598859393744430, -9.248984133260908180 ) ) ;
#46816=CARTESIAN_POINT ( 'NONE',  ( 8.630000000000000782, 4.924138593003999809, -8.484107647018999998 ) ) ;
#46817=CARTESIAN_POINT ( 'NONE',  ( 9.842764158772000727, 5.798263352390999437, -8.113145944980999502 ) ) ;
#46820=FACE_OUTER_BOUND ( 'NONE', #15679, .T. ) ;
#46821=B_SPLINE_CURVE_WITH_KNOTS ( 'NONE', 3,
 ( #16355, #59014, #11117, #64925 ),
 .UNSPECIFIED., .F., .F.,
 ( 4, 4 ),
 ( 0.8745530004746001618, 1.000000000000000000 ),
 .UNSPECIFIED. ) ;
#46826=CARTESIAN_POINT ( 'NONE',  ( 11.08992526467999973, 5.210543602612999869, 8.327598319864998544 ) ) ;
#46828=ORIENTED_EDGE ( 'NONE', *, *, #47663, .T. ) ;
#46829=CARTESIAN_POINT ( 'NONE',  ( 8.938854719593997800, 5.597201461420000967, -8.171008079894999554 ) ) ;
#46836=CARTESIAN_POINT ( 'NONE',  ( 2.392611958083999735, -0.3183524953527000489, -3.745328979271999703 ) ) ;
#46839=CARTESIAN_POINT ( 'NONE',  ( 9.760001502711011412, 5.278381895807264357, 8.694223062418139136 ) ) ;
#46847=DIRECTION ( 'NONE',  ( -1.000000000000000000, 0.000000000000000000, 0.000000000000000000 ) ) ;
#46849=ORIENTED_EDGE ( 'NONE', *, *, #40724, .F. ) ;
#46852=CARTESIAN_POINT ( 'NONE',  ( 10.39297979613035317, 2.713506317168391302, -7.026950959993602197 ) ) ;
#46853=VECTOR ( 'NONE', #57493, 1000.000000000000114 ) ;
#46855=CARTESIAN_POINT ( 'NONE',  ( 27.64127793187000037, -1.199999999999999956, 9.776630298829998011 ) ) ;
#46858=CARTESIAN_POINT ( 'NONE',  ( 1.286366951365282674, 3.276871974290374467, 0.4130264870479211647 ) ) ;
#46860=CARTESIAN_POINT ( 'NONE',  ( 9.471374412057000924, 2.030666183831999927, 7.549764512038000142 ) ) ;
#46861=CARTESIAN_POINT ( 'NONE',  ( 10.85646369190733473, 5.100000000000000533, 6.665341197409740737 ) ) ;
#46863=CARTESIAN_POINT ( 'NONE',  ( 9.765375278055641317, 5.100000000000000533, 6.445686799077642526 ) ) ;
#46868=CARTESIAN_POINT ( 'NONE',  ( 9.099999886593998610, 12.39999890530000037, 0.000000000000000000 ) ) ;
#46875=CARTESIAN_POINT ( 'NONE',  ( 9.786671076420999427, 2.381202181614999525, 7.612749448318000489 ) ) ;
#46876=CARTESIAN_POINT ( 'NONE',  ( 11.02205778663999958, 2.309481324353999554, -7.515673747780000191 ) ) ;
#46889=DIRECTION ( 'NONE',  ( 0.4384236320214023874, 0.000000000000000000, -0.8987684456439055669 ) ) ;
#46891=CARTESIAN_POINT ( 'NONE',  ( 6.607274140103999827, 9.225079388580999407, 5.032532138881999018 ) ) ;
#46899=LINE ( 'NONE', #9829, #19197 ) ;
#46913=CARTESIAN_POINT ( 'NONE',  ( 10.28180471959000108, 3.991526675591000384, -5.814300410279999554 ) ) ;
#46917=CARTESIAN_POINT ( 'NONE',  ( 8.002383708823000319, 5.117451078405999887, -6.702236199791999915 ) ) ;
#46918=ORIENTED_EDGE ( 'NONE', *, *, #48078, .T. ) ;
#46921=ADVANCED_FACE ( 'NONE', ( #61564 ), #45149, .T. ) ;
#46924=CYLINDRICAL_SURFACE ( 'NONE', #68213, 1.350000000000000533 ) ;
#46930=ORIENTED_EDGE ( 'NONE', *, *, #6212, .T. ) ;
#46947=ORIENTED_EDGE ( 'NONE', *, *, #37551, .F. ) ;
#46948=CARTESIAN_POINT ( 'NONE',  ( 9.740360841231000322, 4.047146749018000200, -5.600703114891000034 ) ) ;
#46954=ORIENTED_EDGE ( 'NONE', *, *, #5982, .T. ) ;
#46957=CARTESIAN_POINT ( 'NONE',  ( 9.740360841231000322, 4.047146749018000200, -5.600703114891000034 ) ) ;
#46964=CARTESIAN_POINT ( 'NONE',  ( 8.045639775557999585, 4.604250840901999986, -6.230858151876000228 ) ) ;
#46965=ADVANCED_FACE ( 'NONE', ( #61907 ), #3168, .T. ) ;
#46966=CARTESIAN_POINT ( 'NONE',  ( 10.07367028041000090, 4.905765359186999852, -8.776126235875999271 ) ) ;
#46968=CARTESIAN_POINT ( 'NONE',  ( 10.07930935222999835, 2.718121894972999719, -6.397795030233000446 ) ) ;
#46979=CARTESIAN_POINT ( 'NONE',  ( 10.87947334122999976, 2.817426144593000004, -6.828668581221999823 ) ) ;
#46980=EDGE_CURVE ( 'NONE', #30974, #69017, #13042, .T. ) ;
#46990=AXIS2_PLACEMENT_3D ( 'NONE', #14162, #18716, #55777 ) ;
#46991=CARTESIAN_POINT ( 'NONE',  ( 8.979720280412999855, 5.524776413195999325, -7.147585171405999915 ) ) ;
#47005=CARTESIAN_POINT ( 'NONE',  ( 7.944681758174191977, 4.857212911390003995, 6.360313247088151378 ) ) ;
#47009=CARTESIAN_POINT ( 'NONE',  ( 9.591185841232000797, 2.173570076733999823, -8.023168429484000441 ) ) ;
#47015=CARTESIAN_POINT ( 'NONE',  ( 3.714218779689999916, 1.510359751552999841, -2.741952990197999984 ) ) ;
#47020=CARTESIAN_POINT ( 'NONE',  ( 3.499698285111554785, -2.916600830549739065, -1.425132625272170550 ) ) ;
#47021=CARTESIAN_POINT ( 'NONE',  ( 3.500000000000001332, -1.293366386299026782, 2.969361111422694766 ) ) ;
#47026=CARTESIAN_POINT ( 'NONE',  ( 10.95696410347983729, 8.982905668905601715, 6.421968592709950130 ) ) ;
#47027=CARTESIAN_POINT ( 'NONE',  ( 11.08757144985999865, 2.712428550139000194, 6.571291218949999902 ) ) ;
#47028=CARTESIAN_POINT ( 'NONE',  ( 7.759512367773170105, 2.953550066126335860, -8.377314763178624446 ) ) ;
#47030=ORIENTED_EDGE ( 'NONE', *, *, #55190, .F. ) ;
#47036=ORIENTED_EDGE ( 'NONE', *, *, #32524, .T. ) ;
#47038=CARTESIAN_POINT ( 'NONE',  ( 7.954299074928001367, 3.414461172233999697, -6.283593702261001113 ) ) ;
#47040=CARTESIAN_POINT ( 'NONE',  ( 6.686604719590000023, 5.464161011425000325, -7.581039036848999935 ) ) ;
#47045=EDGE_CURVE ( 'NONE', #46559, #62089, #53882, .T. ) ;
#47049=ORIENTED_EDGE ( 'NONE', *, *, #9463, .T. ) ;
#47051=CARTESIAN_POINT ( 'NONE',  ( 7.961495038489999843, 3.389986099490999827, -6.279439026173999849 ) ) ;
#47063=CARTESIAN_POINT ( 'NONE',  ( 3.313591025678166435, -3.499999999999999112, -0.5549492644885768433 ) ) ;
#47065=CARTESIAN_POINT ( 'NONE',  ( 11.20563302462000088, 3.509134285281999777, 6.118194788334999856 ) ) ;
#47067=CARTESIAN_POINT ( 'NONE',  ( 27.64127793187000037, -11.00717859340000082, 1.432487142323000118 ) ) ;
#47069=CARTESIAN_POINT ( 'NONE',  ( 2.929084992264999965, 3.537580394849999976, -0.2084549283189000013 ) ) ;
#47070=ADVANCED_FACE ( 'NONE', ( #48065 ), #47729, .T. ) ;
#47074=VERTEX_POINT ( 'NONE', #52274 ) ;
#47077=CARTESIAN_POINT ( 'NONE',  ( 10.30208432104581640, 5.580039836084787375, -6.689420770392193738 ) ) ;
#47080=CARTESIAN_POINT ( 'NONE',  ( 9.385781899350000401, 4.980865465981000106, 6.433345686594999613 ) ) ;
#47088=CIRCLE ( 'NONE', #16927, 0.5000000000000000000 ) ;
#47090=CARTESIAN_POINT ( 'NONE',  ( 0.5000220334827000235, 3.499749845413000049, -0.04184518527856000147 ) ) ;
#47091=ORIENTED_EDGE ( 'NONE', *, *, #50157, .T. ) ;
#47098=CARTESIAN_POINT ( 'NONE',  ( 11.24323278040999874, 2.479734175328000223, -7.587230544849999703 ) ) ;
#47106=CYLINDRICAL_SURFACE ( 'NONE', #56713, 1.350000000000000533 ) ;
#47110=CARTESIAN_POINT ( 'NONE',  ( 7.417714158767000576, 4.562063799276000253, -9.314837681783000534 ) ) ;
#47117=DIRECTION ( 'NONE',  ( 0.4682208595142289265, 0.4682208595142289265, 0.7493586947727458591 ) ) ;
#47118=CARTESIAN_POINT ( 'NONE',  ( 10.90000053908999966, 9.856474340180000127, -5.627824942316999923 ) ) ;
#47122=CARTESIAN_POINT ( 'NONE',  ( 8.414360841228999632, 5.461114003844000031, -8.582501063019000398 ) ) ;
#47127=CARTESIAN_POINT ( 'NONE',  ( 9.106135841230999617, 4.192919163547999872, 5.525472271700999194 ) ) ;
#47129=ADVANCED_FACE ( 'NONE', ( #26402 ), #21152, .T. ) ;
#47130=ORIENTED_EDGE ( 'NONE', *, *, #43411, .T. ) ;
#47131=CARTESIAN_POINT ( 'NONE',  ( 10.81499708368641954, 2.650004840405624673, -7.499999822193707644 ) ) ;
#47148=CARTESIAN_POINT ( 'NONE',  ( 10.26368708477999903, 4.794139572939999816, -8.804452601708000259 ) ) ;
#47154=CARTESIAN_POINT ( 'NONE',  ( 10.40726830891999910, 3.797905842462999892, 5.889914049998000500 ) ) ;
#47156=CARTESIAN_POINT ( 'NONE',  ( 8.765417767663000959, 5.029951493281999753, -6.097931603992000404 ) ) ;
#47158=CARTESIAN_POINT ( 'NONE',  ( 9.305881816721999655, 4.945299866898000829, 9.077891794505999812 ) ) ;
#47160=CARTESIAN_POINT ( 'NONE',  ( 10.11260611051000069, 3.359887741436999864, 5.859127722154000573 ) ) ;
#47167=CARTESIAN_POINT ( 'NONE',  ( 10.13049857835000012, 3.092060693447000297, 8.629378633793999498 ) ) ;
#47170=CARTESIAN_POINT ( 'NONE',  ( 10.12339528040999959, 3.988943694240999704, -8.966360307350999648 ) ) ;
#47178=VECTOR ( 'NONE', #21075, 1000.000000000000114 ) ;
#47182=CARTESIAN_POINT ( 'NONE',  ( 9.568039158772000619, 5.336630274082000192, -7.092011739486999922 ) ) ;
#47185=ADVANCED_FACE ( 'NONE', ( #44218 ), #12210, .T. ) ;
#47194=CARTESIAN_POINT ( 'NONE',  ( 7.390489158771000433, 2.216873702600000051, 8.370081218683999680 ) ) ;
#47201=ORIENTED_EDGE ( 'NONE', *, *, #51392, .T. ) ;
#47202=CARTESIAN_POINT ( 'NONE',  ( 0.9049113558389121348, -0.1461257074673270873, 3.299567646954244093 ) ) ;
#47204=CARTESIAN_POINT ( 'NONE',  ( 9.305881816721999655, 4.945299866898000829, 9.077891794505999812 ) ) ;
#47205=CARTESIAN_POINT ( 'NONE',  ( 10.38314899745999931, 5.167567567567999731, 6.822293592207000934 ) ) ;
#47208=CARTESIAN_POINT ( 'NONE',  ( 8.642077642326000841, 2.899999999999999911, 6.463854830420999953 ) ) ;
#47215=ORIENTED_EDGE ( 'NONE', *, *, #33625, .F. ) ;
#47222=CARTESIAN_POINT ( 'NONE',  ( 11.06923869026000062, 5.425682056982999768, 8.012911262916999178 ) ) ;
#47223=CARTESIAN_POINT ( 'NONE',  ( 10.82565186280000091, 5.331165376905000031, -8.542144899688000947 ) ) ;
#47229=CARTESIAN_POINT ( 'NONE',  ( 8.099999999999999645, 0.000000000000000000, 0.000000000000000000 ) ) ;
#47233=CARTESIAN_POINT ( 'NONE',  ( 9.433148997456999751, 5.167567567567999731, 6.822293592207000934 ) ) ;
#47236=CARTESIAN_POINT ( 'NONE',  ( 6.207153620001000682, 9.294285739568001858, 4.825711238106001666 ) ) ;
#47240=DIRECTION ( 'NONE',  ( 1.000000000000000000, 0.000000000000000000, 0.000000000000000000 ) ) ;
#47248=AXIS2_PLACEMENT_3D ( 'NONE', #41107, #51928, #20460 ) ;
#47250=VECTOR ( 'NONE', #17483, 1000.000000000000000 ) ;
#47251=CARTESIAN_POINT ( 'NONE',  ( 0.5651652630779999686, -0.7815069638253000495, -3.281818906455000295 ) ) ;
#47252=CARTESIAN_POINT ( 'NONE',  ( 9.804402243952704765, 2.650150644870925110, -7.676800222058682621 ) ) ;
#47257=CARTESIAN_POINT ( 'NONE',  ( 10.86460778041000097, 3.843601682313000367, -5.985271987931999327 ) ) ;
#47259=DIRECTION ( 'NONE',  ( 0.000000000000000000, 0.000000000000000000, -1.000000000000000000 ) ) ;
#47264=CARTESIAN_POINT ( 'NONE',  ( 7.726822586083000211, 2.853542176918999917, 6.781784851098000111 ) ) ;
#47267=EDGE_CURVE ( 'NONE', #52043, #47074, #58863, .T. ) ;
#47268=EDGE_CURVE ( 'NONE', #46445, #25251, #7105, .T. ) ;
#47273=EDGE_LOOP ( 'NONE', ( #4834, #48826, #63097, #63843 ) ) ;
#47275=EDGE_CURVE ( 'NONE', #2379, #62671, #22782, .T. ) ;
#47284=CARTESIAN_POINT ( 'NONE',  ( 7.885003087483005046, 2.917683036408002195, 6.444041402419006914 ) ) ;
#47288=DIRECTION ( 'NONE',  ( -1.000000000000000000, 0.000000000000000000, 0.000000000000000000 ) ) ;
#47294=CARTESIAN_POINT ( 'NONE',  ( 8.356920280409999791, 4.851303550474000303, -9.008742670124000540 ) ) ;
#47296=EDGE_LOOP ( 'NONE', ( #51936, #8904, #3394, #13584 ) ) ;
#47297=CARTESIAN_POINT ( 'NONE',  ( 7.912439085938001604, 3.534686866976279873, -6.215565689732485133 ) ) ;
#47302=CARTESIAN_POINT ( 'NONE',  ( 9.640910841231999484, 2.212639797530000063, -6.855876382544999537 ) ) ;
#47303=DIRECTION ( 'NONE',  ( 1.000000000000000000, 0.000000000000000000, 0.000000000000000000 ) ) ;
#47306=CARTESIAN_POINT ( 'NONE',  ( 0.2500098862125000321, 0.000000000000000000, 0.000000000000000000 ) ) ;
#47307=CARTESIAN_POINT ( 'NONE',  ( 11.09999999999999964, 5.759298710781000530, 5.143901506165000193 ) ) ;
#47310=CARTESIAN_POINT ( 'NONE',  ( 8.640504719592000171, 2.305580295895999665, -7.860904109308999743 ) ) ;
#47312=CARTESIAN_POINT ( 'NONE',  ( 10.19715290653000217, 4.982626294267999967, -6.124313696433000054 ) ) ;
#47314=EDGE_LOOP ( 'NONE', ( #8779, #17748, #15245, #14901 ) ) ;
#47321=CARTESIAN_POINT ( 'NONE',  ( 4.049969279409727285, 2.099966510537780273, 9.844688305727672900E-09 ) ) ;
#47322=CARTESIAN_POINT ( 'NONE',  ( 11.09999999999999964, 0.5000000000000000000, 5.124965750789000296 ) ) ;
#47329=CARTESIAN_POINT ( 'NONE',  ( 9.196339158776000389, 4.112741311853999271, -5.603466076760000192 ) ) ;
#47332=ORIENTED_EDGE ( 'NONE', *, *, #56063, .T. ) ;
#47334=CARTESIAN_POINT ( 'NONE',  ( 11.05213295625000036, 5.231718854540000407, -4.976717655758000625 ) ) ;
#47336=CARTESIAN_POINT ( 'NONE',  ( 1.248890132540875220, -2.798833948393641080, 2.150913519912190708 ) ) ;
#47337=CARTESIAN_POINT ( 'NONE',  ( 0.1499942179680000265, 0.7197945678028363492, -2.678379783547566895 ) ) ;
#47342=CARTESIAN_POINT ( 'NONE',  ( 8.349082721034115195, 4.945536839314570443, -6.215508931641162249 ) ) ;
#47347=DIRECTION ( 'NONE',  ( 6.273181768770000388E-11, -6.273307657911000434E-11, 1.000000000000000000 ) ) ;
#47353=EDGE_CURVE ( 'NONE', #34779, #798, #53423, .T. ) ;
#47356=DIRECTION ( 'NONE',  ( 0.4384236320214023319, 0.000000000000000000, -0.8987684456439056779 ) ) ;
#47358=FACE_OUTER_BOUND ( 'NONE', #6877, .T. ) ;
#47361=CYLINDRICAL_SURFACE ( 'NONE', #5656, 2.750000000000000000 ) ;
#47362=ORIENTED_EDGE ( 'NONE', *, *, #26487, .T. ) ;
#47367=CARTESIAN_POINT ( 'NONE',  ( 10.16712151127302199, 5.079456268609247260, -8.329490867414714117 ) ) ;
#47372=CARTESIAN_POINT ( 'NONE',  ( 0.5000220334827000235, 3.499749845413000049, -0.04184518527856000147 ) ) ;
#47378=CIRCLE ( 'NONE', #38435, 12.99999867215000116 ) ;
#47380=VERTEX_POINT ( 'NONE', #55993 ) ;
#47385=CARTESIAN_POINT ( 'NONE',  ( 8.289480787584649235, 3.351401960818187753, -6.090076450232053240 ) ) ;
#47386=CARTESIAN_POINT ( 'NONE',  ( 8.268945280408999565, 5.730434958826999825, -7.416203477251000820 ) ) ;
#47388=CARTESIAN_POINT ( 'NONE',  ( 9.490614058485499882, 4.913414349029470607, 8.493955840285781989 ) ) ;
#47400=AXIS2_PLACEMENT_3D ( 'NONE', #43784, #54258, #54960 ) ;
#47402=DIRECTION ( 'NONE',  ( 1.000000000000000000, 0.000000000000000000, 0.000000000000000000 ) ) ;
#47409=CARTESIAN_POINT ( 'NONE',  ( 9.500006116823001889, 2.279680316922000127, 7.877692351087999256 ) ) ;
#47410=CARTESIAN_POINT ( 'NONE',  ( 10.53197665877000055, 2.323713329709999886, -8.279493667389999700 ) ) ;
#47411=CARTESIAN_POINT ( 'NONE',  ( 8.200000998245998929, 0.000000000000000000, 0.000000000000000000 ) ) ;
#47422=CARTESIAN_POINT ( 'NONE',  ( 9.882259685352000389, 4.932708901218999742, 6.390989635557000170 ) ) ;
#47431=ORIENTED_EDGE ( 'NONE', *, *, #47353, .T. ) ;
#47436=CARTESIAN_POINT ( 'NONE',  ( 3.999971066382000284, 2.149963194831999935, 0.000000000000000000 ) ) ;
#47438=EDGE_LOOP ( 'NONE', ( #65881, #36139, #15731, #57859 ) ) ;
#47440=CARTESIAN_POINT ( 'NONE',  ( 0.2471211125914999640, 1.200150369511000070, -3.152926066752000267 ) ) ;
#47443=CARTESIAN_POINT ( 'NONE',  ( 10.69829221958999987, 2.534027248431999890, -6.667786804432999759 ) ) ;
#47451=CARTESIAN_POINT ( 'NONE',  ( 1.750973465873000068, -3.500000000000000000, 0.000000000000000000 ) ) ;
#47452=CARTESIAN_POINT ( 'NONE',  ( 8.412214158772000516, 4.642843096736999797, -9.160097874508000615 ) ) ;
#47453=EDGE_CURVE ( 'NONE', #33299, #62147, #55679, .T. ) ;
#47466=CARTESIAN_POINT ( 'NONE',  ( 8.845310841232000953, 5.851083642416999631, -7.072167224702999633 ) ) ;
#47472=CARTESIAN_POINT ( 'NONE',  ( 9.160308886257000793, 4.122021000979000149, 9.013569734175000292 ) ) ;
#47478=B_SPLINE_SURFACE_WITH_KNOTS ( 'NONE', 3, 3, ( 
 ( #49644, #1751, #44421, #60483, #12592, #33920, #34177, #45012, #29281, #29635, #28590, #45355, #2011, #18439, #17751, #39414, #28944, #50249, #6899, #61083, #2351, #66664, #18783, #7595, #34863, #12848, #33832, #7944, #23333, #23674, #13544, #1315, #39765, #28235, #38724 ),
 ( #13203, #43976, #60734, #22631, #50595, #17395, #60046, #44674, #65282, #65967, #34531, #12156, #18096, #22980, #33487, #24020, #55840, #2697, #66316, #65626, #40114, #56179, #61428, #54799, #8290, #39071, #49550, #1663, #44328, #60394, #12498, #55146, #7249, #49902, #55495 ),
 ( #63123, #51953, #68033, #4054, #35552, #51615, #19461, #9648, #14569, #25740, #46380, #36229, #25389, #4401, #57200, #47069, #35212, #57544, #29977, #19115, #45697, #35885, #46727, #30995, #9996, #8968, #68371, #3711, #20148, #67340, #19808, #9303, #30644, #56524, #41476 ),
 ( #62784, #30307, #25048, #40437, #14906, #52304, #20491, #41816, #67682, #15251, #36572, #57898, #50937, #40782, #3035, #24366, #67006, #41137, #61763, #13882, #8628, #51279, #62447, #3374, #24711, #46035, #62107, #14226, #56870, #59614, #54019, #16618, #64498, #32372, #26432 ) ),
 .UNSPECIFIED., .F., .F., .F.,
 ( 4, 4 ),
 ( 4, 1, 1, 1, 1, 1, 1, 1, 1, 1, 1, 1, 1, 1, 1, 1, 1, 1, 1, 1, 1, 1, 1, 1, 1, 1, 1, 1, 1, 1, 1, 1, 4 ),
 ( -0.1039370721279000015, 1.103937072127999963 ),
 ( -0.01758190005605000245, 0.01098868753504999955, 0.03955927512614999808, 0.06812986271724999487, 0.09670045030835000555, 0.1252710378995000040, 0.1538416254905999869, 0.1824122130816999976, 0.2109828006727999805, 0.2395533882639000189, 0.2681239758550000296, 0.2966945634461000125, 0.3252651510371999954, 0.3538357386283000339, 0.3824063262194000168, 0.4109769138104999997, 0.4395475014015999826, 0.4681180889926999655, 0.4966886765838000040, 0.5252592641748999869, 0.5538298517660000808, 0.5824004393571000637, 0.6109710269481999356, 0.6395416145393000296, 0.6681122021304000125, 0.6966827897214999954, 0.7252533773125999783, 0.7538239649036999612, 0.7823945524947999441, 0.8109651400858999271, 0.8395357276770000210, 0.8681063152681000039, 0.8966769028592000979 ),
 .UNSPECIFIED. ) ;
#47482=CARTESIAN_POINT ( 'NONE',  ( 9.020964430773000586, 2.907392932634000005, 6.146188468825999784 ) ) ;
#47489=ORIENTED_EDGE ( 'NONE', *, *, #14872, .T. ) ;
#47492=CARTESIAN_POINT ( 'NONE',  ( 4.900006121741999010, 0.2617993877991516283, 1.999999999999999112 ) ) ;
#47493=CARTESIAN_POINT ( 'NONE',  ( 11.06133897141000055, 2.503910831767000023, -6.712778933675999760 ) ) ;
#47495=AXIS2_PLACEMENT_3D ( 'NONE', #32697, #43877, #884 ) ;
#47499=CARTESIAN_POINT ( 'NONE',  ( 10.56491664109999995, 4.212242527248999835, 8.933458498617000032 ) ) ;
#47503=ORIENTED_EDGE ( 'NONE', *, *, #50328, .T. ) ;
#47506=CARTESIAN_POINT ( 'NONE',  ( 9.520797373037000355, 3.270552986600999912, 5.711478154812000163 ) ) ;
#47508=CARTESIAN_POINT ( 'NONE',  ( 7.100000000000000533, 5.221516520829000640, -8.074802043613001246 ) ) ;
#47513=LINE ( 'NONE', #68819, #59548 ) ;
#47516=CARTESIAN_POINT ( 'NONE',  ( 9.825045280412000537, 3.116293075258000478, -6.208411413796000033 ) ) ;
#47518=EDGE_CURVE ( 'NONE', #49517, #44553, #29093, .T. ) ;
#47527=B_SPLINE_CURVE_WITH_KNOTS ( 'NONE', 3,
 ( #10537, #47264, #36774, #9500, #43045 ),
 .UNSPECIFIED., .F., .F.,
 ( 4, 1, 4 ),
 ( 0.000000000000000000, 0.5000000000000000000, 1.000000000000000000 ),
 .UNSPECIFIED. ) ;
#47529=CARTESIAN_POINT ( 'NONE',  ( 8.464260841230998977, 2.029098103856999735, 7.726995416028000108 ) ) ;
#47531=FACE_OUTER_BOUND ( 'NONE', #45313, .T. ) ;
#47535=CARTESIAN_POINT ( 'NONE',  ( 10.76010575649000067, 4.535386075958999896, 6.001721352166000223 ) ) ;
#47541=CARTESIAN_POINT ( 'NONE',  ( 7.775614158771000817, 4.636729845879000500, 9.378977473003999421 ) ) ;
#47542=CARTESIAN_POINT ( 'NONE',  ( 27.64127793187000037, 5.599999999999999645, -6.571291218949999902 ) ) ;
#47543=CARTESIAN_POINT ( 'NONE',  ( 11.05675868674000029, 5.188533356467999624, 4.847347870993000463 ) ) ;
#47547=CONICAL_SURFACE ( 'NONE', #18503, 1.600003888856000200, 0.7854004771980920285 ) ;
#47553=CARTESIAN_POINT ( 'NONE',  ( 11.00366064676999933, 2.264078662261999941, 7.798351372501000078 ) ) ;
#47556=ORIENTED_EDGE ( 'NONE', *, *, #42442, .T. ) ;
#47567=ORIENTED_EDGE ( 'NONE', *, *, #39227, .T. ) ;
#47568=CARTESIAN_POINT ( 'NONE',  ( 8.435394291146250723, 3.652552720689497878, 6.005833249671993279 ) ) ;
#47571=CARTESIAN_POINT ( 'NONE',  ( 10.42081182385000027, 2.488452444780999695, -7.717895019962999648 ) ) ;
#47572=CARTESIAN_POINT ( 'NONE',  ( 8.354426260476000010, 5.125517035499999707, 6.367235573876004473 ) ) ;
#47577=CARTESIAN_POINT ( 'NONE',  ( 9.304732780410999382, 5.284130523641000110, 6.489275570566000795 ) ) ;
#47578=VERTEX_POINT ( 'NONE', #66820 ) ;
#47579=CARTESIAN_POINT ( 'NONE',  ( 11.09999999999999787, 2.311256224650723556, -7.128998340778534448 ) ) ;
#47580=CARTESIAN_POINT ( 'NONE',  ( 11.09999999999999964, 4.000000000000000000, -7.500000000000000000 ) ) ;
#47587=CARTESIAN_POINT ( 'NONE',  ( 11.01769844498000062, 7.854486692293001227, 6.517457990503000786 ) ) ;
#47590=ORIENTED_EDGE ( 'NONE', *, *, #24535, .F. ) ;
#47593=DIRECTION ( 'NONE',  ( 0.000000000000000000, 0.000000000000000000, -1.000000000000000000 ) ) ;
#47597=CARTESIAN_POINT ( 'NONE',  ( 0.6885616966234999747, 3.123219710863000209, -0.8105742342224000474 ) ) ;
#47602=CARTESIAN_POINT ( 'NONE',  ( 7.607791299150002295, 3.471796661068001999, -6.504286038290998384 ) ) ;
#47604=CARTESIAN_POINT ( 'NONE',  ( 10.15335165876999923, 3.144981324235999853, -5.860948306964999688 ) ) ;
#47612=CARTESIAN_POINT ( 'NONE',  ( 9.136976429976831682, 5.100000000000000533, 6.167827406374086330 ) ) ;
#47613=CARTESIAN_POINT ( 'NONE',  ( 9.432439766855527097, 4.712051993706990238, -9.127118574761283298 ) ) ;
#47618=CARTESIAN_POINT ( 'NONE',  ( 8.157224700651678262, 3.176774960111513835, 6.225205742771084516 ) ) ;
#47619=ORIENTED_EDGE ( 'NONE', *, *, #29634, .T. ) ;
#47622=VECTOR ( 'NONE', #37063, 1000.000000000000114 ) ;
#47636=CARTESIAN_POINT ( 'NONE',  ( 11.09999999999999964, 7.355239926129000239, 6.360395311517000216 ) ) ;
#47638=B_SPLINE_CURVE_WITH_KNOTS ( 'NONE', 3,
 ( #2487, #23117, #61905, #1801 ),
 .UNSPECIFIED., .F., .F.,
 ( 4, 4 ),
 ( 0.000000000000000000, 0.05661757269142905086 ),
 .UNSPECIFIED. ) ;
#47640=CARTESIAN_POINT ( 'NONE',  ( 9.798945280410000791, 5.639765292528999829, -8.059103558718000215 ) ) ;
#47654=CARTESIAN_POINT ( 'NONE',  ( 8.548770280408998445, 5.203550244299999683, -8.391678825488000371 ) ) ;
#47656=LINE ( 'NONE', #32608, #51535 ) ;
#47663=EDGE_CURVE ( 'NONE', #5496, #16917, #32127, .T. ) ;
#47667=VERTEX_POINT ( 'NONE', #4683 ) ;
#47670=B_SPLINE_CURVE_WITH_KNOTS ( 'NONE', 3,
 ( #68537, #67855, #58067, #53162 ),
 .UNSPECIFIED., .F., .F.,
 ( 4, 4 ),
 ( 0.8747102523717062983, 1.000000000000000000 ),
 .UNSPECIFIED. ) ;
#47679=ORIENTED_EDGE ( 'NONE', *, *, #43929, .T. ) ;
#47683=CARTESIAN_POINT ( 'NONE',  ( 1.186390132541125020, -0.4581489286485234680, 3.499999999999998668 ) ) ;
#47690=ORIENTED_EDGE ( 'NONE', *, *, #45887, .T. ) ;
#47691=CARTESIAN_POINT ( 'NONE',  ( 1.433329478674677748, 2.750000000000000000, 7.763105750930175534E-10 ) ) ;
#47694=DIRECTION ( 'NONE',  ( 1.000000000000000000, 0.000000000000000000, 0.000000000000000000 ) ) ;
#47695=VECTOR ( 'NONE', #36024, 1000.000000000000000 ) ;
#47700=CYLINDRICAL_SURFACE ( 'NONE', #8470, 1.350000000000000533 ) ;
#47703=ADVANCED_FACE ( 'NONE', ( #19405 ), #25334, .T. ) ;
#47704=CARTESIAN_POINT ( 'NONE',  ( 6.999999999999998224, 8.700222682669624064, -4.587862420901095639 ) ) ;
#47707=ORIENTED_EDGE ( 'NONE', *, *, #28495, .T. ) ;
#47713=CARTESIAN_POINT ( 'NONE',  ( 1.717640132541333076, -1.762666431298159475, 3.058252359239895135 ) ) ;
#47726=CARTESIAN_POINT ( 'NONE',  ( 8.073148997456000231, 5.167567567567999731, -6.822293592207000934 ) ) ;
#47728=( GEOMETRIC_REPRESENTATION_CONTEXT ( 3 ) GLOBAL_UNCERTAINTY_ASSIGNED_CONTEXT ( ( #17607 ) ) GLOBAL_UNIT_ASSIGNED_CONTEXT ( ( #17209, #11609, #54619 ) ) REPRESENTATION_CONTEXT ( 'NONE', 'WORKASPACE' ) );
#47729=PLANE ( 'NONE',  #5405 ) ;
#47730=ORIENTED_EDGE ( 'NONE', *, *, #29229, .F. ) ;
#47732=CARTESIAN_POINT ( 'NONE',  ( 6.976095280407999866, 2.557426065706999818, -8.459317650138999056 ) ) ;
#47733=CIRCLE ( 'NONE', #53317, 12.39999890530000037 ) ;
#47735=CARTESIAN_POINT ( 'NONE',  ( 7.925195780913999677, 5.124045530936999882, 6.724518838937999732 ) ) ;
#47736=VERTEX_POINT ( 'NONE', #46326 ) ;
#47742=DIRECTION ( 'NONE',  ( 0.000000000000000000, -0.1218274111675001353, -0.9925512993736016476 ) ) ;
#47743=VERTEX_POINT ( 'NONE', #20092 ) ;
#47747=CARTESIAN_POINT ( 'NONE',  ( 8.112208753304994246, 4.887637668124002133, -6.169107735303001050 ) ) ;
#47754=EDGE_CURVE ( 'NONE', #47736, #25656, #20480, .T. ) ;
#47755=ORIENTED_EDGE ( 'NONE', *, *, #14699, .T. ) ;
#47757=ORIENTED_EDGE ( 'NONE', *, *, #5680, .T. ) ;
#47758=CARTESIAN_POINT ( 'NONE',  ( 10.94796973825000030, 2.864322365205000054, 8.846249469408000721 ) ) ;
#47759=CARTESIAN_POINT ( 'NONE',  ( 10.83487665876999984, 5.800192368099000184, -7.920541111170000370 ) ) ;
#47761=CARTESIAN_POINT ( 'NONE',  ( 8.771960841230001193, 3.061731693614000438, -8.535706278603999664 ) ) ;
#47762=CARTESIAN_POINT ( 'NONE',  ( 9.209204462306731287, 2.899999999999999911, 6.662590550601094286 ) ) ;
#47768=B_SPLINE_CURVE_WITH_KNOTS ( 'NONE', 3,
 ( #22264, #65943, #21915, #12827 ),
 .UNSPECIFIED., .F., .F.,
 ( 4, 4 ),
 ( 0.000000000000000000, 1.000000000000000000 ),
 .UNSPECIFIED. ) ;
#47787=CARTESIAN_POINT ( 'NONE',  ( 9.418864158773999407, 3.210851187372000037, -6.346613542714999667 ) ) ;
#47790=VERTEX_POINT ( 'NONE', #16215 ) ;
#47793=FACE_OUTER_BOUND ( 'NONE', #58740, .T. ) ;
#47794=DIRECTION ( 'NONE',  ( 0.000000000000000000, 0.000000000000000000, -1.000000000000000000 ) ) ;
#47795=CARTESIAN_POINT ( 'NONE',  ( 2.647747939885999990, 0.2284574491649999928, 3.751824152430999426 ) ) ;
#47796=ORIENTED_EDGE ( 'NONE', *, *, #19656, .F. ) ;
#47803=CARTESIAN_POINT ( 'NONE',  ( 7.410857780409000561, 2.302289264429000504, 6.875166305059000393 ) ) ;
#47806=CARTESIAN_POINT ( 'NONE',  ( 7.018770280410000062, 5.447281585506000390, -7.886005609586001164 ) ) ;
#47810=DIRECTION ( 'NONE',  ( -1.000000000000000000, 0.000000000000000000, 0.000000000000000000 ) ) ;
#47812=EDGE_LOOP ( 'NONE', ( #2574, #32758 ) ) ;
#47814=DIRECTION ( 'NONE',  ( 0.000000000000000000, 0.9519535082155350381, -0.3062425806385115079 ) ) ;
#47822=CARTESIAN_POINT ( 'NONE',  ( 7.422239158771000156, 5.361039412362000434, 6.973453640356000349 ) ) ;
#47823=ORIENTED_EDGE ( 'NONE', *, *, #894, .T. ) ;
#47826=CARTESIAN_POINT ( 'NONE',  ( 10.96855433372000022, 6.483894572015000080, -5.213062733535000604 ) ) ;
#47829=CARTESIAN_POINT ( 'NONE',  ( 6.365984310645998789, 10.53289132855000076, -4.483227135235997807 ) ) ;
#47830=LINE ( 'NONE', #11438, #18157 ) ;
#47831=CARTESIAN_POINT ( 'NONE',  ( 10.20000030442999872, -12.49999969551000056, 3.568610900609000272E-10 ) ) ;
#47844=CARTESIAN_POINT ( 'NONE',  ( 9.961465797930001642, 2.787126709928999801, -8.677707706574000923 ) ) ;
#47849=VERTEX_POINT ( 'NONE', #18216 ) ;
#47850=CARTESIAN_POINT ( 'NONE',  ( 9.160535748954998780, 2.900115872948000106, -6.152093930328999427 ) ) ;
#47851=FACE_OUTER_BOUND ( 'NONE', #65549, .T. ) ;
#47852=DIRECTION ( 'NONE',  ( -1.000000000000000000, 0.000000000000000000, 0.000000000000000000 ) ) ;
#47853=CARTESIAN_POINT ( 'NONE',  ( 10.00122429346999908, 2.274087081648999753, 7.851326250696001097 ) ) ;
#47858=EDGE_CURVE ( 'NONE', #64753, #53328, #412, .T. ) ;
#47861=CARTESIAN_POINT ( 'NONE',  ( 8.179999999999999716, 4.924138593003999809, -8.484107647018999998 ) ) ;
#47864=CARTESIAN_POINT ( 'NONE',  ( 9.219485841232998524, 3.892978337449999771, -8.893414073324001023 ) ) ;
#47868=CARTESIAN_POINT ( 'NONE',  ( 10.65729680893149656, 4.825159113303620906, 4.784047223868995502 ) ) ;
#47870=ORIENTED_EDGE ( 'NONE', *, *, #30702, .F. ) ;
#47872=CARTESIAN_POINT ( 'NONE',  ( 8.721010841230999233, 5.983047240001000411, 7.440798119034999658 ) ) ;
#47875=CARTESIAN_POINT ( 'NONE',  ( 8.415504719592000527, 2.469361196073999842, -7.826019481986000059 ) ) ;
#47878=ORIENTED_EDGE ( 'NONE', *, *, #5437, .F. ) ;
#47879=CARTESIAN_POINT ( 'NONE',  ( 11.24053267693000002, 2.774035422596999645, 6.782113650547000105 ) ) ;
#47880=AXIS2_PLACEMENT_3D ( 'NONE', #14425, #18636, #56032 ) ;
#47886=CARTESIAN_POINT ( 'NONE',  ( 9.294718325437999695, 4.148133901461999784, 9.337478696773001019 ) ) ;
#47891=CARTESIAN_POINT ( 'NONE',  ( 1.881520261439000086, 1.670918626813999941, 2.798091744145999815 ) ) ;
#47892=ORIENTED_EDGE ( 'NONE', *, *, #12273, .F. ) ;
#47899=CARTESIAN_POINT ( 'NONE',  ( 8.623264158775000965, 5.288433695693000480, -8.041290150997999930 ) ) ;
#47906=CARTESIAN_POINT ( 'NONE',  ( 11.09999999999999964, 4.000000000000000000, -7.500000000000000000 ) ) ;
#47911=CARTESIAN_POINT ( 'NONE',  ( 10.62924593896999959, 3.609487840896999700, -5.855139066690000504 ) ) ;
#47917=EDGE_CURVE ( 'NONE', #8013, #1268, #53782, .T. ) ;
#47918=CARTESIAN_POINT ( 'NONE',  ( 7.374100552923999352, 4.389299166881000858, 9.135259451319999613 ) ) ;
#47920=ORIENTED_EDGE ( 'NONE', *, *, #46591, .T. ) ;
#47926=CARTESIAN_POINT ( 'NONE',  ( 11.07072893487999998, 7.292360037005000351, 6.230956250625999893 ) ) ;
#47929=ORIENTED_EDGE ( 'NONE', *, *, #27223, .F. ) ;
#47932=DIRECTION ( 'NONE',  ( 0.000000000000000000, -0.9565994702956989171, -0.2914059941558995170 ) ) ;
#47935=ADVANCED_FACE ( 'NONE', ( #26374 ), #47700, .F. ) ;
#47938=CARTESIAN_POINT ( 'NONE',  ( 0.4500951013211000329, -1.019984463426999888, 3.043156295769000153 ) ) ;
#47939=CARTESIAN_POINT ( 'NONE',  ( 9.648120195397835275, 4.680076409640555823, -8.679834369160927210 ) ) ;
#47942=CARTESIAN_POINT ( 'NONE',  ( 9.087338750556188671, 5.286506002567208817, -7.027083108977566717 ) ) ;
#47944=CARTESIAN_POINT ( 'NONE',  ( 8.200215151753006637, 2.889589711576002085, -6.692116421364998402 ) ) ;
#47945=CARTESIAN_POINT ( 'NONE',  ( 10.30480165877000154, 5.828331171948000211, -7.226590957700000928 ) ) ;
#47952=CARTESIAN_POINT ( 'NONE',  ( 1.024155438487000191, -3.140063525497999830, -0.8725182546194000244 ) ) ;
#47953=FACE_OUTER_BOUND ( 'NONE', #42758, .T. ) ;
#47954=CARTESIAN_POINT ( 'NONE',  ( 3.483675495044915138, 1.122406039528702104, -3.256770312453929783 ) ) ;
#47956=B_SPLINE_CURVE_WITH_KNOTS ( 'NONE', 3,
 ( #23652, #44991, #2673, #66294 ),
 .UNSPECIFIED., .F., .F.,
 ( 4, 4 ),
 ( 0.000000000000000000, 1.000000000000000000 ),
 .UNSPECIFIED. ) ;
#47959=CARTESIAN_POINT ( 'NONE',  ( 8.180538548868272031, 3.349946943197689819, 6.152974595870256636 ) ) ;
#47963=LINE ( 'NONE', #31542, #26509 ) ;
#47966=CARTESIAN_POINT ( 'NONE',  ( 8.521585069485796637, 5.099999999999998757, 6.419216326168621478 ) ) ;
#47968=EDGE_CURVE ( 'NONE', #51168, #19886, #29667, .T. ) ;
#47973=LINE ( 'NONE', #71, #63224 ) ;
#47975=LINE ( 'NONE', #74, #43201 ) ;
#47977=EDGE_LOOP ( 'NONE', ( #30991, #3599, #48530, #47556 ) ) ;
#47978=CARTESIAN_POINT ( 'NONE',  ( 8.316054719590999511, 3.826300099041999747, -9.055335252254000267 ) ) ;
#47980=ORIENTED_EDGE ( 'NONE', *, *, #63735, .F. ) ;
#47990=DIRECTION ( 'NONE',  ( 0.000000000000000000, 1.000000000000000000, 0.000000000000000000 ) ) ;
#47997=CARTESIAN_POINT ( 'NONE',  ( 0.1103081484368000076, -1.521127753326000143, -2.712944034833999929 ) ) ;
#48003=CARTESIAN_POINT ( 'NONE',  ( 3.999971066382000284, 2.149963194831999935, 0.000000000000000000 ) ) ;
#48010=ADVANCED_FACE ( 'NONE', ( #55693 ), #6200, .T. ) ;
#48011=CARTESIAN_POINT ( 'NONE',  ( 10.01622971959000097, 4.325866256860000369, -9.125812605905000652 ) ) ;
#48014=ORIENTED_EDGE ( 'NONE', *, *, #54920, .T. ) ;
#48015=VERTEX_POINT ( 'NONE', #19305 ) ;
#48016=CARTESIAN_POINT ( 'NONE',  ( 11.05669206990999953, 5.189224932640000176, -4.849214782927999678 ) ) ;
#48034=FACE_OUTER_BOUND ( 'NONE', #55517, .T. ) ;
#48035=VECTOR ( 'NONE', #27784, 1000.000000000000114 ) ;
#48039=B_SPLINE_SURFACE_WITH_KNOTS ( 'NONE', 3, 3, ( 
 ( #68404, #31373, #20874, #41509, #58968, #46763, #37297, #58275, #25776, #5483, #5819, #68755, #21553, #15289, #42211, #20527, #53036, #20182, #63513, #15630, #52685, #41853, #26470, #36612, #62821, #32066, #57581, #9686, #57938, #52343, #4437, #53382, #26818, #31035, #16311 ),
 ( #10034, #36961, #10378, #64196, #47803, #63854, #48134, #15967, #238, #42889, #37635, #11072, #1970, #22589, #16997, #38679, #39032, #48825, #11751, #1274, #21895, #39370, #27158, #17709, #60000, #6158, #55104, #55452, #54410, #23292, #43582, #60347, #64537, #43931, #64883 ),
 ( #65584, #12455, #65236, #28191, #6510, #17351, #38324, #48479, #37980, #60689, #1619, #33093, #33788, #22934, #7210, #586, #59654, #6854, #43233, #28547, #12806, #27855, #59304, #34135, #12111, #49506, #18053, #16654, #11406, #32745, #49161, #934, #54061, #49857, #44633 ),
 ( #27499, #22244, #65925, #33439, #54755, #44286, #30262, #40071, #29238, #19067, #51568, #18395, #24664, #61038, #35505, #66961, #19414, #45654, #50548, #23977, #39720, #55798, #13159, #3663, #40738, #35839, #62063, #40394, #3331, #67638, #14522, #56825, #61717, #34487, #46336 ) ),
 .UNSPECIFIED., .F., .F., .F.,
 ( 4, 4 ),
 ( 4, 1, 1, 1, 1, 1, 1, 1, 1, 1, 1, 1, 1, 1, 1, 1, 1, 1, 1, 1, 1, 1, 1, 1, 1, 1, 1, 1, 1, 1, 1, 1, 4 ),
 ( -0.1039370721279000015, 1.103937072127999963 ),
 ( -0.02000000000000000042, 0.01250000000000000069, 0.04499999999999999833, 0.07749999999999999944, 0.1100000000000000006, 0.1424999999999999878, 0.1749999999999999889, 0.2074999999999999900, 0.2399999999999999911, 0.2725000000000000200, 0.3049999999999999933, 0.3375000000000000222, 0.3699999999999999956, 0.4025000000000000244, 0.4349999999999999978, 0.4675000000000000266, 0.5000000000000000000, 0.5324999999999999734, 0.5649999999999999467, 0.5975000000000000311, 0.6300000000000000044, 0.6624999999999999778, 0.6949999999999999512, 0.7275000000000000355, 0.7600000000000000089, 0.7924999999999999822, 0.8249999999999999556, 0.8575000000000000400, 0.8900000000000000133, 0.9224999999999999867, 0.9549999999999999600, 0.9875000000000000444, 1.020000000000000018 ),
 .UNSPECIFIED. ) ;
#48061=DIRECTION ( 'NONE',  ( 0.000000000000000000, 1.000000000000000000, 0.000000000000000000 ) ) ;
#48062=ORIENTED_EDGE ( 'NONE', *, *, #48377, .T. ) ;
#48065=FACE_OUTER_BOUND ( 'NONE', #4118, .T. ) ;
#48068=CARTESIAN_POINT ( 'NONE',  ( 7.224720280406000228, 5.425783499582999880, -6.515903575897000088 ) ) ;
#48070=CARTESIAN_POINT ( 'NONE',  ( 7.229686263356974507, 4.176830497180914037, -8.849626747523609893 ) ) ;
#48078=EDGE_CURVE ( 'NONE', #68596, #61815, #68913, .T. ) ;
#48086=CARTESIAN_POINT ( 'NONE',  ( 7.315000000000000391, 2.649999999999999911, -7.500000000000000000 ) ) ;
#48091=CARTESIAN_POINT ( 'NONE',  ( 9.778460659405999067, 5.743717947473999885, 7.748300625457000379 ) ) ;
#48093=CARTESIAN_POINT ( 'NONE',  ( 10.11548915876999999, 2.489190114737999782, -6.434635778494999236 ) ) ;
#48104=ORIENTED_EDGE ( 'NONE', *, *, #25669, .F. ) ;
#48107=CARTESIAN_POINT ( 'NONE',  ( 1.750973465873000068, -3.500000000000000000, 0.000000000000000000 ) ) ;
#48109=CARTESIAN_POINT ( 'NONE',  ( 10.71756692516999898, 3.040224182812999665, 8.808452309630000698 ) ) ;
#48122=ORIENTED_EDGE ( 'NONE', *, *, #55681, .T. ) ;
#48123=CARTESIAN_POINT ( 'NONE',  ( 0.9630201129275000049, 2.655425791298000160, -2.578923811134000044 ) ) ;
#48124=AXIS2_PLACEMENT_3D ( 'NONE', #56859, #14556, #10329 ) ;
#48126=CARTESIAN_POINT ( 'NONE',  ( 2.743111838768000244, -3.411508600277999737, 1.577969057705999933 ) ) ;
#48134=CARTESIAN_POINT ( 'NONE',  ( 7.539232780409000689, 4.696238830159999544, 5.830273622963999536 ) ) ;
#48138=ADVANCED_FACE ( 'NONE', ( #30493 ), #47547, .F. ) ;
#48139=CARTESIAN_POINT ( 'NONE',  ( 7.160229719588000030, 2.268824274702999855, -7.434159913875999948 ) ) ;
#48147=CARTESIAN_POINT ( 'NONE',  ( 7.000000000000000000, 0.000000000000000000, 0.000000000000000000 ) ) ;
#48151=CARTESIAN_POINT ( 'NONE',  ( 9.049999337612000261, 3.268496584495999908E-13, 3.612668863294000056E-14 ) ) ;
#48156=CARTESIAN_POINT ( 'NONE',  ( 7.358051658771000092, 4.561643343497000735, 6.153061759127000485 ) ) ;
#48157=EDGE_CURVE ( 'NONE', #38001, #51068, #63674, .T. ) ;
#48160=CYLINDRICAL_SURFACE ( 'NONE', #54889, 0.5000000000000004441 ) ;
#48161=CARTESIAN_POINT ( 'NONE',  ( 11.12439302932000018, 5.546250282613000238, -5.163688852187999778 ) ) ;
#48175=CARTESIAN_POINT ( 'NONE',  ( 10.31498017945866685, 2.650031506806222570, -7.499998780888569527 ) ) ;
#48177=CARTESIAN_POINT ( 'NONE',  ( 9.947306532704999427, 4.892812229297999416, -9.067756197920999739 ) ) ;
#48179=EDGE_CURVE ( 'NONE', #63173, #47736, #53127, .T. ) ;
#48185=ADVANCED_FACE ( 'NONE', ( #57734 ), #8869, .F. ) ;
#48186=CARTESIAN_POINT ( 'NONE',  ( 1.831685767832333722, -3.258006849854496956, -1.322661048612402857 ) ) ;
#48187=CARTESIAN_POINT ( 'NONE',  ( 11.15982925107999968, 5.578232410510000072, 8.067793621926998782 ) ) ;
#48194=CARTESIAN_POINT ( 'NONE',  ( 9.123551658772999673, 5.558938731259999599, 6.272977177425000050 ) ) ;
#48195=DIRECTION ( 'NONE',  ( 0.000000000000000000, 0.000000000000000000, -1.000000000000000000 ) ) ;
#48196=SURFACE_STYLE_USAGE ( .BOTH. , #22649 ) ;
#48205=CARTESIAN_POINT ( 'NONE',  ( 7.988545280410000338, 3.566637212418000136, 5.743604853744000316 ) ) ;
#48206=CARTESIAN_POINT ( 'NONE',  ( 9.301695280414000067, 5.619431609641999614, -8.115423117607999615 ) ) ;
#48210=CARTESIAN_POINT ( 'NONE',  ( 10.81579666500999970, 5.374569445151000657, 6.698728322222000209 ) ) ;
#48216=CARTESIAN_POINT ( 'NONE',  ( 7.583051658771000625, 4.763536573491999881, 5.668879554882000349 ) ) ;
#48229=ORIENTED_EDGE ( 'NONE', *, *, #27728, .F. ) ;
#48230=CARTESIAN_POINT ( 'NONE',  ( 8.275189158773001097, 3.061731693614000438, -8.535706278603999664 ) ) ;
#48234=CARTESIAN_POINT ( 'NONE',  ( 9.168971206446350664, 4.353237884208152053, -8.814534730582089139 ) ) ;
#48243=CARTESIAN_POINT ( 'NONE',  ( 9.261662452849000360, 2.944259351255000379, 6.507396354981000108 ) ) ;
#48244=CARTESIAN_POINT ( 'NONE',  ( 10.36630583688000051, 5.852743870412999705, -7.568014644338999730 ) ) ;
#48245=CARTESIAN_POINT ( 'NONE',  ( 8.076862807906000086, 5.120521186033995420, 6.727223554611003742 ) ) ;
#48250=CARTESIAN_POINT ( 'NONE',  ( 9.433107780409999421, 4.954905351382000944, 8.825777580285999235 ) ) ;
#48255=B_SPLINE_CURVE_WITH_KNOTS ( 'NONE', 3,
 ( #24917, #40649, #45569, #35081, #46249, #52173, #41346, #9175, #14093, #51153, #30513, #67212, #4274, #35419, #3250, #67904, #50808, #8841 ),
 .UNSPECIFIED., .F., .F.,
 ( 4, 2, 2, 2, 2, 2, 2, 2, 4 ),
 ( 0.000000000000000000, 0.1250000000000000000, 0.2500000000000000000, 0.3750000000000000000, 0.5000000000000000000, 0.6250000000000000000, 0.7500000000000000000, 0.8750000000000000000, 1.000000000000000000 ),
 .UNSPECIFIED. ) ;
#48256=B_SPLINE_CURVE_WITH_KNOTS ( 'NONE', 3,
 ( #2616, #51540, #23948, #3636 ),
 .UNSPECIFIED., .F., .F.,
 ( 4, 4 ),
 ( 0.000000000000000000, 1.000000000000000000 ),
 .UNSPECIFIED. ) ;
#48259=CARTESIAN_POINT ( 'NONE',  ( 11.00881343608999963, 8.459666197630999918, 6.608740754140999485 ) ) ;
#48266=DIRECTION ( 'NONE',  ( 1.000000000000000000, 0.000000000000000000, 0.000000000000000000 ) ) ;
#48273=CARTESIAN_POINT ( 'NONE',  ( 0.6968879684122999407, 0.8965373106021000682, -3.081807587122999958 ) ) ;
#48274=CARTESIAN_POINT ( 'NONE',  ( 8.793505787816332742, 5.100000000000000533, 6.515557531858333640 ) ) ;
#48277=CARTESIAN_POINT ( 'NONE',  ( 8.560885841230001958, 4.228291488957999888, 8.941375734143997889 ) ) ;
#48279=CARTESIAN_POINT ( 'NONE',  ( 7.928980562030001344, 3.137685067990001020, -6.261915436850998162 ) ) ;
#48281=CARTESIAN_POINT ( 'NONE',  ( 10.00190165877000048, 2.729646201450000031, -8.843033333815998986 ) ) ;
#48283=CARTESIAN_POINT ( 'NONE',  ( 7.935109315130008056, 5.090269470254001227, 6.488511505667004187 ) ) ;
#48288=CARTESIAN_POINT ( 'NONE',  ( 9.520528907821001141, 2.899999999999999911, 6.152188490330000370 ) ) ;
#48289=DIRECTION ( 'NONE',  ( 1.000000000000000000, 0.000000000000000000, 0.000000000000000000 ) ) ;
#48290=DIRECTION ( 'NONE',  ( -1.000000000000000000, 1.065814103617000051E-13, -1.598721155425999962E-13 ) ) ;
#48293=CARTESIAN_POINT ( 'NONE',  ( 11.09999999999999964, 4.000000000000000000, -7.500000000000000000 ) ) ;
#48296=EDGE_CURVE ( 'NONE', #47380, #64893, #38674, .T. ) ;
#48303=CARTESIAN_POINT ( 'NONE',  ( 8.554392358909119309, 5.071045932662843647, 6.303914025558337464 ) ) ;
#48305=B_SPLINE_CURVE_WITH_KNOTS ( 'NONE', 3,
 ( #65919, #59993, #2303, #34128, #61376 ),
 .UNSPECIFIED., .F., .F.,
 ( 4, 1, 4 ),
 ( 0.000000000000000000, 0.5000000000000000000, 1.000000000000000000 ),
 .UNSPECIFIED. ) ;
#48315=CARTESIAN_POINT ( 'NONE',  ( 9.749220280410998640, 5.656948148960999845, -6.994239053114000626 ) ) ;
#48317=ORIENTED_EDGE ( 'NONE', *, *, #13448, .F. ) ;
#48318=CIRCLE ( 'NONE', #19320, 1.999999999999999778 ) ;
#48321=ORIENTED_EDGE ( 'NONE', *, *, #17136, .F. ) ;
#48332=CARTESIAN_POINT ( 'NONE',  ( 8.722235841230000730, 3.844886277615000125, -8.888911790991000927 ) ) ;
#48335=CARTESIAN_POINT ( 'NONE',  ( 0.4680276591073351256, -2.422374426748084009, 2.170046970593778823 ) ) ;
#48349=CARTESIAN_POINT ( 'NONE',  ( 9.246064158776000852, 5.200883864107000321, -6.027780766890000308 ) ) ;
#48355=CARTESIAN_POINT ( 'NONE',  ( 8.672510841228998402, 4.686731264770999772, -8.717075579553000608 ) ) ;
#48356=CARTESIAN_POINT ( 'NONE',  ( 10.08061813254432693, 5.349721876211404492, -7.768808602171199951 ) ) ;
#48358=CARTESIAN_POINT ( 'NONE',  ( 4.000000000000000000, 0.000000000000000000, 0.000000000000000000 ) ) ;
#48364=CARTESIAN_POINT ( 'NONE',  ( 2.029064736457000251, 3.399126080497508973, -0.9633645835951684111 ) ) ;
#48377=EDGE_CURVE ( 'NONE', #29064, #65266, #1954, .T. ) ;
#48378=AXIS2_PLACEMENT_3D ( 'NONE', #29268, #2339, #44316 ) ;
#48384=CARTESIAN_POINT ( 'NONE',  ( 0.1499942179679999987, -2.750000000000000000, 0.000000000000000000 ) ) ;
#48389=CARTESIAN_POINT ( 'NONE',  ( 8.392328736400999745, 5.100230418103000041, 6.589669365926999589 ) ) ;
#48402=ORIENTED_EDGE ( 'NONE', *, *, #61726, .T. ) ;
#48404=CARTESIAN_POINT ( 'NONE',  ( 11.01356641589999974, 2.786433584103999994, 6.253463831328000211 ) ) ;
#48409=CARTESIAN_POINT ( 'NONE',  ( 7.116410841227000184, 2.101490574575000103, -7.427795877530000368 ) ) ;
#48411=CARTESIAN_POINT ( 'NONE',  ( 9.498145159330512399, 4.816870420262897134, 8.576492378600933719 ) ) ;
#48414=B_SPLINE_CURVE_WITH_KNOTS ( 'NONE', 3,
 ( #61651, #67228, #35098, #20034, #14110, #45239, #23903, #8513, #30194, #34751, #24596, #24246, #66889, #29861, #24933, #41015, #51169, #46267, #3264, #61997 ),
 .UNSPECIFIED., .F., .F.,
 ( 4, 2, 2, 2, 2, 2, 2, 2, 2, 4 ),
 ( 0.000000000000000000, 0.06250000000000000000, 0.1250000000000000000, 0.2500000000000000555, 0.3750000000000001110, 0.5000000000000001110, 0.6250000000000001110, 0.7500000000000001110, 0.8750000000000001110, 1.000000000000000000 ),
 .UNSPECIFIED. ) ;
#48415=B_SPLINE_CURVE_WITH_KNOTS ( 'NONE', 3,
 ( #61020, #34115, #34801, #67619 ),
 .UNSPECIFIED., .F., .F.,
 ( 4, 4 ),
 ( 0.000000000000000000, 1.000000000000000000 ),
 .UNSPECIFIED. ) ;
#48416=LINE ( 'NONE', #63452, #20586 ) ;
#48418=CIRCLE ( 'NONE', #49566, 12.99999854704999969 ) ;
#48425=CARTESIAN_POINT ( 'NONE',  ( 8.389220148804989563, 5.100598871404000256, -6.637806542482997507 ) ) ;
#48428=CARTESIAN_POINT ( 'NONE',  ( 10.60454270958608625, 3.072761288248648359, 8.633924816819705583 ) ) ;
#48433=CARTESIAN_POINT ( 'NONE',  ( 10.83658792121999959, 5.133186143592999962, 8.848368005200001107 ) ) ;
#48434=CARTESIAN_POINT ( 'NONE',  ( 10.07762665876999897, 2.169012810937000157, -7.244984731085000185 ) ) ;
#48442=AXIS2_PLACEMENT_3D ( 'NONE', #23486, #6355, #27703 ) ;
#48446=EDGE_CURVE ( 'NONE', #58012, #39722, #2893, .T. ) ;
#48447=EDGE_LOOP ( 'NONE', ( #66010, #56360, #27343, #68722 ) ) ;
#48450=FACE_BOUND ( 'NONE', #17989, .T. ) ;
#48451=CARTESIAN_POINT ( 'NONE',  ( 6.899999691988000450, -12.99045401563999924, -1.690592933733000125 ) ) ;
#48453=CARTESIAN_POINT ( 'NONE',  ( 10.53138775541999905, 5.607751175212000838, 7.280102404048999887 ) ) ;
#48465=CARTESIAN_POINT ( 'NONE',  ( 8.921614158776000281, 3.251172436837000301, -6.320036569851000152 ) ) ;
#48468=DIRECTION ( 'NONE',  ( 0.000000000000000000, 1.000000000000000000, 0.000000000000000000 ) ) ;
#48473=CARTESIAN_POINT ( 'NONE',  ( 10.72802334123000101, 3.751278653658999929, -8.836901076820000256 ) ) ;
#48479=CARTESIAN_POINT ( 'NONE',  ( 7.512829719590000010, 5.524123123935000379, 6.910361319981999095 ) ) ;
#48482=CARTESIAN_POINT ( 'NONE',  ( 8.254179719588000452, 3.402419637676000086, -5.873899751133000002 ) ) ;
#48489=VERTEX_POINT ( 'NONE', #45297 ) ;
#48490=EDGE_CURVE ( 'NONE', #4028, #42555, #55403, .T. ) ;
#48491=CARTESIAN_POINT ( 'NONE',  ( 0.2153359931920000025, 3.215315751876999695, 1.126573897625000029E-09 ) ) ;
#48493=VECTOR ( 'NONE', #53394, 1000.000000000000000 ) ;
#48498=DIRECTION ( 'NONE',  ( 1.000000000000000000, 0.000000000000000000, 0.000000000000000000 ) ) ;
#48502=CARTESIAN_POINT ( 'NONE',  ( 8.566232780412001091, 5.212261578733999201, 6.157186134061999994 ) ) ;
#48511=CARTESIAN_POINT ( 'NONE',  ( 9.112942518363999156, 5.100000000000000533, 6.192000867487999827 ) ) ;
#48526=CARTESIAN_POINT ( 'NONE',  ( 8.045433776029998540, 2.903894639863001892, -6.425841880607995549 ) ) ;
#48530=ORIENTED_EDGE ( 'NONE', *, *, #66687, .T. ) ;
#48534=CARTESIAN_POINT ( 'NONE',  ( 9.352253013669001191, 2.817757427878999632, 6.388459691516000127 ) ) ;
#48535=CARTESIAN_POINT ( 'NONE',  ( 10.47094409420000005, 5.100000000000000533, 6.571291218949999902 ) ) ;
#48537=CARTESIAN_POINT ( 'NONE',  ( 9.222206734151470187, 2.649920175418960078, 7.547759605734272625 ) ) ;
#48540=CARTESIAN_POINT ( 'NONE',  ( 7.100000000000436629, 3.640294921184452637, -6.161369192892991897 ) ) ;
#48541=AXIS2_PLACEMENT_3D ( 'NONE', #57873, #25366, #67318 ) ;
#48549=CARTESIAN_POINT ( 'NONE',  ( 10.87208388804061698, 5.035013780143576589, 4.888821408800270163 ) ) ;
#48555=CARTESIAN_POINT ( 'NONE',  ( 8.026329719592000700, 5.601795057054999916, 7.176148573050999957 ) ) ;
#48556=CARTESIAN_POINT ( 'NONE',  ( 9.500595280412998278, 2.334550724494000029, -7.977056617806000283 ) ) ;
#48558=CARTESIAN_POINT ( 'NONE',  ( 2.771536717063348476, 3.252280351444815309, -0.1916433810219522749 ) ) ;
#48560=ORIENTED_EDGE ( 'NONE', *, *, #14607, .T. ) ;
#48561=CARTESIAN_POINT ( 'NONE',  ( 10.48165121391000021, 4.022873529486999722, 9.090897232145000117 ) ) ;
#48579=ORIENTED_EDGE ( 'NONE', *, *, #46541, .F. ) ;
#48580=CARTESIAN_POINT ( 'NONE',  ( 9.459729719592999686, 2.527713920559999661, -6.969421869128999525 ) ) ;
#48584=VERTEX_POINT ( 'NONE', #50879 ) ;
#48585=CARTESIAN_POINT ( 'NONE',  ( 9.314928906318884927, 2.650140463285438397, -7.499996151983930659 ) ) ;
#48586=DIRECTION ( 'NONE',  ( -0.9999999999999978906, 6.450930526679976792E-08, 1.612071427334991320E-09 ) ) ;
#48590=ORIENTED_EDGE ( 'NONE', *, *, #31575, .F. ) ;
#48594=CARTESIAN_POINT ( 'NONE',  ( 10.99933470386000067, 5.081013421858999735, 8.239043921879998678 ) ) ;
#48595=CARTESIAN_POINT ( 'NONE',  ( 9.947306532704999427, 4.892812229297999416, -9.067756197920999739 ) ) ;
#48596=CARTESIAN_POINT ( 'NONE',  ( 9.216851002545999094, 2.832432432432000269, 6.822293592207000934 ) ) ;
#48602=CARTESIAN_POINT ( 'NONE',  ( 8.560885841230001958, 4.228291488957999888, 8.941375734143997889 ) ) ;
#48603=ORIENTED_EDGE ( 'NONE', *, *, #32196, .F. ) ;
#48605=CARTESIAN_POINT ( 'NONE',  ( 10.35685100253999913, 2.832432432432000269, -6.822293592207000934 ) ) ;
#48609=CARTESIAN_POINT ( 'NONE',  ( 11.12484646121000154, 6.576544621967000737, 5.637917610392999990 ) ) ;
#48610=CARTESIAN_POINT ( 'NONE',  ( 11.01659397126999984, 7.354769923016999833, 6.171139243954000264 ) ) ;
#48611=ADVANCED_FACE ( 'NONE', ( #29577 ), #30825, .T. ) ;
#48616=EDGE_CURVE ( 'NONE', #57662, #54751, #66604, .T. ) ;
#48620=CARTESIAN_POINT ( 'NONE',  ( 9.532678149083000818, 4.663044775770000427, 8.669813205957000335 ) ) ;
#48621=CARTESIAN_POINT ( 'NONE',  ( 8.267367474942998840, 3.071849710027000135, -6.244583336620999958 ) ) ;
#48624=CARTESIAN_POINT ( 'NONE',  ( 8.432510841230001830, 5.430400319332999715, 7.210801214872999410 ) ) ;
#48629=CARTESIAN_POINT ( 'NONE',  ( 7.798085185677998687, 3.459333709783000366, -6.382131374430003667 ) ) ;
#48630=CARTESIAN_POINT ( 'NONE',  ( 10.59957028040999916, 4.438147096284001059, -8.958385582135001357 ) ) ;
#48633=CARTESIAN_POINT ( 'NONE',  ( 8.060004013849999538, 5.097451875645002239, 6.450907456765003545 ) ) ;
#48636=CARTESIAN_POINT ( 'NONE',  ( 8.959699012653233652, 5.323639004032087563, 7.230967499102583851 ) ) ;
#48637=ORIENTED_EDGE ( 'NONE', *, *, #32219, .T. ) ;
#48638=VECTOR ( 'NONE', #63058, 1000.000000000000000 ) ;
#48640=LINE ( 'NONE', #6669, #57904 ) ;
#48645=CARTESIAN_POINT ( 'NONE',  ( 8.200000304434999165, 12.49999969551000056, -3.568532357647000425E-10 ) ) ;
#48663=CARTESIAN_POINT ( 'NONE',  ( 8.895035841232999729, 5.751585344281000545, -8.235867044345999588 ) ) ;
#48668=ORIENTED_EDGE ( 'NONE', *, *, #45454, .F. ) ;
#48676=LINE ( 'NONE', #10236, #47178 ) ;
#48679=ORIENTED_EDGE ( 'NONE', *, *, #10336, .F. ) ;
#48680=CARTESIAN_POINT ( 'NONE',  ( 8.579854990165880935, 4.352864158102216940, 8.850923404438425734 ) ) ;
#48683=CARTESIAN_POINT ( 'NONE',  ( 10.13061872827999998, 2.189311095934999951, -7.101639631284999865 ) ) ;
#48684=ORIENTED_EDGE ( 'NONE', *, *, #66350, .F. ) ;
#48694=CARTESIAN_POINT ( 'NONE',  ( 10.33253786428999987, 2.899999999999999911, 6.571291218949999902 ) ) ;
#48695=EDGE_CURVE ( 'NONE', #21003, #61003, #69008, .T. ) ;
#48699=CARTESIAN_POINT ( 'NONE',  ( 7.015090560819000842, 4.719833207100999850, -8.789699670502999496 ) ) ;
#48703=CARTESIAN_POINT ( 'NONE',  ( 8.649364158774000444, 3.038023536984999939, -5.861661709981000001 ) ) ;
#48708=CARTESIAN_POINT ( 'NONE',  ( 3.259306799210500927, -3.058252359239909346, 1.762666431298136605 ) ) ;
#48709=CARTESIAN_POINT ( 'NONE',  ( 8.871410841230998656, 2.721111233225000259, -6.936528696292000085 ) ) ;
#48710=DIRECTION ( 'NONE',  ( 0.000000000000000000, 1.000000000000000000, 0.000000000000000000 ) ) ;
#48723=AXIS2_PLACEMENT_3D ( 'NONE', #59929, #10655, #26752 ) ;
#48739=CARTESIAN_POINT ( 'NONE',  ( 1.985247277619000217, 2.372532593102000043, -2.573147701680999599 ) ) ;
#48741=ORIENTED_EDGE ( 'NONE', *, *, #9483, .F. ) ;
#48746=CARTESIAN_POINT ( 'NONE',  ( 7.000000000000000000, 10.29799223392326546, 4.279123368246552594 ) ) ;
#48750=ORIENTED_EDGE ( 'NONE', *, *, #32023, .T. ) ;
#48753=CARTESIAN_POINT ( 'NONE',  ( 9.658629719592001450, 5.496789211521000418, -7.043125396300999874 ) ) ;
#48754=ORIENTED_EDGE ( 'NONE', *, *, #23916, .T. ) ;
#48757=CARTESIAN_POINT ( 'NONE',  ( 6.876645280409000804, 4.455038580940000159, -9.171635993214000138 ) ) ;
#48759=CARTESIAN_POINT ( 'NONE',  ( 9.493540423042883702, 4.876969314220700014, 8.526773713797128451 ) ) ;
#48765=B_SPLINE_CURVE_WITH_KNOTS ( 'NONE', 3,
 ( #68317, #62732, #66955, #19062, #67633 ),
 .UNSPECIFIED., .F., .F.,
 ( 4, 1, 4 ),
 ( 0.7874025540483345909, 0.8749496349986518595, 1.000000000000000000 ),
 .UNSPECIFIED. ) ;
#48774=DIRECTION ( 'NONE',  ( 0.000000000000000000, -1.000000000000000000, 0.000000000000000000 ) ) ;
#48780=VERTEX_POINT ( 'NONE', #49406 ) ;
#48781=CARTESIAN_POINT ( 'NONE',  ( 11.09999999999999964, 4.000000000000000000, 7.500000000000000000 ) ) ;
#48782=CARTESIAN_POINT ( 'NONE',  ( 10.41838915877000105, 4.531912033713999755, -9.270484952459998595 ) ) ;
#48783=CARTESIAN_POINT ( 'NONE',  ( 1.250973465874999802, -3.500000000000000000, 0.000000000000000000 ) ) ;
#48790=ORIENTED_EDGE ( 'NONE', *, *, #23518, .F. ) ;
#48804=CARTESIAN_POINT ( 'NONE',  ( 8.521235029058406241, 5.099999848902339039, -6.534141629449454314 ) ) ;
#48810=FACE_OUTER_BOUND ( 'NONE', #21379, .T. ) ;
#48816=COLOUR_RGB ( '', 0.66274510, 0.83137255, 0.94901961) ;
#48818=CARTESIAN_POINT ( 'NONE',  ( 10.46298584122999920, 3.993164721578000176, -6.140176455708999725 ) ) ;
#48825=CARTESIAN_POINT ( 'NONE',  ( 8.245295280410999794, 4.283000592898000392, 9.286795422009001655 ) ) ;
#48826=ORIENTED_EDGE ( 'NONE', *, *, #2048, .T. ) ;
#48828=CARTESIAN_POINT ( 'NONE',  ( 8.055279719587000287, 3.504660014889999786, -9.160103207264000957 ) ) ;
#48832=ORIENTED_EDGE ( 'NONE', *, *, #3527, .F. ) ;
#48839=ADVANCED_FACE ( 'NONE', ( #22147, #55351 ), #49758, .T. ) ;
#48840=EDGE_CURVE ( 'NONE', #27697, #10337, #2871, .T. ) ;
#48849=CARTESIAN_POINT ( 'NONE',  ( 9.250899447075999760, 4.135077451221000011, 9.175524215473998879 ) ) ;
#48858=CARTESIAN_POINT ( 'NONE',  ( 7.888897165042807913, 5.521107890873540036, -8.565486907688864449 ) ) ;
#48869=CARTESIAN_POINT ( 'NONE',  ( 8.450464158772000189, 3.789127741898000057, -9.388182174781999123 ) ) ;
#48871=CARTESIAN_POINT ( 'NONE',  ( 11.11264834745999863, 2.146077493652999824, -7.517188756437000130 ) ) ;
#48879=CARTESIAN_POINT ( 'NONE',  ( 1.816329616853666673, -3.450786940248409707, -0.6753594422426503208 ) ) ;
#48880=CARTESIAN_POINT ( 'NONE',  ( 10.87021720923999979, 2.226038107033000202, 7.782753921296999167 ) ) ;
#48884=CARTESIAN_POINT ( 'NONE',  ( 10.95616034570999986, 9.845173301957000689, -5.754287415814000717 ) ) ;
#48886=CARTESIAN_POINT ( 'NONE',  ( 7.100000000000589395, 4.595628095797888335, -6.248885204747992361 ) ) ;
#48893=CARTESIAN_POINT ( 'NONE',  ( 9.667010841233000917, 4.769103072373000352, -8.666849124598000387 ) ) ;
#48898=ORIENTED_EDGE ( 'NONE', *, *, #49045, .T. ) ;
#48900=CARTESIAN_POINT ( 'NONE',  ( 7.475045280409000625, 3.276311362504999991, 5.841989464160999290 ) ) ;
#48901=CARTESIAN_POINT ( 'NONE',  ( 9.061929719594999710, 4.092867382745001059, -5.937785237406000505 ) ) ;
#48905=CARTESIAN_POINT ( 'NONE',  ( 9.980433037259000884, 4.047223446241999589, 9.090360698422999874 ) ) ;
#48906=B_SPLINE_CURVE_WITH_KNOTS ( 'NONE', 3,
 ( #65716, #6641, #18180, #38810 ),
 .UNSPECIFIED., .F., .F.,
 ( 4, 4 ),
 ( 0.000000000000000000, 1.000000000000000000 ),
 .UNSPECIFIED. ) ;
#48916=CARTESIAN_POINT ( 'NONE',  ( 11.09999999999999964, 2.700000000000000178, -6.461133846875999787 ) ) ;
#48925=EDGE_CURVE ( 'NONE', #4028, #16280, #12702, .T. ) ;
#48926=CARTESIAN_POINT ( 'NONE',  ( 9.468589158772999781, 4.034680274230000308, -6.102912434217000026 ) ) ;
#48932=DIRECTION ( 'NONE',  ( 0.000000000000000000, 0.000000000000000000, -1.000000000000000000 ) ) ;
#48940=CARTESIAN_POINT ( 'NONE',  ( 10.68903608760000168, 2.568976842941999905, 7.728092503410000091 ) ) ;
#48941=CARTESIAN_POINT ( 'NONE',  ( 10.83768005408999890, 5.758100475276000552, -6.911469147650000977 ) ) ;
#48949=CARTESIAN_POINT ( 'NONE',  ( 8.406107780410998487, 5.342170561818999630, 8.432311822615000452 ) ) ;
#48950=ORIENTED_EDGE ( 'NONE', *, *, #46980, .F. ) ;
#48951=CARTESIAN_POINT ( 'NONE',  ( 0.2066231058121046349, -2.618168328974044765E-06, -3.206444164765644977 ) ) ;
#48952=CARTESIAN_POINT ( 'NONE',  ( 11.09999999999999964, 4.000000000000000000, -7.500000000000000000 ) ) ;
#48955=CARTESIAN_POINT ( 'NONE',  ( 10.96237843380999877, 6.768007902811000065, 5.462774374486000895 ) ) ;
#48956=CARTESIAN_POINT ( 'NONE',  ( 10.94962848994000026, 8.455114238872999621, 6.519461126146000929 ) ) ;
#48962=CARTESIAN_POINT ( 'NONE',  ( 10.01533268956000100, 4.946987614118000032, 8.559212393557999121 ) ) ;
#48967=CARTESIAN_POINT ( 'NONE',  ( 9.240545280410998430, 4.158911560497999815, 5.873540104660999184 ) ) ;
#48968=CARTESIAN_POINT ( 'NONE',  ( 9.877261637240000169, 2.207988120125000009, 7.624813826992999921 ) ) ;
#48969=ADVANCED_FACE ( 'NONE', ( #57067 ), #34386, .F. ) ;
#48973=CARTESIAN_POINT ( 'NONE',  ( 7.854823341228001077, 4.561643343497000735, 6.153061759127000485 ) ) ;
#48980=ORIENTED_EDGE ( 'NONE', *, *, #16186, .F. ) ;
#48990=CARTESIAN_POINT ( 'NONE',  ( 7.000000000000000000, 0.000000000000000000, 0.000000000000000000 ) ) ;
#48991=CARTESIAN_POINT ( 'NONE',  ( 9.679055905794999859, 2.899999999999999911, 6.571291218949999902 ) ) ;
#48992=CARTESIAN_POINT ( 'NONE',  ( 1.848158326185999956, -2.375092696518000146, -2.913277015014000160 ) ) ;
#49001=ADVANCED_FACE ( 'NONE', ( #35411 ), #50935, .F. ) ;
#49008=CARTESIAN_POINT ( 'NONE',  ( 7.343717773735517262, 3.601282447181377577, 9.195592440584203331 ) ) ;
#49025=CARTESIAN_POINT ( 'NONE',  ( 10.06481084123000080, 5.336630274082000192, -7.092011739486999922 ) ) ;
#49027=EDGE_CURVE ( 'NONE', #10085, #798, #61626, .T. ) ;
#49028=DIRECTION ( 'NONE',  ( 1.000000000000000000, 0.000000000000000000, 0.000000000000000000 ) ) ;
#49031=DIRECTION ( 'NONE',  ( 1.000000000000000000, 0.000000000000000000, 0.000000000000000000 ) ) ;
#49036=CARTESIAN_POINT ( 'NONE',  ( 4.399997082757114875, 2.000000000000000000, 4.865849894060234886E-09 ) ) ;
#49040=CARTESIAN_POINT ( 'NONE',  ( 7.062228317541999978, 5.346164515353000191, -7.398308812559000636 ) ) ;
#49042=DIRECTION ( 'NONE',  ( 0.000000000000000000, 1.000000000000000000, 0.000000000000000000 ) ) ;
#49044=CARTESIAN_POINT ( 'NONE',  ( 8.681370280410998674, 2.949305648881000330, -8.659807625323999503 ) ) ;
#49045=EDGE_CURVE ( 'NONE', #53731, #54722, #54262, .T. ) ;
#49048=ORIENTED_EDGE ( 'NONE', *, *, #56063, .F. ) ;
#49055=CARTESIAN_POINT ( 'NONE',  ( 1.021806799209249883, 3.408904368339103375, 0.9161175952574877046 ) ) ;
#49060=CYLINDRICAL_SURFACE ( 'NONE', #68767, 13.10000000000000142 ) ;
#49076=CARTESIAN_POINT ( 'NONE',  ( 5.500000000000000000, 12.43893545635000031, -2.828937028792000152 ) ) ;
#49079=VERTEX_POINT ( 'NONE', #45894 ) ;
#49087=CARTESIAN_POINT ( 'NONE',  ( 7.000000000000000888, 9.534618748583843839, 4.680683473982556464 ) ) ;
#49093=LINE ( 'NONE', #12384, #59668 ) ;
#49094=CARTESIAN_POINT ( 'NONE',  ( 2.800973465877999669, -3.500000000000000000, 0.000000000000000000 ) ) ;
#49095=CARTESIAN_POINT ( 'NONE',  ( 9.369139158774000720, 2.685250982074999904, -7.026194612421999608 ) ) ;
#49098=CARTESIAN_POINT ( 'NONE',  ( 7.622520280405000292, 3.458959908335999867, -5.854223596299999777 ) ) ;
#49102=DIRECTION ( 'NONE',  ( 1.000000000000000000, 0.000000000000000000, 0.000000000000000000 ) ) ;
#49104=ORIENTED_EDGE ( 'NONE', *, *, #61642, .F. ) ;
#49107=DIRECTION ( 'NONE',  ( -0.8660254038714592095, 4.159366548383805334E-14, 0.4999999998492760667 ) ) ;
#49108=VERTEX_POINT ( 'NONE', #58101 ) ;
#49114=CARTESIAN_POINT ( 'NONE',  ( 10.42499241036494162, 5.349775919985349404, 7.500001834605750872 ) ) ;
#49118=CARTESIAN_POINT ( 'NONE',  ( 9.470944094206000585, 5.100000000000000533, 6.571291218949999902 ) ) ;
#49119=CARTESIAN_POINT ( 'NONE',  ( 10.86460778041000097, 3.843601682313000367, -5.985271987931999327 ) ) ;
#49133=CARTESIAN_POINT ( 'NONE',  ( 7.100000000000000533, 0.000000000000000000, 0.000000000000000000 ) ) ;
#49138=CARTESIAN_POINT ( 'NONE',  ( 8.766851002546001581, 2.832432432432000269, 6.822293592207000934 ) ) ;
#49149=CARTESIAN_POINT ( 'NONE',  ( 9.202245280414000916, 5.095038542659000136, -6.157541456184000062 ) ) ;
#49153=CARTESIAN_POINT ( 'NONE',  ( 0.8807558238970999431, -0.8575131787502999758, -3.600995375387999964 ) ) ;
#49155=CARTESIAN_POINT ( 'NONE',  ( 1.948412681420000014, 1.958206349467000118, -3.033258895291999657 ) ) ;
#49156=ORIENTED_EDGE ( 'NONE', *, *, #1092, .F. ) ;
#49158=CARTESIAN_POINT ( 'NONE',  ( 9.970944094204998720, 5.100000000000000533, 6.571291218949999902 ) ) ;
#49161=CARTESIAN_POINT ( 'NONE',  ( 8.989142219592000771, 5.284130523641000110, 6.489275570566000795 ) ) ;
#49165=ADVANCED_FACE ( 'NONE', ( #6674 ), #21715, .F. ) ;
#49166=CARTESIAN_POINT ( 'NONE',  ( 7.300545280410000615, 2.766448485756999975, -6.536937350656000234 ) ) ;
#49168=CARTESIAN_POINT ( 'NONE',  ( 10.89227882974000039, 3.998355201738000630, 9.261308739708001170 ) ) ;
#49170=ORIENTED_EDGE ( 'NONE', *, *, #41654, .T. ) ;
#49171=DIRECTION ( 'NONE',  ( 0.5298945044129826920, -2.133608886496929164E-08, -0.8480635673066725388 ) ) ;
#49175=CARTESIAN_POINT ( 'NONE',  ( 10.88314899746000108, 5.167567567567999731, 6.822293592207000934 ) ) ;
#49179=EDGE_LOOP ( 'NONE', ( #9275, #43932, #5410 ) ) ;
#49181=LINE ( 'NONE', #60018, #18205 ) ;
#49186=CARTESIAN_POINT ( 'NONE',  ( 8.449239158774000558, 5.458692773671000253, 7.456452194274000078 ) ) ;
#49188=EDGE_CURVE ( 'NONE', #53432, #38357, #10746, .T. ) ;
#49195=ADVANCED_FACE ( 'NONE', ( #11230 ), #64703, .T. ) ;
#49196=CARTESIAN_POINT ( 'NONE',  ( 4.600001223043999943, 0.000000000000000000, 0.000000000000000000 ) ) ;
#49197=FACE_OUTER_BOUND ( 'NONE', #45773, .T. ) ;
#49198=CARTESIAN_POINT ( 'NONE',  ( 5.000030787342999439, 0.2748844998327762412, 2.099962892531004766 ) ) ;
#49207=CARTESIAN_POINT ( 'NONE',  ( 9.444964158775000840, 3.920043641733999884, -9.398198753036000497 ) ) ;
#49208=CARTESIAN_POINT ( 'NONE',  ( 10.07930935222999835, 2.718121894972999719, -6.397795030233000446 ) ) ;
#49210=DIRECTION ( 'NONE',  ( 0.000000000000000000, 0.7071067811865475727, -0.7071067811865475727 ) ) ;
#49211=CARTESIAN_POINT ( 'NONE',  ( 7.928980562030001344, 3.137685067990001020, -6.261915436850998162 ) ) ;
#49215=CARTESIAN_POINT ( 'NONE',  ( 9.215291255903000689, 4.861981595026999337, 8.938817176893000038 ) ) ;
#49216=CARTESIAN_POINT ( 'NONE',  ( 10.43314899746000002, 5.167567567567999731, 6.822293592207000934 ) ) ;
#49220=CARTESIAN_POINT ( 'NONE',  ( 7.100000000000255440, 2.544001923346042027, -7.316064667941583721 ) ) ;
#49224=AXIS2_PLACEMENT_3D ( 'NONE', #7265, #28605, #17412 ) ;
#49234=CARTESIAN_POINT ( 'NONE',  ( 9.143920280410000601, 5.791553967443999973, 7.752111263209999770 ) ) ;
#49235=CARTESIAN_POINT ( 'NONE',  ( 9.012204719595001023, 3.161445734422999809, -6.178649910536000434 ) ) ;
#49238=CARTESIAN_POINT ( 'NONE',  ( 2.813453680541110113, 2.907771984247602859, 1.469325272863359899 ) ) ;
#49240=CARTESIAN_POINT ( 'NONE',  ( 10.57892463485000079, 4.649960478797999563, 5.681084732956000138 ) ) ;
#49244=CARTESIAN_POINT ( 'NONE',  ( 8.040182825300005831, 3.147885656133000420, 6.175979896252004053 ) ) ;
#49245=ORIENTED_EDGE ( 'NONE', *, *, #41572, .F. ) ;
#49246=DIRECTION ( 'NONE',  ( 1.000000000000000000, 5.940303217303999818E-14, -2.897679909401000343E-10 ) ) ;
#49247=ADVANCED_FACE ( 'NONE', ( #59467 ), #22802, .F. ) ;
#49248=EDGE_CURVE ( 'NONE', #13653, #36985, #27319, .T. ) ;
#49254=ORIENTED_EDGE ( 'NONE', *, *, #37583, .F. ) ;
#49255=DIRECTION ( 'NONE',  ( -1.000000000000000000, 0.000000000000000000, 0.000000000000000000 ) ) ;
#49261=CARTESIAN_POINT ( 'NONE',  ( 9.559179719593000613, 4.038835765825999680, -5.935509327774999733 ) ) ;
#49266=CARTESIAN_POINT ( 'NONE',  ( 7.975798314879130935, 5.079350072276184846, -6.595737603274040239 ) ) ;
#49273=EDGE_CURVE ( 'NONE', #13267, #46704, #11918, .T. ) ;
#49276=CARTESIAN_POINT ( 'NONE',  ( 11.07336716268999943, 2.375546981533999791, -8.393546861057000541 ) ) ;
#49277=CARTESIAN_POINT ( 'NONE',  ( 8.523148997455999520, 5.167567567567999731, -6.822293592207000934 ) ) ;
#49281=AXIS2_PLACEMENT_3D ( 'NONE', #48781, #38282, #11707 ) ;
#49284=CARTESIAN_POINT ( 'NONE',  ( 9.123551658772999673, 5.558938731259999599, 6.272977177425000050 ) ) ;
#49286=CARTESIAN_POINT ( 'NONE',  ( 10.34286678428570383, 2.713835889960351633, -7.027064066396564890 ) ) ;
#49287=CARTESIAN_POINT ( 'NONE',  ( 7.256896516720705570, 2.725911303287724685, 6.976330978549669659 ) ) ;
#49292=CARTESIAN_POINT ( 'NONE',  ( 10.89874804681000064, 2.834828962328999502, 9.088465460431999432 ) ) ;
#49304=EDGE_CURVE ( 'NONE', #13153, #62671, #30095, .T. ) ;
#49305=CARTESIAN_POINT ( 'NONE',  ( 7.571670280409000142, 2.531201476950000195, 8.216704145297999418 ) ) ;
#49306=CARTESIAN_POINT ( 'NONE',  ( 10.46432998405999903, 2.042755206296999582, 7.723699495214000343 ) ) ;
#49311=CARTESIAN_POINT ( 'NONE',  ( 9.549696181504543802, 3.998651493754435737, 8.867000060670969575 ) ) ;
#49317=CARTESIAN_POINT ( 'NONE',  ( 0.8874568971869000178, 2.877489654231000227, -1.904074875451999826 ) ) ;
#49323=CARTESIAN_POINT ( 'NONE',  ( 3.500000000000000000, 0.000000000000000000, 0.000000000000000000 ) ) ;
#49325=CARTESIAN_POINT ( 'NONE',  ( 7.933148997457998952, 5.167567567567999731, 6.822293592207000934 ) ) ;
#49326=ORIENTED_EDGE ( 'NONE', *, *, #61644, .T. ) ;
#49327=CARTESIAN_POINT ( 'NONE',  ( 6.649999999999999467, 5.221516520829000640, -8.074802043613001246 ) ) ;
#49331=CARTESIAN_POINT ( 'NONE',  ( 10.49646369190720030, 5.100000000000000533, -6.665341197380429961 ) ) ;
#49332=CARTESIAN_POINT ( 'NONE',  ( 0.7037915396055000050, -2.255103325128000158, 3.007138987545999953 ) ) ;
#49336=FACE_OUTER_BOUND ( 'NONE', #42980, .T. ) ;
#49339=DIRECTION ( 'NONE',  ( -1.000000000000000000, 0.000000000000000000, 0.000000000000000000 ) ) ;
#49345=CARTESIAN_POINT ( 'NONE',  ( 8.646410841231000788, 2.261390688294000029, -6.733978371730000134 ) ) ;
#49346=EDGE_LOOP ( 'NONE', ( #10572, #56821, #41329, #54320 ) ) ;
#49354=CARTESIAN_POINT ( 'NONE',  ( 9.409314688805999083, 2.634692233435000031, 8.920311306029999443 ) ) ;
#49359=B_SPLINE_CURVE_WITH_KNOTS ( 'NONE', 3,
 ( #63771, #64111, #26038, #41429, #21137, #68672, #47713, #10637, #4356, #16226, #15882, #46683, #37214, #68323, #52951, #62738, #58194, #53294 ),
 .UNSPECIFIED., .F., .F.,
 ( 4, 2, 2, 2, 2, 2, 2, 2, 4 ),
 ( 0.000000000000000000, 0.1250000000000000278, 0.2500000000000000000, 0.3749999999999999445, 0.4999999999999999445, 0.6249999999999998890, 0.7499999999999998890, 0.8750000000000000000, 1.000000000000000000 ),
 .UNSPECIFIED. ) ;
#49362=FACE_OUTER_BOUND ( 'NONE', #41549, .T. ) ;
#49366=CIRCLE ( 'NONE', #2464, 12.50000000000000000 ) ;
#49376=CARTESIAN_POINT ( 'NONE',  ( 7.488771682458000178, 4.037115771921000018, -6.023232697733999608 ) ) ;
#49380=CIRCLE ( 'NONE', #32624, 1.700000201121000032 ) ;
#49381=CARTESIAN_POINT ( 'NONE',  ( 9.336654719594999818, 5.095038542659000136, -6.157541456184000062 ) ) ;
#49390=LINE ( 'NONE', #22821, #5064 ) ;
#49392=EDGE_CURVE ( 'NONE', #56588, #25932, #49439, .T. ) ;
#49399=CARTESIAN_POINT ( 'NONE',  ( 7.744301850232000461, 3.130385018321999890, 6.467396599055999395 ) ) ;
#49406=CARTESIAN_POINT ( 'NONE',  ( 10.81499708368641954, 2.650004840405624673, -7.499999822193707644 ) ) ;
#49412=CARTESIAN_POINT ( 'NONE',  ( 10.98768472639999949, 2.860900986606000007, -4.945212061661000469 ) ) ;
#49424=CARTESIAN_POINT ( 'NONE',  ( 2.304719994299625707, -2.744941749261882169, -2.197574953528184771 ) ) ;
#49426=DIRECTION ( 'NONE',  ( 1.000000000000000000, 0.000000000000000000, 0.000000000000000000 ) ) ;
#49430=CARTESIAN_POINT ( 'NONE',  ( 10.84999882987999875, 0.000000000000000000, 0.000000000000000000 ) ) ;
#49434=CARTESIAN_POINT ( 'NONE',  ( 2.790556799211291406, -3.500000000000002220, 0.4581489286484968781 ) ) ;
#49439=B_SPLINE_CURVE_WITH_KNOTS ( 'NONE', 3,
 ( #66094, #61888, #18904, #50027 ),
 .UNSPECIFIED., .F., .F.,
 ( 4, 4 ),
 ( 0.000000000000000000, 1.000000000000000000 ),
 .UNSPECIFIED. ) ;
#49441=EDGE_CURVE ( 'NONE', #24902, #49079, #17445, .T. ) ;
#49444=ORIENTED_EDGE ( 'NONE', *, *, #38934, .T. ) ;
#49445=CARTESIAN_POINT ( 'NONE',  ( 8.861802827888666911, 2.874603711572078613, -6.749639981085472584 ) ) ;
#49447=CARTESIAN_POINT ( 'NONE',  ( 9.942214158770999788, 3.986577607995999806, -9.280166295424001177 ) ) ;
#49449=CARTESIAN_POINT ( 'NONE',  ( 10.42081182385000027, 2.488452444780999695, -7.717895019962999648 ) ) ;
#49455=CARTESIAN_POINT ( 'NONE',  ( 8.433536308088498856, 2.899999999999999911, -6.665341197412902652 ) ) ;
#49459=ORIENTED_EDGE ( 'NONE', *, *, #20825, .F. ) ;
#49460=CARTESIAN_POINT ( 'NONE',  ( 10.96876099447000108, 2.333339469804000199, 6.524055942683999021 ) ) ;
#49461=CARTESIAN_POINT ( 'NONE',  ( 10.05462971959000029, 3.531217403581000003, -9.119235467071000301 ) ) ;
#49465=B_SPLINE_CURVE_WITH_KNOTS ( 'NONE', 3,
 ( #40751, #62415, #62074, #14190 ),
 .UNSPECIFIED., .F., .F.,
 ( 4, 4 ),
 ( 0.000000000000000000, 1.000000000000000000 ),
 .UNSPECIFIED. ) ;
#49472=CARTESIAN_POINT ( 'NONE',  ( 9.336654719594999818, 5.095038542659000136, -6.157541456184000062 ) ) ;
#49480=DIRECTION ( 'NONE',  ( 0.000000000000000000, 0.8350135785638144181, -0.5502293372895092904 ) ) ;
#49482=DIRECTION ( 'NONE',  ( -1.000000000000000000, 0.000000000000000000, 3.552713678810000077E-14 ) ) ;
#49486=AXIS2_PLACEMENT_3D ( 'NONE', #31252, #52561, #4658 ) ;
#49494=CARTESIAN_POINT ( 'NONE',  ( 9.102795280413999990, 3.071719032003000116, -6.037263251225000182 ) ) ;
#49495=( BOUNDED_SURFACE ( )  B_SPLINE_SURFACE ( 3, 3, ( 
 ( #51127, #3230, #40626, #61958, #47944, #59111, #10528, #385, #58767 ),
 ( #21364, #37790, #68560, #21701, #63313, #52492, #9842, #44, #10874 ),
 ( #43391, #42361, #11217, #31520, #48279, #4589, #31868, #42694, #64002 ),
 ( #5624, #16120, #32553, #53866, #37446, #48629, #26625, #47602, #43037 ) ),
 .UNSPECIFIED., .F., .F., .F. ) 
 B_SPLINE_SURFACE_WITH_KNOTS ( ( 4, 4 ),
 ( 4, 1, 1, 1, 1, 1, 4 ),
 ( 0.000000000000000000, 1.000000000000000000 ),
 ( -0.004646279661397999423, 0.000000000000000000, 0.03269534097185999855, 0.06255479614191999937, 0.08986301827557000022, 0.1148786485006999952, 0.1376622693536999897 ),
 .UNSPECIFIED. ) 
 GEOMETRIC_REPRESENTATION_ITEM ( )  RATIONAL_B_SPLINE_SURFACE ( (
 ( 1.187699524740999824, 1.187699524740999824, 1.187699524740999824, 1.187699524740999824, 1.187699524740999824, 1.187699524740999824, 1.187699524740999824, 1.187699524740999824, 1.187699524740999824),
 ( 0.9374334917530999789, 0.9374334917530999789, 0.9374334917530999789, 0.9374334917530999789, 0.9374334917530999789, 0.9374334917530999789, 0.9374334917530999789, 0.9374334917530999789, 0.9374334917530999789),
 ( 0.9374334917530999789, 0.9374334917530999789, 0.9374334917530999789, 0.9374334917530999789, 0.9374334917530999789, 0.9374334917530999789, 0.9374334917530999789, 0.9374334917530999789, 0.9374334917530999789),
 ( 1.187699524740999824, 1.187699524740999824, 1.187699524740999824, 1.187699524740999824, 1.187699524740999824, 1.187699524740999824, 1.187699524740999824, 1.187699524740999824, 1.187699524740999824) ) ) 
 REPRESENTATION_ITEM ( '' )  SURFACE ( )  );
#49499=CARTESIAN_POINT ( 'NONE',  ( 0.8724295521082999771, 2.537743131474000435, -2.464631551651000230 ) ) ;
#49501=CARTESIAN_POINT ( 'NONE',  ( 2.352109567116000388, -0.7825563863409999987, 3.335029682752000291 ) ) ;
#49504=CARTESIAN_POINT ( 'NONE',  ( 6.983066481085000277, 12.13287628867999857, -3.076835277494999854 ) ) ;
#49506=CARTESIAN_POINT ( 'NONE',  ( 8.668204719592999652, 3.979464555644999901, 9.134076336209998814 ) ) ;
#49509=CARTESIAN_POINT ( 'NONE',  ( 8.137010841226000935, 5.144639763962000067, -8.301783154141999077 ) ) ;
#49511=FACE_OUTER_BOUND ( 'NONE', #17704, .T. ) ;
#49517=VERTEX_POINT ( 'NONE', #18561 ) ;
#49526=CARTESIAN_POINT ( 'NONE',  ( 8.158337970077000990E-06, 0.000000000000000000, 0.000000000000000000 ) ) ;
#49529=CARTESIAN_POINT ( 'NONE',  ( 10.09999999999999964, 0.000000000000000000, 0.000000000000000000 ) ) ;
#49531=CARTESIAN_POINT ( 'NONE',  ( 11.09999999999999964, 2.649999999999999911, 7.500000000000000000 ) ) ;
#49537=CARTESIAN_POINT ( 'NONE',  ( 0.3738300074506999970, -3.373808768376999723, -1.182108054635000026E-09 ) ) ;
#49539=CARTESIAN_POINT ( 'NONE',  ( 5.000030787343000327, 2.045306479342562600, 0.5496608443529819032 ) ) ;
#49544=ORIENTED_EDGE ( 'NONE', *, *, #28498, .F. ) ;
#49549=CARTESIAN_POINT ( 'NONE',  ( 9.494689158774999527, 2.824732249080000202, -8.992748220058999209 ) ) ;
#49550=CARTESIAN_POINT ( 'NONE',  ( 3.299581029697000290, 2.884784742943000246, -1.760185852660000050 ) ) ;
#49551=B_SPLINE_CURVE_WITH_KNOTS ( 'NONE', 3,
 ( #19718, #25646, #41040, #51865 ),
 .UNSPECIFIED., .F., .F.,
 ( 4, 4 ),
 ( 0.000000000000000000, 1.000000000000000000 ),
 .UNSPECIFIED. ) ;
#49555=B_SPLINE_CURVE_WITH_KNOTS ( 'NONE', 3,
 ( #1998, #24009, #3023, #65954 ),
 .UNSPECIFIED., .F., .F.,
 ( 4, 4 ),
 ( 0.000000000000000000, 1.000000000000000000 ),
 .UNSPECIFIED. ) ;
#49558=CARTESIAN_POINT ( 'NONE',  ( 1.923822673704333575, -0.09607108383954165998, -3.514941141763996413 ) ) ;
#49561=CARTESIAN_POINT ( 'NONE',  ( 10.58844943056000076, 3.754657019866000311, 5.545350295858999523 ) ) ;
#49565=CARTESIAN_POINT ( 'NONE',  ( 9.218906920141307637, 2.654016165387476089, 7.603667288042461614 ) ) ;
#49566=AXIS2_PLACEMENT_3D ( 'NONE', #43292, #59362, #990 ) ;
#49571=B_SPLINE_CURVE_WITH_KNOTS ( 'NONE', 3,
 ( #56406, #45579, #51496, #14105, #3935, #66885, #52183, #9184, #25272, #4284, #25619, #35430, #57768, #46609, #40661, #3591, #40324, #31221 ),
 .UNSPECIFIED., .F., .F.,
 ( 4, 2, 2, 2, 2, 2, 2, 2, 4 ),
 ( 0.000000000000000000, 0.1250000000000000000, 0.2500000000000000000, 0.3750000000000000000, 0.5000000000000000000, 0.6250000000000000000, 0.7500000000000000000, 0.8750000000000000000, 1.000000000000000000 ),
 .UNSPECIFIED. ) ;
#49582=EDGE_CURVE ( 'NONE', #65344, #57358, #30874, .T. ) ;
#49583=CARTESIAN_POINT ( 'NONE',  ( 8.849385841230999361, 3.975069902178000270, 9.483774112875002160 ) ) ;
#49584=CIRCLE ( 'NONE', #16097, 1.999999999999999778 ) ;
#49585=CARTESIAN_POINT ( 'NONE',  ( 8.994485841233000656, 3.854507394315999758, -9.394302886912999639 ) ) ;
#49586=CARTESIAN_POINT ( 'NONE',  ( 0.5647703222817161972, 3.481129241836969701, 0.6274791494510446599 ) ) ;
#49588=ORIENTED_EDGE ( 'NONE', *, *, #4079, .T. ) ;
#49593=CARTESIAN_POINT ( 'NONE',  ( 7.778861800931997195, 3.520498707107000858, 6.411393241748998051 ) ) ;
#49596=CARTESIAN_POINT ( 'NONE',  ( 8.330224159023998709, 2.898680183691999979, -6.607597200868999820 ) ) ;
#49601=CARTESIAN_POINT ( 'NONE',  ( 11.03644315172999946, 5.222804237133000349, 5.023246923241000417 ) ) ;
#49607=CARTESIAN_POINT ( 'NONE',  ( 7.453125355210004521, 3.231590054310000237, 6.459270056246999125 ) ) ;
#49610=CARTESIAN_POINT ( 'NONE',  ( 9.202245280414000916, 5.095038542659000136, -6.157541456184000062 ) ) ;
#49614=ORIENTED_EDGE ( 'NONE', *, *, #29564, .F. ) ;
#49621=B_SPLINE_SURFACE_WITH_KNOTS ( 'NONE', 3, 3, ( 
 ( #25230, #51458, #9486, #18962, #56019, #8127, #13386, #3224, #14066, #34708, #40288, #46220, #3556, #45541, #8473, #36066, #35391, #29473, #50782 ),
 ( #61604, #40971, #19650, #23859, #35729, #13722, #67528, #39950, #56715, #50427, #9147, #24552, #2531, #35051, #66501, #56369, #45875, #45195, #18622 ),
 ( #21358, #42687, #63308, #25920, #37784, #53526, #21021, #32211, #53178, #63996, #68905, #31862, #10185, #4932, #47251, #52138, #41656, #10521, #47597 ),
 ( #26618, #58082, #5277, #15773, #26959, #21695, #30828, #43031, #4240, #47938, #10867, #64334, #58417, #25580, #42356, #48273, #31514, #57726, #5616 ) ),
 .UNSPECIFIED., .F., .F., .F.,
 ( 4, 4 ),
 ( 4, 1, 1, 1, 1, 1, 1, 1, 1, 1, 1, 1, 1, 1, 1, 1, 4 ),
 ( -0.1039370721279000015, 1.103937072127999963 ),
 ( 0.5600558712726999566, 0.5880915265348000132, 0.6161271817967999276, 0.6441628370587999530, 0.6721984923209000096, 0.7002341475828999240, 0.7282698028449000605, 0.7563054581070000060, 0.7843411133690000314, 0.8123767686310000569, 0.8404124238931000024, 0.8684480791551000278, 0.8964837344171000533, 0.9245193896790999677, 0.9525550449412000242, 0.9805907002032000497, 1.008626355465000124 ),
 .UNSPECIFIED. ) ;
#49626=CARTESIAN_POINT ( 'NONE',  ( 10.87376707263999975, 2.935913933350999816, -5.106852029161000672 ) ) ;
#49628=LINE ( 'NONE', #66044, #36366 ) ;
#49633=CARTESIAN_POINT ( 'NONE',  ( 8.032364158772001161, 3.524748802314000340, 5.573833469815000718 ) ) ;
#49637=CARTESIAN_POINT ( 'NONE',  ( 7.209999981161347549, 2.651351331278276380, 7.772802126760149477 ) ) ;
#49641=CARTESIAN_POINT ( 'NONE',  ( 10.96237823296000080, 5.422576852879000597, 4.905482803814000370 ) ) ;
#49642=FACE_OUTER_BOUND ( 'NONE', #10048, .T. ) ;
#49644=CARTESIAN_POINT ( 'NONE',  ( 2.161066381942999826, 1.253716066476000091, -2.802099984798000154 ) ) ;
#49646=ORIENTED_EDGE ( 'NONE', *, *, #15919, .F. ) ;
#49656=CARTESIAN_POINT ( 'NONE',  ( 9.074385841230999006, 3.981661882377999895, 8.959227447876999761 ) ) ;
#49657=CARTESIAN_POINT ( 'NONE',  ( 10.77462860031000069, 5.575476001419000127, 8.682676628339999425 ) ) ;
#49660=CARTESIAN_POINT ( 'NONE',  ( 9.693589158772999426, 4.047146749018000200, -5.600703114891000034 ) ) ;
#49662=DIRECTION ( 'NONE',  ( 1.000000000000000000, 0.000000000000000000, 0.000000000000000000 ) ) ;
#49663=CARTESIAN_POINT ( 'NONE',  ( 8.229964631809997044, 4.681828315382999151, 6.132208354562998842 ) ) ;
#49669=CARTESIAN_POINT ( 'NONE',  ( 1.357929084572999878, 0.7969358895047999880, 3.160091737778000009 ) ) ;
#49676=CARTESIAN_POINT ( 'NONE',  ( 10.91165259814999899, 2.977149300665999476, 4.913708281391000021 ) ) ;
#49680=CARTESIAN_POINT ( 'NONE',  ( 6.758001042874380637, 3.668692617901999853, -8.939602259005999585 ) ) ;
#49684=CARTESIAN_POINT ( 'NONE',  ( 1.323656882336000207, -3.146289470026999879, -2.056511572473000093 ) ) ;
#49686=CARTESIAN_POINT ( 'NONE',  ( 10.63590686542921304, 5.314851119340273655, -7.853271763851206622 ) ) ;
#49689=CARTESIAN_POINT ( 'NONE',  ( 0.000000000000000000, 2.899999999999999911, 7.500000000000000000 ) ) ;
#49698=CARTESIAN_POINT ( 'NONE',  ( 8.447510841229000533, 4.933589693325000525, -9.154576215408999573 ) ) ;
#49699=ORIENTED_EDGE ( 'NONE', *, *, #47267, .F. ) ;
#49701=CARTESIAN_POINT ( 'NONE',  ( 7.749582268678000929, 3.139123315411999737, 6.460037574229000157 ) ) ;
#49704=FACE_OUTER_BOUND ( 'NONE', #30691, .T. ) ;
#49711=B_SPLINE_CURVE_WITH_KNOTS ( 'NONE', 3,
 ( #61602, #51456, #56710, #23161, #67180, #66154, #18272, #19294, #29118, #39592, #66496, #40619 ),
 .UNSPECIFIED., .F., .F.,
 ( 4, 2, 2, 2, 2, 4 ),
 ( 0.000000000000000000, 0.2500000000000009992, 0.3750000000000003331, 0.4375000000000012768, 0.5000000000000022204, 1.000000000000000000 ),
 .UNSPECIFIED. ) ;
#49714=CARTESIAN_POINT ( 'NONE',  ( 11.01333310117409248, 5.463772421452093297, -7.751599404485491007 ) ) ;
#49719=CARTESIAN_POINT ( 'NONE',  ( 10.73994861561131486, 3.062995749313938365, -4.824365178346956107 ) ) ;
#49721=CARTESIAN_POINT ( 'NONE',  ( 10.66951519566999806, 4.592673277375999952, 5.841403042559999648 ) ) ;
#49727=CARTESIAN_POINT ( 'NONE',  ( 7.849248001123737772, 3.014156315379637352, -6.506962576755648264 ) ) ;
#49730=FACE_OUTER_BOUND ( 'NONE', #27293, .T. ) ;
#49736=CARTESIAN_POINT ( 'NONE',  ( 9.427245280414000561, 4.989193221215000307, -6.287302145481000082 ) ) ;
#49743=DIRECTION ( 'NONE',  ( 1.000000000000000000, 0.000000000000000000, 0.000000000000000000 ) ) ;
#49744=DIRECTION ( 'NONE',  ( 1.000000000000000000, 0.000000000000000000, 0.000000000000000000 ) ) ;
#49745=CARTESIAN_POINT ( 'NONE',  ( 1.084306799208999861, 1.762666431298138825, 3.058252359239908014 ) ) ;
#49749=DIRECTION ( 'NONE',  ( 1.000000000000000000, 0.000000000000000000, 0.000000000000000000 ) ) ;
#49750=CARTESIAN_POINT ( 'NONE',  ( 6.966665954281333839, 12.09896498756869576, -3.276379939815991627 ) ) ;
#49758=PLANE ( 'NONE',  #33014 ) ;
#49759=UNCERTAINTY_MEASURE_WITH_UNIT (LENGTH_MEASURE( 1.000000000000000082E-05 ), #64260, 'distance_accuracy_value', 'NONE');
#49772=CARTESIAN_POINT ( 'NONE',  ( 9.332537864288001472, 2.899999999999999911, 6.571291218949999902 ) ) ;
#49776=CARTESIAN_POINT ( 'NONE',  ( -0.000000000000000000, -0.7586348975815445650, -2.824745580908569309 ) ) ;
#49787=ORIENTED_EDGE ( 'NONE', *, *, #60247, .T. ) ;
#49788=CARTESIAN_POINT ( 'NONE',  ( 8.424688440789140031, 5.350083765069828523, 7.500019236172019710 ) ) ;
#49790=AXIS2_PLACEMENT_3D ( 'NONE', #32781, #23323, #1305 ) ;
#49791=CARTESIAN_POINT ( 'NONE',  ( 8.822164158776001130, 2.644017913812000131, -7.838184857420000817 ) ) ;
#49792=ADVANCED_FACE ( 'NONE', ( #25183 ), #35686, .F. ) ;
#49799=ORIENTED_EDGE ( 'NONE', *, *, #66872, .T. ) ;
#49803=ORIENTED_EDGE ( 'NONE', *, *, #16306, .F. ) ;
#49804=CARTESIAN_POINT ( 'NONE',  ( 9.898128230592000421, 2.965931985296999862, -6.610871072364999712 ) ) ;
#49805=EDGE_LOOP ( 'NONE', ( #14031, #39242, #48980, #36682, #13949 ) ) ;
#49815=CARTESIAN_POINT ( 'NONE',  ( 10.59957028040999916, 4.438147096284001059, -8.958385582135001357 ) ) ;
#49823=EDGE_LOOP ( 'NONE', ( #58103, #64480, #38281, #33646, #15515, #45854, #63104, #25289, #30878, #19276, #22509, #1924, #16816, #53645, #55548, #49853, #25482, #48014, #45564, #9981, #45228, #21920, #40678, #18144, #43074, #37866, #7206, #52212, #3236, #30604, #47823, #59020, #43845, #2310 ) ) ;
#49825=CARTESIAN_POINT ( 'NONE',  ( 8.798539158775000146, 5.851083642416999631, -7.072167224702999633 ) ) ;
#49836=CARTESIAN_POINT ( 'NONE',  ( 7.460824085303098485, 4.353476288197968280, -6.184976426942008665 ) ) ;
#49838=CARTESIAN_POINT ( 'NONE',  ( 10.26947109217999810, 5.100000000000000533, -6.152188490330000370 ) ) ;
#49842=CARTESIAN_POINT ( 'NONE',  ( 4.149992563291998948, -0.2617923565148011500, 1.999946284944287722 ) ) ;
#49846=CARTESIAN_POINT ( 'NONE',  ( 8.266329719591000824, 4.769017407621999993, -8.862909124839001507 ) ) ;
#49850=CARTESIAN_POINT ( 'NONE',  ( 11.09999999999999964, 0.5000000000000000000, -5.124965750789000296 ) ) ;
#49852=CARTESIAN_POINT ( 'NONE',  ( 2.356882905178000254, -3.556067323659000134, 0.5081678699474000416 ) ) ;
#49853=ORIENTED_EDGE ( 'NONE', *, *, #4347, .F. ) ;
#49857=CARTESIAN_POINT ( 'NONE',  ( 9.160308886257000793, 4.122021000979000149, 9.013569734175000292 ) ) ;
#49860=CARTESIAN_POINT ( 'NONE',  ( 10.91988774271260709, 9.626587645410168648, 5.949865614865760932 ) ) ;
#49862=CARTESIAN_POINT ( 'NONE',  ( 0.5181103717477000270, 3.205765437135000173, -1.404659375816999844 ) ) ;
#49867=ORIENTED_EDGE ( 'NONE', *, *, #16333, .T. ) ;
#49873=CARTESIAN_POINT ( 'NONE',  ( 10.98768472638000127, 7.408460564924999936, -6.159405844198999169 ) ) ;
#49875=CARTESIAN_POINT ( 'NONE',  ( 8.383148997457999130, 5.167567567567999731, 6.822293592207000934 ) ) ;
#49879=ADVANCED_FACE ( 'NONE', ( #57677 ), #4881, .F. ) ;
#49881=ORIENTED_EDGE ( 'NONE', *, *, #48157, .T. ) ;
#49883=ADVANCED_FACE ( 'NONE', ( #10136 ), #23387, .F. ) ;
#49886=VECTOR ( 'NONE', #68752, 1000.000000000000000 ) ;
#49888=ORIENTED_EDGE ( 'NONE', *, *, #28497, .F. ) ;
#49891=CARTESIAN_POINT ( 'NONE',  ( 7.341922165042849890, 5.856757650166058760, -7.538504482028591802 ) ) ;
#49892=CARTESIAN_POINT ( 'NONE',  ( 5.500000000000000000, 6.217248937900999058E-14, 3.708144902247999495E-14 ) ) ;
#49899=EDGE_CURVE ( 'NONE', #34575, #34779, #18552, .T. ) ;
#49901=CARTESIAN_POINT ( 'NONE',  ( 9.784179719593000257, 4.042991257420999851, -5.768106221333000327 ) ) ;
#49902=CARTESIAN_POINT ( 'NONE',  ( 3.579027452879000037, -3.225412259932999959, 0.5737794949255000665 ) ) ;
#49905=CARTESIAN_POINT ( 'NONE',  ( 8.061825939490002924, 3.419144686567003877, -6.221559872366999144 ) ) ;
#49910=CARTESIAN_POINT ( 'NONE',  ( 10.65550720192000078, 4.237674045823999869, 9.105219676299999065 ) ) ;
#49913=CARTESIAN_POINT ( 'NONE',  ( 9.220176284132802991, 2.652345181577336231, 7.581873060868147718 ) ) ;
#49916=CARTESIAN_POINT ( 'NONE',  ( 10.51293291887318659, 2.761699336110873926, 6.264570408027259063 ) ) ;
#49920=CARTESIAN_POINT ( 'NONE',  ( 8.129977276175630152, 4.943140683036665983, -6.335257674860757859 ) ) ;
#49923=CARTESIAN_POINT ( 'NONE',  ( 10.19794834123000093, 4.262170647947000290, -8.834315641189999013 ) ) ;
#49924=ORIENTED_EDGE ( 'NONE', *, *, #16412, .T. ) ;
#49928=DIRECTION ( 'NONE',  ( 0.000000000000000000, 1.000000000000000000, 0.000000000000000000 ) ) ;
#49930=VERTEX_POINT ( 'NONE', #26444 ) ;
#49932=CARTESIAN_POINT ( 'NONE',  ( 7.358051658771000092, 4.561643343497000735, 6.153061759127000485 ) ) ;
#49936=ORIENTED_EDGE ( 'NONE', *, *, #6736, .F. ) ;
#49937=CARTESIAN_POINT ( 'NONE',  ( 9.242342830452999536, 5.206708472530999998, 8.808826521083998884 ) ) ;
#49942=CARTESIAN_POINT ( 'NONE',  ( 7.540307192462002206, 2.929979193199001575, 6.558004150875995641 ) ) ;
#49944=DIRECTION ( 'NONE',  ( -0.9999999999999992228, 2.758142135616997833E-08, 2.614631440159998134E-08 ) ) ;
#49945=CARTESIAN_POINT ( 'NONE',  ( 1.292640132541499565, -3.058252359239901796, -1.762666431298149039 ) ) ;
#49956=CARTESIAN_POINT ( 'NONE',  ( 9.003345280414000840, 2.319062457810000311, -7.919229449146000022 ) ) ;
#49960=ADVANCED_FACE ( 'NONE', ( #53355 ), #63760, .F. ) ;
#49967=CARTESIAN_POINT ( 'NONE',  ( 9.099999886593998610, 3.268496584495999908E-13, -12.39999890529996485 ) ) ;
#49972=CARTESIAN_POINT ( 'NONE',  ( 10.21160513988086294, 3.634030556546760327, -8.817876221680393201 ) ) ;
#49973=CARTESIAN_POINT ( 'NONE',  ( 6.649999999999999467, 5.221516520829000640, -8.074802043613001246 ) ) ;
#49983=CARTESIAN_POINT ( 'NONE',  ( 8.481676658773000810, 2.472348777564000066, 6.234194744024999402 ) ) ;
#49990=CARTESIAN_POINT ( 'NONE',  ( 10.60518955639999916, 5.343965917319999370, -7.731522121091999544 ) ) ;
#49994=CARTESIAN_POINT ( 'NONE',  ( 10.34021053755999908, 4.202028620710000162, 9.459600235481000041 ) ) ;
#50005=CARTESIAN_POINT ( 'NONE',  ( 8.020982780409999791, 3.245534453799999941, 8.949623695221001540 ) ) ;
#50006=CARTESIAN_POINT ( 'NONE',  ( 11.08492721656000057, 3.668390701878999849, 5.558148445539999649 ) ) ;
#50010=CARTESIAN_POINT ( 'NONE',  ( 9.196339158776000389, 4.112741311853999271, -5.603466076760000192 ) ) ;
#50020=CARTESIAN_POINT ( 'NONE',  ( 1.977794427304000013, -3.102129433205000009, 0.9990388109167002151 ) ) ;
#50027=CARTESIAN_POINT ( 'NONE',  ( 8.472537864290000442, 2.899999999999999911, -6.571291218949999902 ) ) ;
#50030=EDGE_LOOP ( 'NONE', ( #23035, #29351, #9735, #57392, #8294 ) ) ;
#50031=CARTESIAN_POINT ( 'NONE',  ( 7.594166666663750398, 5.314863113502227066, -7.146640356114973613 ) ) ;
#50033=CARTESIAN_POINT ( 'NONE',  ( 10.86068541168999957, 5.063199384101999989, 5.173500105045000019 ) ) ;
#50036=CARTESIAN_POINT ( 'NONE',  ( 0.4653817924015999918, 2.512752844666000129, -2.494243791339000094 ) ) ;
#50037=ORIENTED_EDGE ( 'NONE', *, *, #13363, .T. ) ;
#50038=CARTESIAN_POINT ( 'NONE',  ( 10.86501009699162701, 2.649983380500041008, -7.500000587580665901 ) ) ;
#50043=DIRECTION ( 'NONE',  ( 1.000000000000000000, 0.000000000000000000, 0.000000000000000000 ) ) ;
#50048=EDGE_CURVE ( 'NONE', #45049, #23998, #61952, .T. ) ;
#50049=ORIENTED_EDGE ( 'NONE', *, *, #4679, .F. ) ;
#50050=CARTESIAN_POINT ( 'NONE',  ( 7.337806197067810565, 3.730756353036506656, 9.220484948575563777 ) ) ;
#50052=EDGE_CURVE ( 'NONE', #38357, #43600, #44265, .T. ) ;
#50057=ORIENTED_EDGE ( 'NONE', *, *, #698, .F. ) ;
#50062=CARTESIAN_POINT ( 'NONE',  ( 11.09999999999999964, 4.000000000000000000, 7.500000000000000000 ) ) ;
#50066=CARTESIAN_POINT ( 'NONE',  ( 4.000000000000000888, -0.5626148410807586542, -2.094138670346520126 ) ) ;
#50070=CARTESIAN_POINT ( 'NONE',  ( 11.09999999999999964, 4.000000000000000000, -7.500000000000000000 ) ) ;
#50073=EDGE_CURVE ( 'NONE', #44936, #58927, #4144, .T. ) ;
#50079=CARTESIAN_POINT ( 'NONE',  ( 10.98768472638000127, 7.408460511344000743, 6.159405790617999976 ) ) ;
#50082=CARTESIAN_POINT ( 'NONE',  ( 7.067909439180999343, 3.037137096735000430, -6.379793420563999895 ) ) ;
#50083=CARTESIAN_POINT ( 'NONE',  ( 8.879093088636166087, 2.650571520623451249, -7.263234620901792837 ) ) ;
#50087=CARTESIAN_POINT ( 'NONE',  ( 8.880270280412998929, 4.146787477634999775, -5.941926545671999627 ) ) ;
#50089=CARTESIAN_POINT ( 'NONE',  ( 11.01430358291000111, 8.153755387268001087, -6.595354411296000308 ) ) ;
#50091=CARTESIAN_POINT ( 'NONE',  ( 8.148264992380649829, 4.679617213703884282, -8.679508107075978529 ) ) ;
#50092=DIRECTION ( 'NONE',  ( 1.000000000000000000, 0.000000000000000000, 0.000000000000000000 ) ) ;
#50096=CARTESIAN_POINT ( 'NONE',  ( 1.000973465875999890, 3.500000000000000000, 0.000000000000000000 ) ) ;
#50107=EDGE_CURVE ( 'NONE', #44936, #14966, #29720, .T. ) ;
#50113=ORIENTED_EDGE ( 'NONE', *, *, #7764, .T. ) ;
#50122=VECTOR ( 'NONE', #54572, 1000.000000000000000 ) ;
#50129=EDGE_CURVE ( 'NONE', #31174, #34088, #53080, .T. ) ;
#50132=CARTESIAN_POINT ( 'NONE',  ( 3.500000000000000000, -2.850358864693896432, 1.327510396322337138 ) ) ;
#50139=VERTEX_POINT ( 'NONE', #43280 ) ;
#50142=CARTESIAN_POINT ( 'NONE',  ( 9.500595280412998278, 2.334550724494000029, -7.977056617806000283 ) ) ;
#50147=ORIENTED_EDGE ( 'NONE', *, *, #44372, .F. ) ;
#50148=CARTESIAN_POINT ( 'NONE',  ( 5.399998535875000449, -12.99045401563999924, -1.690592933733000125 ) ) ;
#50152=CARTESIAN_POINT ( 'NONE',  ( 10.90634530628000043, 3.089682683751000081, -6.534327427410000055 ) ) ;
#50153=CYLINDRICAL_SURFACE ( 'NONE', #45439, 13.10000000000000142 ) ;
#50157=EDGE_CURVE ( 'NONE', #15157, #14563, #47733, .T. ) ;
#50165=CARTESIAN_POINT ( 'NONE',  ( 10.91307008594999850, 2.096286256021000050, 7.827189715349000210 ) ) ;
#50166=CARTESIAN_POINT ( 'NONE',  ( 10.58470471959000037, 2.966809777448999874, -8.831980808885999679 ) ) ;
#50173=B_SPLINE_CURVE_WITH_KNOTS ( 'NONE', 3,
 ( #14061, #51335, #13260, #24076, #7653, #12557, #44387, #60794, #45069, #18151, #3429, #67061 ),
 .UNSPECIFIED., .F., .F.,
 ( 4, 2, 2, 2, 2, 4 ),
 ( 0.000000000000000000, 0.2500000000000015543, 0.3750000000000009992, 0.5000000000000004441, 0.7500000000000002220, 1.000000000000000000 ),
 .UNSPECIFIED. ) ;
#50176=CARTESIAN_POINT ( 'NONE',  ( 9.734454719592999794, 3.021734963141999852, -6.070209284876999511 ) ) ;
#50190=CARTESIAN_POINT ( 'NONE',  ( 11.09999999999999787, 5.584137149005704792, 7.273593798865315208 ) ) ;
#50194=ORIENTED_EDGE ( 'NONE', *, *, #24702, .F. ) ;
#50195=CARTESIAN_POINT ( 'NONE',  ( 11.09999999999999964, 5.350000000000000533, 7.500000000000000000 ) ) ;
#50197=CARTESIAN_POINT ( 'NONE',  ( 9.500595280412998278, 2.334550724494000029, -7.977056617806000283 ) ) ;
#50203=CARTESIAN_POINT ( 'NONE',  ( 2.642974601824000125, 3.419206998487000160, 1.101304841644999977 ) ) ;
#50204=ORIENTED_EDGE ( 'NONE', *, *, #68078, .T. ) ;
#50209=ORIENTED_EDGE ( 'NONE', *, *, #67775, .T. ) ;
#50211=CARTESIAN_POINT ( 'NONE',  ( 10.92974439901735906, 9.483709363500846479, 6.097296706918701403 ) ) ;
#50213=CARTESIAN_POINT ( 'NONE',  ( 7.890669420221000152, 4.660296061153999858, 6.322498784873999078 ) ) ;
#50215=ORIENTED_EDGE ( 'NONE', *, *, #1738, .F. ) ;
#50222=ORIENTED_EDGE ( 'NONE', *, *, #12185, .F. ) ;
#50223=CARTESIAN_POINT ( 'NONE',  ( 10.98803924503897989, 7.901889936912171564, -6.474652332642743424 ) ) ;
#50224=CARTESIAN_POINT ( 'NONE',  ( 10.85685100254000091, 2.832432432432000269, -6.822293592207000934 ) ) ;
#50228=ORIENTED_EDGE ( 'NONE', *, *, #48157, .F. ) ;
#50229=CARTESIAN_POINT ( 'NONE',  ( 8.999999695565000124, -12.49999969551000056, 3.568600202703999990E-10 ) ) ;
#50231=CARTESIAN_POINT ( 'NONE',  ( 10.97763601423218027, 5.200850044898188251, 6.714742154986239164 ) ) ;
#50233=ORIENTED_EDGE ( 'NONE', *, *, #39725, .F. ) ;
#50242=ORIENTED_EDGE ( 'NONE', *, *, #25983, .T. ) ;
#50244=ORIENTED_EDGE ( 'NONE', *, *, #48695, .F. ) ;
#50245=CONICAL_SURFACE ( 'NONE', #31278, 12.37499919541000004, 0.7853980884875938484 ) ;
#50247=CARTESIAN_POINT ( 'NONE',  ( 0.1499942179679999987, -1.689975037551099124, 2.199046806507070517 ) ) ;
#50248=CARTESIAN_POINT ( 'NONE',  ( 9.345514158774999913, 5.775964236216999836, -8.174909295649001706 ) ) ;
#50249=CARTESIAN_POINT ( 'NONE',  ( 2.831737797580999860, 1.751601373051000055, 2.696006073548000259 ) ) ;
#50252=CARTESIAN_POINT ( 'NONE',  ( 8.227131012390005438, 3.380163391545999207, -6.126525137394006393 ) ) ;
#50254=ORIENTED_EDGE ( 'NONE', *, *, #47518, .F. ) ;
#50257=CARTESIAN_POINT ( 'NONE',  ( 10.75109581085999899, 2.822145500011000063, 6.655897464539000552 ) ) ;
#50268=CARTESIAN_POINT ( 'NONE',  ( 8.128093775834376089, 4.971510557325522939, -6.368084714047306250 ) ) ;
#50269=CARTESIAN_POINT ( 'NONE',  ( 11.14451084122999980, 5.035416949823999566, -8.381520599479999944 ) ) ;
#50278=CARTESIAN_POINT ( 'NONE',  ( 8.411454719592999396, 3.882020551409000042, 5.870058896428999695 ) ) ;
#50279=CIRCLE ( 'NONE', #55869, 12.99999867215000116 ) ;
#50280=CARTESIAN_POINT ( 'NONE',  ( 8.944760841233000193, 4.990139824845000405, -9.121472988377998803 ) ) ;
#50284=CARTESIAN_POINT ( 'NONE',  ( 10.78089701270000056, 5.735299658853000082, 7.801561896854000366 ) ) ;
#50289=ORIENTED_EDGE ( 'NONE', *, *, #33056, .F. ) ;
#50293=CARTESIAN_POINT ( 'NONE',  ( 1.334306799207999994, -1.762666431298145708, -3.058252359239904461 ) ) ;
#50301=B_SPLINE_CURVE_WITH_KNOTS ( 'NONE', 3,
 ( #46816, #68121, #58328, #20240, #36319, #57636 ),
 .UNSPECIFIED., .F., .F.,
 ( 4, 2, 4 ),
 ( 0.000000000000000000, 0.3041826760188173218, 0.6083653520376346435 ),
 .UNSPECIFIED. ) ;
#50307=CARTESIAN_POINT ( 'NONE',  ( 9.143660841233000269, 2.235961884443999459, -6.794506518623999902 ) ) ;
#50328=EDGE_CURVE ( 'NONE', #44831, #18982, #1105, .T. ) ;
#50330=CARTESIAN_POINT ( 'NONE',  ( 9.214142219592000416, 5.421534627450999899, 6.381126373995999579 ) ) ;
#50338=CARTESIAN_POINT ( 'NONE',  ( 11.12484647810999938, 5.434130742615000287, 5.164716346185000972 ) ) ;
#50339=CARTESIAN_POINT ( 'NONE',  ( 11.14698693981000055, 5.129806801114000336, 5.886034047559999927 ) ) ;
#50341=CARTESIAN_POINT ( 'NONE',  ( 27.64127793187000037, 2.399999999999999911, 6.571291218949999902 ) ) ;
#50346=CARTESIAN_POINT ( 'NONE',  ( 10.25888757983999966, 4.512388525173999909, 5.993701490107000929 ) ) ;
#50351=CARTESIAN_POINT ( 'NONE',  ( 9.385308886257000438, 4.135077451221000011, 9.175524215473998879 ) ) ;
#50352=CARTESIAN_POINT ( 'NONE',  ( 10.76685100253999927, 2.832432432432000269, 6.822293592207000934 ) ) ;
#50355=CARTESIAN_POINT ( 'NONE',  ( 8.649364158774000444, 3.038023536984999939, -5.861661709981000001 ) ) ;
#50365=CARTESIAN_POINT ( 'NONE',  ( 2.073158326185999822, -2.059315964850999769, -2.525946829712999886 ) ) ;
#50367=CARTESIAN_POINT ( 'NONE',  ( 0.7431103717477000048, 2.848815883361000001, -1.248255999701999963 ) ) ;
#50373=CARTESIAN_POINT ( 'NONE',  ( 7.930984150159567037, 5.149131057101222986, 6.790530764775851935 ) ) ;
#50376=CARTESIAN_POINT ( 'NONE',  ( 7.416892219589999335, 3.448180532882000104, 9.222462917385000125 ) ) ;
#50377=ADVANCED_FACE ( 'NONE', ( #26433 ), #4402, .F. ) ;
#50378=CARTESIAN_POINT ( 'NONE',  ( 11.13224000276999881, 5.320481470723000150, 4.955559672663000015 ) ) ;
#50380=CARTESIAN_POINT ( 'NONE',  ( 6.899999691988000450, -12.20988339176000004, 3.111064831549000154 ) ) ;
#50381=CARTESIAN_POINT ( 'NONE',  ( 0.6513362521023000618, 3.284885639805000146, 1.453889781857000019 ) ) ;
#50382=ORIENTED_EDGE ( 'NONE', *, *, #66834, .F. ) ;
#50383=CARTESIAN_POINT ( 'NONE',  ( 1.959306799206333105, 3.058252359239905793, -1.762666431298143488 ) ) ;
#50385=CARTESIAN_POINT ( 'NONE',  ( 10.01533268956000100, 4.946987614118000032, 8.559212393557999121 ) ) ;
#50393=CARTESIAN_POINT ( 'NONE',  ( 7.787671094692007578, 4.786296140223255335, 9.071322605277833517 ) ) ;
#50402=CARTESIAN_POINT ( 'NONE',  ( 10.61094409420999973, 5.100000000000000533, -6.571291218949999902 ) ) ;
#50403=CARTESIAN_POINT ( 'NONE',  ( 11.02286749330999882, 2.398743616553999924, 6.352468982205000891 ) ) ;
#50404=CARTESIAN_POINT ( 'NONE',  ( 10.80159548023000049, 2.805082485475999476, -8.157276499959001725 ) ) ;
#50407=EDGE_CURVE ( 'NONE', #48584, #523, #41888, .T. ) ;
#50413=CARTESIAN_POINT ( 'NONE',  ( 5.000030787343001215, 1.057581170753189248, -1.834918991542628275 ) ) ;
#50420=ORIENTED_EDGE ( 'NONE', *, *, #45065, .F. ) ;
#50422=CARTESIAN_POINT ( 'NONE',  ( 10.63445696062572310, 4.782035257973576314, -4.772905834451544926 ) ) ;
#50427=CARTESIAN_POINT ( 'NONE',  ( 0.2689139796826999773, -1.124254478562000115, 3.354249223527999924 ) ) ;
#50428=VECTOR ( 'NONE', #44503, 1000.000000000000114 ) ;
#50429=CARTESIAN_POINT ( 'NONE',  ( 10.43314899746000002, 5.167567567567999731, 6.822293592207000934 ) ) ;
#50433=PLANE ( 'NONE',  #56166 ) ;
#50436=FACE_OUTER_BOUND ( 'NONE', #51310, .T. ) ;
#50460=DIRECTION ( 'NONE',  ( -1.000000000000000000, 1.446714696031000002E-14, -6.365544662537999944E-14 ) ) ;
#50464=CARTESIAN_POINT ( 'NONE',  ( -1.222471984994595150E-05, -9.327013418423733093E-16, -2.899969545326207765 ) ) ;
#50469=CARTESIAN_POINT ( 'NONE',  ( 9.070789158774999805, 5.349936549139000519, -7.138437102151999447 ) ) ;
#50478=CARTESIAN_POINT ( 'NONE',  ( 9.450870280412999591, 2.928319778732999978, -8.861178115809998701 ) ) ;
#50483=ORIENTED_EDGE ( 'NONE', *, *, #31744, .T. ) ;
#50486=CARTESIAN_POINT ( 'NONE',  ( 9.842764158772000727, 5.798263352390999437, -8.113145944980999502 ) ) ;
#50487=ORIENTED_EDGE ( 'NONE', *, *, #68166, .F. ) ;
#50488=AXIS2_PLACEMENT_3D ( 'NONE', #58077, #52481, #47932 ) ;
#50489=CARTESIAN_POINT ( 'NONE',  ( 10.81362367151999848, 3.876947539724999725, -9.022206283674000460 ) ) ;
#50491=ORIENTED_EDGE ( 'NONE', *, *, #46396, .F. ) ;
#50499=EDGE_CURVE ( 'NONE', #12624, #58906, #41098, .T. ) ;
#50504=CARTESIAN_POINT ( 'NONE',  ( 10.97819528041000048, 5.476824759564999923, -7.128718425160999850 ) ) ;
#50514=CARTESIAN_POINT ( 'NONE',  ( 9.544414158773999901, 2.173570076733999823, -8.023168429484000441 ) ) ;
#50515=CARTESIAN_POINT ( 'NONE',  ( 9.186946766250802199, 5.739007437171039783, 7.194229541610464018 ) ) ;
#50526=AXIS2_PLACEMENT_3D ( 'NONE', #64857, #38299, #16968 ) ;
#50529=CARTESIAN_POINT ( 'NONE',  ( 8.174990947233153449, 2.650692654198087972, 7.500004443805798005 ) ) ;
#50532=CARTESIAN_POINT ( 'NONE',  ( 4.149992563291999836, 1.999946284944287722, 0.2617923565147994291 ) ) ;
#50533=ORIENTED_EDGE ( 'NONE', *, *, #46178, .F. ) ;
#50536=CARTESIAN_POINT ( 'NONE',  ( 8.713854719593998155, 5.442817578555000146, -8.106149115450000053 ) ) ;
#50537=CARTESIAN_POINT ( 'NONE',  ( 9.293536308085233344, 2.899999999999999911, 6.665341197415443730 ) ) ;
#50543=CARTESIAN_POINT ( 'NONE',  ( 2.976748247909999812, -0.7364029526790000224, -3.515900957781999736 ) ) ;
#50548=CARTESIAN_POINT ( 'NONE',  ( 8.128301658772999261, 3.117378429069999957, 8.662179062556001341 ) ) ;
#50553=CARTESIAN_POINT ( 'NONE',  ( 7.192235841229000393, 4.367071440064000498, -8.848478693904000991 ) ) ;
#50555=FACE_OUTER_BOUND ( 'NONE', #23275, .T. ) ;
#50557=CARTESIAN_POINT ( 'NONE',  ( 8.267367474942998840, 3.071849710027000135, -6.244583336620999958 ) ) ;
#50565=CARTESIAN_POINT ( 'NONE',  ( 10.92306252329737504, 9.582901050001986221, -5.997835859251378743 ) ) ;
#50566=CARTESIAN_POINT ( 'NONE',  ( 0.7431103717477000048, 2.848815883361000001, -1.248255999701999963 ) ) ;
#50570=ORIENTED_EDGE ( 'NONE', *, *, #27386, .T. ) ;
#50574=CARTESIAN_POINT ( 'NONE',  ( 6.899999691988000450, -12.99045401563999924, 1.690592933733000125 ) ) ;
#50580=CYLINDRICAL_SURFACE ( 'NONE', #38830, 1.350000000000000533 ) ;
#50581=CARTESIAN_POINT ( 'NONE',  ( 3.500000000000000000, 2.135761500787233036, 2.632305434550216816 ) ) ;
#50584=DIRECTION ( 'NONE',  ( 0.000000000000000000, 1.000000000000000000, 0.000000000000000000 ) ) ;
#50589=ORIENTED_EDGE ( 'NONE', *, *, #56712, .T. ) ;
#50591=VERTEX_POINT ( 'NONE', #44077 ) ;
#50592=AXIS2_PLACEMENT_3D ( 'NONE', #67655, #53570, #15218 ) ;
#50594=CARTESIAN_POINT ( 'NONE',  ( 8.581920280410001212, 4.769017407621999993, -8.862909124839001507 ) ) ;
#50595=CARTESIAN_POINT ( 'NONE',  ( 2.377407833194000286, 3.071536117060000404, 1.409200688889000075 ) ) ;
#50601=CARTESIAN_POINT ( 'NONE',  ( 9.724611353170001138, 2.928305163963000446, 8.718478150869000132 ) ) ;
#50605=CARTESIAN_POINT ( 'NONE',  ( 10.43579914648999996, 2.587602126999999808, 6.390037244031000263 ) ) ;
#50606=CARTESIAN_POINT ( 'NONE',  ( 10.93333333333430524, 5.319670837135273445, 7.972931767323618857 ) ) ;
#50613=DIRECTION ( 'NONE',  ( -0.7071067811864980568, 0.7071067811865969777, -1.029442514143995792E-08 ) ) ;
#50615=ORIENTED_EDGE ( 'NONE', *, *, #44458, .F. ) ;
#50622=CARTESIAN_POINT ( 'NONE',  ( 7.229676658770999964, 2.630487280353000390, 6.995957894972000268 ) ) ;
#50624=CARTESIAN_POINT ( 'NONE',  ( 9.889535841229999846, 5.798263352390999437, -8.113145944980999502 ) ) ;
#50625=CARTESIAN_POINT ( 'NONE',  ( 0.6001188040607291496, 2.874384006252894252, 2.063114442910663815 ) ) ;
#50626=CARTESIAN_POINT ( 'NONE',  ( 10.53197665877000055, 2.323713329709999886, -8.279493667389999700 ) ) ;
#50627=EDGE_LOOP ( 'NONE', ( #62983, #58459, #27736, #62843 ) ) ;
#50628=CARTESIAN_POINT ( 'NONE',  ( 10.85737917744000036, 2.754548910086000113, 8.976376585747001258 ) ) ;
#50635=CARTESIAN_POINT ( 'NONE',  ( 1.365556799207875205, -0.4581489286485082579, -3.500000000000000888 ) ) ;
#50637=VECTOR ( 'NONE', #4550, 1000.000000000000000 ) ;
#50641=ORIENTED_EDGE ( 'NONE', *, *, #59175, .T. ) ;
#50646=AXIS2_PLACEMENT_3D ( 'NONE', #20919, #32449, #37002 ) ;
#50649=CARTESIAN_POINT ( 'NONE',  ( 9.243110841233001196, 4.112741311853999271, -5.603466076760000192 ) ) ;
#50671=EDGE_CURVE ( 'NONE', #41535, #57987, #10843, .T. ) ;
#50686=CARTESIAN_POINT ( 'NONE',  ( 11.02286749330999882, 2.398743616553999924, 6.352468982205000891 ) ) ;
#50688=ORIENTED_EDGE ( 'NONE', *, *, #2544, .F. ) ;
#50692=CARTESIAN_POINT ( 'NONE',  ( 10.42596030538999941, 5.042177533603999784, 8.702224267793999601 ) ) ;
#50694=AXIS2_PLACEMENT_3D ( 'NONE', #29752, #51735, #24829 ) ;
#50697=CARTESIAN_POINT ( 'NONE',  ( 8.508079719592000600, 2.202812441249000219, 7.706988150133999405 ) ) ;
#50698=CARTESIAN_POINT ( 'NONE',  ( 9.137543006348998631, 2.995704926864999784, 8.544754656710999541 ) ) ;
#50709=CARTESIAN_POINT ( 'NONE',  ( 1.539110206209999943, 0.8784043042010000191, 3.483138632238000021 ) ) ;
#50712=CARTESIAN_POINT ( 'NONE',  ( 0.9681103717476999826, 3.205765437135000173, -1.404659375816999844 ) ) ;
#50714=B_SPLINE_CURVE_WITH_KNOTS ( 'NONE', 3,
 ( #53428, #43282, #58668, #59700 ),
 .UNSPECIFIED., .F., .F.,
 ( 4, 4 ),
 ( 0.000000000000000000, 1.000000000000000000 ),
 .UNSPECIFIED. ) ;
#50717=CARTESIAN_POINT ( 'NONE',  ( 4.900006121742000786, -0.5234957687185600728, -1.947945353336631991 ) ) ;
#50722=CARTESIAN_POINT ( 'NONE',  ( 8.689260841231000398, 2.550241116032999855, 7.666973618349000041 ) ) ;
#50727=CARTESIAN_POINT ( 'NONE',  ( 0.8372907118031999163, -0.1515593316830000370, 3.422260710200999867 ) ) ;
#50728=ORIENTED_EDGE ( 'NONE', *, *, #3932, .T. ) ;
#50731=CARTESIAN_POINT ( 'NONE',  ( 10.00122429346999908, 2.274087081648999753, 7.851326250696001097 ) ) ;
#50733=FACE_OUTER_BOUND ( 'NONE', #11683, .T. ) ;
#50738=CARTESIAN_POINT ( 'NONE',  ( 8.591260603588073863, 4.340498360229820385, 5.786730013295068531 ) ) ;
#50746=CARTESIAN_POINT ( 'NONE',  ( 4.149992563291998948, 1.229060429538529009, -1.599290730647369152 ) ) ;
#50748=CARTESIAN_POINT ( 'NONE',  ( 9.843732751558000871, 4.115124343450999866, 9.466620196856998959 ) ) ;
#50749=CARTESIAN_POINT ( 'NONE',  ( 9.858847045824999711, 2.668090821818000169, -7.206973500459000093 ) ) ;
#50760=APPLICATION_CONTEXT ( 'automotive_design' ) ;
#50771=B_SPLINE_CURVE_WITH_KNOTS ( 'NONE', 3,
 ( #61159, #34940, #66737, #13277, #61499, #34603, #51009, #24441, #55916, #18856 ),
 .UNSPECIFIED., .F., .F.,
 ( 4, 2, 2, 2, 4 ),
 ( 0.000000000000000000, 0.2499999999999996669, 0.4999999999999993339, 0.7499999999999996669, 1.000000000000000000 ),
 .UNSPECIFIED. ) ;
#50780=CARTESIAN_POINT ( 'NONE',  ( 8.854734522757450321, 2.650072343410613485, -7.676796296823138022 ) ) ;
#50782=CARTESIAN_POINT ( 'NONE',  ( 0.5073805749851999503, 3.426971461775999650, -0.8894074146212000986 ) ) ;
#50788=CARTESIAN_POINT ( 'NONE',  ( 10.83487665876999984, 5.800192368099000184, -7.920541111170000370 ) ) ;
#50794=B_SPLINE_CURVE_WITH_KNOTS ( 'NONE', 3,
 ( #56253, #12921, #67073, #8360 ),
 .UNSPECIFIED., .F., .F.,
 ( 4, 4 ),
 ( 0.000000000000000000, 1.000000000000000000 ),
 .UNSPECIFIED. ) ;
#50796=CIRCLE ( 'NONE', #48541, 1.350000000000000533 ) ;
#50808=CARTESIAN_POINT ( 'NONE',  ( 2.740556799209334038, -3.500000000000003109, 0.4581489286484972667 ) ) ;
#50812=CARTESIAN_POINT ( 'NONE',  ( 9.064883232718324635, 5.349954811645839747, -7.500006748065883855 ) ) ;
#50819=CARTESIAN_POINT ( 'NONE',  ( 8.573539158775000502, 5.361622798585000460, -7.185294144754000634 ) ) ;
#50825=CARTESIAN_POINT ( 'NONE',  ( 8.539089945104599622, 4.176610156107851246, 8.851086029037343650 ) ) ;
#50827=CARTESIAN_POINT ( 'NONE',  ( 9.251970280414001380, 5.673443217382001080, -7.051790060464000476 ) ) ;
#50833=CARTESIAN_POINT ( 'NONE',  ( 7.785267505008289568, 3.263780494496031359, -8.649333714453984356 ) ) ;
#50836=CARTESIAN_POINT ( 'NONE',  ( 8.699089158774000907, 4.178200486578000472, -5.608493638783999202 ) ) ;
#50838=CARTESIAN_POINT ( 'NONE',  ( 10.85290485628999946, 3.170386876061999537, -8.782184998573001167 ) ) ;
#50849=LINE ( 'NONE', #3625, #18051 ) ;
#50850=CARTESIAN_POINT ( 'NONE',  ( 11.10664834123000055, 5.324188120986000250, -7.809342242343999985 ) ) ;
#50861=CARTESIAN_POINT ( 'NONE',  ( 8.839404719593998649, 5.140767546012999567, -6.196177269779999719 ) ) ;
#50865=CARTESIAN_POINT ( 'NONE',  ( 3.999985533191000364, -6.914809019160056625E-16, -2.149963194831858715 ) ) ;
#50866=CARTESIAN_POINT ( 'NONE',  ( 4.900006121741999010, -2.000000000000000000, 0.000000000000000000 ) ) ;
#50870=CARTESIAN_POINT ( 'NONE',  ( 0.7431103717477000048, 2.848815883361000001, -1.248255999701999963 ) ) ;
#50872=ORIENTED_EDGE ( 'NONE', *, *, #46487, .F. ) ;
#50879=CARTESIAN_POINT ( 'NONE',  ( 8.316694475082000437, 2.898380349184999982, 6.611503672649000407 ) ) ;
#50880=CARTESIAN_POINT ( 'NONE',  ( 9.911030043039486870, 5.348901746907112731, 7.263562664566891591 ) ) ;
#50883=VECTOR ( 'NONE', #17251, 1000.000000000000000 ) ;
#50884=CYLINDRICAL_SURFACE ( 'NONE', #36699, 11.35000000000000142 ) ;
#50887=CARTESIAN_POINT ( 'NONE',  ( 3.405885792876999663, -3.196388832542000014, -1.639155108791999993 ) ) ;
#50888=ORIENTED_EDGE ( 'NONE', *, *, #47268, .F. ) ;
#50897=CARTESIAN_POINT ( 'NONE',  ( 8.286185841226000548, 2.892522941075999832, -8.352379580902999479 ) ) ;
#50899=CARTESIAN_POINT ( 'NONE',  ( 7.805634476667997035, 3.004029196385564759, 6.538900385249459823 ) ) ;
#50903=VERTEX_POINT ( 'NONE', #28956 ) ;
#50908=CARTESIAN_POINT ( 'NONE',  ( 10.92189663471096672, 9.599264226479007789, -5.980252649074441429 ) ) ;
#50911=CARTESIAN_POINT ( 'NONE',  ( 4.500000125099000492, -12.99999867215000116, 0.000000000000000000 ) ) ;
#50913=EDGE_LOOP ( 'NONE', ( #17772, #47431, #38486, #6588, #57246, #24542, #11109, #27694, #9753 ) ) ;
#50919=CARTESIAN_POINT ( 'NONE',  ( 11.00152743473872796, 5.208048404074126836, 6.643475722637898429 ) ) ;
#50920=DIRECTION ( 'NONE',  ( -1.000000000000000000, 0.000000000000000000, 0.000000000000000000 ) ) ;
#50921=ORIENTED_EDGE ( 'NONE', *, *, #5813, .F. ) ;
#50923=CARTESIAN_POINT ( 'NONE',  ( 10.93769855012999948, 2.936883479403999964, 4.920828759365000415 ) ) ;
#50924=CARTESIAN_POINT ( 'NONE',  ( 3.500000000000000444, 1.881896910667459455, 2.804129112111227062 ) ) ;
#50927=B_SPLINE_CURVE_WITH_KNOTS ( 'NONE', 3,
 ( #41850, #35589, #42208, #68401 ),
 .UNSPECIFIED., .F., .F.,
 ( 4, 4 ),
 ( 0.000000000000000000, 1.000000000000000000 ),
 .UNSPECIFIED. ) ;
#50933=CARTESIAN_POINT ( 'NONE',  ( 10.09181485429000169, 2.440912084162000006, 7.817367409531000177 ) ) ;
#50935=CONICAL_SURFACE ( 'NONE', #38654, 2.049993715513000136, 0.7853981633972997312 ) ;
#50936=CARTESIAN_POINT ( 'NONE',  ( 9.924495280410999598, 4.946705552514000459, -6.253848946732999181 ) ) ;
#50937=CARTESIAN_POINT ( 'NONE',  ( 2.893924662652000102, -0.2530398175331999844, -3.699405519438999868 ) ) ;
#50938=EDGE_CURVE ( 'NONE', #14252, #63419, #28245, .T. ) ;
#50940=CIRCLE ( 'NONE', #55381, 12.99999854704999969 ) ;
#50943=ORIENTED_EDGE ( 'NONE', *, *, #45395, .F. ) ;
#50945=CARTESIAN_POINT ( 'NONE',  ( 10.44079719460000000, 5.435719122931000236, 7.303631812894000319 ) ) ;
#50948=CARTESIAN_POINT ( 'NONE',  ( 9.600491906670001185, 5.206545077004999911, 8.585111878242999595 ) ) ;
#50957=ORIENTED_EDGE ( 'NONE', *, *, #6656, .T. ) ;
#50963=CARTESIAN_POINT ( 'NONE',  ( 7.486426658771000220, 5.321913229613000063, 8.118244847118999630 ) ) ;
#50965=CARTESIAN_POINT ( 'NONE',  ( 9.591185841232000797, 2.173570076733999823, -8.023168429484000441 ) ) ;
#50966=CARTESIAN_POINT ( 'NONE',  ( 0.6119016313204127533, 2.532497055143216880, 2.470245038604635734 ) ) ;
#50967=CARTESIAN_POINT ( 'NONE',  ( 9.964039158770999549, 3.485905350467000119, -9.275749134703000109 ) ) ;
#50969=ORIENTED_EDGE ( 'NONE', *, *, #29634, .F. ) ;
#50990=CARTESIAN_POINT ( 'NONE',  ( 11.09461754388165389, 3.670987266763324985, -9.018203014673396467 ) ) ;
#50991=CARTESIAN_POINT ( 'NONE',  ( 8.854170280414001226, 4.902869380824999901, -8.978557145469999057 ) ) ;
#50996=CARTESIAN_POINT ( 'NONE',  ( 9.170323341230000480, 5.558938731259999599, 6.272977177425000050 ) ) ;
#50998=ORIENTED_EDGE ( 'NONE', *, *, #25478, .F. ) ;
#50999=CARTESIAN_POINT ( 'NONE',  ( 7.669816860518959167, 2.954814231707052929, 8.376417257409977779 ) ) ;
#51009=CARTESIAN_POINT ( 'NONE',  ( 9.824751812578400134, 5.732824308054384588, -7.158329579245652496 ) ) ;
#51014=LINE ( 'NONE', #20222, #51192 ) ;
#51018=AXIS2_PLACEMENT_3D ( 'NONE', #27106, #5429, #52983 ) ;
#51023=CARTESIAN_POINT ( 'NONE',  ( 6.999999085428000534, -11.95749330617000084, 3.642574904853999929 ) ) ;
#51026=CARTESIAN_POINT ( 'NONE',  ( 9.352253013669001191, 2.817757427878999632, 6.388459691516000127 ) ) ;
#51032=CARTESIAN_POINT ( 'NONE',  ( 11.27765994926999937, 3.273804980682999854, 6.368305648407000419 ) ) ;
#51034=VECTOR ( 'NONE', #8919, 1000.000000000000000 ) ;
#51037=CARTESIAN_POINT ( 'NONE',  ( 7.352704719590999360, 4.773081973066999772, 8.927402469597002010 ) ) ;
#51038=CARTESIAN_POINT ( 'NONE',  ( 9.352253013669001191, 2.817757427878999632, 6.388459691516000127 ) ) ;
#51042=CARTESIAN_POINT ( 'NONE',  ( 9.942214158770999788, 3.986577607995999806, -9.280166295424001177 ) ) ;
#51050=CARTESIAN_POINT ( 'NONE',  ( 1.729838003972999916, -3.006852806188000216, -1.965371480138999871 ) ) ;
#51063=CARTESIAN_POINT ( 'NONE',  ( 7.635857780409000206, 2.466388272391000225, 6.935562100014999842 ) ) ;
#51067=CARTESIAN_POINT ( 'NONE',  ( 1.795703038681999875, -2.202566789350000054, 2.837701071685999832 ) ) ;
#51068=VERTEX_POINT ( 'NONE', #3043 ) ;
#51069=CARTESIAN_POINT ( 'NONE',  ( 1.334048900806262150, 2.473082949858750101, 2.189141735302758462 ) ) ;
#51070=CARTESIAN_POINT ( 'NONE',  ( 9.411640687504601033, 2.873222873814825995, -6.752018918871659281 ) ) ;
#51072=CARTESIAN_POINT ( 'NONE',  ( 10.64872393945999995, 2.614781729644000130, 6.717281948314999696 ) ) ;
#51079=CARTESIAN_POINT ( 'NONE',  ( 10.35685100253999913, 2.832432432432000269, -6.822293592207000934 ) ) ;
#51081=CARTESIAN_POINT ( 'NONE',  ( 7.553107481192300909, 3.493056710060427061, 5.802405665999490481 ) ) ;
#51082=ORIENTED_EDGE ( 'NONE', *, *, #19050, .F. ) ;
#51083=VECTOR ( 'NONE', #38478, 1000.000000000000000 ) ;
#51086=VERTEX_POINT ( 'NONE', #51625 ) ;
#51091=CARTESIAN_POINT ( 'NONE',  ( 9.124700695083998170, 4.778663323155000420, 8.799742559280000265 ) ) ;
#51092=CARTESIAN_POINT ( 'NONE',  ( 9.976690600124999975, 4.172224310749999887, -6.147156451669999910 ) ) ;
#51104=ADVANCED_FACE ( 'NONE', ( #41147 ), #19817, .F. ) ;
#51111=CARTESIAN_POINT ( 'NONE',  ( 11.09999999999999964, 2.649999999999999911, -7.500000000000000000 ) ) ;
#51116=DIRECTION ( 'NONE',  ( 0.000000000000000000, -0.8648648648648720183, 0.5020047465136825426 ) ) ;
#51122=CARTESIAN_POINT ( 'NONE',  ( 8.091573680993445095, 3.319738643651897636, 8.680038712423343128 ) ) ;
#51123=CIRCLE ( 'NONE', #8707, 11.84999999999999964 ) ;
#51127=CARTESIAN_POINT ( 'NONE',  ( 8.500392882431995645, 2.902640497153002652, -6.605631719337000440 ) ) ;
#51128=CARTESIAN_POINT ( 'NONE',  ( 10.98632665877000036, 3.015084670878999784, -9.064442106213000727 ) ) ;
#51132=CARTESIAN_POINT ( 'NONE',  ( 8.200000304434999165, -12.49999969551000056, 3.568585274154000017E-10 ) ) ;
#51133=VERTEX_POINT ( 'NONE', #62456 ) ;
#51134=AXIS2_PLACEMENT_3D ( 'NONE', #13585, #34219, #23715 ) ;
#51146=EDGE_CURVE ( 'NONE', #55873, #23381, #31004, .T. ) ;
#51153=CARTESIAN_POINT ( 'NONE',  ( 2.636390132542666631, -0.4581489286485235790, 3.499999999999998224 ) ) ;
#51166=CARTESIAN_POINT ( 'NONE',  ( 9.269689158774999882, 3.135494838036999798, -8.598037907310999373 ) ) ;
#51168=VERTEX_POINT ( 'NONE', #27830 ) ;
#51169=CARTESIAN_POINT ( 'NONE',  ( 4.000000000000000000, -1.878475312369306982, 1.082895748632574762 ) ) ;
#51173=CARTESIAN_POINT ( 'NONE',  ( 2.634306799210667016, 1.762666431298139713, 3.058252359239908458 ) ) ;
#51174=CARTESIAN_POINT ( 'NONE',  ( 9.699495280410998177, 5.048004622677000341, -6.120508709481000231 ) ) ;
#51175=CARTESIAN_POINT ( 'NONE',  ( 7.000000000000000000, 6.255435840762999966, 3.000000000000000000 ) ) ;
#51177=FACE_OUTER_BOUND ( 'NONE', #54805, .T. ) ;
#51179=DIRECTION ( 'NONE',  ( 1.000000000000000000, 0.000000000000000000, 0.000000000000000000 ) ) ;
#51181=CARTESIAN_POINT ( 'NONE',  ( 7.614999999996999946, 5.349999999999999645, -7.500000000000000000 ) ) ;
#51183=CARTESIAN_POINT ( 'NONE',  ( 9.079170280414000871, 4.815598936798999752, -8.835641302565999666 ) ) ;
#51185=AXIS2_PLACEMENT_3D ( 'NONE', #5147, #251, #32081 ) ;
#51186=CARTESIAN_POINT ( 'NONE',  ( 10.79839886931999970, 5.269366011605000288, -6.148705891248999578 ) ) ;
#51187=VERTEX_POINT ( 'NONE', #50866 ) ;
#51190=EDGE_CURVE ( 'NONE', #66190, #44139, #29489, .T. ) ;
#51192=VECTOR ( 'NONE', #62183, 1000.000000000000000 ) ;
#51198=CARTESIAN_POINT ( 'NONE',  ( 11.33382334123000135, 2.642405149457999869, -7.577896731332000257 ) ) ;
#51203=CARTESIAN_POINT ( 'NONE',  ( 7.842433916446627684, 5.025786930142569275, 6.559111426468311024 ) ) ;
#51206=CARTESIAN_POINT ( 'NONE',  ( 9.476970280414001024, 5.511689883260999956, -7.095113581311000672 ) ) ;
#51207=CARTESIAN_POINT ( 'NONE',  ( 9.243873111163818379, 5.510384933080038294, 8.414177276375912840 ) ) ;
#51217=CARTESIAN_POINT ( 'NONE',  ( 7.915025373318000490, 3.368995052637000054, -6.306487705577000114 ) ) ;
#51219=CARTESIAN_POINT ( 'NONE',  ( 7.949652217634350926, 4.891777316758940231, 6.381786135468885846 ) ) ;
#51223=CARTESIAN_POINT ( 'NONE',  ( 9.541460841232000334, 2.824732249080000202, -8.992748220058999209 ) ) ;
#51224=EDGE_CURVE ( 'NONE', #8893, #66228, #51123, .T. ) ;
#51227=CARTESIAN_POINT ( 'NONE',  ( 8.099999999999999645, 0.000000000000000000, 11.84999999999999964 ) ) ;
#51228=CARTESIAN_POINT ( 'NONE',  ( 11.09999999999999964, 2.649999999999999911, 7.500000000000000000 ) ) ;
#51229=CARTESIAN_POINT ( 'NONE',  ( 3.300975217870999678, 3.258359658149000193, 0.06617378549577000724 ) ) ;
#51232=DIRECTION ( 'NONE',  ( 0.000000000000000000, -0.9916377111174247139, 0.1290528957048031888 ) ) ;
#51243=CARTESIAN_POINT ( 'NONE',  ( 1.636390132540125109, -0.4581489286485235790, 3.499999999999998224 ) ) ;
#51252=CARTESIAN_POINT ( 'NONE',  ( 10.90512994902607602, 9.806150973310261421, -5.715962064497588813 ) ) ;
#51259=CARTESIAN_POINT ( 'NONE',  ( 2.053056799206542049, 2.798833948393625537, 2.150913519912209360 ) ) ;
#51264=ORIENTED_EDGE ( 'NONE', *, *, #44335, .F. ) ;
#51268=CARTESIAN_POINT ( 'NONE',  ( 10.90987533632539730, 5.099994864246352400, -5.097495378088114926 ) ) ;
#51269=AXIS2_PLACEMENT_3D ( 'NONE', #53024, #32054, #48468 ) ;
#51276=CARTESIAN_POINT ( 'NONE',  ( 10.64872393945999995, 2.614781729644000130, 6.717281948314999696 ) ) ;
#51278=CARTESIAN_POINT ( 'NONE',  ( 9.725595280412999699, 2.495531372253999791, -7.930944806125000746 ) ) ;
#51279=CARTESIAN_POINT ( 'NONE',  ( 3.271177333949000232, -3.705085452251000167, 0.1482300145088999987 ) ) ;
#51285=CARTESIAN_POINT ( 'NONE',  ( 10.71756692516999898, 3.040224182812999665, 8.808452309630000698 ) ) ;
#51288=CARTESIAN_POINT ( 'NONE',  ( 11.15982925107999968, 5.578232410510000072, 8.067793621926998782 ) ) ;
#51298=VERTEX_POINT ( 'NONE', #5707 ) ;
#51300=EDGE_CURVE ( 'NONE', #36930, #59297, #22632, .T. ) ;
#51302=CARTESIAN_POINT ( 'NONE',  ( 4.000000000000000000, 1.321078631445433471, -1.719326598155805685 ) ) ;
#51306=CARTESIAN_POINT ( 'NONE',  ( 8.641801658773999861, 2.933833973450999721, 8.496479443567000800 ) ) ;
#51309=CARTESIAN_POINT ( 'NONE',  ( 11.07691721959000120, 3.101894630379999906, -8.926552937604000704 ) ) ;
#51310=EDGE_LOOP ( 'NONE', ( #67031, #18780, #25705, #11067, #35948, #8834, #39239 ) ) ;
#51311=B_SPLINE_CURVE_WITH_KNOTS ( 'NONE', 3,
 ( #42616, #36686, #54393, #37030, #41581, #57651, #22574, #58009, #10445, #31107, #10791, #33427, #16035, #33079, #31441, #37365 ),
 .UNSPECIFIED., .F., .F.,
 ( 4, 2, 2, 2, 2, 2, 2, 4 ),
 ( 0.1254285313929423273, 0.2190720462666236046, 0.3127155611403048541, 0.4063590760139861313, 0.5000025908876674086, 0.6872896206350299630, 0.7809331355087112403, 0.8745766503823925175 ),
 .UNSPECIFIED. ) ;
#51328=ORIENTED_EDGE ( 'NONE', *, *, #17671, .T. ) ;
#51329=ADVANCED_FACE ( 'NONE', ( #39958 ), #16473, .T. ) ;
#51335=CARTESIAN_POINT ( 'NONE',  ( 8.320275434042544660, 5.099114858442474585, 6.576956779799525421 ) ) ;
#51338=CARTESIAN_POINT ( 'NONE',  ( 7.308885841229000313, 4.847807297114000491, 9.065373753110998578 ) ) ;
#51349=CARTESIAN_POINT ( 'NONE',  ( 7.000000000000000000, 7.526486366024999874, 3.526486366024999874 ) ) ;
#51355=DIRECTION ( 'NONE',  ( 0.000000000000000000, 1.000000000000000000, 0.000000000000000000 ) ) ;
#51359=DIRECTION ( 'NONE',  ( -1.000000000000000000, 0.000000000000000000, 0.000000000000000000 ) ) ;
#51361=CARTESIAN_POINT ( 'NONE',  ( 10.73506130198999919, 5.202496273738000276, -8.441412224440000500 ) ) ;
#51362=CARTESIAN_POINT ( 'NONE',  ( 8.668193840844024223, 5.051241208858799681, 6.199741807410033445 ) ) ;
#51365=ADVANCED_FACE ( 'NONE', ( #50436 ), #21090, .T. ) ;
#51366=CARTESIAN_POINT ( 'NONE',  ( 9.476372460169001144, 5.098395626600999542, 6.305536056092000408 ) ) ;
#51368=VERTEX_POINT ( 'NONE', #7967 ) ;
#51371=CARTESIAN_POINT ( 'NONE',  ( 10.48165121391000021, 4.022873529486999722, 9.090897232145000117 ) ) ;
#51373=CARTESIAN_POINT ( 'NONE',  ( 8.581920280410001212, 4.769017407621999993, -8.862909124839001507 ) ) ;
#51376=CARTESIAN_POINT ( 'NONE',  ( 7.903989158771000056, 2.095715612964000218, 8.056490963156001328 ) ) ;
#51377=CARTESIAN_POINT ( 'NONE',  ( 9.848730799670999403, 2.769737997918999994, 6.441853401936000090 ) ) ;
#51379=ORIENTED_EDGE ( 'NONE', *, *, #5592, .F. ) ;
#51380=CARTESIAN_POINT ( 'NONE',  ( 9.965360841230999966, 4.034680274230000308, -6.102912434217000026 ) ) ;
#51392=EDGE_CURVE ( 'NONE', #10760, #4735, #5179, .T. ) ;
#51393=CARTESIAN_POINT ( 'NONE',  ( 1.295927120944000199, -3.621562729233000599, -1.006310721376000084 ) ) ;
#51395=CARTESIAN_POINT ( 'NONE',  ( 8.722714158775000115, 3.892978337449999771, -8.893414073324001023 ) ) ;
#51400=CARTESIAN_POINT ( 'NONE',  ( 2.050973465875999935, 3.500000000000000000, 0.000000000000000000 ) ) ;
#51403=CARTESIAN_POINT ( 'NONE',  ( 7.507482780409000078, 3.501518846194999757, 9.055971388486000251 ) ) ;
#51407=CARTESIAN_POINT ( 'NONE',  ( 1.171064357889000096, 3.048238319583999711, -1.563029678068999839 ) ) ;
#51409=CARTESIAN_POINT ( 'NONE',  ( 1.524776698570021516, -3.302120733362293947, 0.06692889220319675481 ) ) ;
#51413=CARTESIAN_POINT ( 'NONE',  ( 10.48165121391000021, 4.022873529486999722, 9.090897232145000117 ) ) ;
#51416=CARTESIAN_POINT ( 'NONE',  ( 9.160535748954998780, 2.900115872948000106, -6.152093930328999427 ) ) ;
#51417=LINE ( 'NONE', #10825, #47622 ) ;
#51420=CARTESIAN_POINT ( 'NONE',  ( 8.196909354935570491, 5.767095180863751835, 7.402880174889286735 ) ) ;
#51425=ORIENTED_EDGE ( 'NONE', *, *, #50499, .F. ) ;
#51430=CARTESIAN_POINT ( 'NONE',  ( 10.87021720923999979, 2.226038107033000202, 7.782753921296999167 ) ) ;
#51431=CARTESIAN_POINT ( 'NONE',  ( 9.675534850247000662, 4.656736118461000551, -8.653212384786000300 ) ) ;
#51435=CARTESIAN_POINT ( 'NONE',  ( 6.899999692065000190, -12.99045401431999913, 1.690592943268000026 ) ) ;
#51437=CARTESIAN_POINT ( 'NONE',  ( 7.854823341228001077, 4.561643343497000735, 6.153061759127000485 ) ) ;
#51442=CARTESIAN_POINT ( 'NONE',  ( 10.60000000000016662, 3.353329715112616238, -4.756097560975664607 ) ) ;
#51449=ORIENTED_EDGE ( 'NONE', *, *, #22606, .T. ) ;
#51452=ORIENTED_EDGE ( 'NONE', *, *, #24999, .T. ) ;
#51456=CARTESIAN_POINT ( 'NONE',  ( 8.409459851179015288, 2.941725506722952854, 6.357402555654233289 ) ) ;
#51457=CARTESIAN_POINT ( 'NONE',  ( 9.520528907821001141, 2.899999999999999911, 6.152188490330000370 ) ) ;
#51458=CARTESIAN_POINT ( 'NONE',  ( -0.1370230224197999946, -1.720643726402999896, -3.153834707638000001 ) ) ;
#51459=DIRECTION ( 'NONE',  ( -1.000000000000000000, 0.000000000000000000, 0.000000000000000000 ) ) ;
#51465=CARTESIAN_POINT ( 'NONE',  ( 10.56983915876999980, 2.152856944368999770, -7.425100664021000441 ) ) ;
#51470=ORIENTED_EDGE ( 'NONE', *, *, #17941, .T. ) ;
#51480=ORIENTED_EDGE ( 'NONE', *, *, #53493, .F. ) ;
#51482=FACE_OUTER_BOUND ( 'NONE', #57890, .T. ) ;
#51487=DIRECTION ( 'NONE',  ( -0.6684585169941805738, -0.6684585169941805738, -0.3260773253629903334 ) ) ;
#51496=CARTESIAN_POINT ( 'NONE',  ( 3.030140132544667519, 3.408904368339106483, -0.9161175952574748260 ) ) ;
#51497=CARTESIAN_POINT ( 'NONE',  ( 9.807804719590000886, 3.988943694240999704, -8.966360307350999648 ) ) ;
#51499=ORIENTED_EDGE ( 'NONE', *, *, #3726, .T. ) ;
#51504=CARTESIAN_POINT ( 'NONE',  ( 2.592640132543833520, 3.058252359239899132, 1.762666431298155034 ) ) ;
#51505=CARTESIAN_POINT ( 'NONE',  ( 8.447510841229000533, 4.933589693325000525, -9.154576215408999573 ) ) ;
#51506=CARTESIAN_POINT ( 'NONE',  ( 9.934999999999998721, 4.640430492595999823, -9.117542781427999898 ) ) ;
#51511=CARTESIAN_POINT ( 'NONE',  ( 8.817462135714999150, 5.100000000000000533, 6.571291218949999902 ) ) ;
#51513=CARTESIAN_POINT ( 'NONE',  ( 10.03280471959000231, 3.987760651117999711, -9.123263301387000368 ) ) ;
#51514=VERTEX_POINT ( 'NONE', #57921 ) ;
#51515=CARTESIAN_POINT ( 'NONE',  ( 10.55068356942999941, 2.412177153420000053, -6.919581319869999803 ) ) ;
#51517=ORIENTED_EDGE ( 'NONE', *, *, #28841, .T. ) ;
#51530=CARTESIAN_POINT ( 'NONE',  ( 7.174999999999994493, 4.000000000000000000, 8.979903810567671840 ) ) ;
#51535=VECTOR ( 'NONE', #27018, 1000.000000000000000 ) ;
#51537=ORIENTED_EDGE ( 'NONE', *, *, #29143, .T. ) ;
#51539=CARTESIAN_POINT ( 'NONE',  ( 9.974220280410998285, 5.496789211521000418, -7.043125396300999874 ) ) ;
#51540=CARTESIAN_POINT ( 'NONE',  ( 5.966666563597951445, 12.43894384121852248, 2.828928431917153485 ) ) ;
#51546=CARTESIAN_POINT ( 'NONE',  ( 7.810832536737804865, 4.190757782081667493, 6.135062409754994839 ) ) ;
#51552=CARTESIAN_POINT ( 'NONE',  ( 7.954939691786412581, 5.004658466033554021, 6.485426177601712361 ) ) ;
#51559=ADVANCED_FACE ( 'NONE', ( #36944 ), #16638, .F. ) ;
#51560=CARTESIAN_POINT ( 'NONE',  ( 0.2813751657999145617, 0.8596862427041435106, 3.195618825391118190 ) ) ;
#51561=CARTESIAN_POINT ( 'NONE',  ( 3.205611318989000313, 1.247253500342999866, -3.010921006634000197 ) ) ;
#51568=CARTESIAN_POINT ( 'NONE',  ( 7.614801658771000348, 3.326263523254000098, 8.794511546544999447 ) ) ;
#51571=DIRECTION ( 'NONE',  ( 1.000000000000000000, 0.000000000000000000, 0.000000000000000000 ) ) ;
#51572=B_SPLINE_CURVE_WITH_KNOTS ( 'NONE', 3,
 ( #51079, #19254, #15042, #57681 ),
 .UNSPECIFIED., .F., .F.,
 ( 4, 4 ),
 ( 0.000000000000000000, 1.000000000000000000 ),
 .UNSPECIFIED. ) ;
#51574=CARTESIAN_POINT ( 'NONE',  ( 0.5839156351703003178, 1.786861044915114549, 3.043887924358878561 ) ) ;
#51587=CARTESIAN_POINT ( 'NONE',  ( 10.90000668870999867, 0.2999999999999999889, -9.776630298829998011 ) ) ;
#51588=CARTESIAN_POINT ( 'NONE',  ( 7.482204719588999353, 2.733910551100999786, -6.580132171107999639 ) ) ;
#51591=ORIENTED_EDGE ( 'NONE', *, *, #53434, .F. ) ;
#51594=FACE_BOUND ( 'NONE', #26032, .T. ) ;
#51596=CARTESIAN_POINT ( 'NONE',  ( 10.90000000011000125, 2.899999999889000257, -6.571291220762999430 ) ) ;
#51597=B_SPLINE_CURVE_WITH_KNOTS ( 'NONE', 3,
 ( #47205, #54415, #4535, #8247 ),
 .UNSPECIFIED., .F., .F.,
 ( 4, 4 ),
 ( 0.000000000000000000, 0.1253746098019370980 ),
 .UNSPECIFIED. ) ;
#51599=CARTESIAN_POINT ( 'NONE',  ( 10.75765839980110528, 5.312263182874568557, 8.656084424456086168 ) ) ;
#51602=CARTESIAN_POINT ( 'NONE',  ( 3.042640132543832809, 3.058252359239899132, 1.762666431298154146 ) ) ;
#51610=ORIENTED_EDGE ( 'NONE', *, *, #53455, .T. ) ;
#51611=CARTESIAN_POINT ( 'NONE',  ( 10.34947814066000049, 4.457562099971999814, 6.154877938302999674 ) ) ;
#51612=B_SPLINE_CURVE_WITH_KNOTS ( 'NONE', 3,
 ( #44841, #65095, #12326, #66147 ),
 .UNSPECIFIED., .F., .F.,
 ( 4, 4 ),
 ( 0.000000000000000000, 1.000000000000000000 ),
 .UNSPECIFIED. ) ;
#51614=CARTESIAN_POINT ( 'NONE',  ( 8.839404719593998649, 5.140767546012999567, -6.196177269779999719 ) ) ;
#51615=CARTESIAN_POINT ( 'NONE',  ( 2.509915357491000254, 2.041422993037000033, 2.896642013889999756 ) ) ;
#51621=B_SPLINE_CURVE_WITH_KNOTS ( 'NONE', 3,
 ( #11133, #9750, #68131, #20249 ),
 .UNSPECIFIED., .F., .F.,
 ( 4, 4 ),
 ( 0.000000000000000000, 1.000000000000000000 ),
 .UNSPECIFIED. ) ;
#51624=EDGE_CURVE ( 'NONE', #50591, #52043, #27732, .T. ) ;
#51625=CARTESIAN_POINT ( 'NONE',  ( 10.90000154029999990, -11.35000000000000142, 0.000000000000000000 ) ) ;
#51626=CARTESIAN_POINT ( 'NONE',  ( 9.476372460169001144, 5.098395626600999542, 6.305536056092000408 ) ) ;
#51630=FACE_OUTER_BOUND ( 'NONE', #1115, .T. ) ;
#51640=CARTESIAN_POINT ( 'NONE',  ( 8.654403730149667240, 2.899999999999999911, 6.499666959930667787 ) ) ;
#51644=CARTESIAN_POINT ( 'NONE',  ( 0.1976626962874999949, 2.474918916286999782, -2.043501580946999852 ) ) ;
#51646=CARTESIAN_POINT ( 'NONE',  ( 10.09249221959000131, 2.841614569232000065, -8.724659027040001291 ) ) ;
#51654=ORIENTED_EDGE ( 'NONE', *, *, #65124, .F. ) ;
#51656=CARTESIAN_POINT ( 'NONE',  ( 7.865239158766999417, 5.556101987819999977, -8.589999141415001205 ) ) ;
#51662=CARTESIAN_POINT ( 'NONE',  ( 2.803056799209541872, -2.798833948393629978, -2.150913519912204031 ) ) ;
#51666=ORIENTED_EDGE ( 'NONE', *, *, #2690, .F. ) ;
#51673=CARTESIAN_POINT ( 'NONE',  ( 7.822385841228999048, 4.636729845879000500, 9.378977473003999421 ) ) ;
#51683=CARTESIAN_POINT ( 'NONE',  ( 10.84254308255000154, 9.576923094808998727, -6.615458963921999391 ) ) ;
#51690=CARTESIAN_POINT ( 'NONE',  ( 10.12947109217999930, 5.100000000000000533, 6.152188490330000370 ) ) ;
#51692=EDGE_LOOP ( 'NONE', ( #30145, #13962, #33597, #7648 ) ) ;
#51693=EDGE_LOOP ( 'NONE', ( #20603, #392, #4629, #55896, #60881, #13853, #16352, #55800, #48832, #50057, #66691, #8383, #1835 ) ) ;
#51698=CARTESIAN_POINT ( 'NONE',  ( 10.94349541711000029, 3.081616890687000065, -8.919380927961000793 ) ) ;
#51699=DIRECTION ( 'NONE',  ( 0.000000000000000000, 1.000000000000000000, 0.000000000000000000 ) ) ;
#51702=CARTESIAN_POINT ( 'NONE',  ( 10.87021720923999979, 2.226038107033000202, 7.782753921296999167 ) ) ;
#51708=CARTESIAN_POINT ( 'NONE',  ( 9.479214860607999782, 4.071727169861000029, 9.089299483126000112 ) ) ;
#51711=CARTESIAN_POINT ( 'NONE',  ( 9.219485841232998524, 3.892978337449999771, -8.893414073324001023 ) ) ;
#51713=PRODUCT ( 'Negative Post', 'Negative Post', '', ( #68327 ) ) ;
#51717=CARTESIAN_POINT ( 'NONE',  ( 8.160739158772001289, 5.944584532500000407, 7.106843289410999631 ) ) ;
#51718=CARTESIAN_POINT ( 'NONE',  ( 9.786671076420999427, 2.381202181614999525, 7.612749448318000489 ) ) ;
#51720=ORIENTED_EDGE ( 'NONE', *, *, #17671, .F. ) ;
#51721=CARTESIAN_POINT ( 'NONE',  ( 9.775320280412000074, 2.527713920559999661, -6.969421869128999525 ) ) ;
#51729=CARTESIAN_POINT ( 'NONE',  ( 1.920565801736000111, 3.542864650996000453, -0.5932612529451999350 ) ) ;
#51731=CIRCLE ( 'NONE', #59518, 13.10000000000000320 ) ;
#51732=CARTESIAN_POINT ( 'NONE',  ( 8.772439158776000667, 3.098073081301000009, -8.567513114264999174 ) ) ;
#51735=DIRECTION ( 'NONE',  ( 1.000000000000000000, 0.000000000000000000, 0.000000000000000000 ) ) ;
#51741=CARTESIAN_POINT ( 'NONE',  ( 8.406107780410998487, 5.342170561818999630, 8.432311822615000452 ) ) ;
#51744=CARTESIAN_POINT ( 'NONE',  ( 10.90760155002999987, 5.030021895791999320, 4.934359348414000479 ) ) ;
#51747=CARTESIAN_POINT ( 'NONE',  ( 1.457156054533999878, -3.424908732075000017, 0.06941761548046999908 ) ) ;
#51748=EDGE_LOOP ( 'NONE', ( #52680, #54973, #13845, #41717, #6164 ) ) ;
#51749=CARTESIAN_POINT ( 'NONE',  ( 1.000275254720587315, -3.126551503801492604, 1.064497837873157327 ) ) ;
#51752=CARTESIAN_POINT ( 'NONE',  ( 10.16829701902000060, 4.567214950372999738, 5.832525041908999341 ) ) ;
#51755=CARTESIAN_POINT ( 'NONE',  ( 9.817462135711998883, 5.100000000000000533, 6.571291218949999902 ) ) ;
#51758=CARTESIAN_POINT ( 'NONE',  ( 7.739871862179882989, 5.559621021845134514, 8.354610903474103623 ) ) ;
#51766=VERTEX_POINT ( 'NONE', #36166 ) ;
#51767=CARTESIAN_POINT ( 'NONE',  ( 8.428055354833562163, 3.943840852781273387, 6.010070386527693209 ) ) ;
#51769=CARTESIAN_POINT ( 'NONE',  ( 10.65550720192000078, 4.237674045823999869, 9.105219676299999065 ) ) ;
#51770=DIRECTION ( 'NONE',  ( -0.9999999999999987788, 4.835295647719984237E-08, -1.472971858110998225E-08 ) ) ;
#51778=EDGE_CURVE ( 'NONE', #13432, #59076, #60166, .T. ) ;
#51779=ORIENTED_EDGE ( 'NONE', *, *, #33486, .T. ) ;
#51785=CARTESIAN_POINT ( 'NONE',  ( 11.88093429839001658, 9.756630077891992769, 5.709945283618997003 ) ) ;
#51803=CARTESIAN_POINT ( 'NONE',  ( 9.860260465798509344, 4.592567190355682172, -8.996616293939812437 ) ) ;
#51806=CARTESIAN_POINT ( 'NONE',  ( 10.20000030442999872, -12.49999969551000056, 3.568610900609000272E-10 ) ) ;
#51817=DIRECTION ( 'NONE',  ( -0.9999999999999613642, 3.249250440393876213E-08, 2.763724548567895895E-07 ) ) ;
#51819=ORIENTED_EDGE ( 'NONE', *, *, #44078, .F. ) ;
#51822=DIRECTION ( 'NONE',  ( 0.7071068207016518725, 0.000000000000000000, -0.7071067416714409415 ) ) ;
#51826=VECTOR ( 'NONE', #47117, 1000.000000000000114 ) ;
#51828=EDGE_CURVE ( 'NONE', #23381, #49108, #3316, .T. ) ;
#51838=CARTESIAN_POINT ( 'NONE',  ( 2.404534975661500429, 1.236092914997090064, -3.291825510064177784 ) ) ;
#51839=CARTESIAN_POINT ( 'NONE',  ( 8.921614158776000281, 3.251172436837000301, -6.320036569851000152 ) ) ;
#51841=EDGE_LOOP ( 'NONE', ( #17274, #12631, #18299, #20799 ) ) ;
#51848=CARTESIAN_POINT ( 'NONE',  ( 9.865041550948095761, 2.650034642413356512, -7.500002425457249267 ) ) ;
#51852=ORIENTED_EDGE ( 'NONE', *, *, #61507, .F. ) ;
#51854=CARTESIAN_POINT ( 'NONE',  ( 9.833904719592002408, 5.048004622677000341, -6.120508709481000231 ) ) ;
#51858=CARTESIAN_POINT ( 'NONE',  ( 10.44486820642000069, 4.964088085664999817, -9.083609801695999408 ) ) ;
#51865=CARTESIAN_POINT ( 'NONE',  ( 9.817462135711998883, 5.100000000000000533, 6.571291218949999902 ) ) ;
#51866=EDGE_LOOP ( 'NONE', ( #21301, #24731, #42899, #29910 ) ) ;
#51868=CARTESIAN_POINT ( 'NONE',  ( 10.38726084123000071, 2.888676266723000374, -6.716337836090000124 ) ) ;
#51871=DIRECTION ( 'NONE',  ( -1.000000000000000000, 0.000000000000000000, -4.629487027253999916E-14 ) ) ;
#51872=ADVANCED_FACE ( 'NONE', ( #46322 ), #46667, .T. ) ;
#51877=ORIENTED_EDGE ( 'NONE', *, *, #60224, .F. ) ;
#51878=CARTESIAN_POINT ( 'NONE',  ( 10.01508584123000034, 4.845406482350000488, -6.387189183984999907 ) ) ;
#51882=CARTESIAN_POINT ( 'NONE',  ( 9.099999999999999645, 0.000000000000000000, 0.000000000000000000 ) ) ;
#51886=CARTESIAN_POINT ( 'NONE',  ( 8.802452061267722172, 4.497572718073743481, 9.205822469557245924 ) ) ;
#51887=FACE_OUTER_BOUND ( 'NONE', #18703, .T. ) ;
#51889=B_SPLINE_CURVE_WITH_KNOTS ( 'NONE', 3,
 ( #59540, #42432, #47337, #63743, #27047, #68643, #37524, #63399, #121, #15853 ),
 .UNSPECIFIED., .F., .F.,
 ( 4, 2, 2, 2, 4 ),
 ( 0.4999999999999994449, 0.6249999999999995559, 0.7499999999999997780, 0.8749999999999998890, 1.000000000000000000 ),
 .UNSPECIFIED. ) ;
#51891=CARTESIAN_POINT ( 'NONE',  ( 11.09999999999999964, 2.700000000000000178, 5.160242713806000303 ) ) ;
#51893=CARTESIAN_POINT ( 'NONE',  ( 7.909880988579637950, 4.709301544937013695, 6.316488363215514212 ) ) ;
#51896=CARTESIAN_POINT ( 'NONE',  ( 9.640910841231999484, 2.212639797530000063, -6.855876382544999537 ) ) ;
#51898=CARTESIAN_POINT ( 'NONE',  ( 7.980579959020838388, 3.019615321986244716, -6.448822506946575217 ) ) ;
#51900=B_SPLINE_SURFACE_WITH_KNOTS ( 'NONE', 3, 3, ( 
 ( #4488, #47158, #57990, #30397, #19899, #21269, #20929, #31425, #42598, #52741, #63569, #3802, #15681, #37015, #63910, #46471, #62536, #54463, #16703, #38380, #43638, #54809, #49561, #58674, #1672, #32119, #6563, #38731, #22989, #17048, #53435, #27551, #6908, #38031, #16363 ),
 ( #289, #49215, #64934, #59706, #22640, #21949, #27906, #37693, #5531, #5871, #28243, #33495, #54114, #44338, #65635, #1323, #987, #21608, #33148, #59022, #43984, #17762, #65290, #22298, #17407, #10773, #26871, #60059, #48880, #640, #11125, #32457, #64249, #48187, #43289 ),
 ( #11807, #12164, #53774, #42941, #27209, #48534, #64594, #59358, #11459, #32800, #6213, #50601, #2023, #28954, #13554, #40120, #60742, #66324, #8635, #2703, #23341, #44685, #45362, #34187, #55503, #60403, #49910, #51285, #29642, #7951, #19121, #18446, #3041, #39080, #7605 ),
 ( #29984, #67349, #34871, #39772, #18792, #24028, #35218, #3381, #12507, #24717, #33840, #56189, #40445, #46042, #66670, #55154, #29290, #56531, #61090, #65977, #61770, #7259, #28599, #61434, #50945, #12857, #8296, #45703, #18104, #50257, #13891, #24374, #13211, #2362, #67012 ) ),
 .UNSPECIFIED., .F., .F., .F.,
 ( 4, 4 ),
 ( 4, 1, 1, 1, 1, 1, 1, 1, 1, 1, 1, 1, 1, 1, 1, 1, 1, 1, 1, 1, 1, 1, 1, 1, 1, 1, 1, 1, 1, 1, 1, 1, 4 ),
 ( -0.1039370721279000015, 1.103937072127999963 ),
 ( -0.01933701211302999920, 0.01208563257065999909, 0.04350827725433999843, 0.07493092193802000645, 0.1063535666217000075, 0.1377762113054000204, 0.1691988559891000055, 0.2006215006727000150, 0.2320441453564000001, 0.2634667900400999851, 0.2948894347238000258, 0.3263120794074999553, 0.3577347240911999959, 0.3891573687748000054, 0.4205800134584999905, 0.4520026581421999756, 0.4834253028259000162, 0.5148479475096000568, 0.5462705921932000663, 0.5776932368768999959, 0.6091158815606000365, 0.6405385262443000771, 0.6719611709280000067, 0.7033838156117000473, 0.7348064602953000568, 0.7662291049789999864, 0.7976517496627000270, 0.8290743943464000676, 0.8604970390300999972, 0.8919196837138000378, 0.9233423283974000473, 0.9547649730810999769, 0.9861876177648000175 ),
 .UNSPECIFIED. ) ;
#51901=CARTESIAN_POINT ( 'NONE',  ( 0.2153359931920000025, 3.215315751876999695, 1.126573897625000029E-09 ) ) ;
#51903=ORIENTED_EDGE ( 'NONE', *, *, #20743, .F. ) ;
#51910=CARTESIAN_POINT ( 'NONE',  ( 3.500000000000000000, -1.789730407083999886, 2.652709005895000249 ) ) ;
#51915=CARTESIAN_POINT ( 'NONE',  ( 0.6466687473056148550, -0.8995628260960769618, 3.414327399381721584 ) ) ;
#51916=CARTESIAN_POINT ( 'NONE',  ( 10.90000000164000049, 5.100000000007000267, 5.160242739040000082 ) ) ;
#51921=ORIENTED_EDGE ( 'NONE', *, *, #2157, .T. ) ;
#51926=VERTEX_POINT ( 'NONE', #24218 ) ;
#51928=DIRECTION ( 'NONE',  ( 1.000000000000000000, 0.000000000000000000, 0.000000000000000000 ) ) ;
#51929=CARTESIAN_POINT ( 'NONE',  ( 8.020320280406000535, 2.268410489563000176, -7.553872882963998947 ) ) ;
#51936=ORIENTED_EDGE ( 'NONE', *, *, #35845, .T. ) ;
#51939=ORIENTED_EDGE ( 'NONE', *, *, #56908, .F. ) ;
#51940=CARTESIAN_POINT ( 'NONE',  ( 10.76566879297876511, 5.188023026155113016, 8.781755977163156146 ) ) ;
#51947=ORIENTED_EDGE ( 'NONE', *, *, #11044, .T. ) ;
#51950=CARTESIAN_POINT ( 'NONE',  ( 9.681187238460999822, 2.612249048987000055, 7.804677627401999551 ) ) ;
#51952=FACE_OUTER_BOUND ( 'NONE', #18863, .T. ) ;
#51953=CARTESIAN_POINT ( 'NONE',  ( 2.356219824740000135, 1.924171680976999976, -2.845918095194999609 ) ) ;
#51964=CARTESIAN_POINT ( 'NONE',  ( 11.02286749330999882, 2.398743616553999924, 6.352468982205000891 ) ) ;
#51965=DIRECTION ( 'NONE',  ( 1.000000000000000000, 0.000000000000000000, 0.000000000000000000 ) ) ;
#51973=CARTESIAN_POINT ( 'NONE',  ( 0.3288139673412197039, 2.029848442696892796, -2.674009039041026270 ) ) ;
#51979=CARTESIAN_POINT ( 'NONE',  ( 0.1648568235610000099, -2.003871238023999801, -2.529037764236000019 ) ) ;
#51981=CARTESIAN_POINT ( 'NONE',  ( 10.82674528040999995, 3.167160000746000126, -6.225151413000000744 ) ) ;
#51988=CARTESIAN_POINT ( 'NONE',  ( 7.911791375976998886, 3.505433841991000499, 6.324291089890995643 ) ) ;
#51993=CARTESIAN_POINT ( 'NONE',  ( 7.666339158767000228, 3.406663518590999917, -5.695144508491999602 ) ) ;
#52004=FACE_OUTER_BOUND ( 'NONE', #16408, .T. ) ;
#52005=CARTESIAN_POINT ( 'NONE',  ( 8.696135841231001251, 3.038023536984999939, -5.861661709981000001 ) ) ;
#52010=CARTESIAN_POINT ( 'NONE',  ( 7.603420280409000753, 5.687206835507000235, 6.847268999608999707 ) ) ;
#52028=CARTESIAN_POINT ( 'NONE',  ( 9.356851002546999752, 2.832432432432000269, -6.822293592207000934 ) ) ;
#52032=DIRECTION ( 'NONE',  ( 0.000000000000000000, -0.1218274111675001214, 0.9925512993736016476 ) ) ;
#52034=CARTESIAN_POINT ( 'NONE',  ( 10.89218604104999955, 2.661903984162000469, -8.236033286991000679 ) ) ;
#52035=CARTESIAN_POINT ( 'NONE',  ( 8.695634021592812957, 5.082571230934349593, 6.279975830437711792 ) ) ;
#52039=CARTESIAN_POINT ( 'NONE',  ( 9.199602729599000384, 2.551394566582000145, 7.536605852160000119 ) ) ;
#52043=VERTEX_POINT ( 'NONE', #57745 ) ;
#52046=CARTESIAN_POINT ( 'NONE',  ( 10.39106065309000115, 4.025321035224999733, 9.261125884460000179 ) ) ;
#52049=CARTESIAN_POINT ( 'NONE',  ( 10.96245927184000024, 7.417218077776000840, -6.111351059656000118 ) ) ;
#52051=CARTESIAN_POINT ( 'NONE',  ( 10.96233853605644093, 4.057274665987934625, -9.264935003284213266 ) ) ;
#52054=CARTESIAN_POINT ( 'NONE',  ( 10.96580581817999978, 4.930645553951000792, 6.170542400361000546 ) ) ;
#52056=ORIENTED_EDGE ( 'NONE', *, *, #11389, .F. ) ;
#52057=CARTESIAN_POINT ( 'NONE',  ( 8.979720280412999855, 5.524776413195999325, -7.147585171405999915 ) ) ;
#52061=CARTESIAN_POINT ( 'NONE',  ( 10.91079984269360637, 5.053022793955669556, 4.907707240338313071 ) ) ;
#52066=CARTESIAN_POINT ( 'NONE',  ( 1.725064665911000050, -3.060375075103999976, 2.182311086106999642 ) ) ;
#52067=CARTESIAN_POINT ( 'NONE',  ( 7.330281674562000305, 4.426928431836000044, 9.293321981113999541 ) ) ;
#52069=CARTESIAN_POINT ( 'NONE',  ( 9.629471092178999214, 5.100000000000000533, 6.152188490330000370 ) ) ;
#52072=ORIENTED_EDGE ( 'NONE', *, *, #28097, .F. ) ;
#52078=VERTEX_POINT ( 'NONE', #15790 ) ;
#52079=CARTESIAN_POINT ( 'NONE',  ( 8.481676658773000810, 2.472348777564000066, 6.234194744024999402 ) ) ;
#52086=CARTESIAN_POINT ( 'NONE',  ( 0.9755632220631000884, -1.955279592509000075, 2.607329530612999768 ) ) ;
#52087=ORIENTED_EDGE ( 'NONE', *, *, #40963, .T. ) ;
#52088=CARTESIAN_POINT ( 'NONE',  ( 1.715504496333042583, 2.382347238673330203, -2.287553813110801748 ) ) ;
#52090=CARTESIAN_POINT ( 'NONE',  ( 10.21609109105999913, 5.961715741921000067, 7.319666990313999477 ) ) ;
#52091=CARTESIAN_POINT ( 'NONE',  ( 10.14750576281000072, 2.602962605360999770, 6.738577830910999822 ) ) ;
#52095=FACE_OUTER_BOUND ( 'NONE', #61136, .T. ) ;
#52098=VECTOR ( 'NONE', #29952, 1000.000000000000000 ) ;
#52109=CARTESIAN_POINT ( 'NONE',  ( 9.724611353170001138, 2.928305163963000446, 8.718478150869000132 ) ) ;
#52110=CARTESIAN_POINT ( 'NONE',  ( 10.49937419337999955, 2.985313722448000195, -6.358656051156999389 ) ) ;
#52114=CARTESIAN_POINT ( 'NONE',  ( 9.061840824070779732, 4.635339463665918203, 8.712817598784141637 ) ) ;
#52122=CARTESIAN_POINT ( 'NONE',  ( 8.524970964081628466, 2.900000000000001688, -6.445556248366430374 ) ) ;
#52123=CARTESIAN_POINT ( 'NONE',  ( 7.254703680423997270, 9.104289213269002090, 5.358377883862995184 ) ) ;
#52128=ADVANCED_FACE ( 'NONE', ( #63325 ), #31200, .T. ) ;
#52135=DIRECTION ( 'NONE',  ( 0.000000000000000000, 1.000000000000000000, 0.000000000000000000 ) ) ;
#52137=CARTESIAN_POINT ( 'NONE',  ( 9.332537864288001472, 2.899999999999999911, 6.571291218949999902 ) ) ;
#52138=CARTESIAN_POINT ( 'NONE',  ( 0.6062974075931000240, 0.9423624982842000453, -3.239329654985999785 ) ) ;
#52143=LINE ( 'NONE', #62300, #32503 ) ;
#52145=CARTESIAN_POINT ( 'NONE',  ( 11.11477971959000044, 2.548217283716999848, -8.356742414746999970 ) ) ;
#52149=CARTESIAN_POINT ( 'NONE',  ( 8.819055905797000605, 2.899999999999999911, -6.571291218949999902 ) ) ;
#52168=VECTOR ( 'NONE', #17428, 1000.000000000000000 ) ;
#52169=ADVANCED_FACE ( 'NONE', ( #68925 ), #45543, .F. ) ;
#52173=CARTESIAN_POINT ( 'NONE',  ( 2.573890132542666187, 2.150913519912194705, 2.798833948393636639 ) ) ;
#52183=CARTESIAN_POINT ( 'NONE',  ( 2.967640132544666631, 1.762666431298152148, -3.058252359239900908 ) ) ;
#52185=CARTESIAN_POINT ( 'NONE',  ( 8.912754719595000097, 2.481540185810000132, -7.878707153279001396 ) ) ;
#52190=ORIENTED_EDGE ( 'NONE', *, *, #66523, .T. ) ;
#52192=CARTESIAN_POINT ( 'NONE',  ( 8.632946129846658323, 2.796778970782894724, 8.203843119991381272 ) ) ;
#52194=CARTESIAN_POINT ( 'NONE',  ( 4.149992563292001613, -0.5234817089163702475, -1.947893036340041517 ) ) ;
#52196=CARTESIAN_POINT ( 'NONE',  ( 0.2500098862125000321, 0.000000000000000000, 0.000000000000000000 ) ) ;
#52201=CARTESIAN_POINT ( 'NONE',  ( 9.427245280414000561, 4.989193221215000307, -6.287302145481000082 ) ) ;
#52204=CARTESIAN_POINT ( 'NONE',  ( 9.792312867577999569, 4.284154069364999984, -9.000485152170000447 ) ) ;
#52212=ORIENTED_EDGE ( 'NONE', *, *, #40024, .T. ) ;
#52214=DIRECTION ( 'NONE',  ( 0.000000000000000000, -0.8897496663235402448, 0.4564488265700210046 ) ) ;
#52217=CYLINDRICAL_SURFACE ( 'NONE', #49486, 1.350000000000000533 ) ;
#52225=CARTESIAN_POINT ( 'NONE',  ( 9.269210841233000764, 3.098073081301000009, -8.567513114264999174 ) ) ;
#52226=CARTESIAN_POINT ( 'NONE',  ( 10.58728840301827923, 2.899999999999999911, -6.305985889763610963 ) ) ;
#52232=CARTESIAN_POINT ( 'NONE',  ( 2.210247277619000084, 2.108360286353999413, -2.286637680308000409 ) ) ;
#52239=B_SPLINE_CURVE_WITH_KNOTS ( 'NONE', 3,
 ( #38727, #28594, #55149, #27902 ),
 .UNSPECIFIED., .F., .F.,
 ( 4, 4 ),
 ( 0.000000000000000000, 1.000000000000000000 ),
 .UNSPECIFIED. ) ;
#52240=CARTESIAN_POINT ( 'NONE',  ( 4.900006121741999010, 2.000000000000000000, 0.000000000000000000 ) ) ;
#52242=CARTESIAN_POINT ( 'NONE',  ( 10.01721296880961631, 5.205658458020796964, 8.206277775804023733 ) ) ;
#52244=EDGE_CURVE ( 'NONE', #62424, #24059, #65226, .T. ) ;
#52248=B_SPLINE_CURVE_WITH_KNOTS ( 'NONE', 3,
 ( #31395, #4806, #4115, #47131 ),
 .UNSPECIFIED., .F., .F.,
 ( 4, 4 ),
 ( 0.000000000000000000, 0.1254181127249429095 ),
 .UNSPECIFIED. ) ;
#52254=CARTESIAN_POINT ( 'NONE',  ( 3.110247420108000149, -2.350685999463999920, -2.257335140124000272 ) ) ;
#52262=ORIENTED_EDGE ( 'NONE', *, *, #21853, .T. ) ;
#52263=CARTESIAN_POINT ( 'NONE',  ( 10.90000000296000060, 5.100000000009000445, -5.160242730682999657 ) ) ;
#52266=CARTESIAN_POINT ( 'NONE',  ( 10.67320712186517362, 2.921171224854686166, 8.329102901498840694 ) ) ;
#52268=EDGE_LOOP ( 'NONE', ( #27445, #56186, #67936, #15598, #37743, #63211, #32273, #21158 ) ) ;
#52270=ORIENTED_EDGE ( 'NONE', *, *, #4184, .F. ) ;
#52271=EDGE_CURVE ( 'NONE', #45997, #15587, #30215, .T. ) ;
#52274=CARTESIAN_POINT ( 'NONE',  ( 4.149992563291999836, 4.286198015044692593E-16, -1.999973142472143861 ) ) ;
#52277=FACE_OUTER_BOUND ( 'NONE', #41442, .T. ) ;
#52279=CARTESIAN_POINT ( 'NONE',  ( 7.771695280404999906, 5.732261791031000087, -7.476053406707000804 ) ) ;
#52282=ORIENTED_EDGE ( 'NONE', *, *, #10392, .T. ) ;
#52285=FACE_OUTER_BOUND ( 'NONE', #28720, .T. ) ;
#52286=ORIENTED_EDGE ( 'NONE', *, *, #58665, .F. ) ;
#52299=CARTESIAN_POINT ( 'NONE',  ( 3.439766623689833658, 0.6157310107295393964, -3.489820053897106700 ) ) ;
#52301=CARTESIAN_POINT ( 'NONE',  ( 10.79500540879000070, 3.503955365545999623, 6.168588659884999714 ) ) ;
#52304=CARTESIAN_POINT ( 'NONE',  ( 2.600505918310000109, 2.136089819110000398, 3.030967877105000152 ) ) ;
#52305=CARTESIAN_POINT ( 'NONE',  ( 7.000000000000000000, 6.255435840762999966, -3.000000000000000000 ) ) ;
#52309=EDGE_CURVE ( 'NONE', #23656, #29419, #23507, .T. ) ;
#52316=CARTESIAN_POINT ( 'NONE',  ( 3.155140132544248743, 0.9161175952574702741, 3.408904368339106927 ) ) ;
#52318=DIRECTION ( 'NONE',  ( 0.9999999999999997780, 1.340555680669999710E-09, 2.196395946400999623E-08 ) ) ;
#52319=CARTESIAN_POINT ( 'NONE',  ( 10.31667774810000004, 3.819530253758000260, 6.062195927068000145 ) ) ;
#52327=CARTESIAN_POINT ( 'NONE',  ( 0.3777305576672876919, 2.683931128707652825, -2.096468434807130077 ) ) ;
#52331=CARTESIAN_POINT ( 'NONE',  ( 5.000030787343001215, -0.5496608443529845678, -2.045306479342562156 ) ) ;
#52335=CARTESIAN_POINT ( 'NONE',  ( 0.5678519969244000265, -2.189299194929000159, -2.346944523683000217 ) ) ;
#52337=CARTESIAN_POINT ( 'NONE',  ( 11.26847444708000090, 2.565620268983000329, -7.116623294300999270 ) ) ;
#52339=CARTESIAN_POINT ( 'NONE',  ( 1.321806799207333460, -3.408904368339104263, -0.9161175952574813763 ) ) ;
#52340=DIRECTION ( 'NONE',  ( 1.000000000000000000, 0.000000000000000000, 0.000000000000000000 ) ) ;
#52343=CARTESIAN_POINT ( 'NONE',  ( 9.106135841230999617, 4.192919163547999872, 5.525472271700999194 ) ) ;
#52350=CARTESIAN_POINT ( 'NONE',  ( 2.980140132543583231, 3.408904368339106927, -0.9161175952574746040 ) ) ;
#52355=CARTESIAN_POINT ( 'NONE',  ( 6.999999691988000095, 12.11716380430000051, 3.069905306952999791 ) ) ;
#52364=CARTESIAN_POINT ( 'NONE',  ( 8.245295280410999794, 4.283000592898000392, 9.286795422009001655 ) ) ;
#52365=ORIENTED_EDGE ( 'NONE', *, *, #34550, .F. ) ;
#52379=ORIENTED_EDGE ( 'NONE', *, *, #36707, .F. ) ;
#52384=CARTESIAN_POINT ( 'NONE',  ( 10.14584353048000054, 5.370502454907000178, -6.826221644974000746 ) ) ;
#52385=CARTESIAN_POINT ( 'NONE',  ( 3.500000000000000000, 0.000000000000000000, 0.000000000000000000 ) ) ;
#52389=CARTESIAN_POINT ( 'NONE',  ( 10.71756692516999898, 3.040224182812999665, 8.808452309630000698 ) ) ;
#52392=CARTESIAN_POINT ( 'NONE',  ( 8.996000993494989828, 3.322909228140538129, -9.141577125681626725 ) ) ;
#52395=ORIENTED_EDGE ( 'NONE', *, *, #41840, .T. ) ;
#52398=CARTESIAN_POINT ( 'NONE',  ( 10.78089701270000056, 5.735299658853000082, 7.801561896854000366 ) ) ;
#52400=DIRECTION ( 'NONE',  ( 1.000000000000000000, -8.605781653910000390E-10, 6.242650264219000041E-09 ) ) ;
#52401=CARTESIAN_POINT ( 'NONE',  ( 7.966901574931999797, 4.609574279519000228, -6.276317554486000816 ) ) ;
#52402=CARTESIAN_POINT ( 'NONE',  ( 11.09999999999999964, 4.000000000000000000, -7.500000000000000000 ) ) ;
#52404=CARTESIAN_POINT ( 'NONE',  ( 9.294718325437999695, 4.148133901461999784, 9.337478696773001019 ) ) ;
#52405=CARTESIAN_POINT ( 'NONE',  ( 10.00637913184999839, 5.119263020957999899, 8.420380450036001108 ) ) ;
#52408=CARTESIAN_POINT ( 'NONE',  ( 9.029445280412998542, 5.442817578555000146, -8.106149115450000053 ) ) ;
#52416=DIRECTION ( 'NONE',  ( 1.000000000000000000, 0.000000000000000000, 0.000000000000000000 ) ) ;
#52418=CARTESIAN_POINT ( 'NONE',  ( 9.700639158771000581, 4.262870449202000422, -8.811513791423999820 ) ) ;
#52422=CARTESIAN_POINT ( 'NONE',  ( 9.569805421428000614, 4.064052243276000453, 8.919241792616000808 ) ) ;
#52428=CARTESIAN_POINT ( 'NONE',  ( 8.995176658772999545, 2.707986230053999854, 5.994446745591000436 ) ) ;
#52434=CARTESIAN_POINT ( 'NONE',  ( 1.738474413115999928, 2.350777309937000403, -2.257240049571999752 ) ) ;
#52438=CARTESIAN_POINT ( 'NONE',  ( 10.09197164456000095, 3.841384681542000301, 5.536408945990000774 ) ) ;
#52457=CARTESIAN_POINT ( 'NONE',  ( 10.46932803217000085, 4.988495740890000363, 6.213106455073000411 ) ) ;
#52458=CARTESIAN_POINT ( 'NONE',  ( 9.882903428397000312, 4.314559027837000293, -9.161039561412001930 ) ) ;
#52462=CARTESIAN_POINT ( 'NONE',  ( 8.975133055567869889, 5.349981391149201571, 7.499992565666659949 ) ) ;
#52464=CARTESIAN_POINT ( 'NONE',  ( 7.533885841228999958, 4.623631324973000112, 8.651459902566999816 ) ) ;
#52469=CARTESIAN_POINT ( 'NONE',  ( 8.668369459057998938, 3.037916315484999963, -6.050520490110999461 ) ) ;
#52477=EDGE_CURVE ( 'NONE', #23303, #10085, #57847, .T. ) ;
#52481=DIRECTION ( 'NONE',  ( 1.000000000000000000, 0.000000000000000000, 0.000000000000000000 ) ) ;
#52487=CARTESIAN_POINT ( 'NONE',  ( 7.555281674562000838, 4.314040636970999820, 8.819134391732999845 ) ) ;
#52492=CARTESIAN_POINT ( 'NONE',  ( 7.920378813398999185, 2.912874113511002783, -6.463705393502997332 ) ) ;
#52494=CARTESIAN_POINT ( 'NONE',  ( 10.97819528041000048, 5.476824759564999923, -7.128718425160999850 ) ) ;
#52497=DIRECTION ( 'NONE',  ( 1.000000000000000000, 0.000000000000000000, 0.000000000000000000 ) ) ;
#52500=ORIENTED_EDGE ( 'NONE', *, *, #44289, .F. ) ;
#52502=CARTESIAN_POINT ( 'NONE',  ( 9.030800552329955266, 2.902287361240370345, 6.174410955706410853 ) ) ;
#52505=CARTESIAN_POINT ( 'NONE',  ( -15.86200481174999943, -11.00717859340000082, -1.432487142323000118 ) ) ;
#52508=CYLINDRICAL_SURFACE ( 'NONE', #55615, 12.50000000000000000 ) ;
#52519=CARTESIAN_POINT ( 'NONE',  ( 7.470056312015993960, 3.527048554922000090, 6.623442700707995456 ) ) ;
#52523=LINE ( 'NONE', #35426, #13216 ) ;
#52530=CARTESIAN_POINT ( 'NONE',  ( 8.713854719593998155, 5.442817578555000146, -8.106149115450000053 ) ) ;
#52538=LINE ( 'NONE', #51175, #65529 ) ;
#52542=CARTESIAN_POINT ( 'NONE',  ( 11.09999999999999964, 6.066544595402000084, 5.234304349664999911 ) ) ;
#52543=ORIENTED_EDGE ( 'NONE', *, *, #66482, .T. ) ;
#52544=CARTESIAN_POINT ( 'NONE',  ( 6.899999692186000289, 12.99045401582999837, -1.690592930688000095 ) ) ;
#52545=CARTESIAN_POINT ( 'NONE',  ( 8.789679719592999874, 4.162493982103000256, -5.775210092227999858 ) ) ;
#52547=CARTESIAN_POINT ( 'NONE',  ( 11.11264834745999863, 2.146077493652999824, -7.517188756437000130 ) ) ;
#52555=CARTESIAN_POINT ( 'NONE',  ( 8.627615234342979278, 2.900000000000000799, 6.423404582975466681 ) ) ;
#52556=EDGE_CURVE ( 'NONE', #34720, #26471, #813, .T. ) ;
#52557=ORIENTED_EDGE ( 'NONE', *, *, #60490, .F. ) ;
#52561=DIRECTION ( 'NONE',  ( 1.000000000000000000, 0.000000000000000000, 0.000000000000000000 ) ) ;
#52567=VERTEX_POINT ( 'NONE', #40623 ) ;
#52569=CARTESIAN_POINT ( 'NONE',  ( 10.16426084122999995, 4.808846957865000604, -8.639578604182998944 ) ) ;
#52577=CARTESIAN_POINT ( 'NONE',  ( 7.752051012050213075, 3.239139382392606681, 6.375725454493062827 ) ) ;
#52581=DIRECTION ( 'NONE',  ( 1.000000000000000000, 1.776356839457000172E-14, -1.776356839457000172E-14 ) ) ;
#52584=CARTESIAN_POINT ( 'NONE',  ( 6.999999691988000095, -12.11716380430000051, -3.069905306952999791 ) ) ;
#52587=CARTESIAN_POINT ( 'NONE',  ( 10.52314899745999988, 5.167567567567999731, -6.822293592207000934 ) ) ;
#52594=CARTESIAN_POINT ( 'NONE',  ( 2.824155723461999390, 3.102089502169999680, 0.9991633116965998873 ) ) ;
#52595=VERTEX_POINT ( 'NONE', #23861 ) ;
#52598=CARTESIAN_POINT ( 'NONE',  ( 8.225195096046167720, 2.649880853682612614, 7.500010424662513664 ) ) ;
#52602=CARTESIAN_POINT ( 'NONE',  ( 10.84999882987999875, 0.000000000000000000, 0.000000000000000000 ) ) ;
#52608=CARTESIAN_POINT ( 'NONE',  ( 7.577152171347006693, 5.350137026785319883, -7.706116878973872097 ) ) ;
#52609=CARTESIAN_POINT ( 'NONE',  ( 27.64127793187000037, 5.599999999999999645, -6.571291218949999902 ) ) ;
#52612=ORIENTED_EDGE ( 'NONE', *, *, #62825, .T. ) ;
#52620=CARTESIAN_POINT ( 'NONE',  ( 7.880004719587999418, 2.759821810153000321, -8.454514188070000102 ) ) ;
#52623=ORIENTED_EDGE ( 'NONE', *, *, #24966, .T. ) ;
#52629=ORIENTED_EDGE ( 'NONE', *, *, #58389, .T. ) ;
#52631=CARTESIAN_POINT ( 'NONE',  ( 10.92587665653180551, 2.333614391320864456, 8.028595212472627196 ) ) ;
#52633=CONICAL_SURFACE ( 'NONE', #15761, 13.04999927352999833, 0.7853981075146502233 ) ;
#52636=DIRECTION ( 'NONE',  ( 1.000000000000000000, 0.000000000000000000, 0.000000000000000000 ) ) ;
#52644=CARTESIAN_POINT ( 'NONE',  ( 9.332933391271998502, 5.100349772922000646, 8.693467186193998941 ) ) ;
#52645=FACE_OUTER_BOUND ( 'NONE', #68061, .T. ) ;
#52649=CARTESIAN_POINT ( 'NONE',  ( 6.999999999999999112, 7.162151381622562596, -3.226150686063063322 ) ) ;
#52652=B_SPLINE_CURVE_WITH_KNOTS ( 'NONE', 3,
 ( #55607, #8396, #29741, #23441 ),
 .UNSPECIFIED., .F., .F.,
 ( 4, 4 ),
 ( 0.000000000000000000, 1.000000000000000000 ),
 .UNSPECIFIED. ) ;
#52656=CARTESIAN_POINT ( 'NONE',  ( 3.248890132543875264, -2.798833948393641080, 2.150913519912190708 ) ) ;
#52659=CARTESIAN_POINT ( 'NONE',  ( 10.84168637167000071, 2.681011538858999899, 6.554754637093000547 ) ) ;
#52667=VECTOR ( 'NONE', #20317, 1000.000000000000000 ) ;
#52672=CARTESIAN_POINT ( 'NONE',  ( 8.126014158770999529, 5.189036231907000030, -8.048606212067999977 ) ) ;
#52675=ORIENTED_EDGE ( 'NONE', *, *, #52556, .F. ) ;
#52679=CARTESIAN_POINT ( 'NONE',  ( 10.18308278041000037, 2.953582937013000009, -8.606284720264998356 ) ) ;
#52680=ORIENTED_EDGE ( 'NONE', *, *, #44074, .F. ) ;
#52684=DIRECTION ( 'NONE',  ( 1.000000000000000000, 0.000000000000000000, 0.000000000000000000 ) ) ;
#52685=CARTESIAN_POINT ( 'NONE',  ( 8.528448341230999930, 2.472348777564000066, 6.234194744024999402 ) ) ;
#52686=ORIENTED_EDGE ( 'NONE', *, *, #6555, .F. ) ;
#52688=CARTESIAN_POINT ( 'NONE',  ( 6.837589158771000264, 5.757004663580000070, -7.968612095259000050 ) ) ;
#52694=ORIENTED_EDGE ( 'NONE', *, *, #1041, .F. ) ;
#52696=CARTESIAN_POINT ( 'NONE',  ( 9.090417628846997999, 10.34502497667999954, -4.677911246888999841 ) ) ;
#52702=CARTESIAN_POINT ( 'NONE',  ( 8.895035841232999729, 5.751585344281000545, -8.235867044345999588 ) ) ;
#52704=B_SPLINE_CURVE_WITH_KNOTS ( 'NONE', 3,
 ( #1304, #61072, #60032, #12486, #11786, #55483, #6190, #18429, #1650, #34165, #22619, #33821, #48858, #22278, #43963, #64914, #17028, #33472, #65269, #7239, #1999, #38361, #28576, #49891, #33125, #12142, #54788, #66991, #29270, #3024, #34520, #61416, #7934, #40101, #24353 ),
 .UNSPECIFIED., .F., .F.,
 ( 4, 1, 1, 1, 1, 1, 1, 1, 1, 1, 1, 1, 1, 1, 1, 1, 1, 1, 1, 1, 1, 1, 1, 1, 1, 1, 1, 1, 1, 1, 1, 1, 4 ),
 ( 0.000000000000000000, 0.01250563797078715726, 0.04500523735960059585, 0.07750483674842403858, 0.1100044361372474744, 0.1425040355260709102, 0.1750036349148943460, 0.2075032343037177818, 0.2400028336925412453, 0.2725024330813646811, 0.3050020324701880892, 0.3375016318590116082, 0.3700012312478350163, 0.4025008306366584798, 0.4350004300254818879, 0.4675000294143053514, 0.4999996288031287039, 0.5324992281919521675, 0.5649988275807755755, 0.5974984269695990946, 0.6299980263584225026, 0.6624976257472459107, 0.6949972251360693187, 0.7274968245248928378, 0.7599964239137162458, 0.7924960233025396539, 0.8249956226913630619, 0.8574952220801865810, 0.8899948214690099890, 0.9224944208578333971, 0.9549940202466568051, 0.9874936196354803242, 1.000000000000000000 ),
 .UNSPECIFIED. ) ;
#52708=CARTESIAN_POINT ( 'NONE',  ( 8.630420280412000267, 5.808262417891000062, 7.446016144116000213 ) ) ;
#52709=ORIENTED_EDGE ( 'NONE', *, *, #27224, .F. ) ;
#52713=CARTESIAN_POINT ( 'NONE',  ( 9.832537864288001472, 2.899999999999999911, 6.571291218949999902 ) ) ;
#52714=ORIENTED_EDGE ( 'NONE', *, *, #65124, .T. ) ;
#52716=CARTESIAN_POINT ( 'NONE',  ( 10.62954538377999647, 10.07873972128999895, -5.168771492221002184 ) ) ;
#52727=AXIS2_PLACEMENT_3D ( 'NONE', #13723, #61606, #29474 ) ;
#52732=CARTESIAN_POINT ( 'NONE',  ( 10.77434248675000106, 4.612886656332999991, -8.898793847069001117 ) ) ;
#52737=CARTESIAN_POINT ( 'NONE',  ( 10.99933470386000067, 5.081013421858999735, 8.239043921879998678 ) ) ;
#52741=CARTESIAN_POINT ( 'NONE',  ( 9.781673028307999118, 5.464749740720999505, 8.817329433105999925 ) ) ;
#52743=CARTESIAN_POINT ( 'NONE',  ( 10.66951519566999806, 4.592673277375999952, 5.841403042559999648 ) ) ;
#52745=CARTESIAN_POINT ( 'NONE',  ( 9.318935841232999451, 2.644017913812000131, -7.838184857420000817 ) ) ;
#52746=CARTESIAN_POINT ( 'NONE',  ( 10.95087244768999923, 9.916146810440000792, -5.627651682437000424 ) ) ;
#52748=EDGE_CURVE ( 'NONE', #47074, #3245, #15354, .T. ) ;
#52751=CARTESIAN_POINT ( 'NONE',  ( 10.81315553411000074, 3.756074350075000012, 6.071610008629000355 ) ) ;
#52754=CARTESIAN_POINT ( 'NONE',  ( 8.988579719593998263, 4.902869380824999901, -8.978557145469999057 ) ) ;
#52766=DIRECTION ( 'NONE',  ( 0.000000000000000000, 1.000000000000000000, 0.000000000000000000 ) ) ;
#52771=CARTESIAN_POINT ( 'NONE',  ( 10.25888757983999966, 4.512388525173999909, 5.993701490107000929 ) ) ;
#52776=VERTEX_POINT ( 'NONE', #26535 ) ;
#52777=CARTESIAN_POINT ( 'NONE',  ( 8.251329719592000345, 5.773189794777000117, 7.141495931231999883 ) ) ;
#52781=CIRCLE ( 'NONE', #20390, 12.50000000000000000 ) ;
#52787=CARTESIAN_POINT ( 'NONE',  ( 9.409314688805999083, 2.634692233435000031, 8.920311306029999443 ) ) ;
#52801=ORIENTED_EDGE ( 'NONE', *, *, #46367, .T. ) ;
#52802=MANIFOLD_SOLID_BREP ( 'Stock-MAS-678-1', #12421 ) ;
#52803=CARTESIAN_POINT ( 'NONE',  ( 9.704564187634398209, 2.648431596117105435, 7.852956029643507918 ) ) ;
#52809=CARTESIAN_POINT ( 'NONE',  ( 10.30296826955000000, 4.081263352980999848, -9.025008366823000117 ) ) ;
#52815=CARTESIAN_POINT ( 'NONE',  ( 8.213545280409999094, 3.608525622520999843, 5.913376237674000002 ) ) ;
#52817=VECTOR ( 'NONE', #46406, 1000.000000000000114 ) ;
#52818=CARTESIAN_POINT ( 'NONE',  ( 7.550000000000000711, 4.000000000000000000, 8.849999999999999645 ) ) ;
#52821=CARTESIAN_POINT ( 'NONE',  ( 8.593644002494778888, 2.940065707283205043, -6.265224637780645978 ) ) ;
#52822=CARTESIAN_POINT ( 'NONE',  ( 6.543367680740003856, 10.50330513573999269, 4.576010683979003346 ) ) ;
#52824=CARTESIAN_POINT ( 'NONE',  ( 10.96418140149000031, 7.492203170189000616, 6.189237391497999674 ) ) ;
#52830=DIRECTION ( 'NONE',  ( 0.000000000000000000, 1.000000000000000000, 0.000000000000000000 ) ) ;
#52836=LINE ( 'NONE', #58761, #6381 ) ;
#52838=EDGE_CURVE ( 'NONE', #25280, #56515, #43299, .T. ) ;
#52843=CARTESIAN_POINT ( 'NONE',  ( 11.07691721959000120, 3.101894630379999906, -8.926552937604000704 ) ) ;
#52850=CARTESIAN_POINT ( 'NONE',  ( 0.7380637418424000895, 3.204751743350000126, -0.5916681129576000231 ) ) ;
#52869=DIRECTION ( 'NONE',  ( -0.8660254037844968833, 0.000000000000000000, 0.4999999999998989142 ) ) ;
#52870=CARTESIAN_POINT ( 'NONE',  ( 8.433148997460000018, 5.167567567567999731, 6.822293592207000934 ) ) ;
#52879=CARTESIAN_POINT ( 'NONE',  ( 8.813304719595000947, 3.880154689736000417, -9.060377011187000562 ) ) ;
#52886=CARTESIAN_POINT ( 'NONE',  ( 8.646410841231000788, 2.261390688294000029, -6.733978371730000134 ) ) ;
#52893=B_SPLINE_CURVE_WITH_KNOTS ( 'NONE', 3,
 ( #51755, #46863, #9105, #3849 ),
 .UNSPECIFIED., .F., .F.,
 ( 4, 4 ),
 ( 0.000000000000000000, 1.000000000000000000 ),
 .UNSPECIFIED. ) ;
#52894=CARTESIAN_POINT ( 'NONE',  ( 10.11094409420000062, 5.100000000000000533, -6.571291218949999902 ) ) ;
#52901=B_SPLINE_CURVE_WITH_KNOTS ( 'NONE', 3,
 ( #68978, #14815, #62361, #40690, #26340, #25992, #4652, #31247, #57112, #62020, #52555, #36138 ),
 .UNSPECIFIED., .F., .F.,
 ( 4, 2, 2, 2, 2, 4 ),
 ( 0.000000000000000000, 0.2500000000000010547, 0.3750000000000015543, 0.5000000000000021094, 0.7500000000000009992, 1.000000000000000000 ),
 .UNSPECIFIED. ) ;
#52914=CARTESIAN_POINT ( 'NONE',  ( 9.942214158770999788, 3.986577607995999806, -9.280166295424001177 ) ) ;
#52917=EDGE_LOOP ( 'NONE', ( #48898, #2188, #24774, #44147, #28610, #38340, #5502 ) ) ;
#52940=CARTESIAN_POINT ( 'NONE',  ( 7.976952457388438944, 3.338438528537961858, -6.270514789011116363 ) ) ;
#52946=ORIENTED_EDGE ( 'NONE', *, *, #52309, .F. ) ;
#52951=CARTESIAN_POINT ( 'NONE',  ( 1.592640132540833253, 3.058252359239899132, 1.762666431298155034 ) ) ;
#52952=ORIENTED_EDGE ( 'NONE', *, *, #60387, .T. ) ;
#52955=EDGE_CURVE ( 'NONE', #38520, #2626, #29996, .T. ) ;
#52959=CARTESIAN_POINT ( 'NONE',  ( 7.723040328487922324, 3.449924197545608084, -8.750316711071878473 ) ) ;
#52971=CARTESIAN_POINT ( 'NONE',  ( 6.736329719590999687, 5.216734614776999734, -8.484106667489999865 ) ) ;
#52973=CARTESIAN_POINT ( 'NONE',  ( 9.464429763972951548, 5.182499815101167862, 8.153205832973403844 ) ) ;
#52974=ORIENTED_EDGE ( 'NONE', *, *, #37341, .T. ) ;
#52977=DIRECTION ( 'NONE',  ( 1.000000000000000000, 0.000000000000000000, 0.000000000000000000 ) ) ;
#52979=EDGE_CURVE ( 'NONE', #47790, #53063, #56200, .T. ) ;
#52980=CIRCLE ( 'NONE', #28436, 12.50000000000000000 ) ;
#52983=DIRECTION ( 'NONE',  ( 0.000000000000000000, -1.000000000000000000, 0.000000000000000000 ) ) ;
#52987=CONICAL_SURFACE ( 'NONE', #22832, 2.050034397132999953, 0.7853981633972997312 ) ;
#52992=EDGE_LOOP ( 'NONE', ( #55922, #31410, #4132 ) ) ;
#52995=CARTESIAN_POINT ( 'NONE',  ( 11.11504246380000005, 3.456610836627000083, 5.970339330302000036 ) ) ;
#52999=CARTESIAN_POINT ( 'NONE',  ( 9.667010841233000917, 4.769103072373000352, -8.666849124598000387 ) ) ;
#53004=ORIENTED_EDGE ( 'NONE', *, *, #45065, .T. ) ;
#53010=DIRECTION ( 'NONE',  ( 0.000000000000000000, -0.1218274111675001353, 0.9925512993736016476 ) ) ;
#53022=CARTESIAN_POINT ( 'NONE',  ( 9.617764158771999305, 5.322769172805999816, -7.951018786192998178 ) ) ;
#53024=CARTESIAN_POINT ( 'NONE',  ( 4.600001223043999943, 0.000000000000000000, 0.000000000000000000 ) ) ;
#53027=CARTESIAN_POINT ( 'NONE',  ( 10.67905590578999941, 2.899999999999999911, 6.571291218949999902 ) ) ;
#53030=CARTESIAN_POINT ( 'NONE',  ( 10.42512334122999995, 3.371064118627999928, -6.294343971198999910 ) ) ;
#53032=CARTESIAN_POINT ( 'NONE',  ( 8.912651967921339846, 2.899999999999999911, 6.383937126463831824 ) ) ;
#53036=CARTESIAN_POINT ( 'NONE',  ( 8.271698341229999585, 5.629399530851999955, 8.631829656822000985 ) ) ;
#53041=CARTESIAN_POINT ( 'NONE',  ( 7.748070280408000166, 2.435036720175999925, -7.494591853605999887 ) ) ;
#53044=VERTEX_POINT ( 'NONE', #45715 ) ;
#53047=ORIENTED_EDGE ( 'NONE', *, *, #32770, .T. ) ;
#53057=VERTEX_POINT ( 'NONE', #8308 ) ;
#53058=CARTESIAN_POINT ( 'NONE',  ( 7.512829719590000010, 5.524123123935000379, 6.910361319981999095 ) ) ;
#53061=CARTESIAN_POINT ( 'NONE',  ( 8.924662153698969647, 5.350575487761837223, 7.500021879703680838 ) ) ;
#53062=CARTESIAN_POINT ( 'NONE',  ( 11.12487846393999824, 5.426360382733999899, -5.164845216807000483 ) ) ;
#53063=VERTEX_POINT ( 'NONE', #24039 ) ;
#53066=EDGE_CURVE ( 'NONE', #30735, #4878, #4170, .T. ) ;
#53079=CARTESIAN_POINT ( 'NONE',  ( 10.13061872827999998, 2.189311095934999951, -7.101639631284999865 ) ) ;
#53080=LINE ( 'NONE', #5863, #35459 ) ;
#53083=CARTESIAN_POINT ( 'NONE',  ( 8.168244718249995984, 3.088031253505000961, -6.162676582372005996 ) ) ;
#53089=CARTESIAN_POINT ( 'NONE',  ( 10.52323372634000087, 3.325642821414999784, 5.689987891230000372 ) ) ;
#53093=CARTESIAN_POINT ( 'NONE',  ( 11.07253275740080234, 2.278112260258351007, -7.888934961064568263 ) ) ;
#53094=EDGE_CURVE ( 'NONE', #40232, #52776, #18440, .T. ) ;
#53096=CARTESIAN_POINT ( 'NONE',  ( 8.195614351789243912, 4.733557677076899672, -8.663326391184606123 ) ) ;
#53104=CARTESIAN_POINT ( 'NONE',  ( 10.79967784532818698, 4.987751806468194715, 4.853501387964938907 ) ) ;
#53109=CARTESIAN_POINT ( 'NONE',  ( 8.143323341229999457, 5.061727314042999915, 5.824077473724000420 ) ) ;
#53110=AXIS2_PLACEMENT_3D ( 'NONE', #38485, #53871, #54913 ) ;
#53111=CARTESIAN_POINT ( 'NONE',  ( 8.614404719593999005, 5.030502105212999453, -6.322203460290999999 ) ) ;
#53112=CARTESIAN_POINT ( 'NONE',  ( 10.57314899745999881, 5.167567567567999731, -6.822293592207000934 ) ) ;
#53115=CARTESIAN_POINT ( 'NONE',  ( 10.31457848836000046, 5.362142879234999882, 6.677781064327999339 ) ) ;
#53121=CARTESIAN_POINT ( 'NONE',  ( 8.508079719592000600, 2.202812441249000219, 7.706988150133999405 ) ) ;
#53127=CIRCLE ( 'NONE', #45303, 1.349999999999999867 ) ;
#53128=CARTESIAN_POINT ( 'NONE',  ( 1.261654918708000173, 2.900008637959000435, -1.487022697228999935 ) ) ;
#53133=CARTESIAN_POINT ( 'NONE',  ( 11.02445190299000011, 3.404087387974999768, 5.822483872269000216 ) ) ;
#53136=VERTEX_POINT ( 'NONE', #25066 ) ;
#53137=CARTESIAN_POINT ( 'NONE',  ( 9.410004719593999312, 2.495531372253999791, -7.930944806125000746 ) ) ;
#53142=EDGE_LOOP ( 'NONE', ( #34431, #69058, #59144, #32771 ) ) ;
#53143=CARTESIAN_POINT ( 'NONE',  ( 3.500000000000000000, 1.140396268832999827, -3.309002319436000317 ) ) ;
#53149=CARTESIAN_POINT ( 'NONE',  ( 10.37873747135000002, 4.882725050998000249, 6.350806206758999650 ) ) ;
#53150=CARTESIAN_POINT ( 'NONE',  ( 10.14584353048000054, 5.370502454907000178, -6.826221644974000746 ) ) ;
#53151=CARTESIAN_POINT ( 'NONE',  ( 8.436984272513997851, 5.098716299041000433, 6.624027315230001101 ) ) ;
#53154=CARTESIAN_POINT ( 'NONE',  ( 8.991737455307951876, 5.328242699075392608, 7.781227856390141362 ) ) ;
#53156=CARTESIAN_POINT ( 'NONE',  ( 8.432510841230001830, 5.430400319332999715, 7.210801214872999410 ) ) ;
#53161=CARTESIAN_POINT ( 'NONE',  ( 9.237254889805134539, 2.665102389433001928, 7.298797478834294417 ) ) ;
#53162=CARTESIAN_POINT ( 'NONE',  ( 8.716851002545999094, 2.832432432432000269, 6.822293592207000934 ) ) ;
#53165=CARTESIAN_POINT ( 'NONE',  ( 10.96428034375000138, 7.885731839849998259, 6.436515532732999922 ) ) ;
#53174=AXIS2_PLACEMENT_3D ( 'NONE', #45130, #14347, #3495 ) ;
#53178=CARTESIAN_POINT ( 'NONE',  ( 0.3183723959866999742, 0.6486458134353999538, 3.310649237188999727 ) ) ;
#53187=CARTESIAN_POINT ( 'NONE',  ( 10.13035471959000056, 2.409325917207000511, -8.058043919563999680 ) ) ;
#53193=CARTESIAN_POINT ( 'NONE',  ( 0.7062757755484999622, 2.610614231003999919, -1.727479700733000056 ) ) ;
#53199=CARTESIAN_POINT ( 'NONE',  ( 8.154250713371753889, 3.097976385119930232, 6.283652888193028474 ) ) ;
#53215=CARTESIAN_POINT ( 'NONE',  ( 9.422953957969571803, 5.349869638328708099, 7.471018043992390112 ) ) ;
#53217=B_SPLINE_CURVE_WITH_KNOTS ( 'NONE', 3,
 ( #60065, #1678, #6572, #53779 ),
 .UNSPECIFIED., .F., .F.,
 ( 4, 4 ),
 ( 0.000000000000000000, 1.000000000000000000 ),
 .UNSPECIFIED. ) ;
#53218=ORIENTED_EDGE ( 'NONE', *, *, #23301, .F. ) ;
#53219=CARTESIAN_POINT ( 'NONE',  ( 9.988985841228000595, 3.986577607995999806, -9.280166295424001177 ) ) ;
#53221=EDGE_LOOP ( 'NONE', ( #67929, #52557, #18973, #27601 ) ) ;
#53222=AXIS2_PLACEMENT_3D ( 'NONE', #52402, #20246, #9064 ) ;
#53227=ADVANCED_FACE ( 'NONE', ( #34722 ), #32268, .T. ) ;
#53233=CARTESIAN_POINT ( 'NONE',  ( 10.15000066238999921, -1.190159082397999942E-13, -12.44999944941012160 ) ) ;
#53235=CARTESIAN_POINT ( 'NONE',  ( 9.368660841232999914, 2.702406276695999754, -6.981052078638000147 ) ) ;
#53236=ORIENTED_EDGE ( 'NONE', *, *, #14830, .F. ) ;
#53251=B_SPLINE_CURVE_WITH_KNOTS ( 'NONE', 3,
 ( #14735, #36054, #30814, #5267 ),
 .UNSPECIFIED., .F., .F.,
 ( 4, 4 ),
 ( 0.000000000000000000, 1.000000000000000000 ),
 .UNSPECIFIED. ) ;
#53252=CARTESIAN_POINT ( 'NONE',  ( 9.643864158774000828, 2.927176851028000293, -5.932007155957999878 ) ) ;
#53255=ADVANCED_FACE ( 'NONE', ( #8825 ), #43387, .F. ) ;
#53258=ORIENTED_EDGE ( 'NONE', *, *, #16211, .T. ) ;
#53278=AXIS2_PLACEMENT_3D ( 'NONE', #64822, #49102, #65169 ) ;
#53284=CARTESIAN_POINT ( 'NONE',  ( 7.573333333330499073, 5.179611624278248172, -6.820114376499284425 ) ) ;
#53287=CARTESIAN_POINT ( 'NONE',  ( 4.500000125099000492, 12.99999867215000116, 0.000000000000000000 ) ) ;
#53289=ORIENTED_EDGE ( 'NONE', *, *, #35747, .T. ) ;
#53294=CARTESIAN_POINT ( 'NONE',  ( 1.550973465874000201, 3.500000000000000000, 0.000000000000000000 ) ) ;
#53295=ORIENTED_EDGE ( 'NONE', *, *, #10584, .F. ) ;
#53300=CARTESIAN_POINT ( 'NONE',  ( 8.470944094208999076, 5.100000000000000533, 6.571291218949999902 ) ) ;
#53301=CARTESIAN_POINT ( 'NONE',  ( 7.883148997456999929, 5.167567567567999731, 6.822293592207000934 ) ) ;
#53307=VERTEX_POINT ( 'NONE', #45210 ) ;
#53312=ORIENTED_EDGE ( 'NONE', *, *, #31966, .T. ) ;
#53315=CARTESIAN_POINT ( 'NONE',  ( 6.777195280410000855, 5.620828677136000096, -7.589710348707000342 ) ) ;
#53317=AXIS2_PLACEMENT_3D ( 'NONE', #26865, #63899, #69154 ) ;
#53323=CARTESIAN_POINT ( 'NONE',  ( 6.899999691988000450, 0.000000000000000000, 0.000000000000000000 ) ) ;
#53325=VECTOR ( 'NONE', #1020, 1000.000000000000000 ) ;
#53328=VERTEX_POINT ( 'NONE', #36081 ) ;
#53332=CARTESIAN_POINT ( 'NONE',  ( 8.080472934640001270, 5.120350537135998081, -6.726184732097004293 ) ) ;
#53334=CARTESIAN_POINT ( 'NONE',  ( 0.000000000000000000, 2.899999999999999911, -7.500000000000000000 ) ) ;
#53337=ORIENTED_EDGE ( 'NONE', *, *, #59530, .T. ) ;
#53340=CARTESIAN_POINT ( 'NONE',  ( 10.27967883605999866, 5.739712809045000697, 7.774963411801000923 ) ) ;
#53341=CARTESIAN_POINT ( 'NONE',  ( 10.30480165877000154, 5.828331171948000211, -7.226590957700000928 ) ) ;
#53345=B_SPLINE_CURVE_WITH_KNOTS ( 'NONE', 3,
 ( #25595, #47612, #21036, #4257 ),
 .UNSPECIFIED., .F., .F.,
 ( 4, 4 ),
 ( 0.000000000000000000, 1.000000000000000000 ),
 .UNSPECIFIED. ) ;
#53350=ADVANCED_FACE ( 'NONE', ( #47953 ), #15787, .F. ) ;
#53355=FACE_OUTER_BOUND ( 'NONE', #29155, .T. ) ;
#53356=DIRECTION ( 'NONE',  ( 0.000000000000000000, 0.000000000000000000, 1.000000000000000000 ) ) ;
#53359=AXIS2_PLACEMENT_3D ( 'NONE', #19932, #46847, #36006 ) ;
#53368=DIRECTION ( 'NONE',  ( 1.000000000000000000, 0.000000000000000000, -3.552713678656000544E-14 ) ) ;
#53369=EDGE_CURVE ( 'NONE', #61815, #8371, #59004, .T. ) ;
#53371=ORIENTED_EDGE ( 'NONE', *, *, #46266, .T. ) ;
#53372=VECTOR ( 'NONE', #55023, 1000.000000000000000 ) ;
#53373=CARTESIAN_POINT ( 'NONE',  ( 0.8229711358043999558, 3.123219710863000209, -0.8105742342224000474 ) ) ;
#53375=CARTESIAN_POINT ( 'NONE',  ( 2.123246496035999797, 1.354718277511999913, 3.506157399516999895 ) ) ;
#53382=CARTESIAN_POINT ( 'NONE',  ( 9.234510841229999656, 5.964723767581000757, 7.776480083716999836 ) ) ;
#53385=CARTESIAN_POINT ( 'NONE',  ( 7.201095280410000576, 2.696863807693000048, -8.366590973307999946 ) ) ;
#53392=CARTESIAN_POINT ( 'NONE',  ( 8.356851002541000994, 2.832432432432000269, -6.822293592207000934 ) ) ;
#53394=DIRECTION ( 'NONE',  ( -2.359070754062999948E-09, 7.431742730979001170E-12, 1.000000000000000000 ) ) ;
#53405=CARTESIAN_POINT ( 'NONE',  ( 8.026329719592000700, 5.601795057054999916, 7.176148573050999957 ) ) ;
#53406=ORIENTED_EDGE ( 'NONE', *, *, #34631, .T. ) ;
#53411=CARTESIAN_POINT ( 'NONE',  ( 5.000000000000000000, 0.2999999999999999889, 3.149999999999999911 ) ) ;
#53422=ORIENTED_EDGE ( 'NONE', *, *, #9052, .F. ) ;
#53423=CIRCLE ( 'NONE', #67933, 11.35000000000000675 ) ;
#53424=DIRECTION ( 'NONE',  ( -1.000000000000000000, 0.000000000000000000, 0.000000000000000000 ) ) ;
#53426=CARTESIAN_POINT ( 'NONE',  ( 10.56271176071999918, 2.509373760909999973, -8.602415192333999983 ) ) ;
#53428=CARTESIAN_POINT ( 'NONE',  ( 9.073148997461000675, 5.167567567567999731, -6.822293592207000934 ) ) ;
#53430=VECTOR ( 'NONE', #25125, 1000.000000000000000 ) ;
#53432=VERTEX_POINT ( 'NONE', #57396 ) ;
#53434=EDGE_CURVE ( 'NONE', #34256, #2379, #30810, .T. ) ;
#53435=CARTESIAN_POINT ( 'NONE',  ( 11.08492721656000057, 3.668390701878999849, 5.558148445539999649 ) ) ;
#53437=CARTESIAN_POINT ( 'NONE',  ( 10.90000000000000036, 4.000000000000000000, -7.500000000000000000 ) ) ;
#53442=CARTESIAN_POINT ( 'NONE',  ( 8.365056901398830291, 2.650139792115765669, -7.500003826568613086 ) ) ;
#53445=ORIENTED_EDGE ( 'NONE', *, *, #30125, .F. ) ;
#53449=EDGE_CURVE ( 'NONE', #64300, #16312, #47527, .T. ) ;
#53450=CARTESIAN_POINT ( 'NONE',  ( 10.68942872719545001, 4.875347057626597369, 4.799721330339216330 ) ) ;
#53453=ORIENTED_EDGE ( 'NONE', *, *, #20682, .F. ) ;
#53455=EDGE_CURVE ( 'NONE', #29277, #23594, #4948, .T. ) ;
#53457=UNCERTAINTY_MEASURE_WITH_UNIT (LENGTH_MEASURE( 1.000000000000000082E-05 ), #64053, 'distance_accuracy_value', 'NONE');
#53458=CARTESIAN_POINT ( 'NONE',  ( 9.003345280414000840, 2.319062457810000311, -7.919229449146000022 ) ) ;
#53460=CARTESIAN_POINT ( 'NONE',  ( 2.645785826631131155, -0.2223228057201264707, -3.250327251304248044 ) ) ;
#53462=CARTESIAN_POINT ( 'NONE',  ( 9.423523952092001110, 4.993991073313000406, 8.578107851305000864 ) ) ;
#53469=CARTESIAN_POINT ( 'NONE',  ( 9.021579719592999425, 2.193665972875999959, 7.400591513898000073 ) ) ;
#53474=CARTESIAN_POINT ( 'NONE',  ( 1.452382716471000146, -1.124102084663000101, 3.059032707631999859 ) ) ;
#53480=B_SPLINE_SURFACE_WITH_KNOTS ( 'NONE', 3, 3, ( 
 ( #63840, #5802, #26806, #53022, #26454, #5118, #42875, #47787, #11060, #69096, #37620, #15954, #64868, #53709, #27145, #37284, #31700, #48465, #16641, #58261, #54047, #573, #64523, #42531, #37968, #16981, #59288, #11393, #32732, #6145, #38313, #10020, #58604, #31358, #52672 ),
 ( #4766, #68742, #42197, #15617, #63497, #36947, #10365, #65914, #7890, #60679, #29224, #6844, #12793, #18042, #7197, #34122, #33775, #28888, #18383, #34474, #33428, #55440, #22922, #50536, #12443, #28178, #23616, #27844, #55090, #59641, #54394, #28533, #49846, #39358, #55785 ),
 ( #33080, #6497, #7533, #12097, #44274, #39019, #44958, #23278, #11737, #50197, #2297, #2638, #65571, #17337, #22575, #49149, #17694, #49494, #66262, #1260, #39705, #44620, #61027, #13144, #23965, #1605, #45299, #66606, #60337, #1956, #43918, #18724, #54745, #38666, #65222 ),
 ( #59985, #61707, #4343, #56120, #40723, #24990, #8232, #62051, #51896, #47009, #51223, #13824, #62393, #25676, #45644, #29579, #3318, #35153, #57144, #9242, #68310, #46324, #3994, #24653, #56468, #40059, #62723, #30252, #41417, #14508, #25330, #8912, #41072, #19402, #14168 ) ),
 .UNSPECIFIED., .F., .F., .F.,
 ( 4, 4 ),
 ( 4, 1, 1, 1, 1, 1, 1, 1, 1, 1, 1, 1, 1, 1, 1, 1, 1, 1, 1, 1, 1, 1, 1, 1, 1, 1, 1, 1, 1, 1, 1, 1, 4 ),
 ( -0.1039370721279000015, 1.103937072127999963 ),
 ( -0.02000000000000000042, 0.01250000000000000069, 0.04499999999999999833, 0.07749999999999999944, 0.1100000000000000006, 0.1424999999999999878, 0.1749999999999999889, 0.2074999999999999900, 0.2399999999999999911, 0.2725000000000000200, 0.3049999999999999933, 0.3375000000000000222, 0.3699999999999999956, 0.4025000000000000244, 0.4349999999999999978, 0.4675000000000000266, 0.5000000000000000000, 0.5324999999999999734, 0.5649999999999999467, 0.5975000000000000311, 0.6300000000000000044, 0.6624999999999999778, 0.6949999999999999512, 0.7275000000000000355, 0.7600000000000000089, 0.7924999999999999822, 0.8249999999999999556, 0.8575000000000000400, 0.8900000000000000133, 0.9224999999999999867, 0.9549999999999999600, 0.9875000000000000444, 1.020000000000000018 ),
 .UNSPECIFIED. ) ;
#53481=CARTESIAN_POINT ( 'NONE',  ( 8.564679719593000229, 4.146787477634999775, -5.941926545671999627 ) ) ;
#53484=B_SPLINE_CURVE_WITH_KNOTS ( 'NONE', 3,
 ( #64670, #11193, #10850, #12241, #33566 ),
 .UNSPECIFIED., .F., .F.,
 ( 4, 1, 4 ),
 ( 0.000000000000000000, 0.5000000000000000000, 1.000000000000000000 ),
 .UNSPECIFIED. ) ;
#53485=FACE_OUTER_BOUND ( 'NONE', #58296, .T. ) ;
#53493=EDGE_CURVE ( 'NONE', #68077, #6526, #53345, .T. ) ;
#53496=CARTESIAN_POINT ( 'NONE',  ( 10.15787172175999942, 4.213497149090000171, -5.822953133183999874 ) ) ;
#53497=CARTESIAN_POINT ( 'NONE',  ( 7.643735281411005111, 4.861037469149006363, 6.423817941563998879 ) ) ;
#53500=CARTESIAN_POINT ( 'NONE',  ( 9.004750526303645586, 5.259872394538027685, 7.984454890150045614 ) ) ;
#53502=B_SPLINE_CURVE_WITH_KNOTS ( 'NONE', 3,
 ( #13659, #66787, #54576, #44449 ),
 .UNSPECIFIED., .F., .F.,
 ( 4, 4 ),
 ( 0.000000000000000000, 1.000000000000000000 ),
 .UNSPECIFIED. ) ;
#53503=CARTESIAN_POINT ( 'NONE',  ( 8.534482780410998615, 3.011620138462000273, 8.801434747080000065 ) ) ;
#53507=DIRECTION ( 'NONE',  ( 1.000000000000000000, 0.000000000000000000, 0.000000000000000000 ) ) ;
#53512=CARTESIAN_POINT ( 'NONE',  ( 11.01861045693000030, 7.589698685664999722, 6.381113859002999433 ) ) ;
#53515=EDGE_CURVE ( 'NONE', #57153, #38028, #38843, .T. ) ;
#53526=CARTESIAN_POINT ( 'NONE',  ( 0.1949759624410999925, 3.323048643578999872, -0.5818070024050000510 ) ) ;
#53527=CARTESIAN_POINT ( 'NONE',  ( 9.814910518647794291, 2.650130971540564317, -7.499994893876710478 ) ) ;
#53530=CARTESIAN_POINT ( 'NONE',  ( 9.115118560745049336, 5.349923934101355805, -7.499992884230159973 ) ) ;
#53533=CARTESIAN_POINT ( 'NONE',  ( 10.19121415877000203, 3.990707652596999555, -5.651362387566000400 ) ) ;
#53538=CARTESIAN_POINT ( 'NONE',  ( 8.800594747508441174, 2.899999999999999911, -6.515385012870885895 ) ) ;
#53543=CYLINDRICAL_SURFACE ( 'NONE', #58609, 1.350000000000000533 ) ;
#53548=ORIENTED_EDGE ( 'NONE', *, *, #31349, .F. ) ;
#53552=CARTESIAN_POINT ( 'NONE',  ( 10.96126252468000040, 5.100438257636001005, -4.932323065253000571 ) ) ;
#53555=CARTESIAN_POINT ( 'NONE',  ( 8.356851002541000994, 2.832432432432000269, -6.822293592207000934 ) ) ;
#53556=CARTESIAN_POINT ( 'NONE',  ( 5.449999267937000624, 6.217248937900999058E-14, 3.708144902247999495E-14 ) ) ;
#53561=CARTESIAN_POINT ( 'NONE',  ( 0.8009734658753000502, -3.500000000000000000, 0.000000000000000000 ) ) ;
#53563=CARTESIAN_POINT ( 'NONE',  ( 8.704995280412999747, 5.140767546012999567, -6.196177269779999719 ) ) ;
#53565=ORIENTED_EDGE ( 'NONE', *, *, #5393, .T. ) ;
#53570=DIRECTION ( 'NONE',  ( 0.4384236320214023319, 0.000000000000000000, 0.8987684456439056779 ) ) ;
#53574=EDGE_CURVE ( 'NONE', #66683, #22688, #48640, .T. ) ;
#53581=CARTESIAN_POINT ( 'NONE',  ( 8.631645280409999899, 3.826300099041999747, -9.055335252254000267 ) ) ;
#53586=VERTEX_POINT ( 'NONE', #740 ) ;
#53603=EDGE_LOOP ( 'NONE', ( #32663, #37843, #34807, #37880 ) ) ;
#53612=CARTESIAN_POINT ( 'NONE',  ( 8.341525531978778218, 4.649628395467509279, -6.060028403045727430 ) ) ;
#53615=ORIENTED_EDGE ( 'NONE', *, *, #2157, .F. ) ;
#53623=B_SPLINE_CURVE_WITH_KNOTS ( 'NONE', 3,
 ( #9451, #41624, #9116, #68522 ),
 .UNSPECIFIED., .F., .F.,
 ( 4, 4 ),
 ( 0.000000000000000000, 1.000000000000000000 ),
 .UNSPECIFIED. ) ;
#53636=DIRECTION ( 'NONE',  ( 0.000000000000000000, 1.000000000000000000, 0.000000000000000000 ) ) ;
#53645=ORIENTED_EDGE ( 'NONE', *, *, #64851, .F. ) ;
#53649=LINE ( 'NONE', #63785, #32874 ) ;
#53655=B_SPLINE_CURVE_WITH_KNOTS ( 'NONE', 3,
 ( #61305, #13425, #28112, #34746, #56055, #49424, #1537, #44206, #61645, #19690, #24241, #18996, #46262, #41011, #51838, #20370, #41694, #30524 ),
 .UNSPECIFIED., .F., .F.,
 ( 4, 2, 2, 2, 2, 2, 2, 2, 4 ),
 ( 0.000000000000000000, 0.1250000000000000000, 0.2500000000000000000, 0.3750000000000000000, 0.5000000000000000000, 0.6250000000000000000, 0.7500000000000000000, 0.8750000000000000000, 1.000000000000000000 ),
 .UNSPECIFIED. ) ;
#53658=CARTESIAN_POINT ( 'NONE',  ( 7.812560841224999386, 5.525377065333000104, -6.367402836891999485 ) ) ;
#53659=CARTESIAN_POINT ( 'NONE',  ( 8.753190465598311931, 3.015364744815148601, -8.459884657046686129 ) ) ;
#53660=EDGE_CURVE ( 'NONE', #8893, #66228, #38947, .T. ) ;
#53665=CARTESIAN_POINT ( 'NONE',  ( 8.299720885770000223, 3.399999999999999911, -6.084164326786999588 ) ) ;
#53667=VERTEX_POINT ( 'NONE', #24484 ) ;
#53674=CARTESIAN_POINT ( 'NONE',  ( 7.724132149008994475, 4.510524588886997144, -6.436036822971000326 ) ) ;
#53677=CARTESIAN_POINT ( 'NONE',  ( 3.240556799211292027, -3.500000000000003109, 0.4581489286484972667 ) ) ;
#53682=CARTESIAN_POINT ( 'NONE',  ( 10.24477918374999952, 5.265206995764999398, 8.959504263949002123 ) ) ;
#53683=CARTESIAN_POINT ( 'NONE',  ( 10.98632665877000036, 3.015084670878999784, -9.064442106213000727 ) ) ;
#53688=CARTESIAN_POINT ( 'NONE',  ( 7.000000000000000000, 7.356391799243646723, -3.356391799243647167 ) ) ;
#53697=CARTESIAN_POINT ( 'NONE',  ( 10.15902941591999920, 4.166415211384999040, 9.114163806478000396 ) ) ;
#53704=CARTESIAN_POINT ( 'NONE',  ( 6.933458400913999675, -12.41496613996999976, -2.805592698698999854 ) ) ;
#53709=CARTESIAN_POINT ( 'NONE',  ( 9.120514158775000269, 5.306366356490000769, -7.996450761531000317 ) ) ;
#53713=CARTESIAN_POINT ( 'NONE',  ( 0.2965795288954000131, -0.5398464557615000325, -3.496157131901000081 ) ) ;
#53715=CARTESIAN_POINT ( 'NONE',  ( 10.27367334122999942, 3.065551304793999510, -8.487910413489000661 ) ) ;
#53717=DIRECTION ( 'NONE',  ( 0.000000000000000000, 0.000000000000000000, -1.000000000000000000 ) ) ;
#53718=CARTESIAN_POINT ( 'NONE',  ( 9.940795537695766626, 5.100000000000000533, 6.662590550604607031 ) ) ;
#53725=CARTESIAN_POINT ( 'NONE',  ( 7.806654719586000546, 4.523949137149999800, -5.848703038986000635 ) ) ;
#53731=VERTEX_POINT ( 'NONE', #26548 ) ;
#53732=CARTESIAN_POINT ( 'NONE',  ( 11.09999999999999432, 2.853660941539340357, -8.651758704407463085 ) ) ;
#53733=CARTESIAN_POINT ( 'NONE',  ( 27.64127793187000037, 2.399999999999999911, 6.571291218949999902 ) ) ;
#53744=CARTESIAN_POINT ( 'NONE',  ( 8.090517219592001652, 5.342170561818999630, 8.432311822615000452 ) ) ;
#53747=CARTESIAN_POINT ( 'NONE',  ( 8.554774139323296112, 5.012966070311602351, -8.578716361322166861 ) ) ;
#53748=DIRECTION ( 'NONE',  ( 0.000000000000000000, 1.000000000000000000, 0.000000000000000000 ) ) ;
#53761=B_SPLINE_CURVE_WITH_KNOTS ( 'NONE', 3,
 ( #26228, #57005, #15393, #19606 ),
 .UNSPECIFIED., .F., .F.,
 ( 4, 4 ),
 ( 0.000000000000000000, 1.000000000000000000 ),
 .UNSPECIFIED. ) ;
#53762=ORIENTED_EDGE ( 'NONE', *, *, #28203, .T. ) ;
#53765=CARTESIAN_POINT ( 'NONE',  ( 4.900006121742001675, -1.229093439949829447, 1.599333684796361732 ) ) ;
#53766=CARTESIAN_POINT ( 'NONE',  ( 9.610944094206999466, 5.100000000000000533, -6.571291218949999902 ) ) ;
#53768=DIRECTION ( 'NONE',  ( -0.7071067783159971087, 0.7071067840570971486, -3.025403634578990376E-08 ) ) ;
#53769=CARTESIAN_POINT ( 'NONE',  ( 8.339994183033994091, 2.871570486036998382, -6.342248726812004911 ) ) ;
#53770=CARTESIAN_POINT ( 'NONE',  ( 9.944319408602000365, 5.443001719280999851, 7.367350382395000175 ) ) ;
#53774=CARTESIAN_POINT ( 'NONE',  ( 9.166073843917999397, 4.023333628930999772, 9.122276991855001071 ) ) ;
#53779=CARTESIAN_POINT ( 'NONE',  ( 11.09999999999999964, 5.538898460221000519, 7.685179721164000277 ) ) ;
#53782=B_SPLINE_CURVE_WITH_KNOTS ( 'NONE', 3,
 ( #1789, #44106, #50031, #53284, #65405, #17524, #58521, #5384, #2138, #38854, #39194, #60177, #12283, #26723, #7029, #23105, #60516, #23458 ),
 .UNSPECIFIED., .F., .F.,
 ( 4, 2, 2, 2, 2, 2, 2, 2, 4 ),
 ( 0.000000000000000000, 0.1250000000000000000, 0.2500000000000000000, 0.3750000000000000000, 0.5000000000000000000, 0.6250000000000000000, 0.7500000000000000000, 0.8750000000000000000, 1.000000000000000000 ),
 .UNSPECIFIED. ) ;
#53792=CARTESIAN_POINT ( 'NONE',  ( -2.444943969992999916E-05, -2.899969545325999931, 0.000000000000000000 ) ) ;
#53793=CARTESIAN_POINT ( 'NONE',  ( 7.833767219591000419, 2.583668273793999770, 6.684750595573999199 ) ) ;
#53794=CARTESIAN_POINT ( 'NONE',  ( 8.142589158771000868, 5.074768364528000397, -8.296267706722000312 ) ) ;
#53796=CARTESIAN_POINT ( 'NONE',  ( 2.561951899676131461, -2.934981565945976367, -1.414191605408132935 ) ) ;
#53797=ORIENTED_EDGE ( 'NONE', *, *, #25480, .T. ) ;
#53798=CARTESIAN_POINT ( 'NONE',  ( 10.20319667131999886, 3.421760346951000287, 6.017732782098999422 ) ) ;
#53804=CARTESIAN_POINT ( 'NONE',  ( 8.455992358796999397, 5.100000000000000533, 6.571291218954000257 ) ) ;
#53808=CARTESIAN_POINT ( 'NONE',  ( 7.000000000000000000, 7.526486366024999874, -3.526486366024999874 ) ) ;
#53817=CARTESIAN_POINT ( 'NONE',  ( 9.568039158772000619, 5.336630274082000192, -7.092011739486999922 ) ) ;
#53819=ADVANCED_FACE ( 'NONE', ( #10797 ), #32282, .F. ) ;
#53823=CARTESIAN_POINT ( 'NONE',  ( 7.947810405765513231, 4.792115117880548780, -6.324572600310053971 ) ) ;
#53827=DIRECTION ( 'NONE',  ( 0.000000000000000000, 0.8684118855788046654, -0.4958435206650028126 ) ) ;
#53832=CARTESIAN_POINT ( 'NONE',  ( 10.56491664109999995, 4.212242527248999835, 8.933458498617000032 ) ) ;
#53833=CARTESIAN_POINT ( 'NONE',  ( 10.05205635875000070, 2.669891600604999748, -8.791543746052999708 ) ) ;
#53834=CARTESIAN_POINT ( 'NONE',  ( 8.060004013849999538, 5.097451875645002239, 6.450907456765003545 ) ) ;
#53840=CARTESIAN_POINT ( 'NONE',  ( 9.459510841229999301, 5.445214367171999470, 7.703373622193999459 ) ) ;
#53844=CARTESIAN_POINT ( 'NONE',  ( 7.100000000000000533, 5.221516520829000640, -8.074802043613001246 ) ) ;
#53845=CARTESIAN_POINT ( 'NONE',  ( 9.241226895148511034, 2.676623112219036482, 7.234156217801734456 ) ) ;
#53846=DIRECTION ( 'NONE',  ( -0.7071134747947538379, 0.000000000000000000, -0.7071000875149777709 ) ) ;
#53847=EDGE_CURVE ( 'NONE', #8734, #10646, #59151, .T. ) ;
#53850=CARTESIAN_POINT ( 'NONE',  ( 10.86291173059000137, 9.763630752138000801, 5.703239193002999308 ) ) ;
#53861=CARTESIAN_POINT ( 'NONE',  ( 8.855420280411999912, 5.633477595780999714, 7.451234169193000412 ) ) ;
#53866=CARTESIAN_POINT ( 'NONE',  ( 8.061825939490002924, 3.419144686567003877, -6.221559872366999144 ) ) ;
#53867=CARTESIAN_POINT ( 'NONE',  ( 10.65229834123000074, 4.944334466443999432, -8.478467788338001299 ) ) ;
#53869=CARTESIAN_POINT ( 'NONE',  ( 8.187982051047001164, 4.942702676859997979, 6.196150354213001421 ) ) ;
#53871=DIRECTION ( 'NONE',  ( -1.000000000000000000, 0.000000000000000000, 0.000000000000000000 ) ) ;
#53873=AXIS2_PLACEMENT_3D ( 'NONE', #58652, #10753, #59000 ) ;
#53875=CARTESIAN_POINT ( 'NONE',  ( 1.500973465873999935, 3.500000000000000000, 0.000000000000000000 ) ) ;
#53879=CARTESIAN_POINT ( 'NONE',  ( 10.86079987841999994, 2.936792838704000097, 5.172914090879999982 ) ) ;
#53880=PLANE ( 'NONE',  #57839 ) ;
#53882=B_SPLINE_CURVE_WITH_KNOTS ( 'NONE', 3,
 ( #56669, #10735, #21229, #51416 ),
 .UNSPECIFIED., .F., .F.,
 ( 4, 4 ),
 ( 0.000000000000000000, 1.000000000000000000 ),
 .UNSPECIFIED. ) ;
#53884=CARTESIAN_POINT ( 'NONE',  ( 9.828775684073081109, 2.650411012611820105, -7.263174729041424804 ) ) ;
#53893=B_SPLINE_SURFACE_WITH_KNOTS ( 'NONE', 3, 3, ( 
 ( #21939, #43277, #54106, #27543, #54453, #65966, #64585, #1662, #54798, #38022, #49549, #49207, #44327, #50248, #60733, #22979, #43630, #28234, #33137, #64924, #23332, #55494, #6554, #65625, #22290, #11451, #7594, #7248, #22630, #17750, #43975, #48869, #18092, #39070, #60392 ),
 ( #12496, #1314, #33831, #28589, #38372, #59696, #49901, #39413, #28943, #16694, #17040, #32790, #6201, #977, #11798, #38723, #27897, #60045, #34862, #19460, #13543, #24019, #39764, #19114, #35211, #51614, #40781, #57199, #62446, #9302, #3710, #23672, #41135, #62105, #61762 ),
 ( #46033, #30643, #14224, #25047, #40113, #50936, #67339, #45010, #66314, #51278, #14567, #24710, #35551, #56869, #2350, #35884, #18438, #8967, #61082, #13202, #30306, #56178, #34530, #55839, #46379, #7943, #67681, #19807, #18782, #61427, #3373, #29279, #50594, #2695, #45354 ),
 ( #66663, #8289, #29633, #3034, #24365, #45696, #67005, #40435, #29976, #13880, #56522, #8627, #52999, #57896, #68370, #10341, #5095, #64161, #5445, #4740, #15929, #20490, #25738, #41815, #26431, #58931, #63816, #32031, #63122, #31334, #47761, #25388, #46726, #31677, #21516 ) ),
 .UNSPECIFIED., .F., .F., .F.,
 ( 4, 4 ),
 ( 4, 1, 1, 1, 1, 1, 1, 1, 1, 1, 1, 1, 1, 1, 1, 1, 1, 1, 1, 1, 1, 1, 1, 1, 1, 1, 1, 1, 1, 1, 1, 1, 4 ),
 ( -0.1039370721279000015, 1.103937072127999963 ),
 ( -0.02000000000000000042, 0.01250000000000000069, 0.04499999999999999833, 0.07749999999999999944, 0.1100000000000000006, 0.1424999999999999878, 0.1749999999999999889, 0.2074999999999999900, 0.2399999999999999911, 0.2725000000000000200, 0.3049999999999999933, 0.3375000000000000222, 0.3699999999999999956, 0.4025000000000000244, 0.4349999999999999978, 0.4675000000000000266, 0.5000000000000000000, 0.5324999999999999734, 0.5649999999999999467, 0.5975000000000000311, 0.6300000000000000044, 0.6624999999999999778, 0.6949999999999999512, 0.7275000000000000355, 0.7600000000000000089, 0.7924999999999999822, 0.8249999999999999556, 0.8575000000000000400, 0.8900000000000000133, 0.9224999999999999867, 0.9549999999999999600, 0.9875000000000000444, 1.020000000000000018 ),
 .UNSPECIFIED. ) ;
#53894=CARTESIAN_POINT ( 'NONE',  ( 11.09999999999999964, 6.593648130222000248, -5.598803514566000672 ) ) ;
#53896=ADVANCED_FACE ( 'NONE', ( #47793 ), #447, .F. ) ;
#53897=CARTESIAN_POINT ( 'NONE',  ( 9.416236906464300560, 5.342733096692782624, 7.360698289850908793 ) ) ;
#53912=CYLINDRICAL_SURFACE ( 'NONE', #67861, 1.350000000000000533 ) ;
#53918=CARTESIAN_POINT ( 'NONE',  ( 9.716735841232001292, 3.941185585667000169, -8.896279800194999865 ) ) ;
#53931=CARTESIAN_POINT ( 'NONE',  ( 7.196271682457999752, 4.719833207100999850, -8.789699670502999496 ) ) ;
#53933=CARTESIAN_POINT ( 'NONE',  ( 4.600001223043999943, 0.000000000000000000, 0.000000000000000000 ) ) ;
#53936=CARTESIAN_POINT ( 'NONE',  ( 9.152446624286001864, 2.899999999999999911, -6.169193161299999950 ) ) ;
#53949=CARTESIAN_POINT ( 'NONE',  ( 8.440751497925912616, 5.098238174920831867, -6.529850537739550376 ) ) ;
#53950=CARTESIAN_POINT ( 'NONE',  ( 6.899999691988000450, 12.20988339176000004, -3.111064831549000154 ) ) ;
#53951=ORIENTED_EDGE ( 'NONE', *, *, #42442, .F. ) ;
#53978=EDGE_CURVE ( 'NONE', #5660, #27749, #33780, .T. ) ;
#53981=CARTESIAN_POINT ( 'NONE',  ( 7.000000000000000000, 10.57888183308256735, 3.948561346722022414 ) ) ;
#53983=EDGE_LOOP ( 'NONE', ( #60195, #33313, #33216, #19613, #16858 ) ) ;
#53984=B_SPLINE_CURVE_WITH_KNOTS ( 'NONE', 3,
 ( #48384, #16220, #63418, #9593, #37542, #5389, #15193, #57841, #58525, #26727 ),
 .UNSPECIFIED., .F., .F.,
 ( 4, 2, 2, 2, 4 ),
 ( 0.000000000000000000, 0.1249999999999998335, 0.2499999999999996669, 0.3749999999999995559, 0.4999999999999994449 ),
 .UNSPECIFIED. ) ;
#53988=VERTEX_POINT ( 'NONE', #49850 ) ;
#53994=CARTESIAN_POINT ( 'NONE',  ( 8.210360841226998829, 3.344658122371999998, -5.716722540613000447 ) ) ;
#53996=CARTESIAN_POINT ( 'NONE',  ( 7.936333771302000351, 5.123034328734999754, 6.721303713258000023 ) ) ;
#53997=ORIENTED_EDGE ( 'NONE', *, *, #13972, .T. ) ;
#54000=ORIENTED_EDGE ( 'NONE', *, *, #34269, .F. ) ;
#54002=DIRECTION ( 'NONE',  ( -1.000000000000000000, 0.000000000000000000, 0.000000000000000000 ) ) ;
#54011=CARTESIAN_POINT ( 'NONE',  ( 9.379129085676606081, 2.650412078218661538, -7.263196332420141843 ) ) ;
#54014=CARTESIAN_POINT ( 'NONE',  ( 9.351497027444999333, 4.821940693094999730, 8.950154065657999425 ) ) ;
#54019=CARTESIAN_POINT ( 'NONE',  ( 3.648430005244999830, 0.04330141671533999093, 3.707787403725999908 ) ) ;
#54025=ORIENTED_EDGE ( 'NONE', *, *, #51624, .F. ) ;
#54029=CARTESIAN_POINT ( 'NONE',  ( 10.47094409420000005, 5.100000000000000533, 6.571291218949999902 ) ) ;
#54032=FACE_OUTER_BOUND ( 'NONE', #54082, .T. ) ;
#54047=CARTESIAN_POINT ( 'NONE',  ( 8.772439158776000667, 3.098073081301000009, -8.567513114264999174 ) ) ;
#54049=ADVANCED_FACE ( 'NONE', ( #65917 ), #50884, .F. ) ;
#54051=CARTESIAN_POINT ( 'NONE',  ( 0.9790647364571333222, 3.399126080497532953, -0.9633645835950521708 ) ) ;
#54052=VECTOR ( 'NONE', #51965, 1000.000000000000000 ) ;
#54053=CARTESIAN_POINT ( 'NONE',  ( 0.7407068467740000051, 0.9423624982842000453, -3.239329654985999785 ) ) ;
#54055=CARTESIAN_POINT ( 'NONE',  ( 2.170928445476999702, -0.8586646638686999955, 3.659381217151000065 ) ) ;
#54056=ORIENTED_EDGE ( 'NONE', *, *, #57313, .T. ) ;
#54061=CARTESIAN_POINT ( 'NONE',  ( 9.117517219591000810, 4.954905351382000944, 8.825777580285999235 ) ) ;
#54064=CARTESIAN_POINT ( 'NONE',  ( 8.344770280407999508, 3.460181152982999997, -6.031076961652000357 ) ) ;
#54068=VERTEX_POINT ( 'NONE', #60682 ) ;
#54080=CARTESIAN_POINT ( 'NONE',  ( 7.100000000000000533, 0.000000000000000000, 0.000000000000000000 ) ) ;
#54082=EDGE_LOOP ( 'NONE', ( #55431, #18507, #28583, #14612 ) ) ;
#54083=CARTESIAN_POINT ( 'NONE',  ( 8.924954719592001595, 4.158911560497999815, 5.873540104660999184 ) ) ;
#54085=EDGE_LOOP ( 'NONE', ( #32275, #67083, #33301, #37383 ) ) ;
#54088=CARTESIAN_POINT ( 'NONE',  ( 10.96255537160999971, 6.761658444318999983, -5.456360451353000407 ) ) ;
#54089=ORIENTED_EDGE ( 'NONE', *, *, #30312, .F. ) ;
#54101=ORIENTED_EDGE ( 'NONE', *, *, #37167, .T. ) ;
#54106=CARTESIAN_POINT ( 'NONE',  ( 9.892489158770999325, 5.099602161831000124, -9.049221499261999924 ) ) ;
#54107=CARTESIAN_POINT ( 'NONE',  ( 10.15787172175999942, 4.213497149090000171, -5.822953133183999874 ) ) ;
#54110=CARTESIAN_POINT ( 'NONE',  ( 7.612465007326000510, 3.179383379803001564, -6.407107007521996245 ) ) ;
#54114=CARTESIAN_POINT ( 'NONE',  ( 9.877261637240000169, 2.207988120125000009, 7.624813826992999921 ) ) ;
#54119=CARTESIAN_POINT ( 'NONE',  ( 11.04951995735000025, 9.925864394642001542, -5.806870034355000598 ) ) ;
#54120=LINE ( 'NONE', #993, #39205 ) ;
#54121=AXIS2_PLACEMENT_3D ( 'NONE', #66899, #24605, #8523 ) ;
#54123=EDGE_CURVE ( 'NONE', #21968, #24059, #29230, .T. ) ;
#54126=CARTESIAN_POINT ( 'NONE',  ( 8.921135841230999119, 3.292387953886000140, -6.294868737226000377 ) ) ;
#54129=EDGE_CURVE ( 'NONE', #63173, #12318, #57150, .T. ) ;
#54135=CARTESIAN_POINT ( 'NONE',  ( 9.170323341230000480, 5.558938731259999599, 6.272977177425000050 ) ) ;
#54136=CARTESIAN_POINT ( 'NONE',  ( 8.704995280412999747, 5.140767546012999567, -6.196177269779999719 ) ) ;
#54138=CARTESIAN_POINT ( 'NONE',  ( 3.316457242269348349, 2.850256168064621232, 1.578002730033648993 ) ) ;
#54140=CARTESIAN_POINT ( 'NONE',  ( 9.924742128742000347, 5.060458431729999873, 8.686130311522999747 ) ) ;
#54144=CARTESIAN_POINT ( 'NONE',  ( 7.544198296194000619, 2.929983868333001951, 6.556648683638004016 ) ) ;
#54145=EDGE_LOOP ( 'NONE', ( #19381, #55392 ) ) ;
#54146=CARTESIAN_POINT ( 'NONE',  ( 8.832537864289999874, 2.899999999999999911, 6.571291218949999902 ) ) ;
#54147=EDGE_CURVE ( 'NONE', #10337, #21003, #41420, .T. ) ;
#54152=DIRECTION ( 'NONE',  ( 1.000000000000000000, 0.000000000000000000, 0.000000000000000000 ) ) ;
#54153=ORIENTED_EDGE ( 'NONE', *, *, #29066, .F. ) ;
#54156=CARTESIAN_POINT ( 'NONE',  ( 7.428092358015002006, 3.524408735919001501, 6.653372890553997721 ) ) ;
#54159=ORIENTED_EDGE ( 'NONE', *, *, #21267, .T. ) ;
#54160=CARTESIAN_POINT ( 'NONE',  ( 9.700639158771000581, 4.262870449202000422, -8.811513791423999820 ) ) ;
#54163=CARTESIAN_POINT ( 'NONE',  ( 9.137709786520556321, 4.829499945559576624, -8.579760339927545942 ) ) ;
#54168=ORIENTED_EDGE ( 'NONE', *, *, #40190, .T. ) ;
#54173=CARTESIAN_POINT ( 'NONE',  ( 9.571961069101000419, 4.084683332033999470, 8.946609345378000455 ) ) ;
#54174=CARTESIAN_POINT ( 'NONE',  ( 10.89212517796999968, 2.946919582117999870, -5.013248949648000163 ) ) ;
#54175=CARTESIAN_POINT ( 'NONE',  ( 7.948904172952001801, 4.897346594336003278, 6.290771953639007208 ) ) ;
#54182=CARTESIAN_POINT ( 'NONE',  ( 7.892607780408998686, 5.480308727866000318, 8.192324747680999053 ) ) ;
#54185=CARTESIAN_POINT ( 'NONE',  ( 9.652931135702420562, 5.100000000000000533, -6.444141223381762096 ) ) ;
#54189=CARTESIAN_POINT ( 'NONE',  ( 11.00094363691999888, 8.784914713122999430, 6.555567193519999947 ) ) ;
#54192=ORIENTED_EDGE ( 'NONE', *, *, #61008, .F. ) ;
#54195=CARTESIAN_POINT ( 'NONE',  ( 10.40516904918000129, 5.216391323504000255, 6.765759859247999941 ) ) ;
#54196=CARTESIAN_POINT ( 'NONE',  ( 8.290071854142535557, 2.941495930016484461, -6.434443241224298227 ) ) ;
#54197=B_SPLINE_SURFACE_WITH_KNOTS ( 'NONE', 3, 3, ( 
 ( #55926, #18867, #40195, #29368, #45437, #23419, #17835, #7331, #61511, #49990, #19200, #60133, #44754, #2102, #12242, #54886, #66058, #28318, #18178, #39499, #45096, #66402, #39847, #14648, #8715, #68112, #25474, #10078, #41896, #19891, #4826, #20571, #4479, #40522, #56950 ),
 ( #30059, #63204, #35294, #15332, #52034, #31416, #20229, #52732, #51361, #3455, #24793, #40868, #46119, #46806, #57627, #67425, #61849, #62191, #26169, #36660, #47148, #35637, #68799, #52384, #57981, #3795, #14312, #41218, #19549, #56609, #9048, #62528, #30388, #35964, #30726 ),
 ( #46464, #31078, #47493, #14983, #13965, #51698, #57279, #25131, #25819, #67764, #9383, #36308, #4137, #41555, #68449, #62865, #9728, #6556, #37684, #27544, #27202, #38023, #33138, #21260, #27898, #54107, #58319, #49208, #58664, #26513, #47844, #63559, #54454, #42590, #20920 ),
 ( #5178, #15674, #6202, #48871, #21941, #16013, #978, #32791, #64241, #10766, #59697, #42256, #37003, #69153, #38373, #16695, #11799, #53426, #43278, #10421, #32109, #42934, #63898, #26864, #11452, #22291, #64586, #31762, #53079, #21595, #37342, #43631, #5524, #48177, #59350 ) ),
 .UNSPECIFIED., .F., .F., .F.,
 ( 4, 4 ),
 ( 4, 1, 1, 1, 1, 1, 1, 1, 1, 1, 1, 1, 1, 1, 1, 1, 1, 1, 1, 1, 1, 1, 1, 1, 1, 1, 1, 1, 1, 1, 1, 1, 4 ),
 ( -0.1039370721279000015, 1.103937072127999963 ),
 ( 0.1942321073450000157, 0.2199060843169000079, 0.2455800612886999967, 0.2712540382605999612, 0.2969280152323999777, 0.3226019922043000254, 0.3482759691761000420, 0.3739499461479999787, 0.3996239231197999953, 0.4252979000916999874, 0.4509718770635000040, 0.4766458540353999962, 0.5023198310072000128, 0.5279938079791000050, 0.5536677849509000771, 0.5793417619227999582, 0.6050157388945999193, 0.6306897158665000225, 0.6563636928382999836, 0.6820376698101999757, 0.7077116467820000478, 0.7333856237539000400, 0.7590596007256998901, 0.7847335776975999933, 0.8104075546693999543, 0.8360815316413000575, 0.8617555086131000186, 0.8874294855850000108, 0.9131034625568000829, 0.9387774395286999640, 0.9644514165004999251, 0.9901253934722999972, 1.015799370444000038 ),
 .UNSPECIFIED. ) ;
#54200=CARTESIAN_POINT ( 'NONE',  ( 8.496698341230001006, 5.198556077301000222, 8.332552905512999430 ) ) ;
#54201=CARTESIAN_POINT ( 'NONE',  ( 9.691082467489000152, 5.335647408863999352, 8.701220655673999715 ) ) ;
#54203=ORIENTED_EDGE ( 'NONE', *, *, #33056, .T. ) ;
#54207=ADVANCED_FACE ( 'NONE', ( #47358 ), #63377, .F. ) ;
#54209=CARTESIAN_POINT ( 'NONE',  ( 10.29667028040999988, 2.755514216060999999, -6.622437150225000124 ) ) ;
#54211=CARTESIAN_POINT ( 'NONE',  ( 7.875072778631000858, 5.143389081112999861, 6.784077933858997156 ) ) ;
#54216=FACE_OUTER_BOUND ( 'NONE', #4549, .T. ) ;
#54227=DIRECTION ( 'NONE',  ( 0.000000000000000000, 0.2461538461537955413, -0.9692307692307821076 ) ) ;
#54232=CARTESIAN_POINT ( 'NONE',  ( 9.532678149083000818, 4.663044775770000427, 8.669813205957000335 ) ) ;
#54240=ORIENTED_EDGE ( 'NONE', *, *, #29774, .T. ) ;
#54241=CARTESIAN_POINT ( 'NONE',  ( 7.477183612850018868, 2.357857793230528465, 6.915030216468147195 ) ) ;
#54247=ORIENTED_EDGE ( 'NONE', *, *, #58785, .F. ) ;
#54250=CARTESIAN_POINT ( 'NONE',  ( 8.410398127216504705, 5.351350780489198655, 7.263115598813870477 ) ) ;
#54254=DIRECTION ( 'NONE',  ( -1.000000000000000000, 0.000000000000000000, 0.000000000000000000 ) ) ;
#54256=EDGE_CURVE ( 'NONE', #19885, #47743, #55672, .T. ) ;
#54258=DIRECTION ( 'NONE',  ( -1.000000000000000000, 0.000000000000000000, 0.000000000000000000 ) ) ;
#54260=CARTESIAN_POINT ( 'NONE',  ( 8.771960841230001193, 3.061731693614000438, -8.535706278603999664 ) ) ;
#54262=CIRCLE ( 'NONE', #45353, 12.39999890530000037 ) ;
#54263=CARTESIAN_POINT ( 'NONE',  ( 10.05205635875000070, 2.669891600604999748, -8.791543746052999708 ) ) ;
#54264=SURFACE_STYLE_USAGE ( .BOTH. , #37845 ) ;
#54273=CARTESIAN_POINT ( 'NONE',  ( 10.27164068750306569, 2.873222873834239799, 6.752018918838213146 ) ) ;
#54276=CARTESIAN_POINT ( 'NONE',  ( 7.132090560819000835, 2.788803157567000035, -8.345558963038001821 ) ) ;
#54280=CARTESIAN_POINT ( 'NONE',  ( 8.830545280412000153, 3.207599814920999659, -6.150466394809999571 ) ) ;
#54281=CARTESIAN_POINT ( 'NONE',  ( 10.97807333593999957, 5.235090452703000885, -6.783100406990000053 ) ) ;
#54283=ORIENTED_EDGE ( 'NONE', *, *, #5982, .F. ) ;
#54285=CARTESIAN_POINT ( 'NONE',  ( 11.05568736158000043, 5.199900061860000200, -4.877315744757000360 ) ) ;
#54289=DIRECTION ( 'NONE',  ( -0.8660254017593186360, 3.394428858350072688E-12, -0.5000000035076106464 ) ) ;
#54295=CARTESIAN_POINT ( 'NONE',  ( 8.455555256449757806, 5.100005072561971886, -6.567582415677733820 ) ) ;
#54298=VECTOR ( 'NONE', #54429, 1000.000000000000000 ) ;
#54307=B_SPLINE_CURVE_WITH_KNOTS ( 'NONE', 3,
 ( #64227, #16344, #15661, #47482 ),
 .UNSPECIFIED., .F., .F.,
 ( 4, 4 ),
 ( 0.000000000000000000, 1.000000000000000000 ),
 .UNSPECIFIED. ) ;
#54313=CARTESIAN_POINT ( 'NONE',  ( 7.000000000000000000, 6.255435840762999966, 3.000000000000000000 ) ) ;
#54314=CARTESIAN_POINT ( 'NONE',  ( 9.906851002540999929, 2.832432432432000269, -6.822293592207000934 ) ) ;
#54317=CARTESIAN_POINT ( 'NONE',  ( 6.433333127195900225, 12.43895222601181771, -2.828919834973015579 ) ) ;
#54320=ORIENTED_EDGE ( 'NONE', *, *, #18274, .F. ) ;
#54326=CARTESIAN_POINT ( 'NONE',  ( 7.000000000000000000, 9.782049358651168092, 4.603971795490571672 ) ) ;
#54334=CARTESIAN_POINT ( 'NONE',  ( 9.459729719592999686, 2.527713920559999661, -6.969421869128999525 ) ) ;
#54335=VERTEX_POINT ( 'NONE', #62909 ) ;
#54338=CARTESIAN_POINT ( 'NONE',  ( 7.613660841224000109, 2.100129367691999871, -7.493434492293999938 ) ) ;
#54340=CARTESIAN_POINT ( 'NONE',  ( 9.450685262603977677, 5.278039455209302844, 7.934618797907818433 ) ) ;
#54346=CARTESIAN_POINT ( 'NONE',  ( 10.91943903453000075, 3.268382602297999817, -6.413946631105000407 ) ) ;
#54350=DIRECTION ( 'NONE',  ( 0.000000000000000000, 0.2461538461537955413, -0.9692307692307821076 ) ) ;
#54352=CARTESIAN_POINT ( 'NONE',  ( 7.857643339617994549, 5.082727619679005215, -6.471061634085996772 ) ) ;
#54355=CARTESIAN_POINT ( 'NONE',  ( 7.279117636432513194, 2.756047754360720692, -8.107296174373129105 ) ) ;
#54356=AXIS2_PLACEMENT_3D ( 'NONE', #29237, #60346, #55103 ) ;
#54361=VERTEX_POINT ( 'NONE', #10128 ) ;
#54363=CARTESIAN_POINT ( 'NONE',  ( 11.05392028041000074, 5.159483628325999938, -8.487146968478000986 ) ) ;
#54370=VERTEX_POINT ( 'NONE', #31460 ) ;
#54371=ORIENTED_EDGE ( 'NONE', *, *, #3137, .F. ) ;
#54372=AXIS2_PLACEMENT_3D ( 'NONE', #15043, #19608, #68513 ) ;
#54373=CARTESIAN_POINT ( 'NONE',  ( 9.799251915619999309, 4.057329420971000467, 9.430703183047999261 ) ) ;
#54378=ADVANCED_FACE ( 'NONE', ( #4873 ), #26215, .T. ) ;
#54381=DIRECTION ( 'NONE',  ( 1.000000000000000000, 0.000000000000000000, 0.000000000000000000 ) ) ;
#54386=CARTESIAN_POINT ( 'NONE',  ( 7.492075307187761268, 4.829186685176425797, -6.421019192411952403 ) ) ;
#54387=CARTESIAN_POINT ( 'NONE',  ( 8.725683545309856015, 2.905353685799620500, -6.303952321520784885 ) ) ;
#54393=CARTESIAN_POINT ( 'NONE',  ( 9.136065740934069979, 5.315322084245146961, -7.853657639600751139 ) ) ;
#54394=CARTESIAN_POINT ( 'NONE',  ( 8.365779719592000063, 2.949305648881000330, -8.659807625323999503 ) ) ;
#54399=CARTESIAN_POINT ( 'NONE',  ( 0.7162272458363000416, -2.757152670777000214, 2.469952924947999673 ) ) ;
#54403=CARTESIAN_POINT ( 'NONE',  ( 10.06949528041000086, 4.910370880657999315, -8.649591080567999413 ) ) ;
#54410=CARTESIAN_POINT ( 'NONE',  ( 8.951357780412001475, 2.821863697211000055, 6.127145479358000024 ) ) ;
#54413=CARTESIAN_POINT ( 'NONE',  ( 8.543670280408999673, 5.311932732455999506, -8.353077699453999472 ) ) ;
#54415=CARTESIAN_POINT ( 'NONE',  ( 10.39709268726349300, 5.286023823538134714, 7.026709681657270501 ) ) ;
#54429=DIRECTION ( 'NONE',  ( 0.9999999999999682476, -2.518940175903920502E-07, 2.686332970438915230E-09 ) ) ;
#54432=CARTESIAN_POINT ( 'NONE',  ( 8.192489158772998437, 2.550241116032999855, 7.666973618349000041 ) ) ;
#54434=DIRECTION ( 'NONE',  ( 1.000000000000000000, 0.000000000000000000, 7.549516567300000767E-14 ) ) ;
#54436=CARTESIAN_POINT ( 'NONE',  ( 11.07128326594000001, 5.551436772566000322, -5.077701490514000326 ) ) ;
#54450=ORIENTED_EDGE ( 'NONE', *, *, #6168, .F. ) ;
#54453=CARTESIAN_POINT ( 'NONE',  ( 9.793039158772000263, 5.817107086401000160, -6.945352709928000579 ) ) ;
#54454=CARTESIAN_POINT ( 'NONE',  ( 9.882903428397000312, 4.314559027837000293, -9.161039561412001930 ) ) ;
#54457=CARTESIAN_POINT ( 'NONE',  ( 11.04384236319999957, 7.001054331151000731, -5.879104662970000561 ) ) ;
#54458=CARTESIAN_POINT ( 'NONE',  ( 5.500000000000000000, -12.43893545635000031, 2.828937028792000152 ) ) ;
#54461=AXIS2_PLACEMENT_3D ( 'NONE', #68993, #36493, #5365 ) ;
#54463=CARTESIAN_POINT ( 'NONE',  ( 10.27815081430999911, 5.521603098753999461, 8.751228458888000716 ) ) ;
#54470=DIRECTION ( 'NONE',  ( 1.000000000000000000, 0.000000000000000000, 0.000000000000000000 ) ) ;
#54476=CARTESIAN_POINT ( 'NONE',  ( 8.970860841232001448, 4.131080973160000447, -6.108642999115999395 ) ) ;
#54479=CARTESIAN_POINT ( 'NONE',  ( 11.09999999999999964, 5.299999999999999822, -5.160242713806000303 ) ) ;
#54483=CARTESIAN_POINT ( 'NONE',  ( 7.410857780409000561, 2.302289264429000504, 6.875166305059000393 ) ) ;
#54485=CARTESIAN_POINT ( 'NONE',  ( 9.649770280412001355, 4.042991257420999851, -5.768106221333000327 ) ) ;
#54488=ORIENTED_EDGE ( 'NONE', *, *, #31012, .F. ) ;
#54489=CARTESIAN_POINT ( 'NONE',  ( 10.39106065309000115, 4.025321035224999733, 9.261125884460000179 ) ) ;
#54493=CARTESIAN_POINT ( 'NONE',  ( 7.654876518126000562, 2.928962009306002479, 6.518628166992000317 ) ) ;
#54494=VERTEX_POINT ( 'NONE', #1939 ) ;
#54508=ORIENTED_EDGE ( 'NONE', *, *, #45395, .T. ) ;
#54509=B_SPLINE_CURVE_WITH_KNOTS ( 'NONE', 3,
 ( #52818, #68535, #5260, #41983 ),
 .UNSPECIFIED., .F., .F.,
 ( 4, 4 ),
 ( 0.000000000000000000, 1.000000000000000000 ),
 .UNSPECIFIED. ) ;
#54510=CARTESIAN_POINT ( 'NONE',  ( 8.324914158772999784, 2.633142096252999664, -7.791134854666999843 ) ) ;
#54519=ORIENTED_EDGE ( 'NONE', *, *, #26611, .T. ) ;
#54531=EDGE_CURVE ( 'NONE', #52043, #51187, #34032, .T. ) ;
#54535=EDGE_CURVE ( 'NONE', #6526, #10927, #4036, .T. ) ;
#54536=EDGE_CURVE ( 'NONE', #3005, #25668, #56551, .T. ) ;
#54537=CARTESIAN_POINT ( 'NONE',  ( 8.508079719592000600, 2.202812441249000219, 7.706988150133999405 ) ) ;
#54541=CARTESIAN_POINT ( 'NONE',  ( 7.131839088562530016, 3.481695193657420084, 8.754754956630815599 ) ) ;
#54545=CARTESIAN_POINT ( 'NONE',  ( 9.442843574488000158, 2.691255504502000129, 6.269523028052000235 ) ) ;
#54552=EDGE_CURVE ( 'NONE', #56890, #57674, #29560, .T. ) ;
#54557=CARTESIAN_POINT ( 'NONE',  ( 9.433107780409999421, 4.954905351382000944, 8.825777580285999235 ) ) ;
#54561=ORIENTED_EDGE ( 'NONE', *, *, #19798, .F. ) ;
#54562=CARTESIAN_POINT ( 'NONE',  ( 8.239948341229000661, 2.735218126362000124, 6.771983639047999937 ) ) ;
#54566=CARTESIAN_POINT ( 'NONE',  ( 8.298061260823001106, 5.118905885020002877, 6.382684838875003486 ) ) ;
#54567=LINE ( 'NONE', #11556, #60746 ) ;
#54570=EDGE_LOOP ( 'NONE', ( #43812, #22061, #8484, #30676 ) ) ;
#54571=CARTESIAN_POINT ( 'NONE',  ( 2.211430836446000026, -0.2901351235585999944, -3.413359411422000278 ) ) ;
#54572=DIRECTION ( 'NONE',  ( 1.000000000000000000, 0.000000000000000000, 7.697546303983999388E-14 ) ) ;
#54576=CARTESIAN_POINT ( 'NONE',  ( 10.01835931249159906, 5.126777126174925314, -6.752018918854003182 ) ) ;
#54577=EDGE_CURVE ( 'NONE', #58602, #6078, #26602, .T. ) ;
#54582=ORIENTED_EDGE ( 'NONE', *, *, #12901, .T. ) ;
#54583=AXIS2_PLACEMENT_3D ( 'NONE', #47411, #46725, #15248 ) ;
#54585=CARTESIAN_POINT ( 'NONE',  ( 10.45746213570999927, 5.100000000000000533, -6.571291218949999902 ) ) ;
#54586=CARTESIAN_POINT ( 'NONE',  ( 0.7514734890462999584, -3.558193753575999985, 1.211459191638999844 ) ) ;
#54595=CARTESIAN_POINT ( 'NONE',  ( 10.90000004630000063, 9.856474695503001371, 5.627825000517000298 ) ) ;
#54598=CARTESIAN_POINT ( 'NONE',  ( 8.546960841229999772, 2.724453559418999582, -8.908010318766001134 ) ) ;
#54606=CARTESIAN_POINT ( 'NONE',  ( 9.347254965556000883, 4.028327103212000715, 9.469449669541999626 ) ) ;
#54614=EDGE_CURVE ( 'NONE', #4517, #56617, #46777, .T. ) ;
#54615=EDGE_CURVE ( 'NONE', #59469, #33299, #48256, .T. ) ;
#54619=( NAMED_UNIT ( * ) SI_UNIT ( $, .STERADIAN. ) SOLID_ANGLE_UNIT ( ) );
#54620=ORIENTED_EDGE ( 'NONE', *, *, #35220, .F. ) ;
#54630=CARTESIAN_POINT ( 'NONE',  ( 7.223909439180999037, 5.321245676936000812, -7.068438969505000280 ) ) ;
#54637=CARTESIAN_POINT ( 'NONE',  ( 9.088029719595001055, 2.881930053949999682, -8.823338183322999129 ) ) ;
#54640=B_SPLINE_CURVE_WITH_KNOTS ( 'NONE', 3,
 ( #44224, #38970, #33726, #55043, #44574, #28838 ),
 .UNSPECIFIED., .F., .F.,
 ( 4, 2, 4 ),
 ( 0.000000000000000000, 0.5000000000000000000, 1.000000000000000000 ),
 .UNSPECIFIED. ) ;
#54651=DIRECTION ( 'NONE',  ( 0.000000000000000000, -1.000000000000000000, 0.000000000000000000 ) ) ;
#54658=EDGE_CURVE ( 'NONE', #61556, #30450, #24469, .T. ) ;
#54663=CARTESIAN_POINT ( 'NONE',  ( 7.100000000000000533, 0.000000000000000000, 0.000000000000000000 ) ) ;
#54665=CARTESIAN_POINT ( 'NONE',  ( 6.999998782146999332, 11.95749337870000062, 3.642574926947999892 ) ) ;
#54666=CARTESIAN_POINT ( 'NONE',  ( 10.94076550314999885, 5.140765503144999471, -6.571291218949999902 ) ) ;
#54670=DIRECTION ( 'NONE',  ( -0.7071068207016518725, 0.000000000000000000, -0.7071067416714409415 ) ) ;
#54679=CARTESIAN_POINT ( 'NONE',  ( 10.49640421544308211, 5.348966112464498934, 7.853238477522235250 ) ) ;
#54682=FACE_OUTER_BOUND ( 'NONE', #62362, .T. ) ;
#54687=CARTESIAN_POINT ( 'NONE',  ( 9.700639158771000581, 4.262870449202000422, -8.811513791423999820 ) ) ;
#54689=CARTESIAN_POINT ( 'NONE',  ( 8.766851002546001581, 2.832432432432000269, 6.822293592207000934 ) ) ;
#54705=CARTESIAN_POINT ( 'NONE',  ( 8.005461299830001209, 5.128003005022999439, -6.747396629211001695 ) ) ;
#54713=CARTESIAN_POINT ( 'NONE',  ( 10.18308278041000037, 2.953582937013000009, -8.606284720264998356 ) ) ;
#54714=ADVANCED_FACE ( 'NONE', ( #34454 ), #29206, .F. ) ;
#54722=VERTEX_POINT ( 'NONE', #24820 ) ;
#54724=B_SPLINE_CURVE_WITH_KNOTS ( 'NONE', 3,
 ( #61001, #29200, #18360, #46302 ),
 .UNSPECIFIED., .F., .F.,
 ( 4, 4 ),
 ( 0.000000000000000000, 1.000000000000000000 ),
 .UNSPECIFIED. ) ;
#54725=CARTESIAN_POINT ( 'NONE',  ( 9.494689158774999527, 2.824732249080000202, -8.992748220058999209 ) ) ;
#54738=CARTESIAN_POINT ( 'NONE',  ( 8.585340200126335475, 5.100000000000000533, -6.496871349812457730 ) ) ;
#54740=CARTESIAN_POINT ( 'NONE',  ( 6.899999691988000450, -12.43893545635000031, -2.828937028792000152 ) ) ;
#54743=DIRECTION ( 'NONE',  ( 1.000000000000000000, 0.000000000000000000, 0.000000000000000000 ) ) ;
#54745=CARTESIAN_POINT ( 'NONE',  ( 8.356920280409999791, 4.851303550474000303, -9.008742670124000540 ) ) ;
#54748=CARTESIAN_POINT ( 'NONE',  ( 0.3705175461371000289, 3.176450105220999909, 1.136354878726999917 ) ) ;
#54750=CARTESIAN_POINT ( 'NONE',  ( 3.167476045672999785, 2.924661563963000255, 2.085714127773000470 ) ) ;
#54751=VERTEX_POINT ( 'NONE', #14676 ) ;
#54755=CARTESIAN_POINT ( 'NONE',  ( 7.229676658770999964, 2.630487280353000390, 6.995957894972000268 ) ) ;
#54758=CARTESIAN_POINT ( 'NONE',  ( 8.534810841228001266, 5.092576903264999899, -6.628615687103999399 ) ) ;
#54760=CARTESIAN_POINT ( 'NONE',  ( 4.600001223043999943, 13.10000000000000142, 0.000000000000000000 ) ) ;
#54775=CARTESIAN_POINT ( 'NONE',  ( 11.03776785110999903, 5.237767851104999650, 6.571291218949999902 ) ) ;
#54777=FACE_OUTER_BOUND ( 'NONE', #30629, .T. ) ;
#54782=CARTESIAN_POINT ( 'NONE',  ( 10.08079553769483461, 5.100000000000000533, -6.662590550628426200 ) ) ;
#54788=CARTESIAN_POINT ( 'NONE',  ( 7.192747165043829938, 3.481309508196248181, -5.716746811592346766 ) ) ;
#54798=CARTESIAN_POINT ( 'NONE',  ( 9.594139158774000364, 2.212639797530000063, -6.855876382544999537 ) ) ;
#54799=CARTESIAN_POINT ( 'NONE',  ( 3.173830139264999683, -1.787327779986999987, -2.868047506627999788 ) ) ;
#54805=EDGE_LOOP ( 'NONE', ( #21256, #40158, #57950, #1241, #23328, #16126, #50872 ) ) ;
#54809=CARTESIAN_POINT ( 'NONE',  ( 10.52638970730999901, 2.451081172664000274, 6.282749363171999946 ) ) ;
#54814=B_SPLINE_CURVE_WITH_KNOTS ( 'NONE', 3,
 ( #2813, #24143, #25519, #30096 ),
 .UNSPECIFIED., .F., .F.,
 ( 4, 4 ),
 ( 0.000000000000000000, 1.000000000000000000 ),
 .UNSPECIFIED. ) ;
#54815=CONICAL_SURFACE ( 'NONE', #48124, 1.949999999867999767, 0.7853981633972997312 ) ;
#54828=ORIENTED_EDGE ( 'NONE', *, *, #24191, .T. ) ;
#54830=CARTESIAN_POINT ( 'NONE',  ( 7.127704719590999716, 4.698356649019999942, 8.789431186081998248 ) ) ;
#54831=CARTESIAN_POINT ( 'NONE',  ( 9.740360841231000322, 4.047146749018000200, -5.600703114891000034 ) ) ;
#54835=EDGE_CURVE ( 'NONE', #33013, #2243, #21499, .T. ) ;
#54836=VERTEX_POINT ( 'NONE', #10792 ) ;
#54842=CARTESIAN_POINT ( 'NONE',  ( 8.186785374738994037, 2.888678623336002005, 6.695956381329003726 ) ) ;
#54857=CARTESIAN_POINT ( 'NONE',  ( 9.649770280412001355, 4.042991257420999851, -5.768106221333000327 ) ) ;
#54869=EDGE_LOOP ( 'NONE', ( #8330, #15363, #29084, #1583, #60657 ) ) ;
#54873=CARTESIAN_POINT ( 'NONE',  ( 10.24846228258000025, 4.234133568259999869, -5.660851473941000300 ) ) ;
#54881=CARTESIAN_POINT ( 'NONE',  ( 7.390489158771000433, 2.216873702600000051, 8.370081218683999680 ) ) ;
#54886=CARTESIAN_POINT ( 'NONE',  ( 10.36950244779999863, 2.719131864236000062, -7.031786688683999920 ) ) ;
#54889=AXIS2_PLACEMENT_3D ( 'NONE', #32774, #32431, #53748 ) ;
#54891=CARTESIAN_POINT ( 'NONE',  ( 9.905792474809000936, 2.698958900805999761, 8.979236532123000103 ) ) ;
#54894=ORIENTED_EDGE ( 'NONE', *, *, #19972, .T. ) ;
#54902=CARTESIAN_POINT ( 'NONE',  ( 8.341920280410999311, 5.601795057054999916, 7.176148573050999957 ) ) ;
#54903=CARTESIAN_POINT ( 'NONE',  ( 10.27815081430999911, 5.521603098753999461, 8.751228458888000716 ) ) ;
#54908=CARTESIAN_POINT ( 'NONE',  ( 9.674960421382234443, 2.650268802166420024, 7.499999178247376719 ) ) ;
#54909=CARTESIAN_POINT ( 'NONE',  ( 7.822787301102997581, 4.879242518472000967, 6.344068876191006012 ) ) ;
#54913=DIRECTION ( 'NONE',  ( 0.000000000000000000, 0.000000000000000000, -1.000000000000000000 ) ) ;
#54916=CARTESIAN_POINT ( 'NONE',  ( 1.210109898187999855, -0.3467249428283000201, -3.408020022541999872 ) ) ;
#54919=CARTESIAN_POINT ( 'NONE',  ( 7.000000000000000000, 7.526486366024999874, -3.526486366024999874 ) ) ;
#54920=EDGE_CURVE ( 'NONE', #4653, #38352, #67438, .T. ) ;
#54921=EDGE_CURVE ( 'NONE', #64347, #35994, #26543, .T. ) ;
#54924=DIRECTION ( 'NONE',  ( -0.7071060865236062920, -0.7071074758488062884, -8.141935074000071186E-10 ) ) ;
#54926=DIRECTION ( 'NONE',  ( 0.000000000000000000, 0.8648648648648717963, -0.5020047465136829867 ) ) ;
#54929=CARTESIAN_POINT ( 'NONE',  ( 7.645552793751999587, 8.186488560794998648, -4.631829788185999774 ) ) ;
#54930=CARTESIAN_POINT ( 'NONE',  ( 9.523148997461001741, 5.167567567567999731, -6.822293592207000934 ) ) ;
#54932=CIRCLE ( 'NONE', #50488, 12.50000000000000178 ) ;
#54933=DIRECTION ( 'NONE',  ( -0.9999999999999978906, 6.939020669836964126E-09, -6.650367360942975276E-08 ) ) ;
#54934=CARTESIAN_POINT ( 'NONE',  ( 0.5130637418424000007, 3.696170276785000208, -0.6823948523853999859 ) ) ;
#54935=CARTESIAN_POINT ( 'NONE',  ( 10.82336322478654544, 2.820284244472439195, -8.179952785015741412 ) ) ;
#54936=CARTESIAN_POINT ( 'NONE',  ( 6.899999691988000450, 11.00717859340000082, -1.432487142323000118 ) ) ;
#54937=CARTESIAN_POINT ( 'NONE',  ( 9.848259964010999568, 4.436917881843999822, 6.148031614254000132 ) ) ;
#54940=DIRECTION ( 'NONE',  ( 0.000000000000000000, 0.8648648648648717963, 0.5020047465136829867 ) ) ;
#54943=CARTESIAN_POINT ( 'NONE',  ( 9.615109647822677630, 5.349900357012234764, -7.499993490198826329 ) ) ;
#54947=EDGE_LOOP ( 'NONE', ( #48122, #58553, #41376, #42205, #20129 ) ) ;
#54949=B_SPLINE_CURVE_WITH_KNOTS ( 'NONE', 3,
 ( #28807, #18647, #2558, #7456 ),
 .UNSPECIFIED., .F., .F.,
 ( 4, 4 ),
 ( 0.000000000000000000, 1.000000000000000000 ),
 .UNSPECIFIED. ) ;
#54951=ORIENTED_EDGE ( 'NONE', *, *, #51300, .F. ) ;
#54955=CARTESIAN_POINT ( 'NONE',  ( 9.504903297738000134, 3.934733353759999552, 5.704831249548000471 ) ) ;
#54960=DIRECTION ( 'NONE',  ( 0.000000000000000000, 0.8648648261949251070, 0.5020048131351152465 ) ) ;
#54962=ORIENTED_EDGE ( 'NONE', *, *, #741, .F. ) ;
#54964=AXIS2_PLACEMENT_3D ( 'NONE', #22441, #65078, #42405 ) ;
#54973=ORIENTED_EDGE ( 'NONE', *, *, #41319, .F. ) ;
#54979=CARTESIAN_POINT ( 'NONE',  ( 7.009409439180999790, 2.534482666265000184, -7.314862106114000007 ) ) ;
#54984=CARTESIAN_POINT ( 'NONE',  ( 9.526695280414001488, 5.462898983065000102, -8.055936939571999744 ) ) ;
#54988=CARTESIAN_POINT ( 'NONE',  ( 8.273285508597860272, 2.795069959664616022, -8.205047406324164072 ) ) ;
#54992=DIRECTION ( 'NONE',  ( 0.000000000000000000, -1.000000000000000000, 0.000000000000000000 ) ) ;
#55006=DIRECTION ( 'NONE',  ( 1.000000000000000000, 0.000000000000000000, 0.000000000000000000 ) ) ;
#55015=CARTESIAN_POINT ( 'NONE',  ( 7.000000000000000000, 6.495985883990673670, 3.000000000000000000 ) ) ;
#55019=CARTESIAN_POINT ( 'NONE',  ( 10.98768472639999949, 5.139099012905000485, 4.945212061661000469 ) ) ;
#55022=EDGE_LOOP ( 'NONE', ( #11333, #53312, #41029, #2585 ) ) ;
#55023=DIRECTION ( 'NONE',  ( 1.000000000000000000, 0.000000000000000000, -7.105427357580000488E-14 ) ) ;
#55025=CARTESIAN_POINT ( 'NONE',  ( 8.296584986412122831, 4.202841942069439618, 6.085974839126271796 ) ) ;
#55027=EDGE_CURVE ( 'NONE', #26858, #12749, #23359, .T. ) ;
#55034=ORIENTED_EDGE ( 'NONE', *, *, #51190, .F. ) ;
#55037=CARTESIAN_POINT ( 'NONE',  ( 8.324914158772999784, 2.633142096252999664, -7.791134854666999843 ) ) ;
#55043=CARTESIAN_POINT ( 'NONE',  ( 8.384365347816494562, 4.198915299351829056, -6.035294823839894462 ) ) ;
#55045=CARTESIAN_POINT ( 'NONE',  ( 8.798539158775000146, 5.851083642416999631, -7.072167224702999633 ) ) ;
#55047=CARTESIAN_POINT ( 'NONE',  ( 9.675534850247000662, 4.656736118461000551, -8.653212384786000300 ) ) ;
#55048=CARTESIAN_POINT ( 'NONE',  ( 9.064883232718324635, 5.349954811645839747, -7.500006748065883855 ) ) ;
#55053=CARTESIAN_POINT ( 'NONE',  ( 8.406851002545000284, 2.832432432432000269, -6.822293592207000934 ) ) ;
#55054=CARTESIAN_POINT ( 'NONE',  ( 0.000000000000000000, 0.000000000000000000, 0.000000000000000000 ) ) ;
#55055=EDGE_CURVE ( 'NONE', #6078, #39994, #45379, .T. ) ;
#55059=ORIENTED_EDGE ( 'NONE', *, *, #32798, .F. ) ;
#55061=CARTESIAN_POINT ( 'NONE',  ( 9.978904719591000116, 5.007782080444000528, -8.772599239991000886 ) ) ;
#55070=ORIENTED_EDGE ( 'NONE', *, *, #3137, .T. ) ;
#55071=CARTESIAN_POINT ( 'NONE',  ( 9.436104719595000745, 5.619431609641999614, -8.115423117607999615 ) ) ;
#55090=CARTESIAN_POINT ( 'NONE',  ( 8.465229719592999302, 2.567871051582000241, -6.869011921437000012 ) ) ;
#55095=B_SPLINE_CURVE_WITH_KNOTS ( 'NONE', 3,
 ( #2960, #62034, #13808, #45959 ),
 .UNSPECIFIED., .F., .F.,
 ( 4, 4 ),
 ( 0.000000000000000000, 1.000000000000000000 ),
 .UNSPECIFIED. ) ;
#55099=CARTESIAN_POINT ( 'NONE',  ( 2.166155107414999836, 2.958863020030999991, 2.036875221550000337 ) ) ;
#55103=DIRECTION ( 'NONE',  ( 0.000000000000000000, -1.000000000000000000, 0.000000000000000000 ) ) ;
#55104=CARTESIAN_POINT ( 'NONE',  ( 8.822982780412001347, 2.678331728353000152, 8.735281589464001684 ) ) ;
#55107=CARTESIAN_POINT ( 'NONE',  ( 10.94037390526893283, 9.311283358094208040, 6.235718259152663201 ) ) ;
#55112=ORIENTED_EDGE ( 'NONE', *, *, #48446, .F. ) ;
#55115=VERTEX_POINT ( 'NONE', #67029 ) ;
#55122=DIRECTION ( 'NONE',  ( 0.9999999999997695177, 3.376118495992897870E-07, 5.889958325272817302E-07 ) ) ;
#55124=CARTESIAN_POINT ( 'NONE',  ( 8.202894943314811727, 2.713916317890099794, 7.026332083725589150 ) ) ;
#55126=ORIENTED_EDGE ( 'NONE', *, *, #6941, .T. ) ;
#55134=AXIS2_PLACEMENT_3D ( 'NONE', #69075, #26435, #20841 ) ;
#55135=CARTESIAN_POINT ( 'NONE',  ( 10.90000000000000036, 5.167567567567999731, 6.822293592207000934 ) ) ;
#55136=CARTESIAN_POINT ( 'NONE',  ( 10.91281046606773231, 2.900003320670894169, -5.078864280888942595 ) ) ;
#55137=CARTESIAN_POINT ( 'NONE',  ( 5.000030787343000327, -1.290525307673963340, 1.679270695423618953 ) ) ;
#55146=CARTESIAN_POINT ( 'NONE',  ( 3.509165847083000056, -1.664658919160000083, 2.940974452548000162 ) ) ;
#55148=CARTESIAN_POINT ( 'NONE',  ( 10.66052890781999984, 2.899999999999999911, -6.152188490330000370 ) ) ;
#55149=CARTESIAN_POINT ( 'NONE',  ( 9.580795537697435194, 5.100000000000000533, -6.662590550605531625 ) ) ;
#55152=CARTESIAN_POINT ( 'NONE',  ( 1.931500749193666655, 0.2450796643850099987, -3.507702501826547081 ) ) ;
#55154=CARTESIAN_POINT ( 'NONE',  ( 9.882259685352000389, 4.932708901218999742, 6.390989635557000170 ) ) ;
#55155=CARTESIAN_POINT ( 'NONE',  ( 10.90000000164000049, 5.100000000007000267, 5.160242739040000082 ) ) ;
#55158=LINE ( 'NONE', #65980, #45137 ) ;
#55159=VECTOR ( 'NONE', #65629, 999.9999999999998863 ) ;
#55161=CARTESIAN_POINT ( 'NONE',  ( 10.21106069398042315, 5.731338304127999272, 7.738475558447463598 ) ) ;
#55164=CARTESIAN_POINT ( 'NONE',  ( 8.113036307363870492, 5.051611909519712285, -6.499327669147922037 ) ) ;
#55175=CARTESIAN_POINT ( 'NONE',  ( 9.250899447075999760, 4.135077451221000011, 9.175524215473998879 ) ) ;
#55176=CARTESIAN_POINT ( 'NONE',  ( 8.696135841231001251, 3.038023536984999939, -5.861661709981000001 ) ) ;
#55178=CARTESIAN_POINT ( 'NONE',  ( 3.494875605349273773, -2.878717222751967064, 1.196277934611101879 ) ) ;
#55180=CARTESIAN_POINT ( 'NONE',  ( 9.687870098586998324, 5.912263966150999472, 7.772301113561999486 ) ) ;
#55184=CARTESIAN_POINT ( 'NONE',  ( 7.762706781754004304, 3.200128145701000904, 6.302820412756005020 ) ) ;
#55190=EDGE_CURVE ( 'NONE', #29277, #34148, #712, .T. ) ;
#55191=B_SPLINE_CURVE_WITH_KNOTS ( 'NONE', 3,
 ( #10047, #25787, #31384, #37992, #52696, #42901, #31728, #47118 ),
 .UNSPECIFIED., .F., .F.,
 ( 4, 1, 1, 1, 1, 4 ),
 ( 0.000000000000000000, 0.2000000000000000111, 0.4000000000000000222, 0.5999999999999999778, 0.8000000000000000444, 1.000000000000000000 ),
 .UNSPECIFIED. ) ;
#55204=CARTESIAN_POINT ( 'NONE',  ( 9.600045280412000892, 3.021734963141999852, -6.070209284876999511 ) ) ;
#55211=ORIENTED_EDGE ( 'NONE', *, *, #38430, .T. ) ;
#55219=CARTESIAN_POINT ( 'NONE',  ( 10.52343057594999998, 3.209665745824000105, -9.177097971982000502 ) ) ;
#55224=CARTESIAN_POINT ( 'NONE',  ( 5.000000000000000000, 0.2999999999999999889, -3.149999999999999911 ) ) ;
#55226=CARTESIAN_POINT ( 'NONE',  ( 8.572267219592999865, 2.606995215518000286, 6.345762205468999717 ) ) ;
#55227=VERTEX_POINT ( 'NONE', #40808 ) ;
#55231=CARTESIAN_POINT ( 'NONE',  ( 11.24053267693000002, 2.774035422596999645, 6.782113650547000105 ) ) ;
#55233=VECTOR ( 'NONE', #36463, 999.9999999999998863 ) ;
#55235=EDGE_CURVE ( 'NONE', #42164, #53044, #1448, .T. ) ;
#55238=CARTESIAN_POINT ( 'NONE',  ( 9.305881816721999655, 4.945299866898000829, 9.077891794505999812 ) ) ;
#55243=B_SPLINE_CURVE_WITH_KNOTS ( 'NONE', 3,
 ( #38584, #22496, #51070, #44197 ),
 .UNSPECIFIED., .F., .F.,
 ( 4, 4 ),
 ( 0.000000000000000000, 1.000000000000000000 ),
 .UNSPECIFIED. ) ;
#55246=VECTOR ( 'NONE', #59330, 1000.000000000000114 ) ;
#55251=CARTESIAN_POINT ( 'NONE',  ( 7.892607780408998686, 5.480308727866000318, 8.192324747680999053 ) ) ;
#55252=CARTESIAN_POINT ( 'NONE',  ( 5.000000000000000000, -1.382741116750999977, 11.26545724788999969 ) ) ;
#55258=EDGE_CURVE ( 'NONE', #32335, #16280, #40573, .T. ) ;
#55266=CARTESIAN_POINT ( 'NONE',  ( 1.591565493715000112, -3.424908732075000017, 0.06941761548046999908 ) ) ;
#55273=CARTESIAN_POINT ( 'NONE',  ( 10.89182487123000165, 2.946653980248000071, 5.014777219802000197 ) ) ;
#55274=CARTESIAN_POINT ( 'NONE',  ( 11.09999999999999964, 5.350000000000000533, -7.500000000000000000 ) ) ;
#55277=CARTESIAN_POINT ( 'NONE',  ( 6.992001042874380623, 4.037115771921000018, -6.023232697733999608 ) ) ;
#55281=CARTESIAN_POINT ( 'NONE',  ( 1.895840275625999771, -0.3183524953527000489, -3.745328979271999703 ) ) ;
#55282=EDGE_LOOP ( 'NONE', ( #57620, #37377, #21658, #16445 ) ) ;
#55283=FACE_OUTER_BOUND ( 'NONE', #11025, .T. ) ;
#55285=DIRECTION ( 'NONE',  ( 0.000000000000000000, 0.9916377111174248249, -0.1290528957048032721 ) ) ;
#55292=CARTESIAN_POINT ( 'NONE',  ( 9.432072800716166938, 10.28058112649079803, 4.885051702730572210 ) ) ;
#55301=CARTESIAN_POINT ( 'NONE',  ( 4.149992563292000725, 1.599290730647370484, -1.229060429538527899 ) ) ;
#55308=CARTESIAN_POINT ( 'NONE',  ( 4.000000000000000000, -0.2816038378556623978, -2.149891155406186805 ) ) ;
#55312=CARTESIAN_POINT ( 'NONE',  ( 10.90000000011000125, 5.100000000110999743, 6.571291220762999430 ) ) ;
#55320=ORIENTED_EDGE ( 'NONE', *, *, #33756, .F. ) ;
#55325=CARTESIAN_POINT ( 'NONE',  ( 0.000000000000000000, 0.000000000000000000, 0.000000000000000000 ) ) ;
#55329=CARTESIAN_POINT ( 'NONE',  ( 9.029445280412998542, 5.442817578555000146, -8.106149115450000053 ) ) ;
#55332=CARTESIAN_POINT ( 'NONE',  ( 10.59999999999999964, 4.599999999999999645, -4.756097560976000338 ) ) ;
#55338=CARTESIAN_POINT ( 'NONE',  ( 1.198890132541874598, -2.798833948393640192, 2.150913519912191152 ) ) ;
#55351=FACE_OUTER_BOUND ( 'NONE', #16227, .T. ) ;
#55355=VECTOR ( 'NONE', #16086, 1000.000000000000000 ) ;
#55359=EDGE_CURVE ( 'NONE', #66683, #37746, #63084, .T. ) ;
#55360=CARTESIAN_POINT ( 'NONE',  ( 7.000000000000000000, 10.80467228076000019, -3.475853456584999890 ) ) ;
#55375=VERTEX_POINT ( 'NONE', #32397 ) ;
#55379=CARTESIAN_POINT ( 'NONE',  ( 8.115081613917173087, 5.350113345104855256, -7.499995474391613293 ) ) ;
#55381=AXIS2_PLACEMENT_3D ( 'NONE', #49892, #12144, #11439 ) ;
#55382=CARTESIAN_POINT ( 'NONE',  ( 8.323770280408998801, 5.332332124071999857, -8.487089944253000340 ) ) ;
#55383=B_SPLINE_CURVE_WITH_KNOTS ( 'NONE', 3,
 ( #60987, #2595, #56084, #57362, #55398, #2939, #44582, #13452, #65530, #23577 ),
 .UNSPECIFIED., .F., .F.,
 ( 4, 2, 2, 2, 4 ),
 ( 0.000000000000000000, 0.2500000000000001665, 0.3750000000000004996, 0.5000000000000007772, 1.000000000000000000 ),
 .UNSPECIFIED. ) ;
#55391=CARTESIAN_POINT ( 'NONE',  ( 9.146614158775999925, 2.981992329588000423, -5.895876591910999664 ) ) ;
#55392=ORIENTED_EDGE ( 'NONE', *, *, #55579, .T. ) ;
#55393=CARTESIAN_POINT ( 'NONE',  ( 10.33022126302999943, 2.650190549566000087, -7.694579890082000162 ) ) ;
#55398=CARTESIAN_POINT ( 'NONE',  ( 10.99284065376738795, 5.922215992749499058, -5.009257842713325637 ) ) ;
#55401=ADVANCED_FACE ( 'NONE', ( #64872 ), #63499, .F. ) ;
#55403=B_SPLINE_CURVE_WITH_KNOTS ( 'NONE', 3,
 ( #13823, #24305, #30251, #40382 ),
 .UNSPECIFIED., .F., .F.,
 ( 4, 4 ),
 ( 0.000000000000000000, 0.1254282067584606419 ),
 .UNSPECIFIED. ) ;
#55405=EDGE_CURVE ( 'NONE', #27697, #31394, #21542, .T. ) ;
#55410=CARTESIAN_POINT ( 'NONE',  ( 10.77401721959000014, 3.826866801954999620, -5.823193568970000733 ) ) ;
#55413=DIRECTION ( 'NONE',  ( 1.000000000000000000, 0.000000000000000000, 0.000000000000000000 ) ) ;
#55420=CARTESIAN_POINT ( 'NONE',  ( 9.693589158772999426, 4.047146749018000200, -5.600703114891000034 ) ) ;
#55424=CARTESIAN_POINT ( 'NONE',  ( 8.348093183609000434, 4.599999999999999645, -6.056236567608999977 ) ) ;
#55425=EDGE_CURVE ( 'NONE', #44911, #31943, #65781, .T. ) ;
#55431=ORIENTED_EDGE ( 'NONE', *, *, #9311, .T. ) ;
#55432=CARTESIAN_POINT ( 'NONE',  ( 8.455992358763001704, 3.399999999999999911, -6.571291218977999726 ) ) ;
#55437=EDGE_LOOP ( 'NONE', ( #15014, #54025, #2390, #3644 ) ) ;
#55440=CARTESIAN_POINT ( 'NONE',  ( 8.813304719595000947, 3.880154689736000417, -9.060377011187000562 ) ) ;
#55445=CARTESIAN_POINT ( 'NONE',  ( 9.447419570353266849, 2.249047413870973067, 7.566365124139655229 ) ) ;
#55446=CARTESIAN_POINT ( 'NONE',  ( 2.447473465997000108, -3.391161957165999663, 0.4846026218182000189 ) ) ;
#55452=CARTESIAN_POINT ( 'NONE',  ( 8.887170280412000523, 2.193665972875999959, 7.400591513898000073 ) ) ;
#55455=CARTESIAN_POINT ( 'NONE',  ( 7.092785841229000354, 5.307493345713999666, -7.572367724995999971 ) ) ;
#55460=AXIS2_PLACEMENT_3D ( 'NONE', #49526, #43604, #18071 ) ;
#55468=CARTESIAN_POINT ( 'NONE',  ( 10.92476424391678869, 9.558588620194553798, -6.023462398105898785 ) ) ;
#55469=CARTESIAN_POINT ( 'NONE',  ( 8.287602312370099256, 2.892084006030188892, 6.689538372556729229 ) ) ;
#55470=CARTESIAN_POINT ( 'NONE',  ( 8.087764158769999767, 5.395910762051999932, -7.432402852051000153 ) ) ;
#55474=VERTEX_POINT ( 'NONE', #5471 ) ;
#55475=PLANE ( 'NONE',  #14214 ) ;
#55477=CARTESIAN_POINT ( 'NONE',  ( 10.90000000000000036, 2.399999999999999911, -6.571291218949999902 ) ) ;
#55482=CARTESIAN_POINT ( 'NONE',  ( 10.92292961924958128, 2.909845827876722968, 5.014592305248326554 ) ) ;
#55483=CARTESIAN_POINT ( 'NONE',  ( 8.236972165045003180, 4.500178187997065038, -5.711464360401827811 ) ) ;
#55487=EDGE_CURVE ( 'NONE', #52776, #3577, #23113, .T. ) ;
#55490=ORIENTED_EDGE ( 'NONE', *, *, #37551, .T. ) ;
#55493=CARTESIAN_POINT ( 'NONE',  ( 0.1499942179679999987, -2.199046806507074070, 1.689975037551095127 ) ) ;
#55494=CARTESIAN_POINT ( 'NONE',  ( 8.947714158774999760, 3.854507394315999758, -9.394302886912999639 ) ) ;
#55495=CARTESIAN_POINT ( 'NONE',  ( 3.592999774037999750, -3.226682447671000098, 0.007234183023254000221 ) ) ;
#55501=DIRECTION ( 'NONE',  ( 0.000000000000000000, -0.8648648648648720183, -0.5020047465136825426 ) ) ;
#55503=CARTESIAN_POINT ( 'NONE',  ( 10.53138775541999905, 5.607751175212000838, 7.280102404048999887 ) ) ;
#55507=DIRECTION ( 'NONE',  ( 1.000000000000000000, 0.000000000000000000, 1.099503168979000057E-13 ) ) ;
#55511=CARTESIAN_POINT ( 'NONE',  ( 10.96503493446309285, 2.823010900888289765, -6.672616844255583324 ) ) ;
#55516=CARTESIAN_POINT ( 'NONE',  ( 10.34939834122999969, 2.653159779809000085, -7.312415497503999440 ) ) ;
#55517=EDGE_LOOP ( 'NONE', ( #28556, #18396, #60370, #7831 ) ) ;
#55518=CARTESIAN_POINT ( 'NONE',  ( 9.957462135714001406, 5.100000000000000533, -6.571291218949999902 ) ) ;
#55522=VERTEX_POINT ( 'NONE', #10367 ) ;
#55525=CARTESIAN_POINT ( 'NONE',  ( 9.342560841233000346, 5.835196551504000517, -7.008466539623000813 ) ) ;
#55526=CARTESIAN_POINT ( 'NONE',  ( 0.5412046677623798541, 3.514844065040157339, -0.4091116460506022956 ) ) ;
#55528=ORIENTED_EDGE ( 'NONE', *, *, #3297, .F. ) ;
#55531=CARTESIAN_POINT ( 'NONE',  ( 9.945533384955998812, 2.906048475816000121, 8.880389653997999844 ) ) ;
#55537=CARTESIAN_POINT ( 'NONE',  ( 8.325004567511003373, 2.868524053507002236, 6.316175840085996640 ) ) ;
#55548=ORIENTED_EDGE ( 'NONE', *, *, #17346, .F. ) ;
#55550=ORIENTED_EDGE ( 'NONE', *, *, #28601, .F. ) ;
#55552=CARTESIAN_POINT ( 'NONE',  ( 9.839810841229999383, 5.817107086401000160, -6.945352709928000579 ) ) ;
#55578=CARTESIAN_POINT ( 'NONE',  ( 8.674239158774001979, 5.983047240001000411, 7.440798119034999658 ) ) ;
#55579=EDGE_CURVE ( 'NONE', #115, #57225, #59048, .T. ) ;
#55582=CARTESIAN_POINT ( 'NONE',  ( 7.366321766359212653, 4.272452671693901749, 6.150367080941864018 ) ) ;
#55586=CARTESIAN_POINT ( 'NONE',  ( 10.15403136780999915, 5.267988602993999514, 5.992335067371000079 ) ) ;
#55587=CIRCLE ( 'NONE', #35476, 12.39999890530000037 ) ;
#55593=CARTESIAN_POINT ( 'NONE',  ( 10.62793268324000096, 3.100586971929999880, 8.599896650316999569 ) ) ;
#55596=EDGE_CURVE ( 'NONE', #19885, #24902, #15561, .T. ) ;
#55599=CARTESIAN_POINT ( 'NONE',  ( 8.058767219590999176, 2.432118421226999949, 6.597517552098000060 ) ) ;
#55600=CARTESIAN_POINT ( 'NONE',  ( 9.318724127987000116, 2.755029797911999978, 8.795125756257000660 ) ) ;
#55604=CARTESIAN_POINT ( 'NONE',  ( 9.485829719593997567, 4.953415418491999844, -8.946479654552000227 ) ) ;
#55606=VECTOR ( 'NONE', #51770, 999.9999999999998863 ) ;
#55607=CARTESIAN_POINT ( 'NONE',  ( 11.09999999999999964, 2.646159083949000124, 6.745271721726000536 ) ) ;
#55612=ORIENTED_EDGE ( 'NONE', *, *, #14797, .T. ) ;
#55613=CARTESIAN_POINT ( 'NONE',  ( 1.834748578981000078, 1.670918626813999941, 2.798091744145999815 ) ) ;
#55615=AXIS2_PLACEMENT_3D ( 'NONE', #30506, #31203, #42027 ) ;
#55617=LINE ( 'NONE', #45810, #38004 ) ;
#55620=CARTESIAN_POINT ( 'NONE',  ( 4.900006121741999898, -6.122517096885939548E-17, -1.999970730383187734 ) ) ;
#55623=CYLINDRICAL_SURFACE ( 'NONE', #44418, 0.4999999999999998335 ) ;
#55625=CARTESIAN_POINT ( 'NONE',  ( 9.163172718159000141, 7.862179196714000007, -5.354466121481999963 ) ) ;
#55629=CARTESIAN_POINT ( 'NONE',  ( 1.991204174508000024, 3.176854988377000311, -1.562936765141999862 ) ) ;
#55630=ORIENTED_EDGE ( 'NONE', *, *, #5903, .T. ) ;
#55631=CARTESIAN_POINT ( 'NONE',  ( 4.950033214355999966, 0.000000000000000000, -2.049966935984999683 ) ) ;
#55640=CARTESIAN_POINT ( 'NONE',  ( 9.646886009120546390, 5.267629041041144156, -8.036546440280751824 ) ) ;
#55642=CARTESIAN_POINT ( 'NONE',  ( 8.558820226389943997, 3.642594333086357050, 5.792987242710919027 ) ) ;
#55652=CARTESIAN_POINT ( 'NONE',  ( 10.65050915380999896, 5.200037120669999346, 5.937706951697999891 ) ) ;
#55653=FACE_OUTER_BOUND ( 'NONE', #26758, .T. ) ;
#55655=DIRECTION ( 'NONE',  ( -1.000000000000000000, 0.000000000000000000, 0.000000000000000000 ) ) ;
#55656=DIRECTION ( 'NONE',  ( 1.000000000000000000, 0.000000000000000000, 0.000000000000000000 ) ) ;
#55657=CARTESIAN_POINT ( 'NONE',  ( 4.000000000000000888, -1.321180510578202849, -1.719428477289353330 ) ) ;
#55662=DIRECTION ( 'NONE',  ( 0.000000000000000000, -0.8648648648648720183, 0.5020047465136825426 ) ) ;
#55672=CIRCLE ( 'NONE', #21119, 2.000000000000000000 ) ;
#55679=CIRCLE ( 'NONE', #69032, 2.000000000000000444 ) ;
#55681=EDGE_CURVE ( 'NONE', #5573, #29932, #58154, .T. ) ;
#55683=CARTESIAN_POINT ( 'NONE',  ( 11.07110280567999894, 7.379437729801000323, -6.320289087312000120 ) ) ;
#55685=CARTESIAN_POINT ( 'NONE',  ( 8.200356874137819219, 3.823158304644485028, -8.849587703040166176 ) ) ;
#55693=FACE_OUTER_BOUND ( 'NONE', #12540, .T. ) ;
#55695=CIRCLE ( 'NONE', #28909, 1.500000000000001110 ) ;
#55705=B_SPLINE_CURVE_WITH_KNOTS ( 'NONE', 3,
 ( #52137, #39948, #30484, #51457 ),
 .UNSPECIFIED., .F., .F.,
 ( 4, 4 ),
 ( 0.000000000000000000, 1.000000000000000000 ),
 .UNSPECIFIED. ) ;
#55707=PLANE ( 'NONE',  #28717 ) ;
#55713=ADVANCED_FACE ( 'NONE', ( #10543 ), #52508, .T. ) ;
#55715=CARTESIAN_POINT ( 'NONE',  ( 5.966666563597951445, 12.43894384121646901, -2.828928431919257580 ) ) ;
#55721=CARTESIAN_POINT ( 'NONE',  ( 8.348093183609000434, 4.599999999999999645, -6.056236567608999977 ) ) ;
#55723=CARTESIAN_POINT ( 'NONE',  ( 4.900006121741999010, 1.599333684796359289, -1.229093439949831224 ) ) ;
#55724=CARTESIAN_POINT ( 'NONE',  ( 8.623264158775000965, 5.288433695693000480, -8.041290150997999930 ) ) ;
#55727=CARTESIAN_POINT ( 'NONE',  ( 0.1103081484368000076, -1.521127753326000143, -2.712944034833999929 ) ) ;
#55730=CARTESIAN_POINT ( 'NONE',  ( 11.09999965054999826, -2.398081733189999864E-14, 0.000000000000000000 ) ) ;
#55732=CARTESIAN_POINT ( 'NONE',  ( 8.316054719590999511, 3.826300099041999747, -9.055335252254000267 ) ) ;
#55738=CARTESIAN_POINT ( 'NONE',  ( 10.09999999999999964, 0.000000000000000000, 11.84999999999999964 ) ) ;
#55740=CARTESIAN_POINT ( 'NONE',  ( 9.196339158776000389, 4.112741311853999271, -5.603466076760000192 ) ) ;
#55743=CARTESIAN_POINT ( 'NONE',  ( 10.97074841058999972, 2.648521302318000092, -6.788870928221999890 ) ) ;
#55755=ORIENTED_EDGE ( 'NONE', *, *, #53978, .T. ) ;
#55756=CYLINDRICAL_SURFACE ( 'NONE', #49281, 1.350000000000000533 ) ;
#55757=CARTESIAN_POINT ( 'NONE',  ( 10.73615471958999912, 3.078044734341000233, -6.088740491863000592 ) ) ;
#55758=CARTESIAN_POINT ( 'NONE',  ( 7.000000000000000000, 0.6769230769231000533, -2.665384615385000266 ) ) ;
#55767=CARTESIAN_POINT ( 'NONE',  ( 8.599639158772999892, 2.261390688294000029, -6.733978371730000134 ) ) ;
#55768=CARTESIAN_POINT ( 'NONE',  ( 9.158483593794224831, 5.507272619768906807, 6.616252076538792437 ) ) ;
#55777=DIRECTION ( 'NONE',  ( 0.000000000000000000, 0.7158784314710767704, 0.6982249432342778617 ) ) ;
#55778=CARTESIAN_POINT ( 'NONE',  ( 7.925588223455998893, 3.381165371184000179, -6.300169931272000312 ) ) ;
#55780=CARTESIAN_POINT ( 'NONE',  ( 8.576923877145999242, 3.399999999999999911, 5.924121105096999962 ) ) ;
#55785=CARTESIAN_POINT ( 'NONE',  ( 8.216604719590000272, 5.331510020787000315, -8.114341808290998159 ) ) ;
#55791=CARTESIAN_POINT ( 'NONE',  ( 3.458341080379000232, 2.282530897026000094, -2.706516516324000143 ) ) ;
#55793=EDGE_CURVE ( 'NONE', #5733, #48489, #43751, .T. ) ;
#55798=CARTESIAN_POINT ( 'NONE',  ( 8.320864158774000430, 3.894644548817000285, 6.044465307984999924 ) ) ;
#55800=ORIENTED_EDGE ( 'NONE', *, *, #6168, .T. ) ;
#55804=CARTESIAN_POINT ( 'NONE',  ( 7.838660841226998244, 2.602490396417999730, -7.495170534277000307 ) ) ;
#55809=ORIENTED_EDGE ( 'NONE', *, *, #14752, .F. ) ;
#55812=CARTESIAN_POINT ( 'NONE',  ( 0.1499942179679999987, 2.750000000000000000, 0.000000000000000000 ) ) ;
#55816=CARTESIAN_POINT ( 'NONE',  ( 10.94027433962292228, 9.313027398374178034, -6.234466045321436667 ) ) ;
#55822=CARTESIAN_POINT ( 'NONE',  ( 8.834364158772999076, 4.141907758973999876, 6.047574021139999978 ) ) ;
#55830=CARTESIAN_POINT ( 'NONE',  ( 3.499999999999999556, 1.472012334232528197, 3.007095132810396976 ) ) ;
#55839=CARTESIAN_POINT ( 'NONE',  ( 9.029445280412998542, 5.442817578555000146, -8.106149115450000053 ) ) ;
#55840=CARTESIAN_POINT ( 'NONE',  ( 2.880411394923000135, 3.016179945678000074, 1.524104863001999988 ) ) ;
#55843=CARTESIAN_POINT ( 'NONE',  ( 7.856851002541000106, 2.832432432432000269, -6.822293592207000934 ) ) ;
#55845=VERTEX_POINT ( 'NONE', #10890 ) ;
#55848=CARTESIAN_POINT ( 'NONE',  ( 10.20577346834789267, 5.100000000000000533, -6.304440313861127798 ) ) ;
#55853=CARTESIAN_POINT ( 'NONE',  ( 9.318724127987000116, 2.755029797911999978, 8.795125756257000660 ) ) ;
#55854=CARTESIAN_POINT ( 'NONE',  ( 9.136338985489343756, 3.395526279446049678, 8.727102369890431532 ) ) ;
#55860=CARTESIAN_POINT ( 'NONE',  ( 8.114220007854932248, 5.048039997173753513, -6.491766777592614446 ) ) ;
#55861=CARTESIAN_POINT ( 'NONE',  ( 10.06949528041000086, 4.910370880657999315, -8.649591080567999413 ) ) ;
#55868=CARTESIAN_POINT ( 'NONE',  ( 8.732392219593000604, 2.806082850903000026, 8.615880516515998622 ) ) ;
#55869=AXIS2_PLACEMENT_3D ( 'NONE', #21419, #10248, #10591 ) ;
#55872=CARTESIAN_POINT ( 'NONE',  ( 9.888314158772001150, 5.105193280231000053, -8.895607399415000671 ) ) ;
#55873=VERTEX_POINT ( 'NONE', #16476 ) ;
#55875=EDGE_CURVE ( 'NONE', #1268, #18238, #37806, .T. ) ;
#55876=CARTESIAN_POINT ( 'NONE',  ( 10.30047009227000032, 4.027768540959000276, 9.431354536774000152 ) ) ;
#55880=CARTESIAN_POINT ( 'NONE',  ( 9.832537864288001472, 2.899999999999999911, 6.571291218949999902 ) ) ;
#55883=ADVANCED_FACE ( 'NONE', ( #32568 ), #53880, .T. ) ;
#55896=ORIENTED_EDGE ( 'NONE', *, *, #42187, .F. ) ;
#55898=CARTESIAN_POINT ( 'NONE',  ( 9.491735841231999871, 3.920043641733999884, -9.398198753036000497 ) ) ;
#55915=CARTESIAN_POINT ( 'NONE',  ( 11.09999607187999970, -1.407106888317999793, -11.46396986501999926 ) ) ;
#55916=CARTESIAN_POINT ( 'NONE',  ( 9.783303357172172809, 5.333269419498685160, -6.342932607636153186 ) ) ;
#55920=DIRECTION ( 'NONE',  ( 0.000000000000000000, 0.000000000000000000, -1.000000000000000000 ) ) ;
#55921=CARTESIAN_POINT ( 'NONE',  ( 8.058767219590999176, 2.432118421226999949, 6.597517552098000060 ) ) ;
#55922=ORIENTED_EDGE ( 'NONE', *, *, #63111, .F. ) ;
#55926=CARTESIAN_POINT ( 'NONE',  ( 10.91943903453000075, 3.268382602297999817, -6.413946631105000407 ) ) ;
#55931=CARTESIAN_POINT ( 'NONE',  ( 9.533434135307000901, 2.564753581125000181, 6.150586364588000343 ) ) ;
#55937=CARTESIAN_POINT ( 'NONE',  ( 11.09425120759000016, 2.431871068503000277, 7.769513029648000391 ) ) ;
#55941=CARTESIAN_POINT ( 'NONE',  ( 7.416892219589999335, 3.448180532882000104, 9.222462917385000125 ) ) ;
#55942=CARTESIAN_POINT ( 'NONE',  ( 9.228133567168001150, 2.875367362387999837, 8.669940206484001877 ) ) ;
#55945=CARTESIAN_POINT ( 'NONE',  ( 9.494689158774999527, 2.824732249080000202, -8.992748220058999209 ) ) ;
#55953=CARTESIAN_POINT ( 'NONE',  ( 2.216204174507999891, 2.754481206214999922, -1.355138954038999977 ) ) ;
#55964=CARTESIAN_POINT ( 'NONE',  ( 8.470295280410999439, 4.255646040929000229, 9.114085578076998928 ) ) ;
#55967=CARTESIAN_POINT ( 'NONE',  ( 10.97216345563000139, 5.142214104516000361, 4.994019176338999166 ) ) ;
#55970=CARTESIAN_POINT ( 'NONE',  ( 1.695565801737999978, 3.378571531507999826, -0.5657499728117999505 ) ) ;
#55972=CARTESIAN_POINT ( 'NONE',  ( 10.62549262324159471, 5.350086361208822971, -7.676738019119362377 ) ) ;
#55974=CARTESIAN_POINT ( 'NONE',  ( 9.442087588264000075, 4.742492734433000123, 8.809983635807000724 ) ) ;
#55981=CARTESIAN_POINT ( 'NONE',  ( 9.629471092178999214, 5.100000000000000533, 6.152188490330000370 ) ) ;
#55983=CARTESIAN_POINT ( 'NONE',  ( 7.651169844548746823, 5.420674159255254310, 6.473016521238817766 ) ) ;
#55992=FACE_OUTER_BOUND ( 'NONE', #13350, .T. ) ;
#55993=CARTESIAN_POINT ( 'NONE',  ( 9.819055905797000605, 2.899999999999999911, -6.571291218949999902 ) ) ;
#55994=CARTESIAN_POINT ( 'NONE',  ( 9.256664404737000140, 4.025830366070999311, 9.295863330698999505 ) ) ;
#55995=CARTESIAN_POINT ( 'NONE',  ( 10.48734600210000067, 4.351287276768000645, -6.182257940481999725 ) ) ;
#56003=CARTESIAN_POINT ( 'NONE',  ( 0.6736883816833351135, 0.9084612428644865956, -3.122795580015885974 ) ) ;
#56009=ORIENTED_EDGE ( 'NONE', *, *, #10783, .F. ) ;
#56016=CARTESIAN_POINT ( 'NONE',  ( -15.86200481174999943, 5.599999999999999645, 6.571291218949999902 ) ) ;
#56018=CARTESIAN_POINT ( 'NONE',  ( 11.07144391099999936, 7.549533471103999638, -6.458582346940000107 ) ) ;
#56019=CARTESIAN_POINT ( 'NONE',  ( -0.02733730371250999922, 2.854424451075999958, -2.356853325602000115 ) ) ;
#56025=DIRECTION ( 'NONE',  ( 1.000000000000000000, 0.000000000000000000, 0.000000000000000000 ) ) ;
#56032=DIRECTION ( 'NONE',  ( 0.000000000000000000, 0.000000000000000000, -1.000000000000000000 ) ) ;
#56046=LINE ( 'NONE', #35420, #4922 ) ;
#56050=ORIENTED_EDGE ( 'NONE', *, *, #8691, .F. ) ;
#56051=CARTESIAN_POINT ( 'NONE',  ( -2.444943969992999916E-05, -2.899969545325999931, 0.000000000000000000 ) ) ;
#56055=CARTESIAN_POINT ( 'NONE',  ( 2.289363843320874725, -3.114462284487641064, -1.632227178342312790 ) ) ;
#56056=CARTESIAN_POINT ( 'NONE',  ( 8.225464158772000545, 3.844886277615000125, -8.888911790991000927 ) ) ;
#56059=AXIS2_PLACEMENT_3D ( 'NONE', #34151, #61735, #23310 ) ;
#56063=EDGE_CURVE ( 'NONE', #15587, #16690, #67125, .T. ) ;
#56065=CARTESIAN_POINT ( 'NONE',  ( 2.665556799210790917, 0.4581489286485003198, 3.500000000000000444 ) ) ;
#56066=CARTESIAN_POINT ( 'NONE',  ( 8.704995280412999747, 5.140767546012999567, -6.196177269779999719 ) ) ;
#56070=DIRECTION ( 'NONE',  ( 0.000000000000000000, -0.8648648648648720183, 0.5020047465136825426 ) ) ;
#56072=CARTESIAN_POINT ( 'NONE',  ( 7.712296824873548395, 4.464687595965251887, -8.784369080928565054 ) ) ;
#56077=CARTESIAN_POINT ( 'NONE',  ( 10.29094007826000023, 2.903522982536999919, -8.310916170934000036 ) ) ;
#56083=CIRCLE ( 'NONE', #59417, 2.999989272562999965 ) ;
#56084=CARTESIAN_POINT ( 'NONE',  ( 10.99107545325904667, 5.690496933828011805, -4.958831622490459168 ) ) ;
#56090=CARTESIAN_POINT ( 'NONE',  ( 10.91733584123000078, 3.256275267152000108, -6.361562334135999919 ) ) ;
#56096=CARTESIAN_POINT ( 'NONE',  ( 7.861476898152417903, 5.109672693010819167, 6.687167769525764527 ) ) ;
#56100=VERTEX_POINT ( 'NONE', #29411 ) ;
#56101=CARTESIAN_POINT ( 'NONE',  ( 8.367589158771000513, 5.461114003844000031, -8.582501063019000398 ) ) ;
#56102=DIRECTION ( 'NONE',  ( -0.000000000000000000, 1.000000000000000000, 0.000000000000000000 ) ) ;
#56104=DIRECTION ( 'NONE',  ( 0.000000000000000000, 0.000000000000000000, 1.000000000000000000 ) ) ;
#56112=DIRECTION ( 'NONE',  ( 0.000000000000000000, 0.9510565162985824550, -0.3090169943643944483 ) ) ;
#56119=CARTESIAN_POINT ( 'NONE',  ( 3.500000000000000000, 3.200000000000000178, 0.000000000000000000 ) ) ;
#56120=CARTESIAN_POINT ( 'NONE',  ( 9.889535841229999846, 5.798263352390999437, -8.113145944980999502 ) ) ;
#56121=EDGE_CURVE ( 'NONE', #35290, #11774, #54814, .T. ) ;
#56128=CARTESIAN_POINT ( 'NONE',  ( 2.881384349028000003, -3.542840650637999911, -0.5934045645267999047 ) ) ;
#56129=ORIENTED_EDGE ( 'NONE', *, *, #38430, .F. ) ;
#56138=CARTESIAN_POINT ( 'NONE',  ( 7.490585841228000419, 4.468431922689999780, -6.183326950307000303 ) ) ;
#56150=CARTESIAN_POINT ( 'NONE',  ( 10.97581046457103326, 8.473166771401304587, -6.548870747866761377 ) ) ;
#56152=CARTESIAN_POINT ( 'NONE',  ( 8.187214158772000872, 4.472863460285000592, -8.721137209586000694 ) ) ;
#56155=ORIENTED_EDGE ( 'NONE', *, *, #34423, .T. ) ;
#56160=AXIS2_PLACEMENT_3D ( 'NONE', #15619, #25763, #25070 ) ;
#56161=B_SPLINE_CURVE_WITH_KNOTS ( 'NONE', 3,
 ( #22945, #34499, #44300, #55812 ),
 .UNSPECIFIED., .F., .F.,
 ( 4, 4 ),
 ( 0.000000000000000000, 1.000000000000000000 ),
 .UNSPECIFIED. ) ;
#56163=EDGE_LOOP ( 'NONE', ( #42480, #20881, #28885, #59231 ) ) ;
#56166=AXIS2_PLACEMENT_3D ( 'NONE', #38560, #33675, #60583 ) ;
#56168=CARTESIAN_POINT ( 'NONE',  ( 10.71654029638703243, 2.829809111552286538, 6.826801520698219328 ) ) ;
#56173=ORIENTED_EDGE ( 'NONE', *, *, #6656, .F. ) ;
#56175=VERTEX_POINT ( 'NONE', #51400 ) ;
#56177=CARTESIAN_POINT ( 'NONE',  ( 0.1499942179680000265, -2.402872127494069421, 1.384928887584812474 ) ) ;
#56178=CARTESIAN_POINT ( 'NONE',  ( 9.128895280414001334, 3.880154689736000417, -9.060377011187000562 ) ) ;
#56179=CARTESIAN_POINT ( 'NONE',  ( 3.089996212309999546, -3.376682894496000120, 0.1350915547969999686 ) ) ;
#56186=ORIENTED_EDGE ( 'NONE', *, *, #44778, .F. ) ;
#56189=CARTESIAN_POINT ( 'NONE',  ( 9.634020792350998619, 3.042978295541999945, 8.588098960242001922 ) ) ;
#56192=CARTESIAN_POINT ( 'NONE',  ( 10.18756025349000005, 5.387489739490000318, 8.640945789268998922 ) ) ;
#56196=CARTESIAN_POINT ( 'NONE',  ( 10.97054688934660049, 2.819834791696201659, -6.661904172904770327 ) ) ;
#56200=LINE ( 'NONE', #33850, #15437 ) ;
#56201=CARTESIAN_POINT ( 'NONE',  ( 10.14522028041000112, 3.576529456695000331, -8.962721799438000403 ) ) ;
#56210=CARTESIAN_POINT ( 'NONE',  ( 8.834364158772999076, 4.141907758973999876, 6.047574021139999978 ) ) ;
#56211=CARTESIAN_POINT ( 'NONE',  ( 8.546960841229999772, 2.724453559418999582, -8.908010318766001134 ) ) ;
#56212=DIRECTION ( 'NONE',  ( 0.000000000000000000, -1.000000000000000000, 0.000000000000000000 ) ) ;
#56213=CARTESIAN_POINT ( 'NONE',  ( 10.22907665877000127, 4.838498214728000235, -5.852435699035000383 ) ) ;
#56231=VERTEX_POINT ( 'NONE', #40909 ) ;
#56237=CARTESIAN_POINT ( 'NONE',  ( 9.251970280414001380, 5.673443217382001080, -7.051790060464000476 ) ) ;
#56243=CARTESIAN_POINT ( 'NONE',  ( 8.207510841230000409, 5.944584532500000407, 7.106843289410999631 ) ) ;
#56245=CARTESIAN_POINT ( 'NONE',  ( 7.766851002543999627, 2.832432432432000269, 6.822293592207000934 ) ) ;
#56253=CARTESIAN_POINT ( 'NONE',  ( 9.317462135714000837, 5.100000000000000533, 6.571291218949999902 ) ) ;
#56263=VECTOR ( 'NONE', #64927, 1000.000000000000000 ) ;
#56269=CARTESIAN_POINT ( 'NONE',  ( 10.98768472639999949, 0.3876847264043000174, -4.945212061661000469 ) ) ;
#56271=CARTESIAN_POINT ( 'NONE',  ( 9.662551629919999385, 4.094830335839000135, 9.119946295870999364 ) ) ;
#56272=ADVANCED_FACE ( 'NONE', ( #9771 ), #18785, .F. ) ;
#56279=CARTESIAN_POINT ( 'NONE',  ( 10.03612394578000000, 3.011788727150999989, 8.746962581836999817 ) ) ;
#56285=CARTESIAN_POINT ( 'NONE',  ( 7.283509992105000386, 4.426928431836000044, 9.293321981113999541 ) ) ;
#56286=CARTESIAN_POINT ( 'NONE',  ( 10.15902941591999920, 4.166415211384999040, 9.114163806478000396 ) ) ;
#56290=CARTESIAN_POINT ( 'NONE',  ( 9.594139158774000364, 2.212639797530000063, -6.855876382544999537 ) ) ;
#56299=CARTESIAN_POINT ( 'NONE',  ( 2.349703346704999696, 1.767505521208999841, -3.127111028022000028 ) ) ;
#56303=CARTESIAN_POINT ( 'NONE',  ( 9.959641781044998865, 5.406625910119999823, 7.700299649248999678 ) ) ;
#56304=DIRECTION ( 'NONE',  ( 1.000000000000000000, 0.000000000000000000, 0.000000000000000000 ) ) ;
#56309=CARTESIAN_POINT ( 'NONE',  ( 7.571670280409000142, 2.531201476950000195, 8.216704145297999418 ) ) ;
#56314=CARTESIAN_POINT ( 'NONE',  ( 2.034112785886000196, 1.767505521208999841, -3.127111028022000028 ) ) ;
#56319=CARTESIAN_POINT ( 'NONE',  ( 9.611387933856001098, 3.334846092635999959, 5.869117602953000556 ) ) ;
#56328=CARTESIAN_POINT ( 'NONE',  ( 8.567869857589764493, 3.845039034713962245, 5.763696154439774233 ) ) ;
#56329=ORIENTED_EDGE ( 'NONE', *, *, #45315, .T. ) ;
#56338=CARTESIAN_POINT ( 'NONE',  ( 11.08992526467999973, 5.210543602612999869, 8.327598319864998544 ) ) ;
#56339=CARTESIAN_POINT ( 'NONE',  ( 10.99693586709999948, 2.980605808171000071, -6.418617723582000778 ) ) ;
#56346=FACE_OUTER_BOUND ( 'NONE', #46303, .T. ) ;
#56350=CARTESIAN_POINT ( 'NONE',  ( 7.000000000000000000, 0.000000000000000000, 0.000000000000000000 ) ) ;
#56360=ORIENTED_EDGE ( 'NONE', *, *, #61587, .T. ) ;
#56367=CARTESIAN_POINT ( 'NONE',  ( 10.07314899745999881, 5.167567567567999731, -6.822293592207000934 ) ) ;
#56369=CARTESIAN_POINT ( 'NONE',  ( 0.5157068467740000273, 0.9881876859693999871, -3.396851722846999877 ) ) ;
#56376=EDGE_CURVE ( 'NONE', #50139, #61746, #3411, .T. ) ;
#56381=EDGE_LOOP ( 'NONE', ( #65741, #32589, #9015, #52612 ) ) ;
#56386=DIRECTION ( 'NONE',  ( 1.000000000000000000, 0.000000000000000000, 0.000000000000000000 ) ) ;
#56389=CARTESIAN_POINT ( 'NONE',  ( 6.949466553314000095, -12.16404195313999992, 3.090625619586999662 ) ) ;
#56397=CARTESIAN_POINT ( 'NONE',  ( 7.761763193589995780, 2.840593260277998411, 6.815714094171000603 ) ) ;
#56400=ADVANCED_FACE ( 'NONE', ( #14939 ), #47106, .F. ) ;
#56406=CARTESIAN_POINT ( 'NONE',  ( 3.050973465878000113, 3.500000000000000000, 0.000000000000000000 ) ) ;
#56407=CARTESIAN_POINT ( 'NONE',  ( 9.120514158775000269, 5.306366356490000769, -7.996450761531000317 ) ) ;
#56414=CARTESIAN_POINT ( 'NONE',  ( 2.603056799210541783, 2.798833948393625981, 2.150913519912208471 ) ) ;
#56415=CARTESIAN_POINT ( 'NONE',  ( 9.550320280412000429, 2.370176859044999862, -6.912649125838000508 ) ) ;
#56419=CYLINDRICAL_SURFACE ( 'NONE', #57457, 0.5000000000000002220 ) ;
#56421=CARTESIAN_POINT ( 'NONE',  ( 8.878359312499435774, 5.126777126183351463, 6.752018918868522235 ) ) ;
#56425=CARTESIAN_POINT ( 'NONE',  ( 9.819565861057999001, 2.688248842995000221, -7.873038103423000145 ) ) ;
#56433=CARTESIAN_POINT ( 'NONE',  ( 8.477766462057999775, 2.899999999999999911, -6.558719934578999933 ) ) ;
#56439=CARTESIAN_POINT ( 'NONE',  ( 10.65229834123000074, 4.944334466443999432, -8.478467788338001299 ) ) ;
#56448=CARTESIAN_POINT ( 'NONE',  ( 9.567560841232999991, 5.349936549139000519, -7.138437102151999447 ) ) ;
#56456=CARTESIAN_POINT ( 'NONE',  ( 2.435247277619000172, 2.372532593102000043, -2.573147701680999599 ) ) ;
#56462=CIRCLE ( 'NONE', #8498, 13.10000000000000320 ) ;
#56468=CARTESIAN_POINT ( 'NONE',  ( 8.845310841232000953, 5.851083642416999631, -7.072167224702999633 ) ) ;
#56471=AXIS2_PLACEMENT_3D ( 'NONE', #48990, #11570, #54227 ) ;
#56473=CARTESIAN_POINT ( 'NONE',  ( 2.347336229053000434, 2.684440549187000258, 1.847963356650000000 ) ) ;
#56477=CARTESIAN_POINT ( 'NONE',  ( 8.741144820356497647, 5.068224986544200839, -6.186394335232312081 ) ) ;
#56483=CARTESIAN_POINT ( 'NONE',  ( 0.6362098952830620435, -0.4390463955410620067, 3.502173745463374122 ) ) ;
#56485=CARTESIAN_POINT ( 'NONE',  ( 7.800894426331000275, 3.218815461055000160, 6.398977422524000147 ) ) ;
#56489=ORIENTED_EDGE ( 'NONE', *, *, #1699, .T. ) ;
#56512=CARTESIAN_POINT ( 'NONE',  ( 3.178056799211042005, -2.150913519912214245, 2.798833948393621984 ) ) ;
#56515=VERTEX_POINT ( 'NONE', #237 ) ;
#56520=CARTESIAN_POINT ( 'NONE',  ( 10.59303303094000093, 2.436236667456999960, 7.793464546548000804 ) ) ;
#56522=CARTESIAN_POINT ( 'NONE',  ( 9.766460841231999979, 3.135494838036999798, -8.598037907310999373 ) ) ;
#56524=CARTESIAN_POINT ( 'NONE',  ( 3.669618013697999892, -3.382257552941999812, 0.6016812345426000297 ) ) ;
#56526=DIRECTION ( 'NONE',  ( -0.7071060865235063719, -0.7071074758489063194, -8.141945933792071646E-10 ) ) ;
#56531=CARTESIAN_POINT ( 'NONE',  ( 10.00637913184999839, 5.119263020957999899, 8.420380450036001108 ) ) ;
#56534=CARTESIAN_POINT ( 'NONE',  ( 9.972850246170999355, 5.044468801812000081, 6.258104779495000436 ) ) ;
#56538=CYLINDRICAL_SURFACE ( 'NONE', #9056, 3.200000000000000178 ) ;
#56540=CARTESIAN_POINT ( 'NONE',  ( 11.02452225494999993, 2.775477745048999800, -6.571291218949999902 ) ) ;
#56542=CARTESIAN_POINT ( 'NONE',  ( 8.114506759233030664, 5.047117657413311420, -6.489853823473402450 ) ) ;
#56551=B_SPLINE_CURVE_WITH_KNOTS ( 'NONE', 3,
 ( #61351, #35478, #3301, #14493 ),
 .UNSPECIFIED., .F., .F.,
 ( 4, 4 ),
 ( 0.000000000000000000, 0.1280414556252505165 ),
 .UNSPECIFIED. ) ;
#56556=CARTESIAN_POINT ( 'NONE',  ( 10.52384528040999889, 5.441915759804999198, -7.989632847918000103 ) ) ;
#56558=CARTESIAN_POINT ( 'NONE',  ( 1.436390132540666942, 0.4581489286485155299, -3.499999999999999556 ) ) ;
#56569=CONICAL_SURFACE ( 'NONE', #8564, 2.050054338200999915, 0.7853981633972997312 ) ;
#56573=CARTESIAN_POINT ( 'NONE',  ( 2.771806799209417083, -3.408904368339104263, -0.9161175952574814874 ) ) ;
#56586=CARTESIAN_POINT ( 'NONE',  ( 8.014948341228999240, 2.280568568659000483, 6.510284508622999233 ) ) ;
#56588=VERTEX_POINT ( 'NONE', #12110 ) ;
#56589=CARTESIAN_POINT ( 'NONE',  ( 9.319055905798999007, 2.899999999999999911, -6.571291218949999902 ) ) ;
#56592=ORIENTED_EDGE ( 'NONE', *, *, #29089, .T. ) ;
#56603=ORIENTED_EDGE ( 'NONE', *, *, #18620, .T. ) ;
#56604=ORIENTED_EDGE ( 'NONE', *, *, #43046, .T. ) ;
#56609=CARTESIAN_POINT ( 'NONE',  ( 9.910156421876999744, 2.531070993918000056, -7.917736616860999277 ) ) ;
#56614=CARTESIAN_POINT ( 'NONE',  ( 10.77962664842000073, 2.397507474987000009, 7.755423212350999407 ) ) ;
#56616=CYLINDRICAL_SURFACE ( 'NONE', #44755, 0.4999999999999998335 ) ;
#56617=VERTEX_POINT ( 'NONE', #17708 ) ;
#56620=CARTESIAN_POINT ( 'NONE',  ( 9.332933391271998502, 5.100349772922000646, 8.693467186193998941 ) ) ;
#56622=CARTESIAN_POINT ( 'NONE',  ( 9.675870280412999236, 3.031907308384000022, -8.729608011560001657 ) ) ;
#56627=CARTESIAN_POINT ( 'NONE',  ( 7.583051658771000625, 4.763536573491999881, 5.668879554882000349 ) ) ;
#56628=CARTESIAN_POINT ( 'NONE',  ( 10.49785886974000171, 3.776281431161999880, 5.717632172928999168 ) ) ;
#56632=CARTESIAN_POINT ( 'NONE',  ( 10.11453584122999949, 5.322769172805999816, -7.951018786192998178 ) ) ;
#56633=CARTESIAN_POINT ( 'NONE',  ( -0.000000000000000000, 2.533832635911827502, 1.460960874862264225 ) ) ;
#56640=CARTESIAN_POINT ( 'NONE',  ( 1.105199323181000004, 1.980426728703999828, 3.194707851357999839 ) ) ;
#56642=CARTESIAN_POINT ( 'NONE',  ( 9.727383000783749623, 5.662315500981915939, 8.092168579200617273 ) ) ;
#56643=CARTESIAN_POINT ( 'NONE',  ( 10.59999999999999964, 3.399999999999999911, -4.756097560976000338 ) ) ;
#56645=CARTESIAN_POINT ( 'NONE',  ( 10.40516904918000129, 5.216391323504000255, 6.765759859247999941 ) ) ;
#56651=CARTESIAN_POINT ( 'NONE',  ( 7.994579719591000000, 2.263558315407000254, 8.007442119518000112 ) ) ;
#56657=CARTESIAN_POINT ( 'NONE',  ( 1.509611342036999870, 0.7365451747729999665, -3.515871166463000019 ) ) ;
#56659=CARTESIAN_POINT ( 'NONE',  ( 1.191003052484043367, 1.577065564342242654, -2.901955378219182258 ) ) ;
#56662=CARTESIAN_POINT ( 'NONE',  ( 9.500006116823001889, 2.279680316922000127, 7.877692351087999256 ) ) ;
#56666=B_SPLINE_CURVE_WITH_KNOTS ( 'NONE', 3,
 ( #27218, #26533, #15693, #20942, #20592, #47861 ),
 .UNSPECIFIED., .F., .F.,
 ( 4, 2, 4 ),
 ( 0.3916346334472008972, 0.6958173167236003653, 1.000000000000000000 ),
 .UNSPECIFIED. ) ;
#56667=CARTESIAN_POINT ( 'NONE',  ( 9.424850063658244181, 5.349972463430670899, 7.500009360578276052 ) ) ;
#56669=CARTESIAN_POINT ( 'NONE',  ( 9.164680296029999340, 2.899999999999999911, -6.162130047625999474 ) ) ;
#56675=CARTESIAN_POINT ( 'NONE',  ( 8.132398138459945969, 5.154119579187411482, 6.184746403960440730 ) ) ;
#56679=EDGE_LOOP ( 'NONE', ( #16175, #42285, #38367, #46849 ) ) ;
#56684=CARTESIAN_POINT ( 'NONE',  ( 10.55991859298999991, 5.094266430778000121, 6.075406703384000018 ) ) ;
#56685=CARTESIAN_POINT ( 'NONE',  ( 10.44806481732999792, 3.684980864017000091, -6.173120265414000052 ) ) ;
#56696=CARTESIAN_POINT ( 'NONE',  ( 6.433333126412498437, -12.43895941528792193, -2.828912463766406482 ) ) ;
#56698=CARTESIAN_POINT ( 'NONE',  ( 9.049464847731002237, 7.846607741563002669, 5.258576131806001364 ) ) ;
#56701=CARTESIAN_POINT ( 'NONE',  ( 11.09999999999999964, 4.000000000000000000, -7.500000000000000000 ) ) ;
#56710=CARTESIAN_POINT ( 'NONE',  ( 8.433335197172079134, 2.968768240344807463, 6.285779305140361650 ) ) ;
#56712=EDGE_CURVE ( 'NONE', #33691, #26552, #29836, .T. ) ;
#56713=AXIS2_PLACEMENT_3D ( 'NONE', #35591, #52684, #36264 ) ;
#56714=CARTESIAN_POINT ( 'NONE',  ( 8.636068280300804645, 5.315145854513802171, -7.853667701454011052 ) ) ;
#56715=CARTESIAN_POINT ( 'NONE',  ( 0.2277818351675000019, 0.6801881511091000254, 3.471639432493999866 ) ) ;
#56716=CYLINDRICAL_SURFACE ( 'NONE', #31527, 11.84999999999999964 ) ;
#56718=VECTOR ( 'NONE', #52318, 1000.000000000000000 ) ;
#56722=DIRECTION ( 'NONE',  ( 0.000000000000000000, 1.000000000000000000, 0.000000000000000000 ) ) ;
#56723=CARTESIAN_POINT ( 'NONE',  ( 10.72128915877000033, 4.673511966357999370, -5.778393480304000462 ) ) ;
#56735=VECTOR ( 'NONE', #17170, 1000.000000000000000 ) ;
#56748=CARTESIAN_POINT ( 'NONE',  ( 0.9051401325418416688, -0.9161175952574773795, -3.408904368339105595 ) ) ;
#56750=CARTESIAN_POINT ( 'NONE',  ( 9.164680296029999340, 2.899999999999999911, -6.162130047625999474 ) ) ;
#56753=ADVANCED_FACE ( 'NONE', ( #62402 ), #8924, .T. ) ;
#56757=CARTESIAN_POINT ( 'NONE',  ( 9.700639158771000581, 4.262870449202000422, -8.811513791423999820 ) ) ;
#56759=VERTEX_POINT ( 'NONE', #41427 ) ;
#56765=CARTESIAN_POINT ( 'NONE',  ( 8.564679719593000229, 4.146787477634999775, -5.941926545671999627 ) ) ;
#56771=ORIENTED_EDGE ( 'NONE', *, *, #67625, .F. ) ;
#56772=FACE_OUTER_BOUND ( 'NONE', #10456, .T. ) ;
#56774=CARTESIAN_POINT ( 'NONE',  ( 8.541054719591000932, 3.807713920470999991, -9.221758713517999695 ) ) ;
#56778=CARTESIAN_POINT ( 'NONE',  ( 10.31499646082999888, 5.458376174241999834, -8.355105941236999456 ) ) ;
#56779=ORIENTED_EDGE ( 'NONE', *, *, #62610, .F. ) ;
#56787=CARTESIAN_POINT ( 'NONE',  ( 8.046924339810814786, 4.567502412556758706, -6.230116480647599708 ) ) ;
#56788=FACE_OUTER_BOUND ( 'NONE', #39547, .T. ) ;
#56795=ORIENTED_EDGE ( 'NONE', *, *, #12479, .F. ) ;
#56797=CARTESIAN_POINT ( 'NONE',  ( 9.327795280414001411, 3.161445734422999809, -6.178649910536000434 ) ) ;
#56799=CARTESIAN_POINT ( 'NONE',  ( 7.202583736560634442, 0.2999999999999999889, 3.098821334907657654 ) ) ;
#56806=CARTESIAN_POINT ( 'NONE',  ( 10.47530200610849604, 5.350262918594154371, 7.499984559551275964 ) ) ;
#56808=CARTESIAN_POINT ( 'NONE',  ( 7.429572863418363760, 3.823161772629042332, -6.150479629790767788 ) ) ;
#56809=CIRCLE ( 'NONE', #965, 12.39999890530000037 ) ;
#56812=CARTESIAN_POINT ( 'NONE',  ( 7.954680807037616042, 4.944643250900698561, 6.423735648896208517 ) ) ;
#56816=DIRECTION ( 'NONE',  ( 1.000000000000000000, 0.000000000000000000, 0.000000000000000000 ) ) ;
#56820=CARTESIAN_POINT ( 'NONE',  ( 3.305748555932999988, 1.181428906966000225, 3.215438517307999788 ) ) ;
#56821=ORIENTED_EDGE ( 'NONE', *, *, #25478, .T. ) ;
#56824=CARTESIAN_POINT ( 'NONE',  ( 11.09999999999999964, 7.281355457699000056, 6.286510842043999681 ) ) ;
#56825=CARTESIAN_POINT ( 'NONE',  ( 8.962739158771999115, 5.445214367171999470, 7.703373622193999459 ) ) ;
#56835=CARTESIAN_POINT ( 'NONE',  ( 7.783732762364405033, 2.886508771623532699, 6.705447760689092540 ) ) ;
#56837=VERTEX_POINT ( 'NONE', #20442 ) ;
#56843=ORIENTED_EDGE ( 'NONE', *, *, #42696, .F. ) ;
#56844=CARTESIAN_POINT ( 'NONE',  ( 8.492977932633323235, 3.398140593268752507, -9.149195927865305222 ) ) ;
#56846=CARTESIAN_POINT ( 'NONE',  ( 8.029179719589000896, 3.460181152982999997, -6.031076961652000357 ) ) ;
#56849=ORIENTED_EDGE ( 'NONE', *, *, #19795, .F. ) ;
#56850=CARTESIAN_POINT ( 'NONE',  ( 2.105140132540083808, 0.9161175952574701631, 3.408904368339106927 ) ) ;
#56851=CARTESIAN_POINT ( 'NONE',  ( 9.406851002546000373, 2.832432432432000269, -6.822293592207000934 ) ) ;
#56856=ORIENTED_EDGE ( 'NONE', *, *, #36301, .F. ) ;
#56859=CARTESIAN_POINT ( 'NONE',  ( 6.949999692120000461, -11.00717859340000082, -1.432487142323000118 ) ) ;
#56867=CARTESIAN_POINT ( 'NONE',  ( 11.29622358543999994, 3.561657733933999648, 6.266050246368000565 ) ) ;
#56868=CARTESIAN_POINT ( 'NONE',  ( 0.1499942179680000265, -0.3599680999394040404, 2.749953718116143087 ) ) ;
#56869=CARTESIAN_POINT ( 'NONE',  ( 9.526695280414001488, 5.462898983065000102, -8.055936939571999744 ) ) ;
#56870=CARTESIAN_POINT ( 'NONE',  ( 3.564596078290000136, 3.244059008440000280, 1.796025925329000072 ) ) ;
#56874=ORIENTED_EDGE ( 'NONE', *, *, #44625, .F. ) ;
#56876=CARTESIAN_POINT ( 'NONE',  ( 10.62795461073813996, 2.419700658069591448, -6.689391080427925296 ) ) ;
#56880=CARTESIAN_POINT ( 'NONE',  ( 10.55991859298999991, 5.094266430778000121, 6.075406703384000018 ) ) ;
#56890=VERTEX_POINT ( 'NONE', #57156 ) ;
#56894=CARTESIAN_POINT ( 'NONE',  ( 10.35646369190143368, 5.100000000000000533, 6.665341197350102220 ) ) ;
#56898=CARTESIAN_POINT ( 'NONE',  ( 10.66042971959000063, 2.315663237570999566, -7.431702255173999738 ) ) ;
#56904=DIRECTION ( 'NONE',  ( -0.7071068156326932863, 0.000000000000000000, -0.7071067467404001938 ) ) ;
#56907=EDGE_CURVE ( 'NONE', #11716, #22688, #20101, .T. ) ;
#56908=EDGE_CURVE ( 'NONE', #68613, #53586, #8876, .T. ) ;
#56909=CARTESIAN_POINT ( 'NONE',  ( 8.263039158770000725, 5.485324155719999872, -6.315380258366999122 ) ) ;
#56913=ORIENTED_EDGE ( 'NONE', *, *, #48078, .F. ) ;
#56915=DIRECTION ( 'NONE',  ( -1.000000000000000000, 0.000000000000000000, 0.000000000000000000 ) ) ;
#56920=CARTESIAN_POINT ( 'NONE',  ( 2.478056799210041738, 2.150913519912206695, -2.798833948393626869 ) ) ;
#56926=CARTESIAN_POINT ( 'NONE',  ( 7.565635841228000480, 3.206360348473000332, 5.681727837477000165 ) ) ;
#56927=ORIENTED_EDGE ( 'NONE', *, *, #43457, .T. ) ;
#56938=CARTESIAN_POINT ( 'NONE',  ( 7.721693597669004205, 9.012061377215999869, -5.588307756570000784 ) ) ;
#56950=CARTESIAN_POINT ( 'NONE',  ( 9.662441121991999893, 4.824173073626999653, -8.517602418144999632 ) ) ;
#56951=DIRECTION ( 'NONE',  ( 0.000000000000000000, 1.000000000000000000, 0.000000000000000000 ) ) ;
#56954=CARTESIAN_POINT ( 'NONE',  ( 11.05639637898999972, 5.030226177531999632, 6.028288223959999748 ) ) ;
#56959=CARTESIAN_POINT ( 'NONE',  ( 9.555697025339000561, 2.440752375194999768, 6.680879724048000234 ) ) ;
#56961=CARTESIAN_POINT ( 'NONE',  ( 9.965360841230999966, 4.034680274230000308, -6.102912434217000026 ) ) ;
#56966=CARTESIAN_POINT ( 'NONE',  ( 9.149954719592001240, 4.175915362023999933, 5.699506188181000077 ) ) ;
#56967=CARTESIAN_POINT ( 'NONE',  ( 11.15982925107999968, 5.578232410510000072, 8.067793621926998782 ) ) ;
#56970=CARTESIAN_POINT ( 'NONE',  ( 8.458179719589999479, 5.332332124071999857, -8.487089944253000340 ) ) ;
#56972=CARTESIAN_POINT ( 'NONE',  ( 8.965984360231564310, 5.205022649008997249, 8.206117015345389731 ) ) ;
#56978=CARTESIAN_POINT ( 'NONE',  ( 1.253018509565999805, -2.315742118336999944, -2.746122198278999615 ) ) ;
#56980=CARTESIAN_POINT ( 'NONE',  ( 9.972021765239443170, 2.299830290065005833, 7.025646633466952728 ) ) ;
#56989=CARTESIAN_POINT ( 'NONE',  ( 7.892607780408998686, 5.480308727866000318, 8.192324747680999053 ) ) ;
#56990=EDGE_CURVE ( 'NONE', #51298, #5657, #3009, .T. ) ;
#56995=CARTESIAN_POINT ( 'NONE',  ( 2.081794735327000545, 3.036063727655999855, -1.493670828108000004 ) ) ;
#56997=CARTESIAN_POINT ( 'NONE',  ( 1.906232294096261715, -0.2008767396709452702, 3.296684669105510945 ) ) ;
#57001=CARTESIAN_POINT ( 'NONE',  ( 10.25888757983999966, 4.512388525173999909, 5.993701490107000929 ) ) ;
#57005=CARTESIAN_POINT ( 'NONE',  ( 10.91441078832384726, 5.114410788323845658, -6.482042798726318722 ) ) ;
#57008=CARTESIAN_POINT ( 'NONE',  ( 7.613904305967312602, 4.827151911712800114, 5.947730341079782157 ) ) ;
#57016=EDGE_CURVE ( 'NONE', #62147, #8401, #64445, .T. ) ;
#57019=CARTESIAN_POINT ( 'NONE',  ( 10.06344080699000010, 5.156228702401000952, 6.125219923432000613 ) ) ;
#57026=CARTESIAN_POINT ( 'NONE',  ( 8.239948341229000661, 2.735218126362000124, 6.771983639047999937 ) ) ;
#57035=ORIENTED_EDGE ( 'NONE', *, *, #7398, .T. ) ;
#57045=EDGE_CURVE ( 'NONE', #24788, #67585, #36362, .T. ) ;
#57048=DIRECTION ( 'NONE',  ( 1.000000000000000000, 0.000000000000000000, 0.000000000000000000 ) ) ;
#57053=CARTESIAN_POINT ( 'NONE',  ( 11.09999999999999964, 4.000000000000000000, 7.500000000000000000 ) ) ;
#57062=CARTESIAN_POINT ( 'NONE',  ( 9.269471092183000138, 5.100000000000000533, -6.152188490330000370 ) ) ;
#57064=CARTESIAN_POINT ( 'NONE',  ( 11.09999999999999964, 2.646159083949000124, 6.745271721726000536 ) ) ;
#57067=FACE_OUTER_BOUND ( 'NONE', #59046, .T. ) ;
#57085=CARTESIAN_POINT ( 'NONE',  ( 9.518314158773000244, 4.845406482350000488, -6.387189183984999907 ) ) ;
#57092=CARTESIAN_POINT ( 'NONE',  ( 2.655140132544082654, 0.9161175952574702741, 3.408904368339106927 ) ) ;
#57102=CARTESIAN_POINT ( 'NONE',  ( 9.526695280414001488, 5.462898983065000102, -8.055936939571999744 ) ) ;
#57104=CARTESIAN_POINT ( 'NONE',  ( 10.56271176071999918, 2.509373760909999973, -8.602415192333999983 ) ) ;
#57112=CARTESIAN_POINT ( 'NONE',  ( 8.579778437876671049, 2.946186682499075005, 6.246120330076514016 ) ) ;
#57115=CARTESIAN_POINT ( 'NONE',  ( 10.06949528041000086, 4.910370880657999315, -8.649591080567999413 ) ) ;
#57120=VECTOR ( 'NONE', #9980, 1000.000000000000000 ) ;
#57122=B_SPLINE_CURVE_WITH_KNOTS ( 'NONE', 3,
 ( #60678, #12792, #28532, #65570 ),
 .UNSPECIFIED., .F., .F.,
 ( 4, 4 ),
 ( 0.000000000000000000, 0.3058235430633697294 ),
 .UNSPECIFIED. ) ;
#57126=CARTESIAN_POINT ( 'NONE',  ( 9.418385841233000377, 3.251172436837000301, -6.320036569851000152 ) ) ;
#57127=CARTESIAN_POINT ( 'NONE',  ( 9.165599386908368729, 5.579491228604561037, 6.755435461345757453 ) ) ;
#57141=CARTESIAN_POINT ( 'NONE',  ( 7.954463414819048950, 4.941043969738770691, 6.420455451648299672 ) ) ;
#57143=CARTESIAN_POINT ( 'NONE',  ( 6.949999692120000461, -11.00717859340000082, 1.432487142323000118 ) ) ;
#57144=CARTESIAN_POINT ( 'NONE',  ( 9.143660841233000269, 2.235961884443999459, -6.794506518623999902 ) ) ;
#57150=LINE ( 'NONE', #5038, #23325 ) ;
#57152=CARTESIAN_POINT ( 'NONE',  ( 2.681109875139000120, 0.2761326424212999786, -3.247312329306000223 ) ) ;
#57153=VERTEX_POINT ( 'NONE', #59218 ) ;
#57156=CARTESIAN_POINT ( 'NONE',  ( 11.08380555355736163, 3.999999927305438963, -9.033895164528459532 ) ) ;
#57161=CARTESIAN_POINT ( 'NONE',  ( 0.7407984155085870492, -3.500070825090493276, 0.4600197968347137789 ) ) ;
#57163=CARTESIAN_POINT ( 'NONE',  ( 1.511390132540624931, 3.499999999999998224, 0.4581489286485194157 ) ) ;
#57168=ORIENTED_EDGE ( 'NONE', *, *, #24618, .T. ) ;
#57171=CIRCLE ( 'NONE', #27039, 3.499999999999999556 ) ;
#57174=CARTESIAN_POINT ( 'NONE',  ( 8.280100731544914439, 3.296994443394544394, -6.103692026910207069 ) ) ;
#57175=CARTESIAN_POINT ( 'NONE',  ( 7.577233589035318850, 3.528879827026006222, 8.787968233516592065 ) ) ;
#57176=CARTESIAN_POINT ( 'NONE',  ( 7.333029719588999740, 3.500992739020000410, -8.983283880004998778 ) ) ;
#57180=VERTEX_POINT ( 'NONE', #52598 ) ;
#57181=CARTESIAN_POINT ( 'NONE',  ( 2.167640132540333386, -1.762666431298160141, 3.058252359239895579 ) ) ;
#57187=ORIENTED_EDGE ( 'NONE', *, *, #54921, .T. ) ;
#57190=CYLINDRICAL_SURFACE ( 'NONE', #18555, 3.500000000000000000 ) ;
#57194=ORIENTED_EDGE ( 'NONE', *, *, #36861, .T. ) ;
#57195=CARTESIAN_POINT ( 'NONE',  ( 3.452384183491000069, 1.140396268832999827, -3.309002319436000317 ) ) ;
#57197=CARTESIAN_POINT ( 'NONE',  ( 11.27765994926999937, 3.273804980682999854, 6.368305648407000419 ) ) ;
#57199=CARTESIAN_POINT ( 'NONE',  ( 8.739954719592999410, 3.122811675949999977, -6.006064052396999919 ) ) ;
#57200=CARTESIAN_POINT ( 'NONE',  ( 2.887168028787000296, 2.953261164984000153, -1.958616092671000120 ) ) ;
#57206=CARTESIAN_POINT ( 'NONE',  ( 3.050973465878000113, 3.500000000000000000, 0.000000000000000000 ) ) ;
#57210=CARTESIAN_POINT ( 'NONE',  ( 11.05639637898999972, 5.030226177531999632, 6.028288223959999748 ) ) ;
#57211=CARTESIAN_POINT ( 'NONE',  ( 11.09999999999999964, 5.350000000000000533, 7.500000000000000000 ) ) ;
#57212=VECTOR ( 'NONE', #10296, 1000.000000000000000 ) ;
#57220=ORIENTED_EDGE ( 'NONE', *, *, #22912, .T. ) ;
#57225=VERTEX_POINT ( 'NONE', #42803 ) ;
#57230=CARTESIAN_POINT ( 'NONE',  ( 10.75102028041000146, 2.478469530773999896, -7.438303846328000013 ) ) ;
#57233=CARTESIAN_POINT ( 'NONE',  ( 9.819055905797000605, 2.899999999999999911, -6.571291218949999902 ) ) ;
#57237=ORIENTED_EDGE ( 'NONE', *, *, #9080, .F. ) ;
#57239=CARTESIAN_POINT ( 'NONE',  ( 7.716064158767000691, 4.574593532473000046, -5.689090339675999530 ) ) ;
#57243=AXIS2_PLACEMENT_3D ( 'NONE', #388, #49662, #1771 ) ;
#57246=ORIENTED_EDGE ( 'NONE', *, *, #14691, .T. ) ;
#57262=ORIENTED_EDGE ( 'NONE', *, *, #48840, .F. ) ;
#57266=CARTESIAN_POINT ( 'NONE',  ( 10.59031493128999912, 7.471983947861001063, -5.946923603349002718 ) ) ;
#57272=DIRECTION ( 'NONE',  ( 1.000000000000000000, 0.000000000000000000, 0.000000000000000000 ) ) ;
#57279=CARTESIAN_POINT ( 'NONE',  ( 10.90421423234000109, 3.863780721621000058, -9.185084890147001246 ) ) ;
#57283=CARTESIAN_POINT ( 'NONE',  ( 10.31167969999000000, 2.874476822401000220, 8.900029516786000627 ) ) ;
#57284=CARTESIAN_POINT ( 'NONE',  ( 1.985247277619000217, 2.372532593102000043, -2.573147701680999599 ) ) ;
#57285=EDGE_CURVE ( 'NONE', #57358, #28975, #14568, .T. ) ;
#57291=CARTESIAN_POINT ( 'NONE',  ( 9.925639158771000226, 4.357364160690000432, -9.282962013144999247 ) ) ;
#57293=CARTESIAN_POINT ( 'NONE',  ( 8.639360841228999277, 5.074768364528000397, -8.296267706722000312 ) ) ;
#57300=CARTESIAN_POINT ( 'NONE',  ( 10.74609776273999984, 4.263105564403999459, 9.276980853981999786 ) ) ;
#57303=CARTESIAN_POINT ( 'NONE',  ( 9.476970280414001024, 5.511689883260999956, -7.095113581311000672 ) ) ;
#57304=CARTESIAN_POINT ( 'NONE',  ( 0.000000000000000000, 2.899969545326000375, 0.3804588500739426449 ) ) ;
#57307=EDGE_CURVE ( 'NONE', #23533, #61768, #39285, .T. ) ;
#57312=CARTESIAN_POINT ( 'NONE',  ( 1.582018817588999982, 2.814509306356999918, 2.491368026013999870 ) ) ;
#57313=EDGE_CURVE ( 'NONE', #39911, #33013, #32887, .T. ) ;
#57315=AXIS2_PLACEMENT_3D ( 'NONE', #33390, #38627, #7156 ) ;
#57316=CARTESIAN_POINT ( 'NONE',  ( 9.070789158774999805, 5.349936549139000519, -7.138437102151999447 ) ) ;
#57325=CARTESIAN_POINT ( 'NONE',  ( 8.160739158772001289, 5.944584532500000407, 7.106843289410999631 ) ) ;
#57329=DIRECTION ( 'NONE',  ( 0.000000000000000000, -0.1218274111675001214, 0.9925512993736016476 ) ) ;
#57330=CARTESIAN_POINT ( 'NONE',  ( 1.366565493715000024, -3.591455136169999562, 0.07279325410826999188 ) ) ;
#57332=CARTESIAN_POINT ( 'NONE',  ( 0.7431103717477000048, 2.848815883361000001, -1.248255999701999963 ) ) ;
#57335=CARTESIAN_POINT ( 'NONE',  ( 10.31457848836000046, 5.362142879234999882, 6.677781064327999339 ) ) ;
#57340=CARTESIAN_POINT ( 'NONE',  ( 8.361173146690900282, 2.869241151408781221, -6.758878718175449052 ) ) ;
#57341=FACE_OUTER_BOUND ( 'NONE', #47314, .T. ) ;
#57342=CARTESIAN_POINT ( 'NONE',  ( 11.09999999999999964, 2.899999999999999911, -4.467422426380999845 ) ) ;
#57343=VERTEX_POINT ( 'NONE', #33003 ) ;
#57347=CARTESIAN_POINT ( 'NONE',  ( 8.427696207745832169, 3.798469702271707771, 6.010277740195467899 ) ) ;
#57349=EDGE_CURVE ( 'NONE', #68545, #67326, #46542, .T. ) ;
#57350=CARTESIAN_POINT ( 'NONE',  ( 10.31167969999000000, 2.874476822401000220, 8.900029516786000627 ) ) ;
#57351=CARTESIAN_POINT ( 'NONE',  ( 9.792312867577999569, 4.284154069364999984, -9.000485152170000447 ) ) ;
#57357=CARTESIAN_POINT ( 'NONE',  ( 8.404999999999999361, 5.190914425723000214, -8.768195054477999406 ) ) ;
#57358=VERTEX_POINT ( 'NONE', #18650 ) ;
#57362=CARTESIAN_POINT ( 'NONE',  ( 10.99249554220161684, 5.864913444040075419, -4.994565819417503327 ) ) ;
#57375=EDGE_CURVE ( 'NONE', #26545, #53432, #43185, .T. ) ;
#57376=CARTESIAN_POINT ( 'NONE',  ( 7.906851002540999929, 2.832432432432000269, -6.822293592207000934 ) ) ;
#57379=ADVANCED_FACE ( 'NONE', ( #17620 ), #39984, .F. ) ;
#57382=CARTESIAN_POINT ( 'NONE',  ( 8.101999744244302804, 3.171054102886417869, 8.579047487216984180 ) ) ;
#57384=B_SPLINE_CURVE_WITH_KNOTS ( 'NONE', 3,
 ( #54595, #55292, #2155, #7387 ),
 .UNSPECIFIED., .F., .F.,
 ( 4, 4 ),
 ( 0.000000000000000000, 1.000000000000000000 ),
 .UNSPECIFIED. ) ;
#57385=CARTESIAN_POINT ( 'NONE',  ( 11.09999999999999964, 2.700688487044999864, -5.124965750789000296 ) ) ;
#57387=CARTESIAN_POINT ( 'NONE',  ( 10.03976415876999972, 2.255572964181999929, -8.111983882175000105 ) ) ;
#57392=ORIENTED_EDGE ( 'NONE', *, *, #64083, .F. ) ;
#57394=DIRECTION ( 'NONE',  ( 0.000000000000000000, 0.9916377111174248249, -0.1290528957048031888 ) ) ;
#57396=CARTESIAN_POINT ( 'NONE',  ( 3.500000000000000000, -1.789730407083999886, 2.652709005895000249 ) ) ;
#57397=CARTESIAN_POINT ( 'NONE',  ( 9.530220962691416275, 2.706107893675387288, -8.716938213633312671 ) ) ;
#57408=CARTESIAN_POINT ( 'NONE',  ( 8.826226023015690814, 5.100000000000000533, -6.272440530347759946 ) ) ;
#57415=FACE_OUTER_BOUND ( 'NONE', #33104, .T. ) ;
#57419=FACE_OUTER_BOUND ( 'NONE', #28866, .T. ) ;
#57420=CARTESIAN_POINT ( 'NONE',  ( 6.899999691988000450, 13.87069231928999891, -4.225386915259999654 ) ) ;
#57423=CARTESIAN_POINT ( 'NONE',  ( 9.061929719594999710, 4.092867382745001059, -5.937785237406000505 ) ) ;
#57430=CARTESIAN_POINT ( 'NONE',  ( 4.149992563292000725, -1.747525841223982912, -1.007210908820215023 ) ) ;
#57435=CARTESIAN_POINT ( 'NONE',  ( 11.09999999999999964, 0.5000000000000000000, -5.124965750789000296 ) ) ;
#57439=CARTESIAN_POINT ( 'NONE',  ( 9.974220280410998285, 5.496789211521000418, -7.043125396300999874 ) ) ;
#57442=CARTESIAN_POINT ( 'NONE',  ( 11.08752642792000032, 2.871528932589999972, -6.302908019754999813 ) ) ;
#57452=CIRCLE ( 'NONE', #63032, 0.5000000000000002220 ) ;
#57455=ADVANCED_FACE ( 'NONE', ( #57415 ), #23156, .F. ) ;
#57457=AXIS2_PLACEMENT_3D ( 'NONE', #29870, #51179, #56070 ) ;
#57460=VERTEX_POINT ( 'NONE', #6256 ) ;
#57462=CARTESIAN_POINT ( 'NONE',  ( 8.731095280410999138, 2.469361196073999842, -7.826019481986000059 ) ) ;
#57464=CARTESIAN_POINT ( 'NONE',  ( 1.134306799208000260, 1.762666431298139713, 3.058252359239908458 ) ) ;
#57470=CARTESIAN_POINT ( 'NONE',  ( 7.744301850232000461, 3.130385018321999890, 6.467396599055999395 ) ) ;
#57480=CARTESIAN_POINT ( 'NONE',  ( 10.12125395348339296, 3.646954034496816099, 8.849054885470943432 ) ) ;
#57484=B_SPLINE_SURFACE_WITH_KNOTS ( 'NONE', 3, 3, ( 
 ( #51338, #19865, #4456, #30701, #34926, #56926, #35269, #41196, #41875, #51673, #3770, #40842, #56586, #62501, #8689, #56243, #68086, #3095, #8349, #3432, #40498, #61825, #62165, #30036, #29695, #67741, #9357, #14961, #9025, #47127, #50996, #19175, #30365, #35943, #68428 ),
 ( #24768, #36285, #14624, #9708, #25107, #46094, #67401, #52010, #19522, #4113, #46782, #24430, #20202, #45754, #57602, #31054, #14287, #52364, #43607, #42567, #59328, #31739, #48502, #52708, #10743, #42912, #64218, #20896, #5841, #16332, #11429, #32769, #21574, #48849, #37661 ),
 ( #27521, #58992, #21236, #607, #11094, #21918, #15311, #53058, #32428, #36635, #43255, #954, #63875, #26147, #22267, #53405, #53744, #57959, #5503, #10057, #31393, #15989, #36984, #4802, #38002, #64561, #16676, #27179, #10400, #54083, #6180, #26492, #32089, #47472, #68778 ),
 ( #26840, #42233, #63539, #15650, #58295, #5157, #48156, #47822, #259, #69131, #37320, #58640, #43954, #27876, #39744, #44311, #18074, #38702, #22611, #54432, #44656, #17018, #65260, #49186, #1992, #12830, #17374, #38349, #60024, #55822, #12477, #59677, #12134, #60371, #7574 ) ),
 .UNSPECIFIED., .F., .F., .F.,
 ( 4, 4 ),
 ( 4, 1, 1, 1, 1, 1, 1, 1, 1, 1, 1, 1, 1, 1, 1, 1, 1, 1, 1, 1, 1, 1, 1, 1, 1, 1, 1, 1, 1, 1, 1, 1, 4 ),
 ( -0.1039370721279000015, 1.103937072127999963 ),
 ( -0.02000000000000000042, 0.01250000000000000069, 0.04499999999999999833, 0.07749999999999999944, 0.1100000000000000006, 0.1424999999999999878, 0.1749999999999999889, 0.2074999999999999900, 0.2399999999999999911, 0.2725000000000000200, 0.3049999999999999933, 0.3375000000000000222, 0.3699999999999999956, 0.4025000000000000244, 0.4349999999999999978, 0.4675000000000000266, 0.5000000000000000000, 0.5324999999999999734, 0.5649999999999999467, 0.5975000000000000311, 0.6300000000000000044, 0.6624999999999999778, 0.6949999999999999512, 0.7275000000000000355, 0.7600000000000000089, 0.7924999999999999822, 0.8249999999999999556, 0.8575000000000000400, 0.8900000000000000133, 0.9224999999999999867, 0.9549999999999999600, 0.9875000000000000444, 1.020000000000000018 ),
 .UNSPECIFIED. ) ;
#57485=CARTESIAN_POINT ( 'NONE',  ( 9.174642513462172744, 2.649442673323004538, 7.499981897072118819 ) ) ;
#57488=CARTESIAN_POINT ( 'NONE',  ( 3.062565470666999801, -3.214256637597999955, -0.5383687126906999687 ) ) ;
#57492=CARTESIAN_POINT ( 'NONE',  ( 8.649445371194000032, 5.100000000000000533, -6.459601070175000181 ) ) ;
#57493=DIRECTION ( 'NONE',  ( 0.7071067811865470176, -0.7011937492001459882, 0.09125418391856598976 ) ) ;
#57500=CARTESIAN_POINT ( 'NONE',  ( 7.798681789217144278, 2.959779466931951486, 6.592102449522434071 ) ) ;
#57510=ORIENTED_EDGE ( 'NONE', *, *, #50048, .F. ) ;
#57511=CARTESIAN_POINT ( 'NONE',  ( 8.449122411348595207, 4.354617778861483934, -9.219396266972353260 ) ) ;
#57513=CARTESIAN_POINT ( 'NONE',  ( 7.660810569926313818, 2.650836722355680575, 7.733623655995972790 ) ) ;
#57514=CARTESIAN_POINT ( 'NONE',  ( 8.169495280408000326, 4.466585441010000324, -5.831585202652000532 ) ) ;
#57526=CARTESIAN_POINT ( 'NONE',  ( 8.218755356758000730, 2.895318267055999595, 6.639774629398000449 ) ) ;
#57533=CARTESIAN_POINT ( 'NONE',  ( 3.000973465876999757, 3.500000000000000000, 0.000000000000000000 ) ) ;
#57540=CARTESIAN_POINT ( 'NONE',  ( 10.46085995768999943, 5.403395036974999677, 7.721808039505000387 ) ) ;
#57544=CARTESIAN_POINT ( 'NONE',  ( 3.012918919220000102, 1.930662435474000072, 2.971610853962999954 ) ) ;
#57548=CARTESIAN_POINT ( 'NONE',  ( 8.073148997456000231, 5.167567567567999731, -6.822293592207000934 ) ) ;
#57550=VERTEX_POINT ( 'NONE', #61137 ) ;
#57552=CARTESIAN_POINT ( 'NONE',  ( 10.26947109217999810, 5.100000000000000533, -6.152188490330000370 ) ) ;
#57555=CARTESIAN_POINT ( 'NONE',  ( 10.93727498060999892, 5.425427353909999972, 7.240585962396000497 ) ) ;
#57556=CARTESIAN_POINT ( 'NONE',  ( 4.500000125099000492, 3.641531520771000148E-13, 3.197442310919999608E-14 ) ) ;
#57575=CARTESIAN_POINT ( 'NONE',  ( 10.22094528040999961, 2.563078870232999851, -8.004103956955001209 ) ) ;
#57576=ORIENTED_EDGE ( 'NONE', *, *, #46541, .T. ) ;
#57581=CARTESIAN_POINT ( 'NONE',  ( 8.913573341230998537, 2.550580605805000012, 8.854682662413999594 ) ) ;
#57584=FACE_OUTER_BOUND ( 'NONE', #31072, .T. ) ;
#57587=ORIENTED_EDGE ( 'NONE', *, *, #22606, .F. ) ;
#57590=VERTEX_POINT ( 'NONE', #34230 ) ;
#57596=CARTESIAN_POINT ( 'NONE',  ( 2.384306799209666927, -1.762666431298145930, -3.058252359239904905 ) ) ;
#57602=CARTESIAN_POINT ( 'NONE',  ( 8.052732780410000402, 4.968147183437999992, 5.971792472497999604 ) ) ;
#57603=EDGE_CURVE ( 'NONE', #4640, #68416, #3085, .T. ) ;
#57605=CARTESIAN_POINT ( 'NONE',  ( 3.500000000000000000, -3.129623072336949807, -0.6860468956751279990 ) ) ;
#57606=VECTOR ( 'NONE', #51817, 999.9999999999998863 ) ;
#57615=DIRECTION ( 'NONE',  ( 0.7071064022000087546, 0.6140603781994079524, 0.3506143007542043555 ) ) ;
#57619=CYLINDRICAL_SURFACE ( 'NONE', #16590, 1.350000000000000533 ) ;
#57620=ORIENTED_EDGE ( 'NONE', *, *, #25669, .T. ) ;
#57626=CARTESIAN_POINT ( 'NONE',  ( 7.717918988116000634, 2.852331522235000083, 6.784355039830999523 ) ) ;
#57627=CARTESIAN_POINT ( 'NONE',  ( 10.49937419337999955, 2.985313722448000195, -6.358656051156999389 ) ) ;
#57631=CARTESIAN_POINT ( 'NONE',  ( 9.447841622600000377, 5.447457912891000120, 7.431328695644999982 ) ) ;
#57636=CARTESIAN_POINT ( 'NONE',  ( 8.564919648097475857, 5.350116636189168773, -7.500005043868485544 ) ) ;
#57637=CARTESIAN_POINT ( 'NONE',  ( 10.74599736040000053, 5.242718773683000322, 8.978699897073999736 ) ) ;
#57639=CARTESIAN_POINT ( 'NONE',  ( 9.468110841233000841, 4.082930418187999955, -6.104944817728999773 ) ) ;
#57648=CARTESIAN_POINT ( 'NONE',  ( 9.327795280414001411, 3.161445734422999809, -6.178649910536000434 ) ) ;
#57651=CARTESIAN_POINT ( 'NONE',  ( 9.188137270893804498, 4.829658083092700060, -8.579838158914373736 ) ) ;
#57656=CARTESIAN_POINT ( 'NONE',  ( 2.472081873819000020, 2.864690124100000013, -2.197449004149000462 ) ) ;
#57659=CARTESIAN_POINT ( 'NONE',  ( 9.939403263311918479, 2.266755596462933564, 7.738633765297627143 ) ) ;
#57662=VERTEX_POINT ( 'NONE', #61478 ) ;
#57668=CARTESIAN_POINT ( 'NONE',  ( 9.385308886257000438, 4.135077451221000011, 9.175524215473998879 ) ) ;
#57670=CARTESIAN_POINT ( 'NONE',  ( 10.40685100253999984, 2.832432432432000269, -6.822293592207000934 ) ) ;
#57674=VERTEX_POINT ( 'NONE', #13934 ) ;
#57677=FACE_OUTER_BOUND ( 'NONE', #60798, .T. ) ;
#57678=CARTESIAN_POINT ( 'NONE',  ( 9.799251915619999309, 4.057329420971000467, 9.430703183047999261 ) ) ;
#57681=CARTESIAN_POINT ( 'NONE',  ( 10.31905590579000176, 2.899999999999999911, -6.571291218949999902 ) ) ;
#57682=EDGE_CURVE ( 'NONE', #47578, #25073, #39566, .T. ) ;
#57685=CARTESIAN_POINT ( 'NONE',  ( 8.352297532185232853, 2.893034095650034665, -6.685148257416485329 ) ) ;
#57686=AXIS2_PLACEMENT_3D ( 'NONE', #54080, #12131, #59674 ) ;
#57689=ORIENTED_EDGE ( 'NONE', *, *, #35220, .T. ) ;
#57692=VERTEX_POINT ( 'NONE', #35260 ) ;
#57696=CARTESIAN_POINT ( 'NONE',  ( 11.11845610223999969, 5.767025078915000158, 7.178418469370999588 ) ) ;
#57697=CARTESIAN_POINT ( 'NONE',  ( 10.04002816746000093, 2.348904337896000172, -7.136750921008999882 ) ) ;
#57702=CARTESIAN_POINT ( 'NONE',  ( 9.002567663965152178, 5.272335535898198700, 7.950868213405990481 ) ) ;
#57721=CARTESIAN_POINT ( 'NONE',  ( 0.000000000000000000, 0.000000000000000000, 0.000000000000000000 ) ) ;
#57726=CARTESIAN_POINT ( 'NONE',  ( 0.7654415426042999737, 2.838478058858999731, -1.283102133118000143 ) ) ;
#57732=CARTESIAN_POINT ( 'NONE',  ( 10.84974221959000218, 5.265003089217000998, -6.385808769407000263 ) ) ;
#57734=FACE_OUTER_BOUND ( 'NONE', #40890, .T. ) ;
#57741=FACE_OUTER_BOUND ( 'NONE', #60739, .T. ) ;
#57745=CARTESIAN_POINT ( 'NONE',  ( 4.149992563292000725, -2.000000000000000000, 0.000000000000000000 ) ) ;
#57748=CARTESIAN_POINT ( 'NONE',  ( 8.154367619217863350, 3.070658246196826369, 6.308684818284896245 ) ) ;
#57758=CARTESIAN_POINT ( 'NONE',  ( 8.212416242268998801, 3.104180772687998857, 6.104177153569003700 ) ) ;
#57759=AXIS2_PLACEMENT_3D ( 'NONE', #17385, #66307, #50584 ) ;
#57768=CARTESIAN_POINT ( 'NONE',  ( 2.873890132544666631, -2.150913519912200922, -2.798833948393631754 ) ) ;
#57769=ORIENTED_EDGE ( 'NONE', *, *, #31966, .F. ) ;
#57770=CARTESIAN_POINT ( 'NONE',  ( 9.550320280412000429, 2.370176859044999862, -6.912649125838000508 ) ) ;
#57772=ORIENTED_EDGE ( 'NONE', *, *, #34631, .F. ) ;
#57773=EDGE_CURVE ( 'NONE', #68416, #53136, #17914, .T. ) ;
#57778=CARTESIAN_POINT ( 'NONE',  ( 8.596685841231000325, 2.141799395716999843, -7.895788736628000848 ) ) ;
#57784=CARTESIAN_POINT ( 'NONE',  ( 11.09999999999999964, 6.518040529534999905, 5.523195900108999190 ) ) ;
#57787=CARTESIAN_POINT ( 'NONE',  ( 10.12339528040999959, 3.988943694240999704, -8.966360307350999648 ) ) ;
#57789=VECTOR ( 'NONE', #40996, 1000.000000000000000 ) ;
#57790=CARTESIAN_POINT ( 'NONE',  ( 10.99480479316000014, 3.850613903518000036, -9.347963496621000345 ) ) ;
#57791=ORIENTED_EDGE ( 'NONE', *, *, #22785, .F. ) ;
#57799=CARTESIAN_POINT ( 'NONE',  ( 4.099967492754000631, 2.049969825927307809, 8.734272638079285836E-09 ) ) ;
#57800=CARTESIAN_POINT ( 'NONE',  ( 10.90000000000000036, 0.2999999999999999889, -4.902439024389999567 ) ) ;
#57804=CARTESIAN_POINT ( 'NONE',  ( 10.35685100253999913, 2.832432432432000269, -6.822293592207000934 ) ) ;
#57807=CARTESIAN_POINT ( 'NONE',  ( 8.400739158770999637, 4.933589693325000525, -9.154576215408999573 ) ) ;
#57811=ORIENTED_EDGE ( 'NONE', *, *, #59986, .T. ) ;
#57813=CARTESIAN_POINT ( 'NONE',  ( 9.020585841232000135, 4.920236664407999783, -6.448229650796999834 ) ) ;
#57820=CARTESIAN_POINT ( 'NONE',  ( 8.684778640374556602, 5.715811837031070652, 7.158423063840858802 ) ) ;
#57825=EDGE_CURVE ( 'NONE', #54335, #1602, #14616, .T. ) ;
#57832=B_SPLINE_CURVE_WITH_KNOTS ( 'NONE', 3,
 ( #49875, #44651, #28919, #23647 ),
 .UNSPECIFIED., .F., .F.,
 ( 4, 4 ),
 ( 0.000000000000000000, 1.000000000000000000 ),
 .UNSPECIFIED. ) ;
#57839=AXIS2_PLACEMENT_3D ( 'NONE', #22060, #64704, #16815 ) ;
#57840=CARTESIAN_POINT ( 'NONE',  ( 0.1359928592618749876, 2.324556273228959184E-06, -3.136013406113613122 ) ) ;
#57841=CARTESIAN_POINT ( 'NONE',  ( 0.1499942179680000265, -0.7197945678028380145, -2.678379783547566451 ) ) ;
#57842=CARTESIAN_POINT ( 'NONE',  ( 2.967201571784999992, -1.671031821269000295, 2.798024169910999781 ) ) ;
#57846=DIRECTION ( 'NONE',  ( 0.000000000000000000, -1.000000000000000000, 0.000000000000000000 ) ) ;
#57847=CIRCLE ( 'NONE', #4242, 1.500000000000000000 ) ;
#57856=CARTESIAN_POINT ( 'NONE',  ( 10.64200660896710637, 3.294104879791080798, 8.705431914969542717 ) ) ;
#57859=ORIENTED_EDGE ( 'NONE', *, *, #38884, .F. ) ;
#57866=ORIENTED_EDGE ( 'NONE', *, *, #24702, .T. ) ;
#57867=CARTESIAN_POINT ( 'NONE',  ( 8.580688975202768631, 2.255905088303147288, -7.709247227175728412 ) ) ;
#57871=CARTESIAN_POINT ( 'NONE',  ( 8.368395280410000581, 4.586183217919999500, -9.013777652867000612 ) ) ;
#57873=CARTESIAN_POINT ( 'NONE',  ( 7.100000000000000533, 4.000000000000000000, 7.500000000000000000 ) ) ;
#57874=EDGE_LOOP ( 'NONE', ( #57035, #26888, #39400, #39096, #50244 ) ) ;
#57881=CARTESIAN_POINT ( 'NONE',  ( 8.424688440789140031, 5.350083765069828523, 7.500019236172019710 ) ) ;
#57882=CARTESIAN_POINT ( 'NONE',  ( 10.83776233157765390, 3.727019380500508738, 9.251996054089767441 ) ) ;
#57886=CARTESIAN_POINT ( 'NONE',  ( 0.000000000000000000, 0.000000000000000000, 0.000000000000000000 ) ) ;
#57890=EDGE_LOOP ( 'NONE', ( #22948, #203, #17815, #22327 ) ) ;
#57893=CARTESIAN_POINT ( 'NONE',  ( 9.555697025339000561, 2.440752375194999768, 6.680879724048000234 ) ) ;
#57895=FACE_OUTER_BOUND ( 'NONE', #45837, .T. ) ;
#57896=CARTESIAN_POINT ( 'NONE',  ( 9.617285841233000454, 5.306366356490000769, -7.996450761531000317 ) ) ;
#57898=CARTESIAN_POINT ( 'NONE',  ( 2.852007699173999988, -2.078510391984000449, -3.070736864395000154 ) ) ;
#57900=CARTESIAN_POINT ( 'NONE',  ( 8.070148464763398977, 5.142014101325858455, -6.778269516176797183 ) ) ;
#57904=VECTOR ( 'NONE', #27315, 1000.000000000000000 ) ;
#57907=CARTESIAN_POINT ( 'NONE',  ( 3.280140132543750475, -3.408904368339108260, 0.9161175952574674985 ) ) ;
#57910=CARTESIAN_POINT ( 'NONE',  ( 10.96580581817999978, 4.930645553951000792, 6.170542400361000546 ) ) ;
#57921=CARTESIAN_POINT ( 'NONE',  ( 10.20000099824999928, -1.190159082397999942E-13, -12.49999978039866733 ) ) ;
#57922=ORIENTED_EDGE ( 'NONE', *, *, #36173, .F. ) ;
#57926=CYLINDRICAL_SURFACE ( 'NONE', #42733, 3.200000000000000178 ) ;
#57931=CARTESIAN_POINT ( 'NONE',  ( 10.33453278041000090, 3.295703187163999459, -6.149878749787999865 ) ) ;
#57932=VERTEX_POINT ( 'NONE', #48491 ) ;
#57933=FACE_OUTER_BOUND ( 'NONE', #45602, .T. ) ;
#57934=B_SPLINE_CURVE_WITH_KNOTS ( 'NONE', 3,
 ( #49873, #7565, #19085, #40088, #13518, #34839, #50223, #60706, #40411, #8599, #28918, #56150, #1986, #23308, #29949, #24338, #39738, #29607, #34503, #18068, #35182, #66976, #2325, #3348, #12471, #44648, #46004, #13854, #23646, #33804, #44985, #7224, #55816, #61733, #39385, #29256, #12824, #34149, #55468, #50565, #50908, #2667, #23993, #51252, #45670 ),
 .UNSPECIFIED., .F., .F.,
 ( 4, 2, 2, 2, 2, 2, 2, 2, 2, 1, 2, 2, 2, 2, 1, 1, 1, 2, 2, 2, 2, 1, 2, 2, 4 ),
 ( 0.000000000000000000, 0.1249999999999692468, 0.1874999999999541478, 0.2499999999999399369, 0.3749999999999112377, 0.4374999999998979150, 0.4687499999998902545, 0.4999999999998826494, 0.5624999999998692157, 0.5937499999998616662, 0.6093749999998585576, 0.6249999999998553379, 0.6874999999998469002, 0.7187499999998420153, 0.7343749999998387956, 0.7421874999998367972, 0.7460937499998359090, 0.7480468749998355760, 0.7499999999998353539, 0.8124999999998712141, 0.8437499999998891997, 0.8593749999998983036, 0.8671874999999030775, 0.8749999999999079625, 1.000000000000000000 ),
 .UNSPECIFIED. ) ;
#57938=CARTESIAN_POINT ( 'NONE',  ( 9.041948341230998665, 2.707986230053999854, 5.994446745591000436 ) ) ;
#57941=CARTESIAN_POINT ( 'NONE',  ( 7.616614158767000653, 2.462963193532999640, -6.383277393009000100 ) ) ;
#57944=ORIENTED_EDGE ( 'NONE', *, *, #37638, .F. ) ;
#57949=CARTESIAN_POINT ( 'NONE',  ( 6.899999691988000450, 12.20988339176000004, 3.111064831550000243 ) ) ;
#57950=ORIENTED_EDGE ( 'NONE', *, *, #31967, .T. ) ;
#57953=CARTESIAN_POINT ( 'NONE',  ( 2.415556799209791716, -0.4581489286485083134, -3.500000000000000888 ) ) ;
#57959=CARTESIAN_POINT ( 'NONE',  ( 8.154704719592000828, 4.255646040929000229, 9.114085578076998928 ) ) ;
#57961=LINE ( 'NONE', #3773, #31787 ) ;
#57966=EDGE_CURVE ( 'NONE', #62671, #12641, #32418, .T. ) ;
#57967=CARTESIAN_POINT ( 'NONE',  ( 8.082952751019996995, 10.21641539395999843, -5.351219519932003621 ) ) ;
#57977=ORIENTED_EDGE ( 'NONE', *, *, #26798, .T. ) ;
#57980=CARTESIAN_POINT ( 'NONE',  ( 4.900006121742000786, -0.2617993877991476315, 2.000000000000000444 ) ) ;
#57981=CARTESIAN_POINT ( 'NONE',  ( 10.10656234570999956, 4.887646627408000377, -6.257286147482000516 ) ) ;
#57987=VERTEX_POINT ( 'NONE', #42900 ) ;
#57988=CARTESIAN_POINT ( 'NONE',  ( 9.144189324567731703, 2.621867583237485810, -6.380228173633875066 ) ) ;
#57990=CARTESIAN_POINT ( 'NONE',  ( 9.347254965556000883, 4.028327103212000715, 9.469449669541999626 ) ) ;
#57992=CARTESIAN_POINT ( 'NONE',  ( 11.09647882763000126, 3.099775370665000196, 6.097099813297999660 ) ) ;
#57994=CARTESIAN_POINT ( 'NONE',  ( 6.875000000000000000, 5.574137966889000317, -8.240733100917999820 ) ) ;
#57995=CARTESIAN_POINT ( 'NONE',  ( 10.97885795247000118, 9.422687720258000610, -6.230811109673999759 ) ) ;
#58000=ADVANCED_FACE ( 'NONE', ( #37650 ), #27169, .F. ) ;
#58001=CARTESIAN_POINT ( 'NONE',  ( 10.68903608760000168, 2.568976842941999905, 7.728092503410000091 ) ) ;
#58004=CARTESIAN_POINT ( 'NONE',  ( 9.178620280414001797, 2.990001567622999623, -8.695425648791999862 ) ) ;
#58005=CARTESIAN_POINT ( 'NONE',  ( -0.000000000000000000, 0.7586348975815447870, 2.824745580908568421 ) ) ;
#58006=EDGE_CURVE ( 'NONE', #58925, #15028, #21114, .T. ) ;
#58009=CARTESIAN_POINT ( 'NONE',  ( 9.219380188869688908, 4.353236832146805568, -8.814507018246107606 ) ) ;
#58012=VERTEX_POINT ( 'NONE', #49175 ) ;
#58015=CARTESIAN_POINT ( 'NONE',  ( 9.711073749820098300, 5.731818165367177365, 7.738391472525679049 ) ) ;
#58019=CARTESIAN_POINT ( 'NONE',  ( 10.68362359175999998, 2.603561947343000060, 7.762063351517999976 ) ) ;
#58025=CARTESIAN_POINT ( 'NONE',  ( 7.647239158771000689, 5.850290547079999293, 6.784176679236000318 ) ) ;
#58037=CARTESIAN_POINT ( 'NONE',  ( 9.285195242305000818, 5.269680202247999823, 8.747831873285999649 ) ) ;
#58038=CARTESIAN_POINT ( 'NONE',  ( 10.30047009227000032, 4.027768540959000276, 9.431354536774000152 ) ) ;
#58040=ORIENTED_EDGE ( 'NONE', *, *, #25983, .F. ) ;
#58054=CARTESIAN_POINT ( 'NONE',  ( 9.843622243630001378, 5.021682716044000294, -8.761466596873999535 ) ) ;
#58060=CARTESIAN_POINT ( 'NONE',  ( 9.039569060871647466, 4.932468115888118732, 8.476030941254864004 ) ) ;
#58062=CARTESIAN_POINT ( 'NONE',  ( 7.545267219589999463, 2.302289264429000504, 6.875166305059000393 ) ) ;
#58063=ORIENTED_EDGE ( 'NONE', *, *, #45024, .T. ) ;
#58066=FACE_OUTER_BOUND ( 'NONE', #60619, .T. ) ;
#58067=CARTESIAN_POINT ( 'NONE',  ( 8.702564146836889947, 2.714984396920538945, 7.027277620402957226 ) ) ;
#58068=CARTESIAN_POINT ( 'NONE',  ( 10.78515324564000011, 10.04038604719000816, 5.237765435261001912 ) ) ;
#58077=CARTESIAN_POINT ( 'NONE',  ( 5.500000000000000000, 0.000000000000000000, 0.000000000000000000 ) ) ;
#58082=CARTESIAN_POINT ( 'NONE',  ( 0.1347486600378000055, -1.491878233134000142, -2.734521550864000172 ) ) ;
#58088=ADVANCED_FACE ( 'NONE', ( #2661 ), #23989, .T. ) ;
#58089=CARTESIAN_POINT ( 'NONE',  ( 10.09249221959000131, 2.841614569232000065, -8.724659027040001291 ) ) ;
#58096=DIRECTION ( 'NONE',  ( 0.8660254037844541397, 0.000000000000000000, -0.4999999999999731326 ) ) ;
#58101=CARTESIAN_POINT ( 'NONE',  ( 10.90000000164000049, 5.100000000007000267, 5.160242739040000082 ) ) ;
#58103=ORIENTED_EDGE ( 'NONE', *, *, #33756, .T. ) ;
#58110=AXIS2_PLACEMENT_3D ( 'NONE', #16181, #64061, #58831 ) ;
#58112=CARTESIAN_POINT ( 'NONE',  ( 8.578316401368688560, 5.031557300139490430, 6.208917336984066893 ) ) ;
#58117=CARTESIAN_POINT ( 'NONE',  ( 8.933536308090499034, 2.899999999999999911, -6.665341197412910645 ) ) ;
#58118=PLANE ( 'NONE',  #40886 ) ;
#58123=ORIENTED_EDGE ( 'NONE', *, *, #49441, .F. ) ;
#58124=CARTESIAN_POINT ( 'NONE',  ( 8.456370280410999030, 2.836879604150999601, -8.783908972046001296 ) ) ;
#58126=VERTEX_POINT ( 'NONE', #23641 ) ;
#58132=CARTESIAN_POINT ( 'NONE',  ( 10.20000099824999928, -12.50000000000000000, 0.000000000000000000 ) ) ;
#58135=B_SPLINE_CURVE_WITH_KNOTS ( 'NONE', 3,
 ( #63203, #31077, #11116, #69152, #68798, #10419, #281, #42589, #47492, #57980, #21259, #63897, #53765, #64239, #15673, #26863, #10077, #15331 ),
 .UNSPECIFIED., .F., .F.,
 ( 4, 2, 2, 2, 2, 2, 2, 2, 4 ),
 ( 0.000000000000000000, 0.1249999999999999722, 0.2500000000000000000, 0.3750000000000000000, 0.5000000000000001110, 0.6250000000000001110, 0.7500000000000000000, 0.8750000000000000000, 1.000000000000000000 ),
 .UNSPECIFIED. ) ;
#58139=LINE ( 'NONE', #52544, #65550 ) ;
#58140=CARTESIAN_POINT ( 'NONE',  ( 9.237204719595000668, 3.071719032003000116, -6.037263251225000182 ) ) ;
#58142=CARTESIAN_POINT ( 'NONE',  ( 8.668369459057998938, 3.037916315484999963, -6.050520490110999461 ) ) ;
#58146=DIRECTION ( 'NONE',  ( -1.000000000000000000, 0.000000000000000000, 0.000000000000000000 ) ) ;
#58147=FACE_OUTER_BOUND ( 'NONE', #53983, .T. ) ;
#58149=ORIENTED_EDGE ( 'NONE', *, *, #53574, .T. ) ;
#58153=DIRECTION ( 'NONE',  ( 1.000000000000000000, 0.000000000000000000, 0.000000000000000000 ) ) ;
#58154=B_SPLINE_CURVE_WITH_KNOTS ( 'NONE', 3,
 ( #62982, #47959, #26292, #41338, #47618, #68929, #30850, #53199, #15458, #5300, #57748, #20698, #68232, #15109, #40991, #26642, #42375 ),
 .UNSPECIFIED., .F., .F.,
 ( 4, 2, 2, 2, 1, 2, 2, 2, 4 ),
 ( 0.000000000000000000, 0.2500000000000131006, 0.3750000000000214273, 0.4375000000000257572, 0.4687500000000269784, 0.4843750000000265898, 0.5000000000000262013, 0.7500000000000131006, 1.000000000000000000 ),
 .UNSPECIFIED. ) ;
#58156=CARTESIAN_POINT ( 'NONE',  ( 9.883629719592001095, 5.656948148960999845, -6.994239053114000626 ) ) ;
#58163=CARTESIAN_POINT ( 'NONE',  ( 7.896812975352940356, 5.287194663100549974, 7.026484571482192187 ) ) ;
#58164=CARTESIAN_POINT ( 'NONE',  ( 4.000000000000000000, -2.750000000000000000, 0.000000000000000000 ) ) ;
#58175=AXIS2_PLACEMENT_3D ( 'NONE', #47906, #20641, #10150 ) ;
#58188=CARTESIAN_POINT ( 'NONE',  ( 10.61094409420999973, 5.100000000000000533, -6.571291218949999902 ) ) ;
#58189=ORIENTED_EDGE ( 'NONE', *, *, #49441, .T. ) ;
#58194=CARTESIAN_POINT ( 'NONE',  ( 1.561390132540708908, 3.499999999999999112, 0.4581489286485193602 ) ) ;
#58199=CARTESIAN_POINT ( 'NONE',  ( 0.000000000000000000, 0.000000000000000000, 0.000000000000000000 ) ) ;
#58200=CARTESIAN_POINT ( 'NONE',  ( 8.191498566858999908, 3.399962487441000381, 6.146646668338000552 ) ) ;
#58210=CARTESIAN_POINT ( 'NONE',  ( 8.646472257129413919, 2.666605646700320076, -6.358381277404491883 ) ) ;
#58212=CARTESIAN_POINT ( 'NONE',  ( 7.034679719589999713, 3.562914451704999763, -5.997303864335000512 ) ) ;
#58217=LINE ( 'NONE', #39657, #18353 ) ;
#58219=VERTEX_POINT ( 'NONE', #2320 ) ;
#58227=EDGE_CURVE ( 'NONE', #9042, #38413, #56161, .T. ) ;
#58229=DIRECTION ( 'NONE',  ( 0.000000000000000000, -1.000000000000000000, 0.000000000000000000 ) ) ;
#58235=CARTESIAN_POINT ( 'NONE',  ( 11.05935155529000014, 2.480238120735000162, 6.610075178640000715 ) ) ;
#58236=CARTESIAN_POINT ( 'NONE',  ( 10.68342665876999931, 3.810131921595000026, -5.661115150006999386 ) ) ;
#58247=EDGE_CURVE ( 'NONE', #51926, #29332, #49465, .T. ) ;
#58249=CARTESIAN_POINT ( 'NONE',  ( 9.509901345851000443, 5.077442745148000647, 8.469003100811999474 ) ) ;
#58250=DIRECTION ( 'NONE',  ( 0.000000000000000000, 1.000000000000000000, 0.000000000000000000 ) ) ;
#58258=CARTESIAN_POINT ( 'NONE',  ( 11.09999999999999964, 4.000000000000000000, -7.500000000000000000 ) ) ;
#58261=CARTESIAN_POINT ( 'NONE',  ( 8.822164158776001130, 2.644017913812000131, -7.838184857420000817 ) ) ;
#58265=VECTOR ( 'NONE', #1410, 999.9999999999998863 ) ;
#58269=CARTESIAN_POINT ( 'NONE',  ( 10.34939834122999969, 2.653159779809000085, -7.312415497503999440 ) ) ;
#58270=ORIENTED_EDGE ( 'NONE', *, *, #36018, .F. ) ;
#58275=CARTESIAN_POINT ( 'NONE',  ( 7.694010841228000608, 5.850290547079999293, 6.784176679236000318 ) ) ;
#58281=ORIENTED_EDGE ( 'NONE', *, *, #18232, .F. ) ;
#58295=CARTESIAN_POINT ( 'NONE',  ( 7.229676658770999964, 2.630487280353000390, 6.995957894972000268 ) ) ;
#58296=EDGE_LOOP ( 'NONE', ( #18778, #64538, #7277, #8676, #37518 ) ) ;
#58297=B_SPLINE_CURVE_WITH_KNOTS ( 'NONE', 3,
 ( #23154, #54273, #65797, #48694 ),
 .UNSPECIFIED., .F., .F.,
 ( 4, 4 ),
 ( 0.000000000000000000, 1.000000000000000000 ),
 .UNSPECIFIED. ) ;
#58319=CARTESIAN_POINT ( 'NONE',  ( 10.11859053700000111, 3.393394511985999618, -5.921995869926000466 ) ) ;
#58323=CARTESIAN_POINT ( 'NONE',  ( 8.076862866721999268, 2.879478799711000292, -6.727223656603999125 ) ) ;
#58326=CARTESIAN_POINT ( 'NONE',  ( 8.831347292302233143, 5.765877224304255755, -7.300045774259967146 ) ) ;
#58328=CARTESIAN_POINT ( 'NONE',  ( 8.608142887202433258, 5.166153502812370846, -8.205198856529275275 ) ) ;
#58329=CARTESIAN_POINT ( 'NONE',  ( 9.687870098586998324, 5.912263966150999472, 7.772301113561999486 ) ) ;
#58331=CARTESIAN_POINT ( 'NONE',  ( 8.921135841230999119, 3.292387953886000140, -6.294868737226000377 ) ) ;
#58339=CARTESIAN_POINT ( 'NONE',  ( 9.567560841232999991, 5.349936549139000519, -7.138437102151999447 ) ) ;
#58342=CARTESIAN_POINT ( 'NONE',  ( 3.500000000000000000, 3.499738125128000199, -0.04281419768536000314 ) ) ;
#58345=ORIENTED_EDGE ( 'NONE', *, *, #4218, .T. ) ;
#58347=DIRECTION ( 'NONE',  ( 0.000000000000000000, 0.000000000000000000, -1.000000000000000000 ) ) ;
#58348=CARTESIAN_POINT ( 'NONE',  ( 7.694010841228000608, 5.850290547079999293, 6.784176679236000318 ) ) ;
#58351=CARTESIAN_POINT ( 'NONE',  ( 9.509454719593000149, 3.116293075258000478, -6.208411413796000033 ) ) ;
#58355=CARTESIAN_POINT ( 'NONE',  ( 10.96207813434000045, 5.399835028078000754, 7.743264559064000352 ) ) ;
#58361=CARTESIAN_POINT ( 'NONE',  ( 8.096551658772000337, 5.061727314042999915, 5.824077473724000420 ) ) ;
#58367=CARTESIAN_POINT ( 'NONE',  ( 2.167611958084000090, -0.2760264376601999636, -3.247374627496999899 ) ) ;
#58371=CARTESIAN_POINT ( 'NONE',  ( 9.910633732652998518, 2.107262079134000210, 7.885285091859000062 ) ) ;
#58383=ORIENTED_EDGE ( 'NONE', *, *, #1699, .F. ) ;
#58386=CARTESIAN_POINT ( 'NONE',  ( 9.758140238852000437, 2.901378080241999946, 6.555076849497999625 ) ) ;
#58387=CARTESIAN_POINT ( 'NONE',  ( 10.90421423234000109, 3.863780721621000058, -9.185084890147001246 ) ) ;
#58389=EDGE_CURVE ( 'NONE', #57460, #10927, #26941, .T. ) ;
#58395=EDGE_CURVE ( 'NONE', #33299, #63876, #53649, .T. ) ;
#58397=CARTESIAN_POINT ( 'NONE',  ( 8.855420280411999912, 5.633477595780999714, 7.451234169193000412 ) ) ;
#58401=CARTESIAN_POINT ( 'NONE',  ( 0.000000000000000000, 0.000000000000000000, 0.000000000000000000 ) ) ;
#58404=CARTESIAN_POINT ( 'NONE',  ( 11.07128326594000001, 6.555132067871999979, 5.493445694320000072 ) ) ;
#58405=CARTESIAN_POINT ( 'NONE',  ( 11.13602668609999924, 9.532506022458999695, 6.386669746941000092 ) ) ;
#58411=DIRECTION ( 'NONE',  ( 0.000000000000000000, -1.000000000000000000, 0.000000000000000000 ) ) ;
#58416=AXIS2_PLACEMENT_3D ( 'NONE', #48952, #28316, #44412 ) ;
#58417=CARTESIAN_POINT ( 'NONE',  ( 0.5734915348667000146, -3.063090672237000156, -0.9584583608479999572 ) ) ;
#58421=CARTESIAN_POINT ( 'NONE',  ( 9.110944094209999733, 5.100000000000000533, -6.571291218949999902 ) ) ;
#58424=CARTESIAN_POINT ( 'NONE',  ( 10.54684221959000112, 3.691673619534999951, -9.157283848447001162 ) ) ;
#58429=CARTESIAN_POINT ( 'NONE',  ( 10.98768472638000127, 7.408460511344000743, 6.159405790617999976 ) ) ;
#58430=ORIENTED_EDGE ( 'NONE', *, *, #51828, .T. ) ;
#58431=CARTESIAN_POINT ( 'NONE',  ( 0.9287915396056000139, -1.955279592509000075, 2.607329530612999768 ) ) ;
#58432=DIRECTION ( 'NONE',  ( 1.000000000000000000, 0.000000000000000000, 0.000000000000000000 ) ) ;
#58434=CARTESIAN_POINT ( 'NONE',  ( 9.399846034910298798, 5.293376409283213846, -8.716279758284748880 ) ) ;
#58448=DIRECTION ( 'NONE',  ( 0.000000000000000000, -0.9916377111174248249, -0.1290528957048032721 ) ) ;
#58459=ORIENTED_EDGE ( 'NONE', *, *, #17346, .T. ) ;
#58460=CARTESIAN_POINT ( 'NONE',  ( 8.233179719589999834, 5.203550244299999683, -8.391678825488000371 ) ) ;
#58466=ORIENTED_EDGE ( 'NONE', *, *, #29936, .F. ) ;
#58469=CARTESIAN_POINT ( 'NONE',  ( 9.292835841232999883, 5.200883864107000321, -6.027780766890000308 ) ) ;
#58477=EDGE_CURVE ( 'NONE', #26858, #58783, #59492, .T. ) ;
#58480=CARTESIAN_POINT ( 'NONE',  ( 8.704862649514709005, 2.649860810595531468, 7.852951878456049251 ) ) ;
#58492=EDGE_CURVE ( 'NONE', #51766, #54068, #18359, .T. ) ;
#58494=CARTESIAN_POINT ( 'NONE',  ( 11.09999999999999964, 4.000000000000000000, 7.500000000000000000 ) ) ;
#58496=CARTESIAN_POINT ( 'NONE',  ( 9.494689158774999527, 2.824732249080000202, -8.992748220058999209 ) ) ;
#58500=ORIENTED_EDGE ( 'NONE', *, *, #36389, .T. ) ;
#58501=CARTESIAN_POINT ( 'NONE',  ( 10.98148521858999871, 5.115205842040000839, -4.906648178026999929 ) ) ;
#58503=CARTESIAN_POINT ( 'NONE',  ( 11.09999999999999964, 5.449702572737000317, -5.124965750789000296 ) ) ;
#58511=CARTESIAN_POINT ( 'NONE',  ( 4.000000000000000000, 2.750000000000000000, 0.000000000000000000 ) ) ;
#58512=CONICAL_SURFACE ( 'NONE', #67441, 3.249989426617000188, 0.7853950157668545540 ) ;
#58519=CARTESIAN_POINT ( 'NONE',  ( 6.999998782146999332, 0.000000000000000000, 0.000000000000000000 ) ) ;
#58521=CARTESIAN_POINT ( 'NONE',  ( 7.531666666664000864, 4.679885623500713798, -6.320388375721750940 ) ) ;
#58524=CARTESIAN_POINT ( 'NONE',  ( 6.999999999999999112, 9.413677030445844807, -4.695585979740934057 ) ) ;
#58525=CARTESIAN_POINT ( 'NONE',  ( 0.1499942179680000542, -0.3599680999393992664, -2.749953718116143087 ) ) ;
#58530=CARTESIAN_POINT ( 'NONE',  ( 3.499684904184919176, -2.717109755674974814, -1.809093184580113700 ) ) ;
#58531=CARTESIAN_POINT ( 'NONE',  ( 10.21921441925191054, 4.353287638978129870, -8.814644987549721478 ) ) ;
#58539=ORIENTED_EDGE ( 'NONE', *, *, #50073, .F. ) ;
#58545=CARTESIAN_POINT ( 'NONE',  ( 7.202583736560634442, 0.2999999999999999889, -3.098821334907657654 ) ) ;
#58548=EDGE_LOOP ( 'NONE', ( #26234, #23727, #63199, #33879 ) ) ;
#58550=CARTESIAN_POINT ( 'NONE',  ( 6.884360841229000272, 5.757004663580000070, -7.968612095259000050 ) ) ;
#58553=ORIENTED_EDGE ( 'NONE', *, *, #786, .T. ) ;
#58564=FACE_OUTER_BOUND ( 'NONE', #47977, .T. ) ;
#58568=CARTESIAN_POINT ( 'NONE',  ( 7.910745297646997187, 4.529763905033002303, -6.316445270365000475 ) ) ;
#58569=CARTESIAN_POINT ( 'NONE',  ( 8.023148997453999343, 5.167567567567999731, -6.822293592207000934 ) ) ;
#58570=PLANE ( 'NONE',  #9452 ) ;
#58571=CARTESIAN_POINT ( 'NONE',  ( 10.10000011340999926, -1.190159082397999942E-13, -1.214010018759999782E-13 ) ) ;
#58572=VERTEX_POINT ( 'NONE', #48404 ) ;
#58576=CARTESIAN_POINT ( 'NONE',  ( 9.667078842372998082, 4.541623431405000133, 5.824038024834000460 ) ) ;
#58577=CARTESIAN_POINT ( 'NONE',  ( 11.02418915877000138, 2.407889430138999920, -8.439554272735000140 ) ) ;
#58578=EDGE_CURVE ( 'NONE', #28207, #129, #7744, .T. ) ;
#58582=DIRECTION ( 'NONE',  ( 0.000000000000000000, 1.000000000000000000, 0.000000000000000000 ) ) ;
#58583=EDGE_CURVE ( 'NONE', #35262, #26212, #49093, .T. ) ;
#58602=VERTEX_POINT ( 'NONE', #44215 ) ;
#58604=CARTESIAN_POINT ( 'NONE',  ( 8.175739158770999992, 4.686731264770999772, -8.717075579553000608 ) ) ;
#58608=CARTESIAN_POINT ( 'NONE',  ( 0.9218879684122999185, 1.034012873651999787, -3.554373790709000058 ) ) ;
#58609=AXIS2_PLACEMENT_3D ( 'NONE', #43047, #53, #28010 ) ;
#58611=CARTESIAN_POINT ( 'NONE',  ( 2.409338192682000113, 0.3184749856117999878, -3.745257128239000366 ) ) ;
#58619=CARTESIAN_POINT ( 'NONE',  ( 5.500000000000000000, 11.95749337870000062, 3.642574926947999892 ) ) ;
#58621=CARTESIAN_POINT ( 'NONE',  ( 8.999999001754000361, 12.50000000000000000, 0.000000000000000000 ) ) ;
#58622=CARTESIAN_POINT ( 'NONE',  ( 8.046420280407000192, 5.281793838578000333, -8.397855149904000172 ) ) ;
#58630=CARTESIAN_POINT ( 'NONE',  ( 11.10000000000000142, 3.333792990081902552, -8.929221575986867165 ) ) ;
#58638=CIRCLE ( 'NONE', #21800, 13.10000000000000142 ) ;
#58640=CARTESIAN_POINT ( 'NONE',  ( 7.678989158771000412, 2.599243720295000060, 7.909344432242998657 ) ) ;
#58651=CARTESIAN_POINT ( 'NONE',  ( 0.3870378418490574290, -3.299192355781437325, -0.8857457579047530727 ) ) ;
#58652=CARTESIAN_POINT ( 'NONE',  ( 0.000000000000000000, 2.899999999999999911, -7.500000000000000000 ) ) ;
#58664=CARTESIAN_POINT ( 'NONE',  ( 10.04002816746000093, 2.348904337896000172, -7.136750921008999882 ) ) ;
#58665=EDGE_CURVE ( 'NONE', #55474, #41793, #60764, .T. ) ;
#58667=CIRCLE ( 'NONE', #56471, 2.749999999999999556 ) ;
#58668=CARTESIAN_POINT ( 'NONE',  ( 9.080795537700433684, 5.100000000000000533, -6.662590550605527184 ) ) ;
#58674=CARTESIAN_POINT ( 'NONE',  ( 10.65050915380999896, 5.200037120669999346, 5.937706951697999891 ) ) ;
#58678=CARTESIAN_POINT ( 'NONE',  ( 11.14434831560999939, 10.07920604617999949, -5.729928524014000324 ) ) ;
#58679=CARTESIAN_POINT ( 'NONE',  ( 11.03120992439402315, 2.698003081065078135, -8.692097047312476121 ) ) ;
#58682=( NAMED_UNIT ( * ) PLANE_ANGLE_UNIT ( ) SI_UNIT ( $, .RADIAN. ) );
#58684=CARTESIAN_POINT ( 'NONE',  ( 9.318935841232999451, 2.644017913812000131, -7.838184857420000817 ) ) ;
#58688=CARTESIAN_POINT ( 'NONE',  ( 10.69798710318595170, 4.886986039840945040, 4.803896147895557966 ) ) ;
#58691=CARTESIAN_POINT ( 'NONE',  ( 11.09999999999999964, 2.700000000000000178, -5.160242730539000178 ) ) ;
#58694=CARTESIAN_POINT ( 'NONE',  ( 9.401145280412999128, 3.927090956378999742, -9.230892435423001530 ) ) ;
#58695=CARTESIAN_POINT ( 'NONE',  ( 4.966698988835610784, -2.066632171653634664, 9.814764551474491144E-10 ) ) ;
#58696=CARTESIAN_POINT ( 'NONE',  ( 2.268533155335109353, 3.242759788008271915, -0.3142191302543209663 ) ) ;
#58698=ORIENTED_EDGE ( 'NONE', *, *, #41435, .F. ) ;
#58700=CARTESIAN_POINT ( 'NONE',  ( 11.18706938844999854, 3.186790175674999670, 6.232702730851999995 ) ) ;
#58706=CARTESIAN_POINT ( 'NONE',  ( 8.417489158772999858, 2.029098103856999735, 7.726995416028000108 ) ) ;
#58720=CARTESIAN_POINT ( 'NONE',  ( 8.664129719593997692, 5.524776413195999325, -7.147585171405999915 ) ) ;
#58729=ORIENTED_EDGE ( 'NONE', *, *, #33500, .F. ) ;
#58732=CARTESIAN_POINT ( 'NONE',  ( 10.31498017945866685, 2.650031506806222570, -7.499998780888569527 ) ) ;
#58733=CARTESIAN_POINT ( 'NONE',  ( 10.35427764559999986, 4.879113829302000660, -8.944031201701999834 ) ) ;
#58734=CARTESIAN_POINT ( 'NONE',  ( 8.229964631809997044, 4.681828315382999151, 6.132208354562998842 ) ) ;
#58737=CARTESIAN_POINT ( 'NONE',  ( 9.051837186271754376, 4.773597817256774789, 8.611999504439044273 ) ) ;
#58739=CARTESIAN_POINT ( 'NONE',  ( 8.689260841231000398, 2.550241116032999855, 7.666973618349000041 ) ) ;
#58740=EDGE_LOOP ( 'NONE', ( #45886, #25172, #1420, #43053, #773, #16749 ) ) ;
#58741=DIRECTION ( 'NONE',  ( 0.000000000000000000, 1.000000000000000000, 0.000000000000000000 ) ) ;
#58748=CARTESIAN_POINT ( 'NONE',  ( 11.05758752493000152, 9.474230211708000837, 6.311392455611000152 ) ) ;
#58755=CARTESIAN_POINT ( 'NONE',  ( 8.295159150710981422, 2.930861795617814014, -6.461078406439177080 ) ) ;
#58761=CARTESIAN_POINT ( 'NONE',  ( 5.000000000000000000, 0.2999999999999999889, -3.149999999999999911 ) ) ;
#58762=CARTESIAN_POINT ( 'NONE',  ( 9.585607375975767397, 5.315314066450707919, -7.853683613172021794 ) ) ;
#58765=CARTESIAN_POINT ( 'NONE',  ( 8.496698341230001006, 5.198556077301000222, 8.332552905512999430 ) ) ;
#58767=CARTESIAN_POINT ( 'NONE',  ( 7.859795284898003942, 2.854589328742001886, -6.788356039251000063 ) ) ;
#58768=CARTESIAN_POINT ( 'NONE',  ( 10.77401721959000014, 3.826866801954999620, -5.823193568970000733 ) ) ;
#58772=CARTESIAN_POINT ( 'NONE',  ( 8.069038185141000241, 5.112620281584000281, -6.682995288704000281 ) ) ;
#58775=CARTESIAN_POINT ( 'NONE',  ( 9.051550650638001017, 2.899999999999999911, 6.227445478845999638 ) ) ;
#58778=ADVANCED_FACE ( 'NONE', ( #1545 ), #58512, .T. ) ;
#58783=VERTEX_POINT ( 'NONE', #55379 ) ;
#58784=EDGE_CURVE ( 'NONE', #25251, #34596, #68650, .T. ) ;
#58785=EDGE_CURVE ( 'NONE', #47667, #59469, #49584, .T. ) ;
#58789=CIRCLE ( 'NONE', #33102, 2.000000000000000444 ) ;
#58790=CYLINDRICAL_SURFACE ( 'NONE', #8641, 1.350000000000000533 ) ;
#58796=B_SPLINE_CURVE_WITH_KNOTS ( 'NONE', 3,
 ( #25241, #36077, #31873, #9497 ),
 .UNSPECIFIED., .F., .F.,
 ( 4, 4 ),
 ( 0.000000000000000000, 0.1254150264828375605 ),
 .UNSPECIFIED. ) ;
#58803=DIRECTION ( 'NONE',  ( 1.000000000000000000, 0.000000000000000000, 0.000000000000000000 ) ) ;
#58804=ORIENTED_EDGE ( 'NONE', *, *, #25394, .F. ) ;
#58805=CARTESIAN_POINT ( 'NONE',  ( 9.889535841229999846, 5.798263352390999437, -8.113145944980999502 ) ) ;
#58821=CARTESIAN_POINT ( 'NONE',  ( 8.921135841230999119, 3.292387953886000140, -6.294868737226000377 ) ) ;
#58822=EDGE_LOOP ( 'NONE', ( #39039, #50533, #16238, #56913, #35358, #7100 ) ) ;
#58823=CARTESIAN_POINT ( 'NONE',  ( 0.2623669365312372159, 3.203502798912969851, -0.5608766408606025156 ) ) ;
#58831=DIRECTION ( 'NONE',  ( 0.000000000000000000, 0.9916377111174248249, -0.1290528957048032721 ) ) ;
#58839=CARTESIAN_POINT ( 'NONE',  ( 9.444964158775000840, 3.920043641733999884, -9.398198753036000497 ) ) ;
#58842=B_SPLINE_CURVE_WITH_KNOTS ( 'NONE', 3,
 ( #17990, #49445, #1553, #22876 ),
 .UNSPECIFIED., .F., .F.,
 ( 4, 4 ),
 ( 0.000000000000000000, 1.000000000000000000 ),
 .UNSPECIFIED. ) ;
#58845=CARTESIAN_POINT ( 'NONE',  ( 11.13709883339000051, 5.336586328279000035, -5.177930967251000105 ) ) ;
#58857=VECTOR ( 'NONE', #4174, 1000.000000000000000 ) ;
#58860=DIRECTION ( 'NONE',  ( 0.000000000000000000, 0.000000000000000000, -1.000000000000000000 ) ) ;
#58863=B_SPLINE_CURVE_WITH_KNOTS ( 'NONE', 3,
 ( #36117, #25284, #9536, #57430, #46618, #25629, #20039, #52194, #4293, #59845 ),
 .UNSPECIFIED., .F., .F.,
 ( 4, 2, 2, 2, 4 ),
 ( 0.000000000000000000, 0.1249999999999998890, 0.2499999999999997780, 0.3749999999999996669, 0.4999999999999994449 ),
 .UNSPECIFIED. ) ;
#58870=CARTESIAN_POINT ( 'NONE',  ( 6.702501388090612799, 4.665922358581495288, -8.797387867328911426 ) ) ;
#58875=VERTEX_POINT ( 'NONE', #29247 ) ;
#58878=CARTESIAN_POINT ( 'NONE',  ( 5.477523075960000654, -12.82224764859999766, 2.276049205302000278 ) ) ;
#58879=CARTESIAN_POINT ( 'NONE',  ( 2.134821978926408459, 2.196258588983220683, -2.381953655762986788 ) ) ;
#58880=CARTESIAN_POINT ( 'NONE',  ( 3.500000000000000888, -1.551591189650207037, 2.828749889131733752 ) ) ;
#58884=( BOUNDED_SURFACE ( )  B_SPLINE_SURFACE ( 3, 3, ( 
 ( #21598, #68802, #5183, #10081, #42937, #58323, #64245, #11120, #37688 ),
 ( #20923, #53769, #27205, #26172, #48526, #42259, #63563, #15677, #37006 ),
 ( #10424, #31766, #53083, #60737, #49211, #60050, #7253, #54110, #6206 ),
 ( #50252, #33835, #44677, #49905, #18443, #45015, #982, #1318, #33141 ) ),
 .UNSPECIFIED., .F., .F., .T. ) 
 B_SPLINE_SURFACE_WITH_KNOTS ( ( 4, 4 ),
 ( 4, 1, 1, 1, 1, 1, 4 ),
 ( 0.000000000000000000, 1.000000000000000000 ),
 ( -0.004646279661397999423, 0.000000000000000000, 0.03269534097185999855, 0.06255479614191999937, 0.08986301827557000022, 0.1148786485006999952, 0.1376622693536999897 ),
 .UNSPECIFIED. ) 
 GEOMETRIC_REPRESENTATION_ITEM ( )  RATIONAL_B_SPLINE_SURFACE ( (
 ( 1.187699524740999824, 1.187699524740999824, 1.187699524740999824, 1.187699524740999824, 1.187699524740999824, 1.187699524740999824, 1.187699524740999824, 1.187699524740999824, 1.187699524740999824),
 ( 0.9374334917530999789, 0.9374334917530999789, 0.9374334917530999789, 0.9374334917530999789, 0.9374334917530999789, 0.9374334917530999789, 0.9374334917530999789, 0.9374334917530999789, 0.9374334917530999789),
 ( 0.9374334917530999789, 0.9374334917530999789, 0.9374334917530999789, 0.9374334917530999789, 0.9374334917530999789, 0.9374334917530999789, 0.9374334917530999789, 0.9374334917530999789, 0.9374334917530999789),
 ( 1.187699524740999824, 1.187699524740999824, 1.187699524740999824, 1.187699524740999824, 1.187699524740999824, 1.187699524740999824, 1.187699524740999824, 1.187699524740999824, 1.187699524740999824) ) ) 
 REPRESENTATION_ITEM ( '' )  SURFACE ( )  );
#58889=LINE ( 'NONE', #53301, #6016 ) ;
#58899=CARTESIAN_POINT ( 'NONE',  ( 9.667489158770999680, 4.808846957865000604, -8.639578604182998944 ) ) ;
#58900=EDGE_LOOP ( 'NONE', ( #47362, #48321, #34060, #47130 ) ) ;
#58902=CARTESIAN_POINT ( 'NONE',  ( 7.572795280404999829, 2.598436872309000112, -6.481704782070000448 ) ) ;
#58905=CARTESIAN_POINT ( 'NONE',  ( 9.488130154828182228, 4.942993110859213779, 8.465850029259959442 ) ) ;
#58906=VERTEX_POINT ( 'NONE', #50557 ) ;
#58918=CARTESIAN_POINT ( 'NONE',  ( 7.737176379004002236, 4.819032099609000142, -6.334771630424004485 ) ) ;
#58920=CARTESIAN_POINT ( 'NONE',  ( 10.42914631115497315, 5.349770684922701136, 7.570573233677396097 ) ) ;
#58925=VERTEX_POINT ( 'NONE', #23985 ) ;
#58927=VERTEX_POINT ( 'NONE', #6862 ) ;
#58928=CARTESIAN_POINT ( 'NONE',  ( 10.55813337864000090, 2.466561068647000532, 6.633529813744000414 ) ) ;
#58931=CARTESIAN_POINT ( 'NONE',  ( 9.020585841232000135, 4.920236664407999783, -6.448229650796999834 ) ) ;
#58941=CARTESIAN_POINT ( 'NONE',  ( 11.08992526467999973, 5.210543602612999869, 8.327598319864998544 ) ) ;
#58953=CARTESIAN_POINT ( 'NONE',  ( 8.150000662387999029, 3.037570195374000164E-13, -3.945735770681999509E-14 ) ) ;
#58955=ADVANCED_FACE ( 'NONE', ( #59227 ), #63437, .T. ) ;
#58957=CARTESIAN_POINT ( 'NONE',  ( 10.98768472567999943, 6.720753181080999283, 5.471698459870999898 ) ) ;
#58958=ORIENTED_EDGE ( 'NONE', *, *, #894, .F. ) ;
#58959=VECTOR ( 'NONE', #30598, 1000.000000000000000 ) ;
#58960=CARTESIAN_POINT ( 'NONE',  ( 0.7818389912891999805, 2.420060471650000267, -2.350339292168000416 ) ) ;
#58962=CARTESIAN_POINT ( 'NONE',  ( 10.91733584123000078, 3.256275267152000108, -6.361562334135999919 ) ) ;
#58968=CARTESIAN_POINT ( 'NONE',  ( 7.501448341228000416, 2.138190256467000339, 6.814770510101999967 ) ) ;
#58972=CARTESIAN_POINT ( 'NONE',  ( 6.911604719590999757, 5.620828677136000096, -7.589710348707000342 ) ) ;
#58976=VECTOR ( 'NONE', #54289, 1000.000000000000114 ) ;
#58982=DIRECTION ( 'NONE',  ( 1.000000000000000000, 0.000000000000000000, 0.000000000000000000 ) ) ;
#58983=DIRECTION ( 'NONE',  ( 1.000000000000000000, 0.000000000000000000, 0.000000000000000000 ) ) ;
#58992=CARTESIAN_POINT ( 'NONE',  ( 7.149100552923999707, 4.351669901925999895, 8.977196921526999773 ) ) ;
#58996=CARTESIAN_POINT ( 'NONE',  ( 11.07071178722999960, 5.425106496613000040, -5.078392693150000525 ) ) ;
#59000=DIRECTION ( 'NONE',  ( 0.000000000000000000, 0.000000000000000000, -1.000000000000000000 ) ) ;
#59001=CARTESIAN_POINT ( 'NONE',  ( 5.000030787343000327, -2.099962892531005210, 0.2748844998327746869 ) ) ;
#59003=B_SPLINE_CURVE_WITH_KNOTS ( 'NONE', 3,
 ( #7330, #2101, #23418, #66057, #18175, #18866, #40521, #40194, #61510, #34613, #61168, #9382, #19199, #24451 ),
 .UNSPECIFIED., .F., .F.,
 ( 4, 2, 2, 2, 2, 2, 4 ),
 ( 0.1252897355259763035, 0.3125850975489872230, 0.4998804595719981148, 0.5935281405835034496, 0.6871758215950088955, 0.7808235026065142304, 0.8744711836180196762 ),
 .UNSPECIFIED. ) ;
#59004=CIRCLE ( 'NONE', #16571, 12.50000000000000000 ) ;
#59010=ORIENTED_EDGE ( 'NONE', *, *, #52244, .F. ) ;
#59014=CARTESIAN_POINT ( 'NONE',  ( 9.961660622462840564, 5.351629337096509786, 7.263483964539687143 ) ) ;
#59019=CARTESIAN_POINT ( 'NONE',  ( 10.62697636434999993, 3.142921793056999924, 8.668445734229999644 ) ) ;
#59020=ORIENTED_EDGE ( 'NONE', *, *, #48840, .T. ) ;
#59022=CARTESIAN_POINT ( 'NONE',  ( 10.31167969999000000, 2.874476822401000220, 8.900029516786000627 ) ) ;
#59023=CARTESIAN_POINT ( 'NONE',  ( 2.103056799209332528, 2.798833948393625981, 2.150913519912208471 ) ) ;
#59027=CARTESIAN_POINT ( 'NONE',  ( 11.00075737667999931, 8.791598996395000754, -6.553657304443999188 ) ) ;
#59032=EDGE_LOOP ( 'NONE', ( #16418, #17103, #10833 ) ) ;
#59042=CARTESIAN_POINT ( 'NONE',  ( 7.731795280408999993, 4.580608786027000612, 9.213365309690999538 ) ) ;
#59043=CARTESIAN_POINT ( 'NONE',  ( 8.854170280414001226, 4.902869380824999901, -8.978557145469999057 ) ) ;
#59045=CARTESIAN_POINT ( 'NONE',  ( 10.65445404538374241, 3.176394930960259266, 4.782660509943262639 ) ) ;
#59046=EDGE_LOOP ( 'NONE', ( #36377, #47332, #8856, #28019 ) ) ;
#59047=CARTESIAN_POINT ( 'NONE',  ( 9.500006116823001889, 2.279680316922000127, 7.877692351087999256 ) ) ;
#59048=CIRCLE ( 'NONE', #30077, 1.350000000000000533 ) ;
#59053=EDGE_LOOP ( 'NONE', ( #41876, #27779, #50483, #17296 ) ) ;
#59054=LINE ( 'NONE', #53804, #67833 ) ;
#59067=CARTESIAN_POINT ( 'NONE',  ( 8.813304719595000947, 3.880154689736000417, -9.060377011187000562 ) ) ;
#59070=ORIENTED_EDGE ( 'NONE', *, *, #29769, .F. ) ;
#59071=CARTESIAN_POINT ( 'NONE',  ( 7.948851576340711489, 4.916978202369310935, -6.401965507567116020 ) ) ;
#59076=VERTEX_POINT ( 'NONE', #60618 ) ;
#59079=CARTESIAN_POINT ( 'NONE',  ( 10.50285691784999997, 5.158890929072000198, 8.369954994793999958 ) ) ;
#59080=CARTESIAN_POINT ( 'NONE',  ( 10.87696123885999810, 5.827079664135999870, -7.814747088295999511 ) ) ;
#59086=CARTESIAN_POINT ( 'NONE',  ( 7.507482780409000078, 3.501518846194999757, 9.055971388486000251 ) ) ;
#59087=EDGE_LOOP ( 'NONE', ( #66104, #6186, #39366, #45017, #26843 ) ) ;
#59090=CARTESIAN_POINT ( 'NONE',  ( 9.246656068972805897, 2.697145242899015471, 7.146653512472456171 ) ) ;
#59093=EDGE_CURVE ( 'NONE', #12815, #55845, #61113, .T. ) ;
#59094=CARTESIAN_POINT ( 'NONE',  ( 11.02144803208000035, 6.116354541702999192, 5.112466721998999652 ) ) ;
#59096=CARTESIAN_POINT ( 'NONE',  ( 11.12483613036000030, 7.237663138348001013, 6.298788344941000261 ) ) ;
#59106=DIRECTION ( 'NONE',  ( 1.000000000000000000, 0.000000000000000000, 0.000000000000000000 ) ) ;
#59111=CARTESIAN_POINT ( 'NONE',  ( 8.076862866721999268, 2.879478799711000292, -6.727223656603999125 ) ) ;
#59113=CARTESIAN_POINT ( 'NONE',  ( 11.06878584122999953, 5.318802051720999735, -7.168446171767000052 ) ) ;
#59115=CARTESIAN_POINT ( 'NONE',  ( 8.196365526475007712, 5.108366921470007149, 6.411205986879997099 ) ) ;
#59118=DIRECTION ( 'NONE',  ( 0.000000000000000000, -1.000000000000000000, 0.000000000000000000 ) ) ;
#59126=CARTESIAN_POINT ( 'NONE',  ( 11.05213295841000054, 2.768281150710999672, 4.976717609956999411 ) ) ;
#59127=CARTESIAN_POINT ( 'NONE',  ( 7.364999999998000035, 2.649999999999999911, -7.500000000000000000 ) ) ;
#59136=CARTESIAN_POINT ( 'NONE',  ( 8.474485200571999499, 5.100000000000000533, 6.560614371780999043 ) ) ;
#59138=DIRECTION ( 'NONE',  ( 0.000000000000000000, 0.000000000000000000, -1.000000000000000000 ) ) ;
#59144=ORIENTED_EDGE ( 'NONE', *, *, #54536, .F. ) ;
#59145=CARTESIAN_POINT ( 'NONE',  ( 7.382526753210433945, 2.847550462391403858, 8.801350187526136182 ) ) ;
#59149=B_SPLINE_CURVE_WITH_KNOTS ( 'NONE', 3,
 ( #57485, #19755, #9592, #67289 ),
 .UNSPECIFIED., .F., .F.,
 ( 4, 4 ),
 ( 0.8745776555051315571, 1.000000000000000000 ),
 .UNSPECIFIED. ) ;
#59151=B_SPLINE_CURVE_WITH_KNOTS ( 'NONE', 3,
 ( #53027, #15622, #14593, #25421 ),
 .UNSPECIFIED., .F., .F.,
 ( 4, 4 ),
 ( 0.000000000000000000, 1.000000000000000000 ),
 .UNSPECIFIED. ) ;
#59155=DIRECTION ( 'NONE',  ( 0.000000000000000000, -0.1218274111675001353, 0.9925512993736016476 ) ) ;
#59162=ORIENTED_EDGE ( 'NONE', *, *, #31344, .F. ) ;
#59167=CARTESIAN_POINT ( 'NONE',  ( 10.20918109782000016, 3.334760637131999772, -5.769467581755999497 ) ) ;
#59175=EDGE_CURVE ( 'NONE', #34148, #7076, #31968, .T. ) ;
#59180=ORIENTED_EDGE ( 'NONE', *, *, #58784, .T. ) ;
#59181=CARTESIAN_POINT ( 'NONE',  ( 6.956590560819000402, 5.278582711742999756, -7.933273873238999130 ) ) ;
#59185=CARTESIAN_POINT ( 'NONE',  ( 9.793039158772000263, 5.817107086401000160, -6.945352709928000579 ) ) ;
#59189=CARTESIAN_POINT ( 'NONE',  ( 8.771960841230001193, 3.061731693614000438, -8.535706278603999664 ) ) ;
#59197=CARTESIAN_POINT ( 'NONE',  ( 2.050973465875999935, 3.500000000000000000, 0.000000000000000000 ) ) ;
#59199=EDGE_LOOP ( 'NONE', ( #36552, #10487, #49699, #27715, #44495, #56329 ) ) ;
#59204=CARTESIAN_POINT ( 'NONE',  ( 11.09999999999999964, 6.080160889643000388, -5.239944403408999918 ) ) ;
#59218=CARTESIAN_POINT ( 'NONE',  ( 1.500973465873999935, 3.500000000000000000, 0.000000000000000000 ) ) ;
#59225=LINE ( 'NONE', #6424, #16482 ) ;
#59227=FACE_OUTER_BOUND ( 'NONE', #17896, .T. ) ;
#59228=ORIENTED_EDGE ( 'NONE', *, *, #64851, .T. ) ;
#59231=ORIENTED_EDGE ( 'NONE', *, *, #37520, .F. ) ;
#59234=CARTESIAN_POINT ( 'NONE',  ( 8.225464158772000545, 3.844886277615000125, -8.888911790991000927 ) ) ;
#59237=CARTESIAN_POINT ( 'NONE',  ( 7.025820280407000240, 2.268824274702999855, -7.434159913875999948 ) ) ;
#59239=CARTESIAN_POINT ( 'NONE',  ( 9.502125899204576953, 4.762576840438827119, 8.617734806663701619 ) ) ;
#59254=CARTESIAN_POINT ( 'NONE',  ( 3.230140132544583764, -3.408904368339107815, 0.9161175952574674985 ) ) ;
#59256=CIRCLE ( 'NONE', #18004, 1.349999999999999201 ) ;
#59260=ORIENTED_EDGE ( 'NONE', *, *, #24786, .F. ) ;
#59261=CARTESIAN_POINT ( 'NONE',  ( 9.966324641169999055, 2.303991951421000106, 6.575630951545000435 ) ) ;
#59262=CARTESIAN_POINT ( 'NONE',  ( 10.03976415876999972, 2.255572964181999929, -8.111983882175000105 ) ) ;
#59269=ORIENTED_EDGE ( 'NONE', *, *, #8449, .T. ) ;
#59275=ADVANCED_FACE ( 'NONE', ( #66292 ), #29260, .F. ) ;
#59279=CYLINDRICAL_SURFACE ( 'NONE', #64121, 1.350000000000000533 ) ;
#59288=CARTESIAN_POINT ( 'NONE',  ( 8.474089158773999486, 4.131080973160000447, -6.108642999115999395 ) ) ;
#59291=DIRECTION ( 'NONE',  ( -0.7071064907087092344, 0.08614501498594114015, -0.7018400438780093564 ) ) ;
#59293=CARTESIAN_POINT ( 'NONE',  ( 0.8312974075931000018, 0.9881876859693999871, -3.396851722846999877 ) ) ;
#59296=FACE_OUTER_BOUND ( 'NONE', #42393, .T. ) ;
#59297=VERTEX_POINT ( 'NONE', #54775 ) ;
#59304=CARTESIAN_POINT ( 'NONE',  ( 8.475642219593000348, 5.095085596809999728, 6.286981168432999922 ) ) ;
#59309=CARTESIAN_POINT ( 'NONE',  ( 7.449720280409000139, 5.287968704092000927, -6.611025344044000107 ) ) ;
#59318=CYLINDRICAL_SURFACE ( 'NONE', #27940, 0.5000000000000000000 ) ;
#59328=CARTESIAN_POINT ( 'NONE',  ( 8.437857780412000963, 2.606995215518000286, 6.345762205468999717 ) ) ;
#59329=VERTEX_POINT ( 'NONE', #28212 ) ;
#59330=DIRECTION ( 'NONE',  ( 0.9999999999998953060, -4.575887298088981526E-07, 2.007391389072990910E-09 ) ) ;
#59337=CARTESIAN_POINT ( 'NONE',  ( 7.913901703519866437, 2.864539049585775654, -6.759697255404577554 ) ) ;
#59347=EDGE_LOOP ( 'NONE', ( #19217, #25367, #49799, #40530, #10953, #28261, #59010, #37925 ) ) ;
#59350=CARTESIAN_POINT ( 'NONE',  ( 9.934212804449000345, 5.120437537252000126, -8.883398686237999442 ) ) ;
#59354=CARTESIAN_POINT ( 'NONE',  ( 10.06843885510000014, 4.148608506723999945, 8.941445591976998841 ) ) ;
#59356=ORIENTED_EDGE ( 'NONE', *, *, #20847, .F. ) ;
#59358=CARTESIAN_POINT ( 'NONE',  ( 9.476372460169001144, 5.098395626600999542, 6.305536056092000408 ) ) ;
#59362=DIRECTION ( 'NONE',  ( 1.000000000000000000, 0.000000000000000000, 0.000000000000000000 ) ) ;
#59365=CARTESIAN_POINT ( 'NONE',  ( 10.24369552910394532, 5.492882802562766287, 8.410537742903038350 ) ) ;
#59369=DIRECTION ( 'NONE',  ( 1.000000000000000000, 0.000000000000000000, -4.146618578177000290E-14 ) ) ;
#59371=DIRECTION ( 'NONE',  ( 0.000000000000000000, 0.000000000000000000, -1.000000000000000000 ) ) ;
#59378=CARTESIAN_POINT ( 'NONE',  ( 8.694607780412001219, 5.290207928847999064, 8.768105151414001597 ) ) ;
#59379=CARTESIAN_POINT ( 'NONE',  ( 8.754720280412998434, 5.687930027805999877, -7.109876198051000351 ) ) ;
#59381=CARTESIAN_POINT ( 'NONE',  ( 3.190706351837349075, 1.551038532097675393, -2.865019036274451203 ) ) ;
#59382=ORIENTED_EDGE ( 'NONE', *, *, #31882, .T. ) ;
#59383=CARTESIAN_POINT ( 'NONE',  ( 9.813360311708999362, 5.349397258738000538, 6.657026394682000081 ) ) ;
#59388=CARTESIAN_POINT ( 'NONE',  ( 8.146781841545999825, 3.121749852590999907, 6.130949854565998614 ) ) ;
#59396=CYLINDRICAL_SURFACE ( 'NONE', #27661, 0.5000000000000002220 ) ;
#59398=CIRCLE ( 'NONE', #56059, 11.35000000000000675 ) ;
#59401=CARTESIAN_POINT ( 'NONE',  ( 8.228219317832992985, 3.441361860949001539, 6.127431671619995690 ) ) ;
#59404=CARTESIAN_POINT ( 'NONE',  ( 8.374639158773000247, 2.721111233225000259, -6.936528696292000085 ) ) ;
#59407=CARTESIAN_POINT ( 'NONE',  ( 7.966901574931999797, 4.609574279519000228, -6.276317554486000816 ) ) ;
#59410=EDGE_LOOP ( 'NONE', ( #61799, #26860, #41201, #34766 ) ) ;
#59414=EDGE_LOOP ( 'NONE', ( #287, #54247, #41373, #50147, #66988 ) ) ;
#59417=AXIS2_PLACEMENT_3D ( 'NONE', #63985, #38466, #32880 ) ;
#59419=CARTESIAN_POINT ( 'NONE',  ( 10.09133754351999990, 2.216715295763999727, -8.007133643737999407 ) ) ;
#59427=CARTESIAN_POINT ( 'NONE',  ( 9.566490007895001924, 4.108964550738000376, 8.851615252874999840 ) ) ;
#59430=FACE_OUTER_BOUND ( 'NONE', #39130, .T. ) ;
#59434=CARTESIAN_POINT ( 'NONE',  ( 11.02038863743000086, 6.425337680708999244, 5.276379190389000051 ) ) ;
#59435=CARTESIAN_POINT ( 'NONE',  ( 10.67905590578999941, 2.899999999999999911, 6.571291218949999902 ) ) ;
#59442=CARTESIAN_POINT ( 'NONE',  ( 10.29378723213999969, 3.483632952461999999, 6.176337842045999338 ) ) ;
#59445=AXIS2_PLACEMENT_3D ( 'NONE', #12779, #33762, #49480 ) ;
#59446=EDGE_CURVE ( 'NONE', #57225, #115, #50796, .T. ) ;
#59449=CARTESIAN_POINT ( 'NONE',  ( 9.587885841227999251, 3.762712042852999872, 8.787816121229999666 ) ) ;
#59450=CARTESIAN_POINT ( 'NONE',  ( 9.905792474809000936, 2.698958900805999761, 8.979236532123000103 ) ) ;
#59455=CARTESIAN_POINT ( 'NONE',  ( 10.57657334123000048, 5.344886503256999433, -7.298885378918000377 ) ) ;
#59456=FACE_OUTER_BOUND ( 'NONE', #46419, .T. ) ;
#59457=CARTESIAN_POINT ( 'NONE',  ( 7.712330476186004979, 4.866816057961001363, 6.392636141994996635 ) ) ;
#59464=CARTESIAN_POINT ( 'NONE',  ( 3.452384183491000069, 1.140396268832999827, -3.309002319436000317 ) ) ;
#59467=FACE_OUTER_BOUND ( 'NONE', #233, .T. ) ;
#59469=VERTEX_POINT ( 'NONE', #62423 ) ;
#59473=FACE_OUTER_BOUND ( 'NONE', #10941, .T. ) ;
#59476=CARTESIAN_POINT ( 'NONE',  ( 10.46085995768999943, 5.403395036974999677, 7.721808039505000387 ) ) ;
#59484=CARTESIAN_POINT ( 'NONE',  ( 5.500000000000000000, -12.78667792605000031, 2.345384795463000049 ) ) ;
#59486=CARTESIAN_POINT ( 'NONE',  ( 9.390724454320221071, 5.236106858288462007, 6.940950143625023827 ) ) ;
#59488=CARTESIAN_POINT ( 'NONE',  ( 9.193385841233000733, 2.981992329588000423, -5.895876591910999664 ) ) ;
#59491=CONICAL_SURFACE ( 'NONE', #57243, 1.449999999967999553, 0.7853981633972997312 ) ;
#59492=B_SPLINE_CURVE_WITH_KNOTS ( 'NONE', 3,
 ( #47726, #856, #5411, #32340 ),
 .UNSPECIFIED., .F., .F.,
 ( 4, 4 ),
 ( 0.000000000000000000, 0.3916346334472008972 ),
 .UNSPECIFIED. ) ;
#59495=VERTEX_POINT ( 'NONE', #14202 ) ;
#59502=CARTESIAN_POINT ( 'NONE',  ( 11.10000001610000098, 9.513034266426000585, -6.346422930067999957 ) ) ;
#59505=CARTESIAN_POINT ( 'NONE',  ( 4.000000000000000000, -2.040156275101109973, -0.6926574996740213486 ) ) ;
#59508=CARTESIAN_POINT ( 'NONE',  ( 9.617285841233000454, 5.306366356490000769, -7.996450761531000317 ) ) ;
#59509=EDGE_CURVE ( 'NONE', #60354, #36822, #16105, .T. ) ;
#59512=CARTESIAN_POINT ( 'NONE',  ( 0.5502919481377350763, -3.103829730453177671, -0.9712058421138561881 ) ) ;
#59513=PRESENTATION_STYLE_ASSIGNMENT (( #54264 ) ) ;
#59514=EDGE_CURVE ( 'NONE', #29064, #57460, #21919, .T. ) ;
#59518=AXIS2_PLACEMENT_3D ( 'NONE', #4225, #46551, #30808 ) ;
#59520=CARTESIAN_POINT ( 'NONE',  ( 8.999999001754000361, 0.000000000000000000, 0.000000000000000000 ) ) ;
#59523=CARTESIAN_POINT ( 'NONE',  ( 7.854336256796271343, 2.876636076216872340, -6.723928215619836557 ) ) ;
#59525=ORIENTED_EDGE ( 'NONE', *, *, #20144, .T. ) ;
#59526=CARTESIAN_POINT ( 'NONE',  ( 7.371771682458000186, 2.534482666265000184, -7.314862106114000007 ) ) ;
#59530=EDGE_CURVE ( 'NONE', #59750, #25932, #32005, .T. ) ;
#59531=CARTESIAN_POINT ( 'NONE',  ( 9.377520280414000098, 4.092867382745001059, -5.937785237406000505 ) ) ;
#59535=CARTESIAN_POINT ( 'NONE',  ( 8.179520121434947555, 4.176734390553195730, -8.849463778351122301 ) ) ;
#59536=CARTESIAN_POINT ( 'NONE',  ( 11.04796807810000026, 5.246614701511999712, -5.093099051827000068 ) ) ;
#59540=CARTESIAN_POINT ( 'NONE',  ( 0.1499942179679999987, 5.893556041935713383E-16, -2.749976859058071543 ) ) ;
#59545=CARTESIAN_POINT ( 'NONE',  ( 8.335860198546281907, 4.831625175398913896, -6.127235342693542641 ) ) ;
#59546=CARTESIAN_POINT ( 'NONE',  ( 10.90540321535448420, 2.790089835004012198, -6.887843015912778810 ) ) ;
#59548=VECTOR ( 'NONE', #10785, 1000.000000000000000 ) ;
#59560=CARTESIAN_POINT ( 'NONE',  ( 8.061933748689000367, 4.603465626214999773, -6.221450782568999749 ) ) ;
#59561=EDGE_CURVE ( 'NONE', #12318, #1268, #36169, .T. ) ;
#59566=CARTESIAN_POINT ( 'NONE',  ( 8.630000000000000782, 4.924138593003999809, -8.484107647018999998 ) ) ;
#59567=CARTESIAN_POINT ( 'NONE',  ( 1.040556799208345984, 3.500000000000000888, -0.4581489286485045387 ) ) ;
#59576=PLANE ( 'NONE',  #45155 ) ;
#59581=CARTESIAN_POINT ( 'NONE',  ( 9.617764158771999305, 5.322769172805999816, -7.951018786192998178 ) ) ;
#59585=CARTESIAN_POINT ( 'NONE',  ( 7.075545280406999815, 2.634456420141999988, -6.433888043919999689 ) ) ;
#59587=CARTESIAN_POINT ( 'NONE',  ( 7.903233148129999996, 5.126111344052000085, 6.730859635691999188 ) ) ;
#59590=VECTOR ( 'NONE', #65896, 1000.000000000000000 ) ;
#59592=DIRECTION ( 'NONE',  ( -1.000000000000000000, 0.000000000000000000, 0.000000000000000000 ) ) ;
#59602=CARTESIAN_POINT ( 'NONE',  ( 8.298828076409998644, 5.104449167533000598, -6.663856854024003518 ) ) ;
#59604=CARTESIAN_POINT ( 'NONE',  ( 7.135647982796729849, 4.855545130758272876, -8.555041308852223025 ) ) ;
#59610=CARTESIAN_POINT ( 'NONE',  ( 11.17788388625999829, 2.412139249855000056, -7.075601348558000048 ) ) ;
#59614=CARTESIAN_POINT ( 'NONE',  ( 3.606513041767000161, 1.901420734585999917, 3.183432923345000276 ) ) ;
#59621=EDGE_LOOP ( 'NONE', ( #38969, #25558, #54951, #63393 ) ) ;
#59622=CARTESIAN_POINT ( 'NONE',  ( 10.46754281781999829, 2.318340407652000223, 6.549777679168999001 ) ) ;
#59633=CARTESIAN_POINT ( 'NONE',  ( 7.523326529072416946, 5.204747376180668184, -6.795163621442438462 ) ) ;
#59638=DIRECTION ( 'NONE',  ( 1.000000000000000000, 0.000000000000000000, 0.000000000000000000 ) ) ;
#59641=CARTESIAN_POINT ( 'NONE',  ( 8.415504719592000527, 2.469361196073999842, -7.826019481986000059 ) ) ;
#59642=LINE ( 'NONE', #16644, #6999 ) ;
#59644=CARTESIAN_POINT ( 'NONE',  ( 0.5845045405018999274, -1.124254478562000115, 3.354249223527999924 ) ) ;
#59646=CARTESIAN_POINT ( 'NONE',  ( 10.53871084122999946, 5.103389446345000025, -6.705205355781999721 ) ) ;
#59654=CARTESIAN_POINT ( 'NONE',  ( 8.090517219592001652, 5.342170561818999630, 8.432311822615000452 ) ) ;
#59659=CARTESIAN_POINT ( 'NONE',  ( 7.797795280408000629, 2.733910551100999786, -6.580132171107999639 ) ) ;
#59663=ORIENTED_EDGE ( 'NONE', *, *, #3732, .F. ) ;
#59665=ORIENTED_EDGE ( 'NONE', *, *, #44078, .T. ) ;
#59666=CARTESIAN_POINT ( 'NONE',  ( 11.10000000000000142, 2.264782496563556791, -7.479749973481406577 ) ) ;
#59668=VECTOR ( 'NONE', #66202, 1000.000000000000114 ) ;
#59674=DIRECTION ( 'NONE',  ( 0.000000000000000000, 0.000000000000000000, 1.000000000000000000 ) ) ;
#59677=CARTESIAN_POINT ( 'NONE',  ( 8.962739158771999115, 5.445214367171999470, 7.703373622193999459 ) ) ;
#59678=CARTESIAN_POINT ( 'NONE',  ( 8.564919648097475857, 5.350116636189168773, -7.500005043868485544 ) ) ;
#59682=CARTESIAN_POINT ( 'NONE',  ( 11.12487850024999858, 6.581971541694000116, -5.643519261885000304 ) ) ;
#59696=CARTESIAN_POINT ( 'NONE',  ( 9.833904719592002408, 5.048004622677000341, -6.120508709481000231 ) ) ;
#59697=CARTESIAN_POINT ( 'NONE',  ( 10.83768005408999890, 5.758100475276000552, -6.911469147650000977 ) ) ;
#59700=CARTESIAN_POINT ( 'NONE',  ( 9.110944094209999733, 5.100000000000000533, -6.571291218949999902 ) ) ;
#59706=CARTESIAN_POINT ( 'NONE',  ( 9.318724127987000116, 2.755029797911999978, 8.795125756257000660 ) ) ;
#59707=CARTESIAN_POINT ( 'NONE',  ( 10.44079553768663615, 5.100000000000000533, 6.662590550639045262 ) ) ;
#59717=ORIENTED_EDGE ( 'NONE', *, *, #43371, .F. ) ;
#59721=CARTESIAN_POINT ( 'NONE',  ( 11.09999999999999964, 5.299771130038000599, -5.136740763824000133 ) ) ;
#59725=CARTESIAN_POINT ( 'NONE',  ( 8.630420280412000267, 5.808262417891000062, 7.446016144116000213 ) ) ;
#59726=CARTESIAN_POINT ( 'NONE',  ( 9.708354719591000048, 5.481267232667000222, -8.005061172455999241 ) ) ;
#59730=B_SPLINE_CURVE_WITH_KNOTS ( 'NONE', 3,
 ( #22992, #39427, #2026, #24032, #18107, #66674, #39083, #60406, #60745, #44688, #13895, #29646, #18449, #8301, #50606, #18797, #39775, #2707 ),
 .UNSPECIFIED., .F., .F.,
 ( 4, 2, 2, 2, 2, 2, 2, 2, 4 ),
 ( 0.000000000000000000, 0.1249999999999994726, 0.2499999999999989453, 0.3749999999999991673, 0.4999999999999994449, 0.6249999999999994449, 0.7499999999999994449, 0.8749999999999995559, 1.000000000000000000 ),
 .UNSPECIFIED. ) ;
#59731=CARTESIAN_POINT ( 'NONE',  ( 10.83658792121999959, 5.133186143592999962, 8.848368005200001107 ) ) ;
#59735=CARTESIAN_POINT ( 'NONE',  ( 7.764631182151003230, 2.924915923740001311, 6.482382710726004582 ) ) ;
#59748=CARTESIAN_POINT ( 'NONE',  ( 7.545207810761997536, 3.529659010889000026, 6.570477302111996210 ) ) ;
#59750=VERTEX_POINT ( 'NONE', #20043 ) ;
#59751=CARTESIAN_POINT ( 'NONE',  ( 8.573539158775000502, 5.361622798585000460, -7.185294144754000634 ) ) ;
#59759=ORIENTED_EDGE ( 'NONE', *, *, #23411, .F. ) ;
#59762=ORIENTED_EDGE ( 'NONE', *, *, #6289, .T. ) ;
#59770=DIRECTION ( 'NONE',  ( -1.000000000000000000, -1.308972661142999917E-10, -2.029855754503000182E-09 ) ) ;
#59774=CARTESIAN_POINT ( 'NONE',  ( 8.738426658774001154, 5.414918126383000185, 8.890678916765999418 ) ) ;
#59782=CARTESIAN_POINT ( 'NONE',  ( 11.05294428647999894, 9.762867297161999858, 6.037733508755000145 ) ) ;
#59783=EDGE_CURVE ( 'NONE', #42751, #25355, #15053, .T. ) ;
#59786=AXIS2_PLACEMENT_3D ( 'NONE', #30149, #9143, #52135 ) ;
#59791=CARTESIAN_POINT ( 'NONE',  ( 8.268281802725203633, 3.021318042435896079, -6.294810243494267432 ) ) ;
#59796=CARTESIAN_POINT ( 'NONE',  ( 8.662857780412000608, 2.741641653469999884, 6.457329666915000210 ) ) ;
#59797=CARTESIAN_POINT ( 'NONE',  ( 9.595493858556999101, 3.928424745541000185, 5.531312048131000303 ) ) ;
#59798=B_SPLINE_CURVE_WITH_KNOTS ( 'NONE', 3,
 ( #66583, #18701, #56096, #67601, #40034, #51203, #35132, #61346, #29896, #29556, #24633, #13466, #41050, #45953, #8207 ),
 .UNSPECIFIED., .F., .F.,
 ( 4, 2, 2, 2, 1, 2, 2, 4 ),
 ( 0.000000000000000000, 0.2500000000000130451, 0.3750000000000203726, 0.4375000000000243139, 0.4687500000000262568, 0.4843750000000273670, 0.5000000000000285327, 1.000000000000000000 ),
 .UNSPECIFIED. ) ;
#59801=CARTESIAN_POINT ( 'NONE',  ( 10.00975366370549757, 4.592545519478158589, -8.996633650733423693 ) ) ;
#59805=CARTESIAN_POINT ( 'NONE',  ( 8.222961399606997901, 4.680050665548002087, 6.135920769709001021 ) ) ;
#59810=CARTESIAN_POINT ( 'NONE',  ( 1.596338831776999978, -1.247131703260000002, -3.010971457459999723 ) ) ;
#59816=CARTESIAN_POINT ( 'NONE',  ( 10.95289953070000166, 2.845666449107000062, 5.174586383325000760 ) ) ;
#59821=ADVANCED_FACE ( 'NONE', ( #9197 ), #56419, .T. ) ;
#59825=CARTESIAN_POINT ( 'NONE',  ( 0.9898832362503998672, 3.344697682836000219, -1.715043639744999959 ) ) ;
#59828=FACE_OUTER_BOUND ( 'NONE', #52268, .T. ) ;
#59833=CARTESIAN_POINT ( 'NONE',  ( 10.42499241036494162, 5.349775919985349404, 7.500001834605750872 ) ) ;
#59834=CARTESIAN_POINT ( 'NONE',  ( 9.424850063658244181, 5.349972463430670899, 7.500009360578276052 ) ) ;
#59836=ORIENTED_EDGE ( 'NONE', *, *, #39245, .T. ) ;
#59837=CARTESIAN_POINT ( 'NONE',  ( 7.436329166470820873, 2.279372969473476118, 7.816946968581012456 ) ) ;
#59845=CARTESIAN_POINT ( 'NONE',  ( 4.149992563291999836, 4.286198015044692593E-16, -1.999973142472143861 ) ) ;
#59847=CARTESIAN_POINT ( 'NONE',  ( 10.58844943056000076, 3.754657019866000311, 5.545350295858999523 ) ) ;
#59852=CARTESIAN_POINT ( 'NONE',  ( 11.02214804248266766, 5.404890988670800311, -8.010352125880700669 ) ) ;
#59855=VERTEX_POINT ( 'NONE', #32602 ) ;
#59860=CARTESIAN_POINT ( 'NONE',  ( 10.87208388895120770, 2.964986218627933212, -4.888821409244461513 ) ) ;
#59866=B_SPLINE_CURVE_WITH_KNOTS ( 'NONE', 3,
 ( #39498, #60820, #22715, #45094, #18523, #55582, #6986, #7684, #44061, #6283, #49287, #32872, #49637, #29026, #17124, #1743, #54541, #27631, #1060, #11881 ),
 .UNSPECIFIED., .F., .F.,
 ( 4, 2, 2, 2, 2, 2, 2, 2, 2, 4 ),
 ( 0.000000000000000000, 0.1250000000000000555, 0.2500000000000001110, 0.3750000000000001665, 0.5000000000000002220, 0.6250000000000002220, 0.7500000000000003331, 0.8750000000000004441, 0.9375000000000002220, 1.000000000000000000 ),
 .UNSPECIFIED. ) ;
#59869=ORIENTED_EDGE ( 'NONE', *, *, #39665, .F. ) ;
#59870=CARTESIAN_POINT ( 'NONE',  ( 7.586271682458000321, 5.321245676936000812, -7.068438969505000280 ) ) ;
#59874=CARTESIAN_POINT ( 'NONE',  ( 9.178620280414001797, 2.990001567622999623, -8.695425648791999862 ) ) ;
#59891=B_SPLINE_CURVE_WITH_KNOTS ( 'NONE', 3,
 ( #51916, #46688, #62068, #67992 ),
 .UNSPECIFIED., .F., .F.,
 ( 4, 4 ),
 ( 0.000000000000000000, 1.000000000000000000 ),
 .UNSPECIFIED. ) ;
#59900=ADVANCED_FACE ( 'NONE', ( #6017 ), #783, .F. ) ;
#59901=EDGE_CURVE ( 'NONE', #33691, #51514, #26678, .T. ) ;
#59903=VECTOR ( 'NONE', #37707, 1000.000000000000114 ) ;
#59904=CARTESIAN_POINT ( 'NONE',  ( 11.09999999999999964, 2.649999999999999911, -7.500000000000000000 ) ) ;
#59911=CARTESIAN_POINT ( 'NONE',  ( 5.500000000000000000, 0.000000000000000000, 0.000000000000000000 ) ) ;
#59918=CARTESIAN_POINT ( 'NONE',  ( 3.500000000000000000, -2.069127319938742993, 2.446168983457449819 ) ) ;
#59919=CARTESIAN_POINT ( 'NONE',  ( 6.999999999999999112, 8.786168856256553639, 4.620315609150635439 ) ) ;
#59922=DIRECTION ( 'NONE',  ( 1.000000000000000000, 0.000000000000000000, 0.000000000000000000 ) ) ;
#59925=EDGE_CURVE ( 'NONE', #22688, #5733, #39395, .T. ) ;
#59928=CARTESIAN_POINT ( 'NONE',  ( 8.871889158775999817, 2.702406276695999754, -6.981052078638000147 ) ) ;
#59929=CARTESIAN_POINT ( 'NONE',  ( 5.500000000000000000, 11.00717859340000082, 1.432487142323000118 ) ) ;
#59931=CARTESIAN_POINT ( 'NONE',  ( 7.365035841224999658, 5.899473592675000155, -7.539390303202999633 ) ) ;
#59932=CARTESIAN_POINT ( 'NONE',  ( 8.660633043440231660, 4.489919511865821278, -8.784469522291857402 ) ) ;
#59936=CARTESIAN_POINT ( 'NONE',  ( 10.90000000000000036, 5.100000000000000533, -6.436740704805999691 ) ) ;
#59947=CARTESIAN_POINT ( 'NONE',  ( 7.740705559937997471, 4.511742753184996957, -6.425237059776996773 ) ) ;
#59950=VECTOR ( 'NONE', #50460, 1000.000000000000000 ) ;
#59954=CARTESIAN_POINT ( 'NONE',  ( 10.46754281781999829, 2.318340407652000223, 6.549777679168999001 ) ) ;
#59955=CARTESIAN_POINT ( 'NONE',  ( 10.29667028040999988, 2.755514216060999999, -6.622437150225000124 ) ) ;
#59966=VECTOR ( 'NONE', #14121, 1000.000000000000000 ) ;
#59967=CARTESIAN_POINT ( 'NONE',  ( 9.793039158772000263, 5.817107086401000160, -6.945352709928000579 ) ) ;
#59971=CARTESIAN_POINT ( 'NONE',  ( 10.96985955311839867, 2.886498072322427166, -4.936516855179674756 ) ) ;
#59985=CARTESIAN_POINT ( 'NONE',  ( 9.988985841228000595, 3.986577607995999806, -9.280166295424001177 ) ) ;
#59986=EDGE_CURVE ( 'NONE', #11316, #3245, #40268, .T. ) ;
#59989=VECTOR ( 'NONE', #17255, 1000.000000000000000 ) ;
#59990=EDGE_CURVE ( 'NONE', #21830, #56890, #10166, .T. ) ;
#59993=CARTESIAN_POINT ( 'NONE',  ( 8.193905507992999659, 3.399974105831999882, 6.145257027059000343 ) ) ;
#59994=CARTESIAN_POINT ( 'NONE',  ( 2.452246804060000507, -1.767275544862999981, -3.127392849687999909 ) ) ;
#59997=CARTESIAN_POINT ( 'NONE',  ( 6.999999691988000095, 12.11716380430000051, -3.069905306952000146 ) ) ;
#60000=CARTESIAN_POINT ( 'NONE',  ( 8.694607780412001219, 5.290207928847999064, 8.768105151414001597 ) ) ;
#60003=CARTESIAN_POINT ( 'NONE',  ( 7.558029719586000006, 3.447598131391000020, -9.141997724497999300 ) ) ;
#60005=CARTESIAN_POINT ( 'NONE',  ( 10.83658792121999959, 5.133186143592999962, 8.848368005200001107 ) ) ;
#60008=ORIENTED_EDGE ( 'NONE', *, *, #33084, .F. ) ;
#60018=CARTESIAN_POINT ( 'NONE',  ( 8.099999999999999645, 0.000000000000000000, -11.84999999999999964 ) ) ;
#60023=ORIENTED_EDGE ( 'NONE', *, *, #19425, .F. ) ;
#60024=CARTESIAN_POINT ( 'NONE',  ( 8.770176658772999900, 3.049618631524000367, 6.392542946894000266 ) ) ;
#60031=CARTESIAN_POINT ( 'NONE',  ( 0.4464730966431282311, -0.4520039235917613363, -3.446451393816258868 ) ) ;
#60032=CARTESIAN_POINT ( 'NONE',  ( 8.375950119029546670, 5.618014493828255240, -8.286326870345469331 ) ) ;
#60033=CARTESIAN_POINT ( 'NONE',  ( 9.123929153134385572, 5.099761357576720222, 6.165062780802453624 ) ) ;
#60041=VERTEX_POINT ( 'NONE', #28398 ) ;
#60042=B_SPLINE_CURVE_WITH_KNOTS ( 'NONE', 3,
 ( #9924, #20760, #37183, #10608, #47336, #26705, #42090, #14832, #47683, #62377, #68994, #57464, #15170, #10266, #46652, #9227, #14494, #30566 ),
 .UNSPECIFIED., .F., .F.,
 ( 4, 2, 2, 2, 2, 2, 2, 2, 4 ),
 ( 0.000000000000000000, 0.1250000000000000278, 0.2500000000000000000, 0.3749999999999999445, 0.4999999999999999445, 0.6249999999999998890, 0.7499999999999998890, 0.8750000000000000000, 1.000000000000000000 ),
 .UNSPECIFIED. ) ;
#60045=CARTESIAN_POINT ( 'NONE',  ( 9.237204719595000668, 3.071719032003000116, -6.037263251225000182 ) ) ;
#60046=CARTESIAN_POINT ( 'NONE',  ( 2.461241760148999980, 0.2941929363790999896, 3.366553971799000067 ) ) ;
#60050=CARTESIAN_POINT ( 'NONE',  ( 7.802644552000999489, 3.157760251094000825, -6.317964942532003469 ) ) ;
#60053=EDGE_CURVE ( 'NONE', #57674, #58925, #4967, .T. ) ;
#60059=CARTESIAN_POINT ( 'NONE',  ( 10.80815748598999981, 2.937526572573000205, 8.948458885032000154 ) ) ;
#60065=CARTESIAN_POINT ( 'NONE',  ( 10.97843137008999825, 5.235400103863000254, 6.782920672145000829 ) ) ;
#60069=CARTESIAN_POINT ( 'NONE',  ( 8.179999999999999716, 4.924138593003999809, -8.484107647018999998 ) ) ;
#60070=VECTOR ( 'NONE', #18572, 1000.000000000000114 ) ;
#60078=ORIENTED_EDGE ( 'NONE', *, *, #14410, .T. ) ;
#60080=CARTESIAN_POINT ( 'NONE',  ( 8.822982780412001347, 2.678331728353000152, 8.735281589464001684 ) ) ;
#60081=CARTESIAN_POINT ( 'NONE',  ( 9.640910841231999484, 2.212639797530000063, -6.855876382544999537 ) ) ;
#60083=CARTESIAN_POINT ( 'NONE',  ( 2.478117972721348927, -2.680622207154140568, 1.851572140801842625 ) ) ;
#60084=ORIENTED_EDGE ( 'NONE', *, *, #35139, .T. ) ;
#60085=CARTESIAN_POINT ( 'NONE',  ( 9.465106464520001595, 2.290037071913000322, 6.601704384062999864 ) ) ;
#60089=CARTESIAN_POINT ( 'NONE',  ( 7.640464943433003420, 3.216280862983999622, 6.362631827276998386 ) ) ;
#60091=CARTESIAN_POINT ( 'NONE',  ( 8.350412160844999931, 2.899104497346000286, -6.601769487399000269 ) ) ;
#60105=CARTESIAN_POINT ( 'NONE',  ( 8.142589158771000868, 5.074768364528000397, -8.296267706722000312 ) ) ;
#60107=VECTOR ( 'NONE', #15694, 1000.000000000000114 ) ;
#60111=CARTESIAN_POINT ( 'NONE',  ( 7.988487219432808040, 5.103181190368189846, -6.649650124670951179 ) ) ;
#60116=EDGE_LOOP ( 'NONE', ( #22829, #20238, #37680, #32506 ) ) ;
#60120=CARTESIAN_POINT ( 'NONE',  ( 10.85939066780000140, 2.936977800747000433, -5.180095930491999567 ) ) ;
#60122=CARTESIAN_POINT ( 'NONE',  ( 7.690241772926001751, 4.592291064388997590, 6.438923047733998928 ) ) ;
#60128=CARTESIAN_POINT ( 'NONE',  ( 9.316114158771000575, 3.677414437776999723, 9.250745771096999803 ) ) ;
#60133=CARTESIAN_POINT ( 'NONE',  ( 10.52662718686000076, 4.933722097448000277, -6.506013113666999637 ) ) ;
#60136=CARTESIAN_POINT ( 'NONE',  ( 9.471374412057000924, 2.030666183831999927, 7.549764512038000142 ) ) ;
#60137=ADVANCED_FACE ( 'NONE', ( #13281 ), #29021, .T. ) ;
#60139=ADVANCED_FACE ( 'NONE', ( #24100 ), #52987, .F. ) ;
#60145=CARTESIAN_POINT ( 'NONE',  ( 11.09999999999999964, 2.700228869961999845, 5.136740763824000133 ) ) ;
#60151=CARTESIAN_POINT ( 'NONE',  ( 9.010198341230998054, 5.040787533781999841, 8.522957620707000359 ) ) ;
#60152=CARTESIAN_POINT ( 'NONE',  ( 10.15403136780999915, 5.267988602993999514, 5.992335067371000079 ) ) ;
#60156=FACE_OUTER_BOUND ( 'NONE', #18543, .T. ) ;
#60159=CARTESIAN_POINT ( 'NONE',  ( 9.649875981546212955, 2.700874656648012184, 7.923553693498652351 ) ) ;
#60160=CARTESIAN_POINT ( 'NONE',  ( 9.819055905797000605, 2.899999999999999911, -6.571291218949999902 ) ) ;
#60166=B_SPLINE_CURVE_WITH_KNOTS ( 'NONE', 3,
 ( #52240, #30250, #67622, #19400 ),
 .UNSPECIFIED., .F., .F.,
 ( 4, 4 ),
 ( 0.000000000000000000, 1.000000000000000000 ),
 .UNSPECIFIED. ) ;
#60167=CARTESIAN_POINT ( 'NONE',  ( 1.448519645393000044, 0.8376700968564000371, 3.321615185007000370 ) ) ;
#60171=CARTESIAN_POINT ( 'NONE',  ( 10.62947109217999930, 5.100000000000000533, 6.152188490330000370 ) ) ;
#60173=CARTESIAN_POINT ( 'NONE',  ( 10.87371169044000041, 2.935964136801999746, 5.107130734584000464 ) ) ;
#60177=CARTESIAN_POINT ( 'NONE',  ( 7.448333333331000006, 3.320114376499284425, -6.320388375721752716 ) ) ;
#60181=CARTESIAN_POINT ( 'NONE',  ( 1.514384680100000047, 3.707157770482000014, -0.6207725330884000803 ) ) ;
#60184=CARTESIAN_POINT ( 'NONE',  ( 10.34947814066000049, 4.457562099971999814, 6.154877938302999674 ) ) ;
#60188=EDGE_CURVE ( 'NONE', #42732, #32376, #20185, .T. ) ;
#60194=CARTESIAN_POINT ( 'NONE',  ( 7.325000000000000178, 4.000000000000000000, 9.239711431703000244 ) ) ;
#60195=ORIENTED_EDGE ( 'NONE', *, *, #57285, .T. ) ;
#60202=CARTESIAN_POINT ( 'NONE',  ( 9.471374412057000924, 2.030666183831999927, 7.549764512038000142 ) ) ;
#60204=CARTESIAN_POINT ( 'NONE',  ( 11.09999999997999964, 7.815194234324999378, -6.645247174075000096 ) ) ;
#60210=ORIENTED_EDGE ( 'NONE', *, *, #38119, .T. ) ;
#60214=CARTESIAN_POINT ( 'NONE',  ( 10.91079984335361353, 2.946977204686775931, -4.907707240660267090 ) ) ;
#60221=CARTESIAN_POINT ( 'NONE',  ( 7.856038276909000473, 2.869044596334999753, -6.744487387516000076 ) ) ;
#60224=EDGE_CURVE ( 'NONE', #26452, #57662, #35190, .T. ) ;
#60226=CARTESIAN_POINT ( 'NONE',  ( 7.366090560818999933, 5.017953588770000195, -6.429833855306000601 ) ) ;
#60231=CARTESIAN_POINT ( 'NONE',  ( 10.10682028041000002, 4.294368353031000396, -8.968663198664000191 ) ) ;
#60232=CARTESIAN_POINT ( 'NONE',  ( 4.049969279409727285, -2.099966510537780273, -9.844681520548669431E-09 ) ) ;
#60241=ADVANCED_FACE ( 'NONE', ( #11023 ), #58570, .F. ) ;
#60247=EDGE_CURVE ( 'NONE', #18238, #65620, #67723, .T. ) ;
#60259=DIRECTION ( 'NONE',  ( -1.000000000000000000, 0.000000000000000000, 0.000000000000000000 ) ) ;
#60265=CARTESIAN_POINT ( 'NONE',  ( 10.99999999883999990, 0.3999999988385999905, -7.388315149414999894 ) ) ;
#60267=ORIENTED_EDGE ( 'NONE', *, *, #45454, .T. ) ;
#60273=CARTESIAN_POINT ( 'NONE',  ( 8.099999999999999645, 0.000000000000000000, 11.84999999999999964 ) ) ;
#60275=ORIENTED_EDGE ( 'NONE', *, *, #41907, .F. ) ;
#60276=CARTESIAN_POINT ( 'NONE',  ( 6.949999692292999853, -1.332267629549999942E-14, 1.576516694967999966E-14 ) ) ;
#60281=CARTESIAN_POINT ( 'NONE',  ( 9.021064158776001207, 4.883347899767999323, -6.417062834774999835 ) ) ;
#60290=CARTESIAN_POINT ( 'NONE',  ( 9.096889158776001238, 2.235961884443999459, -6.794506518623999902 ) ) ;
#60292=CARTESIAN_POINT ( 'NONE',  ( 10.38153063908000107, 2.772139908660999907, -8.408082511401000048 ) ) ;
#60294=ORIENTED_EDGE ( 'NONE', *, *, #8365, .F. ) ;
#60301=ADVANCED_FACE ( 'NONE', ( #22539 ), #35179, .T. ) ;
#60306=CARTESIAN_POINT ( 'NONE',  ( 11.00119221959000093, 4.640446572790000168, -9.059321223816999336 ) ) ;
#60316=CARTESIAN_POINT ( 'NONE',  ( 8.351014158771000950, 5.616457598545999907, -8.245813000738998255 ) ) ;
#60334=VERTEX_POINT ( 'NONE', #34775 ) ;
#60336=CARTESIAN_POINT ( 'NONE',  ( 8.927279675098239053, 5.100000000000000533, -6.498507975215145116 ) ) ;
#60337=CARTESIAN_POINT ( 'NONE',  ( 8.555820280412000045, 2.414630869937000046, -6.801495146585999407 ) ) ;
#60338=FACE_OUTER_BOUND ( 'NONE', #10387, .T. ) ;
#60342=CARTESIAN_POINT ( 'NONE',  ( 2.638201263761000170, 2.164689359125999690, -2.654983729890999733 ) ) ;
#60346=DIRECTION ( 'NONE',  ( 1.000000000000000000, 0.000000000000000000, 0.000000000000000000 ) ) ;
#60347=CARTESIAN_POINT ( 'NONE',  ( 9.143920280410000601, 5.791553967443999973, 7.752111263209999770 ) ) ;
#60350=CARTESIAN_POINT ( 'NONE',  ( 10.93613845918347138, 9.381696929438323451, 6.182830334041338638 ) ) ;
#60352=CARTESIAN_POINT ( 'NONE',  ( 0.000000000000000000, 5.100000000000000533, 7.500000000000000000 ) ) ;
#60354=VERTEX_POINT ( 'NONE', #13453 ) ;
#60359=AXIS2_PLACEMENT_3D ( 'NONE', #60740, #25307, #55501 ) ;
#60363=ADVANCED_FACE ( 'NONE', ( #34085, #12059 ), #38981, .F. ) ;
#60367=CARTESIAN_POINT ( 'NONE',  ( 7.391614158769000298, 2.869384229876999814, -6.678559560168999987 ) ) ;
#60370=ORIENTED_EDGE ( 'NONE', *, *, #42187, .T. ) ;
#60371=CARTESIAN_POINT ( 'NONE',  ( 9.069718325438000051, 4.108964550738000376, 8.851615252874999840 ) ) ;
#60374=CARTESIAN_POINT ( 'NONE',  ( 11.03776785110999903, 5.237767851104999650, 6.571291218949999902 ) ) ;
#60377=EDGE_LOOP ( 'NONE', ( #54101, #47036, #2384, #32365 ) ) ;
#60382=CARTESIAN_POINT ( 'NONE',  ( 5.000030787343000327, -0.5496608443529829024, 2.045306479342562156 ) ) ;
#60386=ORIENTED_EDGE ( 'NONE', *, *, #38919, .F. ) ;
#60387=EDGE_CURVE ( 'NONE', #58572, #15150, #16836, .T. ) ;
#60391=CARTESIAN_POINT ( 'NONE',  ( 0.1499942179680000542, 2.749953718116142642, 0.3599680999394014314 ) ) ;
#60392=CARTESIAN_POINT ( 'NONE',  ( 8.351014158771000950, 5.616457598545999907, -8.245813000738998255 ) ) ;
#60394=CARTESIAN_POINT ( 'NONE',  ( 3.425331920129000007, 1.732887122961999982, 2.901267362544000417 ) ) ;
#60401=AXIS2_PLACEMENT_3D ( 'NONE', #10619, #47694, #58860 ) ;
#60403=CARTESIAN_POINT ( 'NONE',  ( 10.59344747867000081, 5.297752619853000944, 8.474195539311001113 ) ) ;
#60406=CARTESIAN_POINT ( 'NONE',  ( 11.01666666666767469, 3.382745367833757122, 8.852578401491365767 ) ) ;
#60410=CARTESIAN_POINT ( 'NONE',  ( 7.100000000000521894, 4.275133281870672874, -6.140122557344056098 ) ) ;
#60414=CARTESIAN_POINT ( 'NONE',  ( 8.113858213201577740, 5.049150732340172532, -6.494099727906681885 ) ) ;
#60423=CARTESIAN_POINT ( 'NONE',  ( 8.373670280412000011, 2.202812441249000219, 7.706988150133999405 ) ) ;
#60424=CARTESIAN_POINT ( 'NONE',  ( 8.397785841227999981, 5.616457598545999907, -8.245813000738998255 ) ) ;
#60425=DIRECTION ( 'NONE',  ( 1.000000000000000000, 0.000000000000000000, 0.000000000000000000 ) ) ;
#60426=CARTESIAN_POINT ( 'NONE',  ( 10.64556415877000006, 2.988929467935999895, -5.952329570726999641 ) ) ;
#60428=CARTESIAN_POINT ( 'NONE',  ( 9.910633732652998518, 2.107262079134000210, 7.885285091859000062 ) ) ;
#60433=ORIENTED_EDGE ( 'NONE', *, *, #66436, .F. ) ;
#60434=CARTESIAN_POINT ( 'NONE',  ( 11.09999999999999964, 5.299311513382999550, 5.124965750789000296 ) ) ;
#60447=EDGE_CURVE ( 'NONE', #55474, #61815, #4649, .T. ) ;
#60449=CARTESIAN_POINT ( 'NONE',  ( 9.301695280414000067, 5.619431609641999614, -8.115423117607999615 ) ) ;
#60464=CARTESIAN_POINT ( 'NONE',  ( 10.75911768454999873, 4.477564074640000058, -5.708570851020999370 ) ) ;
#60472=CARTESIAN_POINT ( 'NONE',  ( 9.059364158773000497, 4.192919163547999872, 5.525472271700999194 ) ) ;
#60476=CARTESIAN_POINT ( 'NONE',  ( 10.62793268324000096, 3.100586971929999880, 8.599896650316999569 ) ) ;
#60477=EDGE_CURVE ( 'NONE', #24606, #28975, #68686, .T. ) ;
#60481=CARTESIAN_POINT ( 'NONE',  ( 9.380783851237000093, 2.204242311415999911, 7.545378292079000460 ) ) ;
#60483=CARTESIAN_POINT ( 'NONE',  ( 2.244900308897999963, 3.200088964812000114, -0.3100843839799999890 ) ) ;
#60490=EDGE_CURVE ( 'NONE', #8323, #57590, #19318, .T. ) ;
#60492=CARTESIAN_POINT ( 'NONE',  ( 8.946010841230998878, 5.458692773671000253, 7.456452194274000078 ) ) ;
#60493=CARTESIAN_POINT ( 'NONE',  ( 10.02991192131000098, 2.506457833269999824, 6.215406506815000398 ) ) ;
#60496=CARTESIAN_POINT ( 'NONE',  ( 9.734454719592999794, 3.021734963141999852, -6.070209284876999511 ) ) ;
#60498=DIRECTION ( 'NONE',  ( 0.000000000000000000, 0.000000000000000000, -1.000000000000000000 ) ) ;
#60506=CARTESIAN_POINT ( 'NONE',  ( 1.019382100425000104, -2.055220836715000221, 2.740599349591000156 ) ) ;
#60510=CARTESIAN_POINT ( 'NONE',  ( 7.717918988116000634, 2.852331522235000083, 6.784355039830999523 ) ) ;
#60515=ORIENTED_EDGE ( 'NONE', *, *, #21940, .F. ) ;
#60516=CARTESIAN_POINT ( 'NONE',  ( 7.375416666664626142, 2.649999999999999467, -7.323285413235579355 ) ) ;
#60520=CARTESIAN_POINT ( 'NONE',  ( 10.70577346828306453, 5.100000000000000533, -6.304440314035878679 ) ) ;
#60521=CARTESIAN_POINT ( 'NONE',  ( 1.132929084573000011, 0.9191385115525000371, 3.644662079466999938 ) ) ;
#60523=CARTESIAN_POINT ( 'NONE',  ( 10.79212049822984554, 3.170455386494787309, -8.579526322294437790 ) ) ;
#60525=CARTESIAN_POINT ( 'NONE',  ( 9.959641781044998865, 5.406625910119999823, 7.700299649248999678 ) ) ;
#60535=LINE ( 'NONE', #17540, #38840 ) ;
#60538=CARTESIAN_POINT ( 'NONE',  ( 8.696135841231001251, 3.038023536984999939, -5.861661709981000001 ) ) ;
#60546=CARTESIAN_POINT ( 'NONE',  ( 9.629022744239000176, 5.794335169544999609, 7.414871903737999759 ) ) ;
#60551=CARTESIAN_POINT ( 'NONE',  ( 11.04859286640838256, 4.978068212549554339, -8.665561624473726354 ) ) ;
#60556=B_SPLINE_CURVE_WITH_KNOTS ( 'NONE', 3,
 ( #59407, #22000, #11857, #53823, #5577, #38784, #37744, #26920, #43346, #59071, #64648, #339, #65690, #38081, #6263, #49266, #60111, #27603 ),
 .UNSPECIFIED., .F., .F.,
 ( 4, 2, 2, 2, 2, 2, 2, 2, 4 ),
 ( 0.000000000000000000, 0.2500000000000080491, 0.3750000000000123235, 0.4375000000000129896, 0.4687500000000133227, 0.5000000000000136557, 0.6250000000000094369, 0.7500000000000052180, 1.000000000000000000 ),
 .UNSPECIFIED. ) ;
#60560=CARTESIAN_POINT ( 'NONE',  ( 5.000030787343000327, 1.679270695423614956, -1.290525307673968003 ) ) ;
#60568=CARTESIAN_POINT ( 'NONE',  ( 7.605771682457999283, 5.346164515353000191, -7.398308812559000636 ) ) ;
#60573=CARTESIAN_POINT ( 'NONE',  ( 8.590779719591999708, 2.836879604150999601, -8.783908972046001296 ) ) ;
#60577=DIRECTION ( 'NONE',  ( -1.000000000000000000, 0.000000000000000000, 0.000000000000000000 ) ) ;
#60583=DIRECTION ( 'NONE',  ( 0.000000000000000000, 0.000000000000000000, 1.000000000000000000 ) ) ;
#60589=ORIENTED_EDGE ( 'NONE', *, *, #5349, .T. ) ;
#60600=CARTESIAN_POINT ( 'NONE',  ( 10.98768472569999943, 5.449702578894000560, 4.945212061318999375 ) ) ;
#60614=CARTESIAN_POINT ( 'NONE',  ( 8.379056333468048123, 2.650684137603387835, -7.263287199838283748 ) ) ;
#60618=CARTESIAN_POINT ( 'NONE',  ( 5.000030787343000327, 2.099962892530999881, 0.000000000000000000 ) ) ;
#60619=EDGE_LOOP ( 'NONE', ( #7678, #27312, #44156, #24245, #30258 ) ) ;
#60620=CARTESIAN_POINT ( 'NONE',  ( 0.1189017606508744468, -1.063211791521875504, -2.979546336419315544 ) ) ;
#60623=CARTESIAN_POINT ( 'NONE',  ( 8.445233760363150211, 5.313925467271168657, 7.853812692271652907 ) ) ;
#60625=CARTESIAN_POINT ( 'NONE',  ( 8.406645280410000254, 3.807713920470999991, -9.221758713517999695 ) ) ;
#60633=CARTESIAN_POINT ( 'NONE',  ( 9.594139158774000364, 2.212639797530000063, -6.855876382544999537 ) ) ;
#60634=ORIENTED_EDGE ( 'NONE', *, *, #41319, .T. ) ;
#60636=CARTESIAN_POINT ( 'NONE',  ( 10.93146722582000052, 2.472885155055999817, -7.514158739122999364 ) ) ;
#60642=FACE_OUTER_BOUND ( 'NONE', #51841, .T. ) ;
#60646=VERTEX_POINT ( 'NONE', #5343 ) ;
#60648=CARTESIAN_POINT ( 'NONE',  ( 10.75102028041000146, 2.478469530773999896, -7.438303846328000013 ) ) ;
#60657=ORIENTED_EDGE ( 'NONE', *, *, #54256, .F. ) ;
#60658=CARTESIAN_POINT ( 'NONE',  ( 8.690229719593000723, 2.414630869937000046, -6.801495146585999407 ) ) ;
#60659=EDGE_CURVE ( 'NONE', #45966, #52078, #7266, .T. ) ;
#60671=CIRCLE ( 'NONE', #57315, 3.200000000000000178 ) ;
#60672=CARTESIAN_POINT ( 'NONE',  ( 10.45746213570999927, 5.100000000000000533, -6.571291218949999902 ) ) ;
#60673=CARTESIAN_POINT ( 'NONE',  ( 7.877465161153600626, 5.139684818804880706, 6.768899810017460439 ) ) ;
#60678=CARTESIAN_POINT ( 'NONE',  ( 9.573148997458000409, 5.167567567567999731, -6.822293592207000934 ) ) ;
#60679=CARTESIAN_POINT ( 'NONE',  ( 9.410004719593999312, 2.495531372253999791, -7.930944806125000746 ) ) ;
#60682=CARTESIAN_POINT ( 'NONE',  ( 8.200000998245998929, 3.037570195374000164E-13, -12.49999978039658544 ) ) ;
#60684=CARTESIAN_POINT ( 'NONE',  ( 3.072112146792000065, 3.006932304320000249, -1.965249848430999924 ) ) ;
#60689=CARTESIAN_POINT ( 'NONE',  ( 7.641204719590000138, 4.524487726177000013, 9.047753146378999745 ) ) ;
#60694=CARTESIAN_POINT ( 'NONE',  ( 10.95262535236630086, 9.076036533295676278, 6.378678306765203310 ) ) ;
#60696=CARTESIAN_POINT ( 'NONE',  ( 7.844724277266999835, 4.719412473309000156, 6.357657803787000184 ) ) ;
#60698=ORIENTED_EDGE ( 'NONE', *, *, #35747, .F. ) ;
#60699=AXIS2_PLACEMENT_3D ( 'NONE', #54457, #6558, #49210 ) ;
#60706=CARTESIAN_POINT ( 'NONE',  ( 10.98606062297321806, 8.050563008166918166, -6.521190260545529860 ) ) ;
#60708=CARTESIAN_POINT ( 'NONE',  ( 8.038039158770001080, 5.092576903264999899, -6.628615687103999399 ) ) ;
#60721=CIRCLE ( 'NONE', #48442, 1.999999999999999778 ) ;
#60731=ORIENTED_EDGE ( 'NONE', *, *, #28896, .F. ) ;
#60733=CARTESIAN_POINT ( 'NONE',  ( 9.295789158775001226, 5.835196551504000517, -7.008466539623000813 ) ) ;
#60734=CARTESIAN_POINT ( 'NONE',  ( 2.293573906239000149, 2.743716934200000068, -1.972779657783999996 ) ) ;
#60737=CARTESIAN_POINT ( 'NONE',  ( 8.066302634316002695, 3.111242948840002409, -6.203702194951995708 ) ) ;
#60739=EDGE_LOOP ( 'NONE', ( #25964, #54192, #48637, #18682, #14350 ) ) ;
#60740=CARTESIAN_POINT ( 'NONE',  ( 27.64127793187000037, 5.599999999999999645, -6.571291218949999902 ) ) ;
#60742=CARTESIAN_POINT ( 'NONE',  ( 10.03490996941999924, 5.615906393494999982, 7.351455918368999143 ) ) ;
#60745=CARTESIAN_POINT ( 'NONE',  ( 11.00833333333434183, 3.620091288824011766, 8.928205453214854259 ) ) ;
#60746=VECTOR ( 'NONE', #44781, 1000.000000000000000 ) ;
#60748=CARTESIAN_POINT ( 'NONE',  ( 4.500000000000000000, 0.000000000000000000, 0.000000000000000000 ) ) ;
#60753=CARTESIAN_POINT ( 'NONE',  ( 0.8414471766558753174, -1.482381544592732414, -3.195448105648677650 ) ) ;
#60754=CARTESIAN_POINT ( 'NONE',  ( 10.10735778041000010, 4.293584699549000128, -8.994197232567001876 ) ) ;
#60755=EDGE_LOOP ( 'NONE', ( #47679, #39378, #12807, #14378, #16622 ) ) ;
#60762=B_SPLINE_CURVE_WITH_KNOTS ( 'NONE', 3,
 ( #2225, #39981, #45222, #17257, #55015, #54313 ),
 .UNSPECIFIED., .F., .F.,
 ( 4, 2, 4 ),
 ( 0.000000000000000000, 0.5000000000000000000, 1.000000000000000000 ),
 .UNSPECIFIED. ) ;
#60763=CARTESIAN_POINT ( 'NONE',  ( 8.898551658772998252, 5.146726419831999522, 6.597424767138000412 ) ) ;
#60764=CIRCLE ( 'NONE', #25035, 12.24999851416000141 ) ;
#60767=CARTESIAN_POINT ( 'NONE',  ( 10.26693915877000052, 5.500023470133998948, -6.419501519420999891 ) ) ;
#60769=CARTESIAN_POINT ( 'NONE',  ( 10.55813337864000090, 2.466561068647000532, 6.633529813744000414 ) ) ;
#60792=CARTESIAN_POINT ( 'NONE',  ( 9.790085841230000696, 5.149303692842000402, -5.987168472229000393 ) ) ;
#60794=CARTESIAN_POINT ( 'NONE',  ( 8.244294876368201130, 4.976357605550050245, 6.306308086258407997 ) ) ;
#60798=EDGE_LOOP ( 'NONE', ( #22776, #51452, #45622, #64502 ) ) ;
#60811=DIRECTION ( 'NONE',  ( 0.000000000000000000, -0.1218274111675001214, -0.9925512993736016476 ) ) ;
#60816=CARTESIAN_POINT ( 'NONE',  ( 7.283509992105000386, 4.426928431836000044, 9.293321981113999541 ) ) ;
#60817=ORIENTED_EDGE ( 'NONE', *, *, #14526, .T. ) ;
#60820=CARTESIAN_POINT ( 'NONE',  ( 7.460114837477927807, 5.349842312901899710, 7.234364343742836212 ) ) ;
#60827=CARTESIAN_POINT ( 'NONE',  ( 10.06344080699000010, 5.156228702401000952, 6.125219923432000613 ) ) ;
#60828=FACE_OUTER_BOUND ( 'NONE', #68445, .T. ) ;
#60829=CARTESIAN_POINT ( 'NONE',  ( 8.100000113405998903, 3.037570195374000164E-13, -3.946654265865999873E-14 ) ) ;
#60830=ORIENTED_EDGE ( 'NONE', *, *, #55425, .F. ) ;
#60833=CARTESIAN_POINT ( 'NONE',  ( 9.792569055495000896, 3.463432304708999876, 6.184396499233999478 ) ) ;
#60840=CARTESIAN_POINT ( 'NONE',  ( 7.326301658771000369, 3.394842219570000097, 9.388954446285000088 ) ) ;
#60841=CARTESIAN_POINT ( 'NONE',  ( 9.194604681486000075, 5.157771204918000230, 8.637848577075999401 ) ) ;
#60844=CARTESIAN_POINT ( 'NONE',  ( 9.892489158770999325, 5.099602161831000124, -9.049221499261999924 ) ) ;
#60852=CARTESIAN_POINT ( 'NONE',  ( 2.306794735327000190, 2.895272466935999933, -1.424404891072999835 ) ) ;
#60855=DIRECTION ( 'NONE',  ( 0.7071082394066439125, 0.7071053229634438608, -3.846805239771239731E-11 ) ) ;
#60858=CARTESIAN_POINT ( 'NONE',  ( 4.900006121742001675, -1.229093439949833444, -1.599333684796358401 ) ) ;
#60859=CARTESIAN_POINT ( 'NONE',  ( 7.933148997457998952, 5.167567567567999731, 6.822293592207000934 ) ) ;
#60867=LINE ( 'NONE', #7727, #43748 ) ;
#60868=CARTESIAN_POINT ( 'NONE',  ( 0.8945193373687000404, -0.3804460121770000258, -3.739470302966999782 ) ) ;
#60870=CARTESIAN_POINT ( 'NONE',  ( 10.71922080291976265, 4.353435520373844625, -8.814860677227555286 ) ) ;
#60873=DIRECTION ( 'NONE',  ( -0.000000000000000000, 1.000000000000000000, 0.000000000000000000 ) ) ;
#60881=ORIENTED_EDGE ( 'NONE', *, *, #48296, .T. ) ;
#60882=CARTESIAN_POINT ( 'NONE',  ( 8.229134761907859641, 5.632572539116967647, 8.109682519133768253 ) ) ;
#60883=ORIENTED_EDGE ( 'NONE', *, *, #50499, .T. ) ;
#60886=ORIENTED_EDGE ( 'NONE', *, *, #47858, .F. ) ;
#60887=FACE_OUTER_BOUND ( 'NONE', #37667, .T. ) ;
#60890=EDGE_CURVE ( 'NONE', #44629, #44553, #30971, .T. ) ;
#60892=CARTESIAN_POINT ( 'NONE',  ( 10.09197164456000095, 3.841384681542000301, 5.536408945990000774 ) ) ;
#60894=CARTESIAN_POINT ( 'NONE',  ( 11.10000012945999970, 9.963297611412999188, -5.844090155092000138 ) ) ;
#60895=PLANE ( 'NONE',  #1412 ) ;
#60900=ORIENTED_EDGE ( 'NONE', *, *, #56376, .F. ) ;
#60904=CARTESIAN_POINT ( 'NONE',  ( 6.477679953015996084, 8.358404271369996863, 3.996200428631998314 ) ) ;
#60916=CARTESIAN_POINT ( 'NONE',  ( 9.228345280414000484, 2.481540185810000132, -7.878707153279001396 ) ) ;
#60918=CARTESIAN_POINT ( 'NONE',  ( 11.09999999999999964, 4.000000000000000000, -7.500000000000000000 ) ) ;
#60919=CARTESIAN_POINT ( 'NONE',  ( 11.00865415830999972, 8.467328835748000770, -6.608351749142999942 ) ) ;
#60920=EDGE_CURVE ( 'NONE', #19641, #68613, #26762, .T. ) ;
#60921=EDGE_CURVE ( 'NONE', #49079, #54494, #45261, .T. ) ;
#60935=CARTESIAN_POINT ( 'NONE',  ( 9.099999886593998610, -12.39999890530000037, 0.000000000000000000 ) ) ;
#60942=CARTESIAN_POINT ( 'NONE',  ( 10.89999835797000038, -1.382741308456999940, -11.26545887848999961 ) ) ;
#60950=VECTOR ( 'NONE', #25591, 1000.000000000000000 ) ;
#60955=CARTESIAN_POINT ( 'NONE',  ( 0.9155567992084958640, -0.4581489286485083134, -3.500000000000000888 ) ) ;
#60962=CARTESIAN_POINT ( 'NONE',  ( 7.000000000000000888, 8.490173021533447439, 4.467909175706600067 ) ) ;
#60972=CARTESIAN_POINT ( 'NONE',  ( 9.301695280414000067, 5.619431609641999614, -8.115423117607999615 ) ) ;
#60976=EDGE_CURVE ( 'NONE', #56759, #1011, #123, .T. ) ;
#60981=CARTESIAN_POINT ( 'NONE',  ( 9.395239158775000377, 5.045571591548999812, -9.086294919530001124 ) ) ;
#60982=ORIENTED_EDGE ( 'NONE', *, *, #41104, .F. ) ;
#60983=CARTESIAN_POINT ( 'NONE',  ( 9.910156421876999744, 2.531070993918000056, -7.917736616860999277 ) ) ;
#60987=CARTESIAN_POINT ( 'NONE',  ( 10.98768472567999943, 5.449702577258999980, -4.945212061305999107 ) ) ;
#60992=ORIENTED_EDGE ( 'NONE', *, *, #13050, .F. ) ;
#60994=CARTESIAN_POINT ( 'NONE',  ( 10.88760471959000142, 5.634847467408999222, -7.088990678556999825 ) ) ;
#61001=CARTESIAN_POINT ( 'NONE',  ( 10.17905590578999941, 2.899999999999999911, 6.571291218949999902 ) ) ;
#61003=VERTEX_POINT ( 'NONE', #32726 ) ;
#61005=CARTESIAN_POINT ( 'NONE',  ( 8.699089158774000907, 4.178200486578000472, -5.608493638783999202 ) ) ;
#61008=EDGE_CURVE ( 'NONE', #23338, #68419, #9277, .T. ) ;
#61009=EDGE_CURVE ( 'NONE', #8323, #18734, #48415, .T. ) ;
#61017=EDGE_LOOP ( 'NONE', ( #6532, #67319, #64973 ) ) ;
#61020=CARTESIAN_POINT ( 'NONE',  ( 9.356851002546999752, 2.832432432432000269, -6.822293592207000934 ) ) ;
#61023=CARTESIAN_POINT ( 'NONE',  ( 4.149992563291999836, -1.947893036340042849, 0.5234817089163666948 ) ) ;
#61027=CARTESIAN_POINT ( 'NONE',  ( 8.854170280414001226, 4.902869380824999901, -8.978557145469999057 ) ) ;
#61033=CARTESIAN_POINT ( 'NONE',  ( 2.495155415437999569, -3.073701342168999595, -1.512342069823999990 ) ) ;
#61038=CARTESIAN_POINT ( 'NONE',  ( 7.807364158771999740, 3.650414032626000171, 6.083147621602999600 ) ) ;
#61042=CARTESIAN_POINT ( 'NONE',  ( 10.91882084328970670, 9.640838713336684407, 5.933495657908773424 ) ) ;
#61044=CARTESIAN_POINT ( 'NONE',  ( 10.64831157502399073, 4.679757719901597390, -8.679446014678214638 ) ) ;
#61051=DIRECTION ( 'NONE',  ( 0.000000000000000000, -1.000000000000000000, 0.000000000000000000 ) ) ;
#61058=CARTESIAN_POINT ( 'NONE',  ( 8.170639158770999444, 4.727211190310000255, -8.622645617656999661 ) ) ;
#61061=CARTESIAN_POINT ( 'NONE',  ( 11.09999999999999964, 4.000000000000000000, 7.500000000000000000 ) ) ;
#61063=DIRECTION ( 'NONE',  ( -0.7071068156326932863, 0.000000000000000000, -0.7071067467404001938 ) ) ;
#61072=CARTESIAN_POINT ( 'NONE',  ( 8.398903073012702336, 5.292594335792998095, -8.672717482341102624 ) ) ;
#61078=VERTEX_POINT ( 'NONE', #50529 ) ;
#61080=EDGE_LOOP ( 'NONE', ( #23708, #2741, #28120, #9265, #58958 ) ) ;
#61082=CARTESIAN_POINT ( 'NONE',  ( 9.278070280414000948, 2.546924812613000189, -6.918870225297999887 ) ) ;
#61083=CARTESIAN_POINT ( 'NONE',  ( 2.915571724536000442, -1.477002359740999804, 2.855699589946999684 ) ) ;
#61085=CARTESIAN_POINT ( 'NONE',  ( 7.858269739253733732, 2.859091829101807480, -6.771441901864826640 ) ) ;
#61087=ORIENTED_EDGE ( 'NONE', *, *, #7962, .T. ) ;
#61090=CARTESIAN_POINT ( 'NONE',  ( 10.06843885510000014, 4.148608506723999945, 8.941445591976998841 ) ) ;
#61096=CONICAL_SURFACE ( 'NONE', #65522, 12.37499919541000004, 0.7853980884875938484 ) ;
#61097=CARTESIAN_POINT ( 'NONE',  ( 10.92117502560267361, 2.832205961051685428, -6.780502835040467247 ) ) ;
#61102=CARTESIAN_POINT ( 'NONE',  ( 0.9500156295917255855, 2.823650222959981804, -2.106025417230501962 ) ) ;
#61104=CARTESIAN_POINT ( 'NONE',  ( 10.16008584122999991, 4.812959680871000678, -8.526582921144999716 ) ) ;
#61111=ORIENTED_EDGE ( 'NONE', *, *, #54614, .F. ) ;
#61112=CONICAL_SURFACE ( 'NONE', #27571, 13.04999934368000147, 0.7853981075146502233 ) ;
#61113=B_SPLINE_CURVE_WITH_KNOTS ( 'NONE', 3,
 ( #1540, #13078, #22858, #62670 ),
 .UNSPECIFIED., .F., .F.,
 ( 4, 4 ),
 ( 0.000000000000000000, 0.1253179912170450105 ),
 .UNSPECIFIED. ) ;
#61115=CARTESIAN_POINT ( 'NONE',  ( 8.604017219593000476, 5.165497731316000873, 8.645531386060000045 ) ) ;
#61117=CYLINDRICAL_SURFACE ( 'NONE', #66648, 12.50000000000000000 ) ;
#61118=CARTESIAN_POINT ( 'NONE',  ( 9.900934992105000276, 4.883852641422000040, -9.070888919673000927 ) ) ;
#61119=ORIENTED_EDGE ( 'NONE', *, *, #61266, .F. ) ;
#61120=CARTESIAN_POINT ( 'NONE',  ( 9.576488281553999116, 4.593976206186999534, 5.662041230125000268 ) ) ;
#61122=CARTESIAN_POINT ( 'NONE',  ( 9.766851002543001314, 2.832432432432000269, 6.822293592207000934 ) ) ;
#61125=CARTESIAN_POINT ( 'NONE',  ( 8.228219317832992985, 3.441361860949001539, 6.127431671619995690 ) ) ;
#61126=EDGE_LOOP ( 'NONE', ( #47049, #56173, #50969, #64124 ) ) ;
#61127=DIRECTION ( 'NONE',  ( 1.000000000000000000, 0.000000000000000000, 0.000000000000000000 ) ) ;
#61136=EDGE_LOOP ( 'NONE', ( #38973, #54000, #7941, #13161 ) ) ;
#61137=CARTESIAN_POINT ( 'NONE',  ( 4.000000000000000000, 2.750000000000000000, 0.000000000000000000 ) ) ;
#61140=CARTESIAN_POINT ( 'NONE',  ( 9.442010841233001273, 5.045571591548999812, -9.086294919530001124 ) ) ;
#61142=DIRECTION ( 'NONE',  ( 0.000000000000000000, -0.8648648648648720183, 0.5020047465136825426 ) ) ;
#61146=( BOUNDED_SURFACE ( )  B_SPLINE_SURFACE ( 3, 3, ( 
 ( #54705, #16261, #53332, #5432, #59602, #22537, #48425 ),
 ( #881, #54352, #21846, #38626, #33389, #10672, #43181 ),
 ( #12057, #58918, #6804, #32019, #32695, #17301, #47747 ),
 ( #53674, #59947, #69062, #58568, #22197, #21168, #43533 ) ),
 .UNSPECIFIED., .F., .F., .T. ) 
 B_SPLINE_SURFACE_WITH_KNOTS ( ( 4, 4 ),
 ( 4, 1, 1, 1, 4 ),
 ( 0.000000000000000000, 1.000000000000000000 ),
 ( 0.8949772423043999003, 0.9056938526918999477, 0.9344431701380999655, 0.9658387281735000274, 0.9801003582285999771 ),
 .UNSPECIFIED. ) 
 GEOMETRIC_REPRESENTATION_ITEM ( )  RATIONAL_B_SPLINE_SURFACE ( (
 ( 1.200981758128000010, 1.200981758128000010, 1.200981758128000010, 1.200981758128000010, 1.200981758128000010, 1.200981758128000010, 1.200981758128000010),
 ( 0.9330060806240999538, 0.9330060806240999538, 0.9330060806240999538, 0.9330060806240999538, 0.9330060806240999538, 0.9330060806240999538, 0.9330060806240999538),
 ( 0.9330060806240999538, 0.9330060806240999538, 0.9330060806240999538, 0.9330060806240999538, 0.9330060806240999538, 0.9330060806240999538, 0.9330060806240999538),
 ( 1.200981758128000010, 1.200981758128000010, 1.200981758128000010, 1.200981758128000010, 1.200981758128000010, 1.200981758128000010, 1.200981758128000010) ) ) 
 REPRESENTATION_ITEM ( '' )  SURFACE ( )  );
#61147=ORIENTED_EDGE ( 'NONE', *, *, #53574, .F. ) ;
#61149=ORIENTED_EDGE ( 'NONE', *, *, #2690, .T. ) ;
#61151=CARTESIAN_POINT ( 'NONE',  ( 7.931011803055000975, 3.387313518888000363, -6.297038610257000180 ) ) ;
#61157=FACE_OUTER_BOUND ( 'NONE', #7488, .T. ) ;
#61159=CARTESIAN_POINT ( 'NONE',  ( 9.934999999999998721, 4.640430492595999823, -9.117542781427999898 ) ) ;
#61164=CARTESIAN_POINT ( 'NONE',  ( 7.994579719591000000, 2.263558315407000254, 8.007442119518000112 ) ) ;
#61165=ORIENTED_EDGE ( 'NONE', *, *, #698, .T. ) ;
#61168=CARTESIAN_POINT ( 'NONE',  ( 8.017297003156361512, 5.179978819780632016, 8.180934229233717048 ) ) ;
#61172=CARTESIAN_POINT ( 'NONE',  ( 10.09197164456000095, 3.841384681542000301, 5.536408945990000774 ) ) ;
#61174=CARTESIAN_POINT ( 'NONE',  ( 8.023148997453999343, 5.167567567567999731, -6.822293592207000934 ) ) ;
#61179=EDGE_CURVE ( 'NONE', #13153, #13611, #4675, .T. ) ;
#61181=CARTESIAN_POINT ( 'NONE',  ( 10.14750576281000072, 2.602962605360999770, 6.738577830910999822 ) ) ;
#61186=CARTESIAN_POINT ( 'NONE',  ( 7.481079719589999399, 2.374037589774999901, 8.293392681990997772 ) ) ;
#61187=CARTESIAN_POINT ( 'NONE',  ( 9.290193290418001126, 2.377818438998999806, 7.540992072119000689 ) ) ;
#61198=B_SPLINE_CURVE_WITH_KNOTS ( 'NONE', 3,
 ( #48535, #59707, #27552, #49216 ),
 .UNSPECIFIED., .F., .F.,
 ( 4, 4 ),
 ( 0.000000000000000000, 1.000000000000000000 ),
 .UNSPECIFIED. ) ;
#61199=CARTESIAN_POINT ( 'NONE',  ( 2.120840275626000082, -0.2760264376601999636, -3.247374627496999899 ) ) ;
#61202=CARTESIAN_POINT ( 'NONE',  ( 0.8183045265946674585, 2.967694544611792828, -1.300349661452710803 ) ) ;
#61204=B_SPLINE_CURVE_WITH_KNOTS ( 'NONE', 3,
 ( #62771, #30983, #42159, #14894 ),
 .UNSPECIFIED., .F., .F.,
 ( 4, 4 ),
 ( 0.000000000000000000, 1.000000000000000000 ),
 .UNSPECIFIED. ) ;
#61211=ORIENTED_EDGE ( 'NONE', *, *, #43797, .T. ) ;
#61212=CARTESIAN_POINT ( 'NONE',  ( 8.625073341231001223, 3.117378429069999957, 8.662179062556001341 ) ) ;
#61213=CARTESIAN_POINT ( 'NONE',  ( 11.05220172920000010, 5.231347787620000744, 4.974789424501000923 ) ) ;
#61217=CARTESIAN_POINT ( 'NONE',  ( 0.9278812726222999130, -0.1441893070566999946, 3.255843074068999865 ) ) ;
#61218=ORIENTED_EDGE ( 'NONE', *, *, #44778, .T. ) ;
#61219=CARTESIAN_POINT ( 'NONE',  ( 10.72963504510710564, 4.176677120266796273, -8.849854844400319109 ) ) ;
#61221=CARTESIAN_POINT ( 'NONE',  ( 10.53734212242000012, 2.992816679959000137, 8.731689474572998932 ) ) ;
#61227=CARTESIAN_POINT ( 'NONE',  ( 0.4843736936024935491, 2.045128573188879972, -2.872081862618736547 ) ) ;
#61229=CARTESIAN_POINT ( 'NONE',  ( 8.274731576662917476, 5.048784206079365511, 8.903984921411593589 ) ) ;
#61234=ORIENTED_EDGE ( 'NONE', *, *, #18620, .F. ) ;
#61238=CARTESIAN_POINT ( 'NONE',  ( 9.215291255903000689, 4.861981595026999337, 8.938817176893000038 ) ) ;
#61240=CARTESIAN_POINT ( 'NONE',  ( 10.01597178489000051, 4.792666960550000077, -6.390258598531999290 ) ) ;
#61241=CARTESIAN_POINT ( 'NONE',  ( 8.706911754519369495, 3.704150863171606467, -8.842717511604519132 ) ) ;
#61251=CARTESIAN_POINT ( 'NONE',  ( 5.000030787343000327, 2.045306479342561268, -0.5496608443529887866 ) ) ;
#61265=CARTESIAN_POINT ( 'NONE',  ( 7.000000000000000000, 8.307879248642999315, -4.307879248643000203 ) ) ;
#61266=EDGE_CURVE ( 'NONE', #64893, #29332, #39260, .T. ) ;
#61268=FACE_OUTER_BOUND ( 'NONE', #69115, .T. ) ;
#61272=LINE ( 'NONE', #45199, #39713 ) ;
#61275=CARTESIAN_POINT ( 'NONE',  ( 10.94846415877000112, 3.841064079579000090, -9.341816855317999213 ) ) ;
#61294=CARTESIAN_POINT ( 'NONE',  ( 6.966665878460972294, 12.09896511371893446, 3.276379751798347506 ) ) ;
#61305=CARTESIAN_POINT ( 'NONE',  ( 2.250973465874000379, -3.500000000000000000, 0.000000000000000000 ) ) ;
#61306=CARTESIAN_POINT ( 'NONE',  ( 8.142589158771000868, 5.074768364528000397, -8.296267706722000312 ) ) ;
#61314=CARTESIAN_POINT ( 'NONE',  ( 8.912754719595000097, 2.481540185810000132, -7.878707153279001396 ) ) ;
#61315=EDGE_CURVE ( 'NONE', #53307, #55375, #4258, .T. ) ;
#61317=EDGE_CURVE ( 'NONE', #59495, #14714, #37640, .T. ) ;
#61320=ADVANCED_FACE ( 'NONE', ( #57741 ), #53543, .F. ) ;
#61323=CARTESIAN_POINT ( 'NONE',  ( 7.700135044850973998, 4.657064392362385341, -8.696559172435133434 ) ) ;
#61327=CARTESIAN_POINT ( 'NONE',  ( 10.13381533919000077, 5.176445833090999926, -8.189798585019000043 ) ) ;
#61336=CARTESIAN_POINT ( 'NONE',  ( 8.440795537699267825, 5.100000000000000533, 6.662590550601105832 ) ) ;
#61340=CARTESIAN_POINT ( 'NONE',  ( 10.41025778040999938, 4.690688562647999937, -6.142866736126999960 ) ) ;
#61346=CARTESIAN_POINT ( 'NONE',  ( 7.838687487314834890, 4.995567223853333516, 6.525491811874558401 ) ) ;
#61347=B_SPLINE_CURVE_WITH_KNOTS ( 'NONE', 3,
 ( #39877, #13315, #40218, #61535, #40548, #35318, #13650, #46145, #67451, #41924, #63584, #5203, #17336, #69174, #38665, #15360, #21284, #58342 ),
 .UNSPECIFIED., .F., .F.,
 ( 4, 2, 2, 2, 2, 2, 2, 2, 4 ),
 ( 0.000000000000000000, 0.1249999999999999445, 0.2499999999999998890, 0.3749999999999998335, 0.4999999999999997780, 0.6249999999999997780, 0.7499999999999998890, 0.8749999999999998890, 1.000000000000000000 ),
 .UNSPECIFIED. ) ;
#61350=CARTESIAN_POINT ( 'NONE',  ( 8.789679719592999874, 4.162493982103000256, -5.775210092227999858 ) ) ;
#61351=CARTESIAN_POINT ( 'NONE',  ( 10.57314899745999881, 5.167567567567999731, -6.822293592207000934 ) ) ;
#61363=CARTESIAN_POINT ( 'NONE',  ( 8.573148997459998810, 5.167567567567999731, -6.822293592207000934 ) ) ;
#61369=CARTESIAN_POINT ( 'NONE',  ( 9.924988015501618577, 5.349815781279066762, 7.500001845592777272 ) ) ;
#61376=CARTESIAN_POINT ( 'NONE',  ( 8.205992358813000820, 3.399999999999999911, 6.138278517057000450 ) ) ;
#61377=CARTESIAN_POINT ( 'NONE',  ( 2.070791208532999583, 2.973679562143999533, -2.014976181196999949 ) ) ;
#61386=CARTESIAN_POINT ( 'NONE',  ( 7.291685841229000431, 2.836301549691000012, -8.273864296493000481 ) ) ;
#61390=VERTEX_POINT ( 'NONE', #43745 ) ;
#61397=EDGE_LOOP ( 'NONE', ( #59759, #43695, #44794, #65391 ) ) ;
#61398=CARTESIAN_POINT ( 'NONE',  ( 9.140753410162000492, 5.100000000000000533, 6.175944241622000064 ) ) ;
#61399=EDGE_CURVE ( 'NONE', #48015, #43460, #16131, .T. ) ;
#61416=CARTESIAN_POINT ( 'NONE',  ( 6.944122165046020534, 4.487799988764965775, -9.291988751869498131 ) ) ;
#61423=ORIENTED_EDGE ( 'NONE', *, *, #62643, .T. ) ;
#61427=CARTESIAN_POINT ( 'NONE',  ( 8.731095280410999138, 2.469361196073999842, -7.826019481986000059 ) ) ;
#61428=CARTESIAN_POINT ( 'NONE',  ( 3.131913175787999659, -2.986881754985999837, -1.580751239308999967 ) ) ;
#61434=CARTESIAN_POINT ( 'NONE',  ( 10.37873747135000002, 4.882725050998000249, 6.350806206758999650 ) ) ;
#61437=CARTESIAN_POINT ( 'NONE',  ( 9.414312736919001168, 3.941041961981000430, 5.878350450964999752 ) ) ;
#61438=CARTESIAN_POINT ( 'NONE',  ( 9.084332157886041870, 4.271970605703780066, 8.830901773243875041 ) ) ;
#61440=DIRECTION ( 'NONE',  ( -1.000000000000000000, 0.000000000000000000, 0.000000000000000000 ) ) ;
#61445=CARTESIAN_POINT ( 'NONE',  ( 8.061933748689000367, 4.603465626214999773, -6.221450782568999749 ) ) ;
#61447=CARTESIAN_POINT ( 'NONE',  ( 11.29596084123000210, 2.828872990872000059, -8.191118698770999629 ) ) ;
#61451=DIRECTION ( 'NONE',  ( -1.000000000000000000, -5.329070518030000242E-14, 1.243449787539999965E-13 ) ) ;
#61452=CARTESIAN_POINT ( 'NONE',  ( 10.37835931248476662, 5.126777126150539488, 6.752018918811991455 ) ) ;
#61454=CARTESIAN_POINT ( 'NONE',  ( 8.705989158774000813, 2.542862824481000317, 7.419808961972999661 ) ) ;
#61456=CARTESIAN_POINT ( 'NONE',  ( 9.044210841233001119, 2.773858540272000184, -8.951250717848999727 ) ) ;
#61469=VECTOR ( 'NONE', #25166, 1000.000000000000114 ) ;
#61478=CARTESIAN_POINT ( 'NONE',  ( 10.67500447327519097, 2.650284540010591439, 7.500001951671590561 ) ) ;
#61481=CARTESIAN_POINT ( 'NONE',  ( 8.903895280414001689, 3.867331042029999999, -9.227339949050001877 ) ) ;
#61490=CARTESIAN_POINT ( 'NONE',  ( 7.633428764671157829, 3.449330106466649060, 8.750263298858765637 ) ) ;
#61499=CARTESIAN_POINT ( 'NONE',  ( 9.866200267984439165, 5.673313433347823675, -8.064784397742297273 ) ) ;
#61507=EDGE_CURVE ( 'NONE', #29684, #52776, #15112, .T. ) ;
#61510=CARTESIAN_POINT ( 'NONE',  ( 8.048510972020503473, 4.829207235971519907, 8.579008051763146625 ) ) ;
#61511=CARTESIAN_POINT ( 'NONE',  ( 10.64447074117000014, 5.073827170570999634, -8.340679549192000053 ) ) ;
#61516=CARTESIAN_POINT ( 'NONE',  ( 10.46432998405999903, 2.042755206296999582, 7.723699495214000343 ) ) ;
#61517=CIRCLE ( 'NONE', #46990, 2.100000000000000977 ) ;
#61522=CARTESIAN_POINT ( 'NONE',  ( 9.444315208305999576, 2.927258006877999641, 8.897018628538001295 ) ) ;
#61526=CARTESIAN_POINT ( 'NONE',  ( 7.968176658772001097, 2.280568568659000483, 6.510284508622999233 ) ) ;
#61527=CARTESIAN_POINT ( 'NONE',  ( 10.43579914648999996, 2.587602126999999808, 6.390037244031000263 ) ) ;
#61535=CARTESIAN_POINT ( 'NONE',  ( 3.292477888231665872, -3.061624279823272232, -1.756338733055054835 ) ) ;
#61539=CARTESIAN_POINT ( 'NONE',  ( 1.391291019826000008, -0.3804460121770000258, -3.739470302966999782 ) ) ;
#61549=CARTESIAN_POINT ( 'NONE',  ( 8.341920280410999311, 5.601795057054999916, 7.176148573050999957 ) ) ;
#61554=CARTESIAN_POINT ( 'NONE',  ( 1.028018509565999938, -2.208354302538000358, -2.618776384398000090 ) ) ;
#61556=VERTEX_POINT ( 'NONE', #23097 ) ;
#61559=CARTESIAN_POINT ( 'NONE',  ( 9.869051220224999810, 5.575171928796999410, 7.724300137354000562 ) ) ;
#61563=DIRECTION ( 'NONE',  ( 0.000000000000000000, 0.9693731749023103417, -0.2455924424322025734 ) ) ;
#61564=FACE_OUTER_BOUND ( 'NONE', #44734, .T. ) ;
#61569=CARTESIAN_POINT ( 'NONE',  ( 7.907666719952700873, 2.506162197551407012, 8.397413729663252724 ) ) ;
#61573=ORIENTED_EDGE ( 'NONE', *, *, #52955, .F. ) ;
#61578=CARTESIAN_POINT ( 'NONE',  ( 10.03490996941999924, 5.615906393494999982, 7.351455918368999143 ) ) ;
#61579=CARTESIAN_POINT ( 'NONE',  ( 9.701722306758000514, 4.253749110891999585, -8.839930742927998963 ) ) ;
#61587=EDGE_CURVE ( 'NONE', #4653, #20297, #18208, .T. ) ;
#61589=CARTESIAN_POINT ( 'NONE',  ( 6.899999691988000450, -12.43893545635000031, -2.828937028792000152 ) ) ;
#61595=ORIENTED_EDGE ( 'NONE', *, *, #34469, .F. ) ;
#61599=CARTESIAN_POINT ( 'NONE',  ( 3.500000000000000000, 0.000000000000000000, 0.000000000000000000 ) ) ;
#61602=CARTESIAN_POINT ( 'NONE',  ( 8.379867906096000851, 2.923743482149999906, 6.439439799146000176 ) ) ;
#61604=CARTESIAN_POINT ( 'NONE',  ( -0.06014317643898999671, -2.101315454803999838, -2.652019770012000066 ) ) ;
#61605=VECTOR ( 'NONE', #1024, 1000.000000000000114 ) ;
#61606=DIRECTION ( 'NONE',  ( 1.000000000000000000, 0.000000000000000000, 0.000000000000000000 ) ) ;
#61626=LINE ( 'NONE', #60942, #57606 ) ;
#61630=CARTESIAN_POINT ( 'NONE',  ( 8.620740978634000129, 4.599999999999999645, 5.898823289756999877 ) ) ;
#61635=CARTESIAN_POINT ( 'NONE',  ( 7.726096713366001900, 2.834812733921999062, 6.825604963486997079 ) ) ;
#61637=CARTESIAN_POINT ( 'NONE',  ( 9.023148997459999876, 5.167567567567999731, -6.822293592207000934 ) ) ;
#61638=VERTEX_POINT ( 'NONE', #41247 ) ;
#61642=EDGE_CURVE ( 'NONE', #16931, #34575, #65396, .T. ) ;
#61643=DIRECTION ( 'NONE',  ( 1.000000000000000000, 0.000000000000000000, 0.000000000000000000 ) ) ;
#61644=EDGE_CURVE ( 'NONE', #19777, #39380, #22526, .T. ) ;
#61645=CARTESIAN_POINT ( 'NONE',  ( 2.335432296257125451, -1.713969392196469377, -3.070236115647940078 ) ) ;
#61646=CARTESIAN_POINT ( 'NONE',  ( 9.170239158775000732, 4.769103072373000352, -8.666849124598000387 ) ) ;
#61648=ORIENTED_EDGE ( 'NONE', *, *, #30234, .F. ) ;
#61650=ADVANCED_FACE ( 'NONE', ( #47531 ), #27114, .T. ) ;
#61651=CARTESIAN_POINT ( 'NONE',  ( 3.999971066382000284, 2.149963194831999935, 0.000000000000000000 ) ) ;
#61656=CARTESIAN_POINT ( 'NONE',  ( 9.749220280410998640, 5.656948148960999845, -6.994239053114000626 ) ) ;
#61662=CARTESIAN_POINT ( 'NONE',  ( 7.748782164940981154, 3.848159210716703971, -8.857024363427377978 ) ) ;
#61664=CARTESIAN_POINT ( 'NONE',  ( 8.649364158774000444, 3.038023536984999939, -5.861661709981000001 ) ) ;
#61666=VECTOR ( 'NONE', #15430, 1000.000000000000114 ) ;
#61667=CARTESIAN_POINT ( 'NONE',  ( 10.18512471524999974, 5.526143977810000329, -7.556025088797999167 ) ) ;
#61672=AXIS2_PLACEMENT_3D ( 'NONE', #60829, #2108, #28325 ) ;
#61674=LINE ( 'NONE', #56433, #36910 ) ;
#61682=B_SPLINE_CURVE_WITH_KNOTS ( 'NONE', 3,
 ( #44910, #17992, #12397, #45599 ),
 .UNSPECIFIED., .F., .F.,
 ( 4, 4 ),
 ( 0.000000000000000000, 1.000000000000000000 ),
 .UNSPECIFIED. ) ;
#61688=CARTESIAN_POINT ( 'NONE',  ( 10.07367028041000090, 4.905765359186999852, -8.776126235875999271 ) ) ;
#61689=CARTESIAN_POINT ( 'NONE',  ( 9.272336283620196795, 5.086552246568830427, 8.869404539491238637 ) ) ;
#61695=CARTESIAN_POINT ( 'NONE',  ( 8.936935970859920531, 2.275488567576319010, 7.787316285718978826 ) ) ;
#61702=EDGE_CURVE ( 'NONE', #62483, #22269, #16704, .T. ) ;
#61707=CARTESIAN_POINT ( 'NONE',  ( 9.972410841228999345, 4.357364160690000432, -9.282962013144999247 ) ) ;
#61711=CARTESIAN_POINT ( 'NONE',  ( 0.3011869175822131095, -0.4312571925403625994, 3.301166135663313295 ) ) ;
#61717=CARTESIAN_POINT ( 'NONE',  ( 9.026926658770998202, 4.852728889087999598, 8.683917172082999514 ) ) ;
#61721=CARTESIAN_POINT ( 'NONE',  ( 10.94020963518341460, 9.314146368041843260, 6.233663971910207380 ) ) ;
#61722=CARTESIAN_POINT ( 'NONE',  ( 10.63789391302369580, 4.829717262113647713, -8.579596796882025700 ) ) ;
#61723=CARTESIAN_POINT ( 'NONE',  ( 1.584306799206999905, 1.762666431298138825, 3.058252359239908014 ) ) ;
#61726=EDGE_CURVE ( 'NONE', #5681, #34720, #44226, .T. ) ;
#61732=VERTEX_POINT ( 'NONE', #6324 ) ;
#61733=CARTESIAN_POINT ( 'NONE',  ( 10.93864331818477176, 9.341686757170215571, -6.213842809792356370 ) ) ;
#61735=DIRECTION ( 'NONE',  ( -1.000000000000000000, 0.000000000000000000, 0.000000000000000000 ) ) ;
#61746=VERTEX_POINT ( 'NONE', #7031 ) ;
#61751=CARTESIAN_POINT ( 'NONE',  ( 3.500000000000000000, 3.126788493178761730, 1.462720483632788060 ) ) ;
#61759=CARTESIAN_POINT ( 'NONE',  ( 10.53734212242000012, 2.992816679959000137, 8.731689474572998932 ) ) ;
#61762=CARTESIAN_POINT ( 'NONE',  ( 8.441604719589999917, 5.473983809665999622, -8.180077404516000072 ) ) ;
#61763=CARTESIAN_POINT ( 'NONE',  ( 3.145426443515999981, 0.1831839624298000069, 3.703521834897999909 ) ) ;
#61768=VERTEX_POINT ( 'NONE', #17528 ) ;
#61770=CARTESIAN_POINT ( 'NONE',  ( 10.19255830160000009, 2.560287027313000063, 7.664549200117999561 ) ) ;
#61771=LINE ( 'NONE', #55155, #42706 ) ;
#61774=CARTESIAN_POINT ( 'NONE',  ( 9.194604681486000075, 5.157771204918000230, 8.637848577075999401 ) ) ;
#61783=DIRECTION ( 'NONE',  ( -0.7071067811859638175, 0.6115524522396686979, -0.3549698552841819010 ) ) ;
#61791=CARTESIAN_POINT ( 'NONE',  ( 5.000015393671500163, -2.571712834666313134E-16, -2.099962892531002545 ) ) ;
#61793=ORIENTED_EDGE ( 'NONE', *, *, #36784, .F. ) ;
#61794=CIRCLE ( 'NONE', #9283, 1.900000000000000577 ) ;
#61795=CARTESIAN_POINT ( 'NONE',  ( 7.058509992104999853, 4.314040636970999820, 8.819134391732999845 ) ) ;
#61799=ORIENTED_EDGE ( 'NONE', *, *, #45540, .F. ) ;
#61800=CARTESIAN_POINT ( 'NONE',  ( 1.540556799207333238, 3.500000000000000888, -0.4581489286485045387 ) ) ;
#61804=LINE ( 'NONE', #7986, #64489 ) ;
#61809=CIRCLE ( 'NONE', #24931, 12.39999890530000037 ) ;
#61815=VERTEX_POINT ( 'NONE', #43754 ) ;
#61820=CARTESIAN_POINT ( 'NONE',  ( 9.898395280408998076, 3.987760651117999711, -9.123263301387000368 ) ) ;
#61825=CARTESIAN_POINT ( 'NONE',  ( 8.592635841230999105, 3.856772556595000179, 5.521246073317000125 ) ) ;
#61826=VERTEX_POINT ( 'NONE', #16819 ) ;
#61833=EDGE_CURVE ( 'NONE', #12035, #60646, #58667, .T. ) ;
#61844=ORIENTED_EDGE ( 'NONE', *, *, #21000, .F. ) ;
#61849=CARTESIAN_POINT ( 'NONE',  ( 10.42081182385000027, 2.488452444780999695, -7.717895019962999648 ) ) ;
#61852=DIRECTION ( 'NONE',  ( 0.8660254037844289376, 0.000000000000000000, 0.5000000000000169864 ) ) ;
#61853=CARTESIAN_POINT ( 'NONE',  ( 10.59344747867000081, 5.297752619853000944, 8.474195539311001113 ) ) ;
#61858=CARTESIAN_POINT ( 'NONE',  ( 9.590596677641999079, 2.445964682955000136, 7.841184989245001624 ) ) ;
#61864=CARTESIAN_POINT ( 'NONE',  ( 7.673642219589999591, 4.696238830159999544, 5.830273622963999536 ) ) ;
#61865=CARTESIAN_POINT ( 'NONE',  ( 10.03490996941999924, 5.615906393494999982, 7.351455918368999143 ) ) ;
#61869=CARTESIAN_POINT ( 'NONE',  ( 10.19741084123000086, 4.262870449202000422, -8.811513791423999820 ) ) ;
#61870=B_SPLINE_CURVE_WITH_KNOTS ( 'NONE', 3,
 ( #63548, #59337, #21928, #15997 ),
 .UNSPECIFIED., .F., .F.,
 ( 4, 4 ),
 ( 0.000000000000000000, 1.000000000000000000 ),
 .UNSPECIFIED. ) ;
#61871=CARTESIAN_POINT ( 'NONE',  ( -0.000000000000000000, 2.824612379753681513, 0.7585797238568994239 ) ) ;
#61881=CARTESIAN_POINT ( 'NONE',  ( 1.200563222062999813, -2.255103325128000158, 3.007138987545999953 ) ) ;
#61882=DIRECTION ( 'NONE',  ( 0.000000000000000000, 0.000000000000000000, 1.000000000000000000 ) ) ;
#61884=CARTESIAN_POINT ( 'NONE',  ( 5.440293001548999641, -12.88483958404999896, -2.133988467673999967 ) ) ;
#61886=CARTESIAN_POINT ( 'NONE',  ( 10.23809632363000155, 2.752447932331000047, 6.820051270595000048 ) ) ;
#61888=CARTESIAN_POINT ( 'NONE',  ( 8.476023596135332738, 2.899999999999999911, -6.562910362702667477 ) ) ;
#61892=CARTESIAN_POINT ( 'NONE',  ( 7.930392219590000735, 3.164805384346000228, 9.104735843897000080 ) ) ;
#61896=AXIS2_PLACEMENT_3D ( 'NONE', #5792, #32041, #53356 ) ;
#61897=FACE_OUTER_BOUND ( 'NONE', #35181, .T. ) ;
#61898=CARTESIAN_POINT ( 'NONE',  ( 1.981657498383000204, -3.284887521161000024, -0.9717780471415999877 ) ) ;
#61903=CARTESIAN_POINT ( 'NONE',  ( 9.555697025339000561, 2.440752375194999768, 6.680879724048000234 ) ) ;
#61905=CARTESIAN_POINT ( 'NONE',  ( 7.110192589515543560, 5.350273814425614560, -7.415195716910538692 ) ) ;
#61907=FACE_OUTER_BOUND ( 'NONE', #34830, .T. ) ;
#61910=B_SPLINE_CURVE_WITH_KNOTS ( 'NONE', 3,
 ( #16973, #17685, #59633, #54386, #28524, #49836, #5795, #56808, #35147, #39350, #8905, #39697, #7523, #28879 ),
 .UNSPECIFIED., .F., .F.,
 ( 4, 2, 2, 2, 2, 2, 4 ),
 ( 0.000000000000000000, 0.2499999999999995559, 0.3749999999999995559, 0.4999999999999995559, 0.6249999999999995559, 0.7499999999999995559, 1.000000000000000000 ),
 .UNSPECIFIED. ) ;
#61911=CARTESIAN_POINT ( 'NONE',  ( 7.765771671202282178, 5.188776208877133200, 8.801183839191253355 ) ) ;
#61921=CARTESIAN_POINT ( 'NONE',  ( 10.09696969267000100, 5.253376380222999131, 8.530663119653999260 ) ) ;
#61922=DIRECTION ( 'NONE',  ( -1.000000000000000000, 0.000000000000000000, 0.000000000000000000 ) ) ;
#61930=EDGE_LOOP ( 'NONE', ( #63593, #23447, #4794, #4791, #39802 ) ) ;
#61939=FACE_OUTER_BOUND ( 'NONE', #12297, .T. ) ;
#61949=B_SPLINE_SURFACE_WITH_KNOTS ( 'NONE', 3, 3, ( 
 ( #63396, #48016, #32296, #15517 ),
 ( #11291, #54285, #58501, #21104 ),
 ( #37181, #47334, #32631, #10604 ),
 ( #68638, #59536, #20758, #43114 ),
 ( #58845, #10954, #42429, #42087 ),
 ( #811, #15850, #5702, #10264 ) ),
 .UNSPECIFIED., .F., .F., .F.,
 ( 4, 1, 1, 4 ),
 ( 4, 4 ),
 ( 0.8990819262081000129, 0.9285714285714000704, 1.000000000000000000, 1.007603470489000008 ),
 ( -0.1835655481301000091, 1.183565547943999929 ),
 .UNSPECIFIED. ) ;
#61952=B_SPLINE_CURVE_WITH_KNOTS ( 'NONE', 3,
 ( #25132, #62193, #45438, #52035, #67089, #4138, #36310, #51362, #9729, #46465, #19892, #31080 ),
 .UNSPECIFIED., .F., .F.,
 ( 4, 2, 2, 2, 2, 4 ),
 ( 0.000000000000000000, 0.2500000000000149880, 0.3750000000000213163, 0.4375000000000214828, 0.5000000000000216493, 1.000000000000000000 ),
 .UNSPECIFIED. ) ;
#61954=CARTESIAN_POINT ( 'NONE',  ( 8.122851870746000458, 2.921728982776850003, 8.328193042680714697 ) ) ;
#61958=CARTESIAN_POINT ( 'NONE',  ( 8.335548758400999958, 2.897657723982001166, -6.653323589456997311 ) ) ;
#61961=CARTESIAN_POINT ( 'NONE',  ( 11.02418915877000138, 2.407889430138999920, -8.439554272735000140 ) ) ;
#61966=EDGE_LOOP ( 'NONE', ( #63541, #20409, #7491, #67859, #30562, #50113 ) ) ;
#61967=ADVANCED_BREP_SHAPE_REPRESENTATION ( '', ( #52802, #9676 ), #67766 ) ;
#61975=CARTESIAN_POINT ( 'NONE',  ( 6.983066493190000834, -12.13287627744000119, 3.076835272540999977 ) ) ;
#61984=DIRECTION ( 'NONE',  ( 0.000000000000000000, 0.000000000000000000, -1.000000000000000000 ) ) ;
#61988=ORIENTED_EDGE ( 'NONE', *, *, #61399, .F. ) ;
#61990=DIRECTION ( 'NONE',  ( 0.000000000000000000, 0.000000000000000000, -1.000000000000000000 ) ) ;
#61992=DIRECTION ( 'NONE',  ( 0.000000000000000000, -1.000000000000000000, 0.000000000000000000 ) ) ;
#61994=CARTESIAN_POINT ( 'NONE',  ( 8.523814158775000038, 4.920236664407999783, -6.448229650796999834 ) ) ;
#61997=CARTESIAN_POINT ( 'NONE',  ( 3.999971066382000284, -2.149963194831999935, 0.000000000000000000 ) ) ;
#62000=CARTESIAN_POINT ( 'NONE',  ( 5.500000000000000000, 13.87069231928999891, 4.225386915259999654 ) ) ;
#62002=CARTESIAN_POINT ( 'NONE',  ( 8.962479719595000560, 2.546924812613000189, -6.918870225297999887 ) ) ;
#62006=DIRECTION ( 'NONE',  ( 0.000000000000000000, 0.000000000000000000, -1.000000000000000000 ) ) ;
#62009=CARTESIAN_POINT ( 'NONE',  ( 3.500000000000000000, 1.113524292603000010, -3.231029921506000324 ) ) ;
#62011=CARTESIAN_POINT ( 'NONE',  ( 9.386379719595000282, 5.673443217382001080, -7.051790060464000476 ) ) ;
#62013=CARTESIAN_POINT ( 'NONE',  ( 9.856715971886000460, 4.814120192353000149, -8.929574926876000518 ) ) ;
#62018=CARTESIAN_POINT ( 'NONE',  ( 9.314928906318884927, 2.650140463285438397, -7.499996151983930659 ) ) ;
#62020=CARTESIAN_POINT ( 'NONE',  ( 8.611367346726332528, 2.905107952767239876, 6.370216469110514979 ) ) ;
#62021=VERTEX_POINT ( 'NONE', #65929 ) ;
#62022=CARTESIAN_POINT ( 'NONE',  ( 10.31905590579000176, 2.899999999999999911, -6.571291218949999902 ) ) ;
#62023=CARTESIAN_POINT ( 'NONE',  ( 10.42512334122999995, 3.371064118627999928, -6.294343971198999910 ) ) ;
#62030=ORIENTED_EDGE ( 'NONE', *, *, #46345, .T. ) ;
#62031=ORIENTED_EDGE ( 'NONE', *, *, #28320, .F. ) ;
#62032=CARTESIAN_POINT ( 'NONE',  ( 8.830545280412000153, 3.207599814920999659, -6.150466394809999571 ) ) ;
#62033=DIRECTION ( 'NONE',  ( 0.000000000000000000, -0.8734457522908377625, -0.4869214698543208875 ) ) ;
#62034=CARTESIAN_POINT ( 'NONE',  ( 10.43353630809279942, 2.899999999999999911, -6.665341197380437066 ) ) ;
#62042=CARTESIAN_POINT ( 'NONE',  ( 10.90000000000000036, 5.100000000000000533, -6.436740704805999691 ) ) ;
#62048=CARTESIAN_POINT ( 'NONE',  ( 7.924408822415808018, 4.759987200975432486, 6.322386952704928120 ) ) ;
#62051=CARTESIAN_POINT ( 'NONE',  ( 9.690635841230999858, 2.927176851028000293, -5.932007155957999878 ) ) ;
#62052=B_SPLINE_CURVE_WITH_KNOTS ( 'NONE', 3,
 ( #39633, #23545, #30184, #18990 ),
 .UNSPECIFIED., .F., .F.,
 ( 4, 4 ),
 ( 0.000000000000000000, 1.000000000000000000 ),
 .UNSPECIFIED. ) ;
#62053=CARTESIAN_POINT ( 'NONE',  ( 7.990070311382211798, 3.072494164717982201, -6.390217723318725618 ) ) ;
#62056=CARTESIAN_POINT ( 'NONE',  ( 4.000000000000000000, 0.000000000000000000, 0.000000000000000000 ) ) ;
#62057=CARTESIAN_POINT ( 'NONE',  ( 3.623628218870999618, 1.587559571644000078, -2.882103889560999832 ) ) ;
#62063=CARTESIAN_POINT ( 'NONE',  ( 8.641801658773999861, 2.933833973450999721, 8.496479443567000800 ) ) ;
#62064=DIRECTION ( 'NONE',  ( 0.7071193432624600650, 0.7070942188874600465, 1.398349818569919760E-09 ) ) ;
#62065=ORIENTED_EDGE ( 'NONE', *, *, #41609, .T. ) ;
#62067=CARTESIAN_POINT ( 'NONE',  ( 10.98768472638000127, 7.408460511344000743, 6.159405790617999976 ) ) ;
#62068=CARTESIAN_POINT ( 'NONE',  ( 10.92594639162300041, 5.087027437888981929, 4.995424258306049303 ) ) ;
#62069=CARTESIAN_POINT ( 'NONE',  ( 7.844613792771893301, 2.729327499216226194, -7.000868400899764588 ) ) ;
#62074=CARTESIAN_POINT ( 'NONE',  ( 9.205773468340201049, 5.100000000000000533, -6.304440313902172299 ) ) ;
#62078=CARTESIAN_POINT ( 'NONE',  ( 8.624544496487235534, 2.406435347409131786, -6.761471569661993364 ) ) ;
#62080=CARTESIAN_POINT ( 'NONE',  ( 8.178354719590000599, 5.563172860439999923, -7.424303164651000486 ) ) ;
#62084=CARTESIAN_POINT ( 'NONE',  ( 2.198890132540458175, -2.798833948393640192, 2.150913519912191152 ) ) ;
#62089=VERTEX_POINT ( 'NONE', #39375 ) ;
#62091=AXIS2_PLACEMENT_3D ( 'NONE', #42481, #12040, #6095 ) ;
#62095=CARTESIAN_POINT ( 'NONE',  ( 3.146806799210916772, -0.9161175952574931447, 3.408904368339100710 ) ) ;
#62102=CARTESIAN_POINT ( 'NONE',  ( 10.87148757351999961, 5.567567343464999929, 7.772413227960999649 ) ) ;
#62105=CARTESIAN_POINT ( 'NONE',  ( 8.458179719589999479, 5.332332124071999857, -8.487089944253000340 ) ) ;
#62107=CARTESIAN_POINT ( 'NONE',  ( 3.480762151334999555, 3.165347270645999966, -1.931374428620000083 ) ) ;
#62109=LINE ( 'NONE', #68035, #404 ) ;
#62116=DIRECTION ( 'NONE',  ( -0.5000000000000169864, 0.000000000000000000, -0.8660254037844288266 ) ) ;
#62117=CARTESIAN_POINT ( 'NONE',  ( 9.939321360490000146, 2.638097915594000309, 6.328629954376999933 ) ) ;
#62133=CARTESIAN_POINT ( 'NONE',  ( 7.871551658771999804, 4.780986922229000236, 6.267222470044999660 ) ) ;
#62138=CARTESIAN_POINT ( 'NONE',  ( 10.44812028041000040, 5.235600787608000850, -6.609970743661000903 ) ) ;
#62146=CARTESIAN_POINT ( 'NONE',  ( 8.455992358812000731, 3.399999999999999911, 6.571291218949999902 ) ) ;
#62147=VERTEX_POINT ( 'NONE', #11634 ) ;
#62149=CARTESIAN_POINT ( 'NONE',  ( 8.014414158768000007, 2.494419548310999879, -8.658783402411998509 ) ) ;
#62160=CARTESIAN_POINT ( 'NONE',  ( 2.436390132543208686, 0.4581489286485155299, -3.499999999999999556 ) ) ;
#62162=CARTESIAN_POINT ( 'NONE',  ( 10.20000099824999928, 12.50000000000000000, 0.000000000000000000 ) ) ;
#62165=CARTESIAN_POINT ( 'NONE',  ( 8.656823341231000057, 5.329437560656000272, 6.027391099688998999 ) ) ;
#62167=CARTESIAN_POINT ( 'NONE',  ( 7.474999999999999645, 5.349999999999999645, 7.500000000000000000 ) ) ;
#62170=ORIENTED_EDGE ( 'NONE', *, *, #61644, .F. ) ;
#62175=CARTESIAN_POINT ( 'NONE',  ( 2.457156007037999856, 3.012404793772358591, -1.845954168039164678 ) ) ;
#62183=DIRECTION ( 'NONE',  ( 0.000000000000000000, 1.000000000000000000, 0.000000000000000000 ) ) ;
#62187=DIRECTION ( 'NONE',  ( -1.000000000000000000, 0.000000000000000000, 0.000000000000000000 ) ) ;
#62191=CARTESIAN_POINT ( 'NONE',  ( 10.38153063908000107, 2.772139908660999907, -8.408082511401000048 ) ) ;
#62192=B_SPLINE_CURVE_WITH_KNOTS ( 'NONE', 3,
 ( #5077, #57526, #14208, #20132, #62767 ),
 .UNSPECIFIED., .F., .F.,
 ( 4, 1, 4 ),
 ( 0.000000000000000000, 0.5000000000000000000, 1.000000000000000000 ),
 .UNSPECIFIED. ) ;
#62193=CARTESIAN_POINT ( 'NONE',  ( 8.731512351913153225, 5.100000000000000533, 6.372362022305052776 ) ) ;
#62195=DIRECTION ( 'NONE',  ( 0.000000000000000000, 1.000000000000000000, 0.000000000000000000 ) ) ;
#62196=CARTESIAN_POINT ( 'NONE',  ( 10.99433665574000152, 3.697618584609999814, 5.729302299903000772 ) ) ;
#62201=CARTESIAN_POINT ( 'NONE',  ( 10.96207813434000045, 5.399835028078000754, 7.743264559064000352 ) ) ;
#62203=CARTESIAN_POINT ( 'NONE',  ( 10.11453584122999949, 5.322769172805999816, -7.951018786192998178 ) ) ;
#62207=CARTESIAN_POINT ( 'NONE',  ( 7.609454719589999527, 3.276311362504999991, 5.841989464160999290 ) ) ;
#62209=CARTESIAN_POINT ( 'NONE',  ( 9.724611353170001138, 2.928305163963000446, 8.718478150869000132 ) ) ;
#62213=CARTESIAN_POINT ( 'NONE',  ( 9.237204719595000668, 3.071719032003000116, -6.037263251225000182 ) ) ;
#62214=CYLINDRICAL_SURFACE ( 'NONE', #4506, 1.350000000000000533 ) ;
#62215=CARTESIAN_POINT ( 'NONE',  ( 9.153455117183014522, 2.649843614532819469, 7.852866721134448724 ) ) ;
#62221=CARTESIAN_POINT ( 'NONE',  ( 1.968247751176999794, 3.260257002997999809, 1.508168810892000167 ) ) ;
#62224=CARTESIAN_POINT ( 'NONE',  ( 9.468589158772999781, 4.034680274230000308, -6.102912434217000026 ) ) ;
#62230=DIRECTION ( 'NONE',  ( -0.7071067759742961645, 0.7071067863987962054, 5.966942998097971758E-08 ) ) ;
#62234=CARTESIAN_POINT ( 'NONE',  ( 7.956795280408998750, 4.524487726177000013, 9.047753146378999745 ) ) ;
#62236=CARTESIAN_POINT ( 'NONE',  ( 10.98435104515999861, 5.105444214897000066, 4.879787924579000347 ) ) ;
#62239=DIRECTION ( 'NONE',  ( 0.8843050097021416533, -0.1786785991673574547, -0.4313682974156609062 ) ) ;
#62240=CARTESIAN_POINT ( 'NONE',  ( 1.318883544274000119, -2.924745949230000086, 2.085595834630999956 ) ) ;
#62242=CARTESIAN_POINT ( 'NONE',  ( 0.7716437780931045820, 3.201127686947116580, -0.2025159996193092726 ) ) ;
#62245=CARTESIAN_POINT ( 'NONE',  ( 10.37026939687000038, 5.571553923009999743, 7.748385725654999945 ) ) ;
#62251=CARTESIAN_POINT ( 'NONE',  ( 8.246455660830299905, 5.453956472524233767, 8.461650011249977510 ) ) ;
#62255=DIRECTION ( 'NONE',  ( 0.5000000000000169864, 0.000000000000000000, -0.8660254037844288266 ) ) ;
#62259=CARTESIAN_POINT ( 'NONE',  ( 8.486008579191000933, 3.399999999999999911, 5.976611076844000614 ) ) ;
#62261=CARTESIAN_POINT ( 'NONE',  ( 9.476372460169001144, 5.098395626600999542, 6.305536056092000408 ) ) ;
#62262=CARTESIAN_POINT ( 'NONE',  ( 10.77434248675000106, 4.612886656332999991, -8.898793847069001117 ) ) ;
#62267=AXIS2_PLACEMENT_3D ( 'NONE', #25980, #27969, #25635 ) ;
#62271=EDGE_CURVE ( 'NONE', #27423, #63357, #49390, .T. ) ;
#62277=LINE ( 'NONE', #14394, #24728 ) ;
#62282=EDGE_LOOP ( 'NONE', ( #42560, #11859, #35146, #943 ) ) ;
#62292=B_SPLINE_CURVE_WITH_KNOTS ( 'NONE', 3,
 ( #35272, #35617, #14626, #5160 ),
 .UNSPECIFIED., .F., .F.,
 ( 4, 4 ),
 ( 0.8745867815654175814, 1.000000000000000000 ),
 .UNSPECIFIED. ) ;
#62298=FACE_OUTER_BOUND ( 'NONE', #62282, .T. ) ;
#62300=CARTESIAN_POINT ( 'NONE',  ( 10.97499895057999986, -2.398081733189999864E-14, -12.37499919541000004 ) ) ;
#62301=CARTESIAN_POINT ( 'NONE',  ( 10.38052665877000003, 5.283793195606000026, -8.830196380017000024 ) ) ;
#62304=DIRECTION ( 'NONE',  ( 0.000000000000000000, 1.000000000000000000, 0.000000000000000000 ) ) ;
#62309=CARTESIAN_POINT ( 'NONE',  ( 9.334658571019252449, 5.771500264757192689, -7.375358915183060304 ) ) ;
#62312=AXIS2_PLACEMENT_3D ( 'NONE', #66373, #39822, #61142 ) ;
#62320=CARTESIAN_POINT ( 'NONE',  ( 6.649999999999999467, 5.221516520829000640, -8.074802043613001246 ) ) ;
#62332=CARTESIAN_POINT ( 'NONE',  ( 11.10000000432000000, 9.172263358062000549, 6.560374562178000524 ) ) ;
#62334=CARTESIAN_POINT ( 'NONE',  ( 9.319414158774000256, 2.656512020013999997, -7.884832994446999699 ) ) ;
#62342=CARTESIAN_POINT ( 'NONE',  ( 9.442010841233001273, 5.045571591548999812, -9.086294919530001124 ) ) ;
#62345=CARTESIAN_POINT ( 'NONE',  ( 8.970944094206998898, 5.100000000000000533, 6.571291218949999902 ) ) ;
#62351=CARTESIAN_POINT ( 'NONE',  ( 9.874770280412001000, 4.038835765825999680, -5.935509327774999733 ) ) ;
#62353=CARTESIAN_POINT ( 'NONE',  ( 10.71983649979000042, 3.571741329336999726, -5.696148467328000287 ) ) ;
#62361=CARTESIAN_POINT ( 'NONE',  ( 8.558656770618505050, 3.294700107201707695, 5.942504245731808687 ) ) ;
#62362=EDGE_LOOP ( 'NONE', ( #15481, #10462, #52087, #48104, #13449 ) ) ;
#62364=CARTESIAN_POINT ( 'NONE',  ( 11.25809834123000108, 3.275514549383000240, -8.650774600386998969 ) ) ;
#62365=EDGE_CURVE ( 'NONE', #21989, #56231, #61272, .T. ) ;
#62375=CARTESIAN_POINT ( 'NONE',  ( 9.766460841231999979, 3.135494838036999798, -8.598037907310999373 ) ) ;
#62377=CARTESIAN_POINT ( 'NONE',  ( 1.165556799207875249, 0.4581489286485003198, 3.500000000000000444 ) ) ;
#62382=CARTESIAN_POINT ( 'NONE',  ( 11.09999999999999964, 4.000000000000000000, 7.500000000000000000 ) ) ;
#62388=CARTESIAN_POINT ( 'NONE',  ( 7.940355219341154402, 4.833259259596939472, 6.348670065445725541 ) ) ;
#62391=EDGE_CURVE ( 'NONE', #35353, #2331, #13392, .T. ) ;
#62393=CARTESIAN_POINT ( 'NONE',  ( 9.442010841233001273, 5.045571591548999812, -9.086294919530001124 ) ) ;
#62395=CARTESIAN_POINT ( 'NONE',  ( 7.978216579186597990, 3.009178048233850156, -6.462117657976292229 ) ) ;
#62397=CARTESIAN_POINT ( 'NONE',  ( 0.2021281585065432262, 3.118434889361825668, -0.8389436472200255679 ) ) ;
#62398=CARTESIAN_POINT ( 'NONE',  ( 3.634748863956000164, -1.556094637422999805, -2.863599491026000088 ) ) ;
#62399=ORIENTED_EDGE ( 'NONE', *, *, #28841, .F. ) ;
#62402=FACE_OUTER_BOUND ( 'NONE', #36058, .T. ) ;
#62405=EDGE_LOOP ( 'NONE', ( #32094, #24323, #14736, #64547, #30957, #66280, #54056, #3142, #62674, #12911, #54828, #627 ) ) ;
#62415=CARTESIAN_POINT ( 'NONE',  ( 9.152931135682532471, 5.100000000000000533, -6.444141223442171551 ) ) ;
#62419=CARTESIAN_POINT ( 'NONE',  ( -0.000000000000000000, 1.460960874861672698, -2.533832635912068199 ) ) ;
#62421=CARTESIAN_POINT ( 'NONE',  ( 6.993814158770001121, 4.468431922689999780, -6.183326950307000303 ) ) ;
#62423=CARTESIAN_POINT ( 'NONE',  ( 5.500000000000000000, 12.43893545635000031, 2.828937028792000152 ) ) ;
#62424=VERTEX_POINT ( 'NONE', #25583 ) ;
#62430=VERTEX_POINT ( 'NONE', #25924 ) ;
#62432=DIRECTION ( 'NONE',  ( -0.7071067759742961645, -0.7071067863987962054, -5.966942998097971758E-08 ) ) ;
#62437=CARTESIAN_POINT ( 'NONE',  ( 8.933148997457999840, 5.167567567567999731, 6.822293592207000934 ) ) ;
#62443=CARTESIAN_POINT ( 'NONE',  ( 9.736878146978000359, 2.742182981761000171, 6.839230404018000087 ) ) ;
#62446=CARTESIAN_POINT ( 'NONE',  ( 8.690229719593000723, 2.414630869937000046, -6.801495146585999407 ) ) ;
#62447=CARTESIAN_POINT ( 'NONE',  ( 3.313094297425999812, -3.277373826264000201, -1.734488728539000046 ) ) ;
#62448=ADVANCED_FACE ( 'NONE', ( #62298 ), #63311, .T. ) ;
#62450=CARTESIAN_POINT ( 'NONE',  ( 10.93769855012999948, 2.936883479403999964, 4.920828759365000415 ) ) ;
#62454=CARTESIAN_POINT ( 'NONE',  ( 10.35096486449576503, 5.732427394192054493, -7.739054094300635178 ) ) ;
#62456=CARTESIAN_POINT ( 'NONE',  ( 10.90000000162999960, 2.899999999992999733, -5.160242739096000619 ) ) ;
#62458=CARTESIAN_POINT ( 'NONE',  ( 10.24961997674000003, 4.184221916050000267, 9.286882020979000174 ) ) ;
#62459=DIRECTION ( 'NONE',  ( 0.000000000000000000, -1.000000000000000000, 0.000000000000000000 ) ) ;
#62470=CARTESIAN_POINT ( 'NONE',  ( 5.000030787343001215, -1.290525307673963118, -1.679270695423619175 ) ) ;
#62474=CARTESIAN_POINT ( 'NONE',  ( 10.84974221959000218, 5.265003089217000998, -6.385808769407000263 ) ) ;
#62478=CARTESIAN_POINT ( 'NONE',  ( 1.373890132540666720, -2.150913519912200922, -2.798833948393631754 ) ) ;
#62482=CARTESIAN_POINT ( 'NONE',  ( 5.500000000000000000, -11.95749337870000062, -3.642574926947999892 ) ) ;
#62483=VERTEX_POINT ( 'NONE', #3559 ) ;
#62501=CARTESIAN_POINT ( 'NONE',  ( 8.079135841228998416, 3.524748802314000340, 5.573833469815000718 ) ) ;
#62509=LINE ( 'NONE', #52713, #20091 ) ;
#62511=B_SPLINE_SURFACE_WITH_KNOTS ( 'NONE', 3, 3, ( 
 ( #1076, #1766, #28693, #39516, #17143, #32891, #59797, #65381, #38825, #2117, #23084, #59450, #65729, #60493, #12953, #60152, #33238, #54903, #7006, #27997, #49306, #1418, #28338, #12257, #17852, #49657, #39170, #12602, #2452, #7348, #50006, #23434, #44773, #66073, #18194 ),
 ( #60841, #38475, #34280, #55600, #7701, #29042, #23777, #45112, #38123, #54201, #6302, #27649, #48968, #65026, #35653, #25150, #8391, #13985, #19910, #24121, #35311, #61527, #56628, #24812, #35982, #19566, #57300, #34969, #40888, #8732, #34629, #3476, #18541, #56967, #46482 ),
 ( #9068, #29735, #30406, #55942, #61187, #51038, #13642, #25496, #41235, #30076, #62546, #62209, #51718, #51377, #14330, #67106, #61865, #24468, #56286, #3811, #67788, #45793, #3140, #14669, #19214, #9403, #39867, #40541, #67443, #46137, #30745, #52054, #4157, #8044, #46826 ),
 ( #13307, #29388, #45456, #50698, #2795, #66768, #18885, #40211, #37359, #4498, #5195, #69167, #21616, #36680, #10439, #31099, #25839, #52405, #37024, #47167, #31435, #16029, #68470, #41575, #15352, #16373, #42951, #63578, #58001, #10100, #52751, #63917, #32128, #26190, #32467 ) ),
 .UNSPECIFIED., .F., .F., .F.,
 ( 4, 4 ),
 ( 4, 1, 1, 1, 1, 1, 1, 1, 1, 1, 1, 1, 1, 1, 1, 1, 1, 1, 1, 1, 1, 1, 1, 1, 1, 1, 1, 1, 1, 1, 1, 1, 4 ),
 ( -0.1039370721279000015, 1.103937072127999963 ),
 ( -0.01933701211302999920, 0.01208563257065999909, 0.04350827725433999843, 0.07493092193802000645, 0.1063535666217000075, 0.1377762113054000204, 0.1691988559891000055, 0.2006215006727000150, 0.2320441453564000001, 0.2634667900400999851, 0.2948894347238000258, 0.3263120794074999553, 0.3577347240911999959, 0.3891573687748000054, 0.4205800134584999905, 0.4520026581421999756, 0.4834253028259000162, 0.5148479475096000568, 0.5462705921932000663, 0.5776932368768999959, 0.6091158815606000365, 0.6405385262443000771, 0.6719611709280000067, 0.7033838156117000473, 0.7348064602953000568, 0.7662291049789999864, 0.7976517496627000270, 0.8290743943464000676, 0.8604970390300999972, 0.8919196837138000378, 0.9233423283974000473, 0.9547649730810999769, 0.9861876177648000175 ),
 .UNSPECIFIED. ) ;
#62515=CARTESIAN_POINT ( 'NONE',  ( 6.345434501008996975, 9.270874106397998915, -4.897694007782000369 ) ) ;
#62523=ORIENTED_EDGE ( 'NONE', *, *, #57603, .F. ) ;
#62528=CARTESIAN_POINT ( 'NONE',  ( 9.831594052344000190, 3.539229510464000139, -8.956011942092999334 ) ) ;
#62529=EDGE_CURVE ( 'NONE', #15832, #67326, #49628, .T. ) ;
#62530=CARTESIAN_POINT ( 'NONE',  ( 6.999998782146999332, 0.000000000000000000, 0.000000000000000000 ) ) ;
#62533=CARTESIAN_POINT ( 'NONE',  ( 9.323722176100000425, 3.947350570199999797, 6.051869652381999920 ) ) ;
#62536=CARTESIAN_POINT ( 'NONE',  ( 10.21609109105999913, 5.961715741921000067, 7.319666990313999477 ) ) ;
#62538=CARTESIAN_POINT ( 'NONE',  ( 10.31457848836000046, 5.362142879234999882, 6.677781064327999339 ) ) ;
#62540=CARTESIAN_POINT ( 'NONE',  ( 9.716735841232001292, 3.941185585667000169, -8.896279800194999865 ) ) ;
#62546=CARTESIAN_POINT ( 'NONE',  ( 9.662551629919999385, 4.094830335839000135, 9.119946295870999364 ) ) ;
#62549=CARTESIAN_POINT ( 'NONE',  ( 8.830545280412000153, 3.207599814920999659, -6.150466394809999571 ) ) ;
#62551=CARTESIAN_POINT ( 'NONE',  ( 9.007644528442998677, 4.705791426005982991, 8.704816259181130889 ) ) ;
#62556=ORIENTED_EDGE ( 'NONE', *, *, #42525, .F. ) ;
#62557=CARTESIAN_POINT ( 'NONE',  ( 1.772746615351999955, -3.758001540264999996, 0.07616889274500000806 ) ) ;
#62560=CARTESIAN_POINT ( 'NONE',  ( 9.808929255601938735, 4.355736776651455422, 9.240861898867757773 ) ) ;
#62563=EDGE_CURVE ( 'NONE', #26452, #23033, #27968, .T. ) ;
#62571=CARTESIAN_POINT ( 'NONE',  ( 8.791232780412000736, 5.095085596809999728, 6.286981168432999922 ) ) ;
#62575=FACE_OUTER_BOUND ( 'NONE', #40682, .T. ) ;
#62576=CARTESIAN_POINT ( 'NONE',  ( 0.7371534748590999886, 2.178673723483000035, -2.162625512369000358 ) ) ;
#62577=ORIENTED_EDGE ( 'NONE', *, *, #61317, .F. ) ;
#62578=DIRECTION ( 'NONE',  ( 1.000000000000000000, 0.000000000000000000, 0.000000000000000000 ) ) ;
#62580=CARTESIAN_POINT ( 'NONE',  ( 9.657553581808000942, 5.333455947841000189, 6.049916795084000043 ) ) ;
#62581=CARTESIAN_POINT ( 'NONE',  ( 9.646287586158999616, 2.591467678478000192, 6.760055064032999717 ) ) ;
#62588=FACE_OUTER_BOUND ( 'NONE', #22603, .T. ) ;
#62592=DIRECTION ( 'NONE',  ( 0.000000000000000000, 1.000000000000000000, 0.000000000000000000 ) ) ;
#62593=ORIENTED_EDGE ( 'NONE', *, *, #66317, .F. ) ;
#62595=CARTESIAN_POINT ( 'NONE',  ( 9.972850246170999355, 5.044468801812000081, 6.258104779495000436 ) ) ;
#62596=CARTESIAN_POINT ( 'NONE',  ( 10.27571527605999968, 5.689443924112000062, -7.562019866568999049 ) ) ;
#62602=DIRECTION ( 'NONE',  ( 0.9999999999985111909, -8.580731922641101058E-07, -1.497129875399016346E-06 ) ) ;
#62610=EDGE_CURVE ( 'NONE', #798, #52567, #44217, .T. ) ;
#62611=CARTESIAN_POINT ( 'NONE',  ( 7.000000000000000000, 8.307879248642999315, -4.307879248643000203 ) ) ;
#62613=FACE_OUTER_BOUND ( 'NONE', #47438, .T. ) ;
#62619=CARTESIAN_POINT ( 'NONE',  ( 9.883148997457000817, 5.167567567567999731, 6.822293592207000934 ) ) ;
#62622=CARTESIAN_POINT ( 'NONE',  ( 9.817462135711998883, 5.100000000000000533, 6.571291218949999902 ) ) ;
#62629=CYLINDRICAL_SURFACE ( 'NONE', #46226, 1.350000000000000533 ) ;
#62630=CARTESIAN_POINT ( 'NONE',  ( 9.978904719591000116, 5.007782080444000528, -8.772599239991000886 ) ) ;
#62632=CARTESIAN_POINT ( 'NONE',  ( 10.16966711471859952, 2.650353857333680896, 7.590422934968386492 ) ) ;
#62638=DIRECTION ( 'NONE',  ( 1.000000000000000000, 0.000000000000000000, 0.000000000000000000 ) ) ;
#62643=EDGE_CURVE ( 'NONE', #25251, #64076, #33904, .T. ) ;
#62663=DIRECTION ( 'NONE',  ( -1.000000000000000000, -3.552713678992000385E-14, 7.105427357983999508E-14 ) ) ;
#62669=CARTESIAN_POINT ( 'NONE',  ( 9.251970280414001380, 5.673443217382001080, -7.051790060464000476 ) ) ;
#62670=CARTESIAN_POINT ( 'NONE',  ( 10.22514748322308797, 2.649941783575544108, 7.500008211948054893 ) ) ;
#62671=VERTEX_POINT ( 'NONE', #14299 ) ;
#62674=ORIENTED_EDGE ( 'NONE', *, *, #8449, .F. ) ;
#62677=CARTESIAN_POINT ( 'NONE',  ( 9.193385841233000733, 2.981992329588000423, -5.895876591910999664 ) ) ;
#62684=CARTESIAN_POINT ( 'NONE',  ( 8.938854719593997800, 5.597201461420000967, -8.171008079894999554 ) ) ;
#62685=VERTEX_POINT ( 'NONE', #35954 ) ;
#62686=CARTESIAN_POINT ( 'NONE',  ( 10.32702465212000043, 5.663794543395000325, -6.682030833630000721 ) ) ;
#62698=CARTESIAN_POINT ( 'NONE',  ( 11.22023584123000006, 3.883089684441999978, -8.854806321849000739 ) ) ;
#62699=LINE ( 'NONE', #57804, #20712 ) ;
#62700=DIRECTION ( 'NONE',  ( 1.000000000000000000, 0.000000000000000000, 0.000000000000000000 ) ) ;
#62705=ORIENTED_EDGE ( 'NONE', *, *, #23940, .F. ) ;
#62707=CARTESIAN_POINT ( 'NONE',  ( 9.120035841232999374, 5.288433695693000480, -8.041290150997999930 ) ) ;
#62720=CARTESIAN_POINT ( 'NONE',  ( 6.949659606017999813, -12.16386295504999993, -3.090546161407999648 ) ) ;
#62723=CARTESIAN_POINT ( 'NONE',  ( 8.745860841232000027, 4.178200486578000472, -5.608493638783999202 ) ) ;
#62724=EDGE_CURVE ( 'NONE', #27484, #10323, #50771, .T. ) ;
#62730=CARTESIAN_POINT ( 'NONE',  ( 0.3209986693645116018, -1.671708792466147120, 2.902155973540134326 ) ) ;
#62732=CARTESIAN_POINT ( 'NONE',  ( 9.870826602350810219, 2.650039321431383765, -7.402527530260877953 ) ) ;
#62738=CARTESIAN_POINT ( 'NONE',  ( 1.571806799207417393, 3.408904368339104263, 0.9161175952574878156 ) ) ;
#62742=CARTESIAN_POINT ( 'NONE',  ( 10.96620111615414928, 8.758729369432925793, 6.500226485814697419 ) ) ;
#62743=EDGE_CURVE ( 'NONE', #15849, #24516, #46794, .T. ) ;
#62745=CARTESIAN_POINT ( 'NONE',  ( 1.709306799206499861, -3.058252359239909790, 1.762666431298136382 ) ) ;
#62756=CARTESIAN_POINT ( 'NONE',  ( 8.427194650706185897, 4.807287621755191864, -9.060105673721203345 ) ) ;
#62757=CARTESIAN_POINT ( 'NONE',  ( 11.10000057264999995, 0.4999994248636999705, 9.776630284457000997 ) ) ;
#62758=CARTESIAN_POINT ( 'NONE',  ( 6.645739158770999744, 5.086541985415000688, -8.378805615758999181 ) ) ;
#62762=CARTESIAN_POINT ( 'NONE',  ( 2.240556799207291672, -3.500000000000003109, 0.4581489286484972667 ) ) ;
#62765=ORIENTED_EDGE ( 'NONE', *, *, #44146, .T. ) ;
#62767=CARTESIAN_POINT ( 'NONE',  ( 8.316694475082000437, 2.898380349184999982, 6.611503672649000407 ) ) ;
#62771=CARTESIAN_POINT ( 'NONE',  ( 8.687922088694000067, 3.419384128876999718, -5.860036257779999147 ) ) ;
#62773=CARTESIAN_POINT ( 'NONE',  ( 11.09999999999999964, 4.000000000000000000, 7.500000000000000000 ) ) ;
#62781=CARTESIAN_POINT ( 'NONE',  ( 10.40516904918000129, 5.216391323504000255, 6.765759859247999941 ) ) ;
#62784=CARTESIAN_POINT ( 'NONE',  ( 2.432838064400999922, 1.445961631832999972, -3.231775658717000344 ) ) ;
#62791=CARTESIAN_POINT ( 'NONE',  ( 11.09999999999999964, 4.000000000000000000, -7.500000000000000000 ) ) ;
#62794=CARTESIAN_POINT ( 'NONE',  ( 10.06344080699000010, 5.156228702401000952, 6.125219923432000613 ) ) ;
#62812=ORIENTED_EDGE ( 'NONE', *, *, #63517, .T. ) ;
#62815=CARTESIAN_POINT ( 'NONE',  ( 10.58470471959000037, 2.966809777448999874, -8.831980808885999679 ) ) ;
#62817=CARTESIAN_POINT ( 'NONE',  ( 1.300973465874000201, -3.500000000000000000, 0.000000000000000000 ) ) ;
#62821=CARTESIAN_POINT ( 'NONE',  ( 8.785198341231000185, 5.414918126383000185, 8.890678916765999418 ) ) ;
#62824=CARTESIAN_POINT ( 'NONE',  ( 7.119364158768999751, 2.502464354543000091, -6.330838737160999763 ) ) ;
#62825=EDGE_CURVE ( 'NONE', #68596, #7028, #25461, .T. ) ;
#62837=CARTESIAN_POINT ( 'NONE',  ( 2.530140132543583498, 3.408904368339106483, -0.9161175952574748260 ) ) ;
#62843=ORIENTED_EDGE ( 'NONE', *, *, #29143, .F. ) ;
#62848=ORIENTED_EDGE ( 'NONE', *, *, #47275, .F. ) ;
#62852=CARTESIAN_POINT ( 'NONE',  ( 7.946130483458992977, 8.084765295500995208, -4.735587142431003649 ) ) ;
#62865=CARTESIAN_POINT ( 'NONE',  ( 10.55068356942999941, 2.412177153420000053, -6.919581319869999803 ) ) ;
#62866=DIRECTION ( 'NONE',  ( -0.8660254037844289376, 0.000000000000000000, 0.5000000000000169864 ) ) ;
#62869=CARTESIAN_POINT ( 'NONE',  ( 10.80815748598999981, 2.937526572573000205, 8.948458885032000154 ) ) ;
#62871=CARTESIAN_POINT ( 'NONE',  ( 8.798416552063660134, 5.540558544858231294, -6.616773852782482201 ) ) ;
#62875=CARTESIAN_POINT ( 'NONE',  ( 9.298033738970000073, 4.087077023028999001, 9.429414864145000408 ) ) ;
#62882=CARTESIAN_POINT ( 'NONE',  ( 9.316114158771000575, 3.677414437776999723, 9.250745771096999803 ) ) ;
#62885=ORIENTED_EDGE ( 'NONE', *, *, #28758, .F. ) ;
#62886=CARTESIAN_POINT ( 'NONE',  ( 10.02394528041000044, 5.481267232667000222, -8.005061172455999241 ) ) ;
#62887=DIRECTION ( 'NONE',  ( 1.000000000000000000, 0.000000000000000000, 0.000000000000000000 ) ) ;
#62889=EDGE_CURVE ( 'NONE', #64076, #28965, #34927, .T. ) ;
#62896=CARTESIAN_POINT ( 'NONE',  ( 1.629700767030000108, 0.9191385115525000371, 3.644662079466999938 ) ) ;
#62898=CARTESIAN_POINT ( 'NONE',  ( 9.743692251747383182, 5.492527719313065937, 8.410238609252001396 ) ) ;
#62908=CARTESIAN_POINT ( 'NONE',  ( 7.283509992105000386, 4.426928431836000044, 9.293321981113999541 ) ) ;
#62909=CARTESIAN_POINT ( 'NONE',  ( 10.98768472639999949, 0.3876847264043000174, 4.945212061661000469 ) ) ;
#62915=CARTESIAN_POINT ( 'NONE',  ( 2.096960091860043285, -2.086971693014386897, -2.559869209799199741 ) ) ;
#62917=EDGE_CURVE ( 'NONE', #12815, #12021, #10068, .T. ) ;
#62918=DIRECTION ( 'NONE',  ( 1.000000000000000000, 0.000000000000000000, 0.000000000000000000 ) ) ;
#62933=CARTESIAN_POINT ( 'NONE',  ( 10.68403803949000164, 5.436614310638000269, 8.578436083822998270 ) ) ;
#62934=CARTESIAN_POINT ( 'NONE',  ( 10.55068356942999941, 2.412177153420000053, -6.919581319869999803 ) ) ;
#62938=CARTESIAN_POINT ( 'NONE',  ( 9.032940059871402028, 5.014669081864663980, 8.393627007547543428 ) ) ;
#62943=CYLINDRICAL_SURFACE ( 'NONE', #45062, 2.000000000000000444 ) ;
#62945=CARTESIAN_POINT ( 'NONE',  ( 10.91900351868999408, 8.255374249431000067, 7.037317811674005164 ) ) ;
#62955=CARTESIAN_POINT ( 'NONE',  ( 8.814947692958833514, 2.650138447187985413, -7.499997389691697158 ) ) ;
#62967=CARTESIAN_POINT ( 'NONE',  ( 9.964039158770999549, 3.485905350467000119, -9.275749134703000109 ) ) ;
#62969=CARTESIAN_POINT ( 'NONE',  ( 9.924988015501618577, 5.349815781279066762, 7.500001845592777272 ) ) ;
#62974=EDGE_CURVE ( 'NONE', #6526, #23153, #4062, .T. ) ;
#62982=CARTESIAN_POINT ( 'NONE',  ( 8.191498566858999908, 3.399962487441000381, 6.146646668338000552 ) ) ;
#62983=ORIENTED_EDGE ( 'NONE', *, *, #36301, .T. ) ;
#62988=EDGE_CURVE ( 'NONE', #1808, #24606, #50940, .T. ) ;
#62993=CARTESIAN_POINT ( 'NONE',  ( 7.540307192462002206, 2.929979193199001575, 6.558004150875995641 ) ) ;
#63001=ORIENTED_EDGE ( 'NONE', *, *, #28097, .T. ) ;
#63002=CARTESIAN_POINT ( 'NONE',  ( 8.564679719593000229, 4.146787477634999775, -5.941926545671999627 ) ) ;
#63007=ORIENTED_EDGE ( 'NONE', *, *, #66088, .F. ) ;
#63016=CARTESIAN_POINT ( 'NONE',  ( 9.286929719595001131, 4.102804347295999854, -5.770625657082999460 ) ) ;
#63019=CARTESIAN_POINT ( 'NONE',  ( 11.03408597791999846, 2.992846905312999795, -9.056576857348998644 ) ) ;
#63023=CARTESIAN_POINT ( 'NONE',  ( 9.328814160995289484, 2.650569397798120619, -7.263217323294509420 ) ) ;
#63024=ADVANCED_FACE ( 'NONE', ( #17741 ), #39061, .T. ) ;
#63031=CARTESIAN_POINT ( 'NONE',  ( 10.61443584123000150, 5.287628373050000441, -7.937241318065001217 ) ) ;
#63032=AXIS2_PLACEMENT_3D ( 'NONE', #23504, #7078, #1493 ) ;
#63033=CARTESIAN_POINT ( 'NONE',  ( 9.975298369746390392, 5.350379160513678123, 7.499985214262784083 ) ) ;
#63041=CARTESIAN_POINT ( 'NONE',  ( 9.667010841233000917, 4.769103072373000352, -8.666849124598000387 ) ) ;
#63049=CARTESIAN_POINT ( 'NONE',  ( 8.735210106471628322, 5.610874584628978923, 8.247390189602128885 ) ) ;
#63058=DIRECTION ( 'NONE',  ( -7.774844867625903451E-08, 7.808575926866904497E-08, -0.9999999999999940048 ) ) ;
#63061=CARTESIAN_POINT ( 'NONE',  ( 7.995055131332884812, 3.139660977872365422, -6.336962724805712988 ) ) ;
#63065=CARTESIAN_POINT ( 'NONE',  ( 0.2087320758492651196, 3.208711876255013529, -0.4208838518088701131 ) ) ;
#63066=PRODUCT_DEFINITION_FORMATION_WITH_SPECIFIED_SOURCE ( 'ANY', '', #51713, .NOT_KNOWN. ) ;
#63067=DIRECTION ( 'NONE',  ( 0.000000000000000000, -0.7158784314710772145, 0.6982249432342778617 ) ) ;
#63068=CARTESIAN_POINT ( 'NONE',  ( 3.157929369547999965, -0.6681045838537000847, -3.189815491325000085 ) ) ;
#63073=DIRECTION ( 'NONE',  ( 1.000000000000000000, 0.000000000000000000, 0.000000000000000000 ) ) ;
#63076=ORIENTED_EDGE ( 'NONE', *, *, #6401, .T. ) ;
#63079=CARTESIAN_POINT ( 'NONE',  ( 10.96940393808957381, 8.671713867168650225, 6.520930117690211247 ) ) ;
#63080=CARTESIAN_POINT ( 'NONE',  ( 11.09392659058483233, 2.706073409411867914, 6.603326177255940621 ) ) ;
#63083=EDGE_LOOP ( 'NONE', ( #21487, #63187, #12049, #23361 ) ) ;
#63084=B_SPLINE_CURVE_WITH_KNOTS ( 'NONE', 3,
 ( #58957, #63842, #5122, #11063, #42535, #922, #10708, #43573, #26457, #37971 ),
 .UNSPECIFIED., .F., .F.,
 ( 4, 2, 2, 2, 4 ),
 ( 0.000000000000000000, 0.2500000000000009992, 0.3750000000000014988, 0.5000000000000019984, 1.000000000000000000 ),
 .UNSPECIFIED. ) ;
#63091=ORIENTED_EDGE ( 'NONE', *, *, #6551, .T. ) ;
#63094=CARTESIAN_POINT ( 'NONE',  ( 7.581654719587999303, 4.473304741848999733, -6.008315738301999609 ) ) ;
#63097=ORIENTED_EDGE ( 'NONE', *, *, #49248, .F. ) ;
#63103=CARTESIAN_POINT ( 'NONE',  ( 7.956697741658004475, 3.406302814652999889, -6.282208831379191949 ) ) ;
#63104=ORIENTED_EDGE ( 'NONE', *, *, #33962, .T. ) ;
#63111=EDGE_CURVE ( 'NONE', #59076, #42164, #66608, .T. ) ;
#63115=CARTESIAN_POINT ( 'NONE',  ( 4.650001602240106280, 2.000000000000000000, 2.043842969622812301E-09 ) ) ;
#63119=ORIENTED_EDGE ( 'NONE', *, *, #22867, .F. ) ;
#63120=CARTESIAN_POINT ( 'NONE',  ( 9.298033738970000073, 4.087077023028999001, 9.429414864145000408 ) ) ;
#63122=CARTESIAN_POINT ( 'NONE',  ( 8.871410841230998656, 2.721111233225000259, -6.936528696292000085 ) ) ;
#63123=CARTESIAN_POINT ( 'NONE',  ( 2.342247503581000423, 1.381879776714000085, -3.088550434077999896 ) ) ;
#63131=CARTESIAN_POINT ( 'NONE',  ( 3.300973465876999580, -3.500000000000000000, 0.000000000000000000 ) ) ;
#63133=EDGE_CURVE ( 'NONE', #8000, #54361, #29622, .T. ) ;
#63135=CARTESIAN_POINT ( 'NONE',  ( 9.447841622600000377, 5.447457912891000120, 7.431328695644999982 ) ) ;
#63145=CARTESIAN_POINT ( 'NONE',  ( 0.3043556721781856544, 1.649503828942506578, -2.894701909231111703 ) ) ;
#63151=CARTESIAN_POINT ( 'NONE',  ( 0.08797697758023999282, -1.491878233134000142, -2.734521550864000172 ) ) ;
#63153=CARTESIAN_POINT ( 'NONE',  ( 10.59957028040999916, 4.438147096284001059, -8.958385582135001357 ) ) ;
#63160=FACE_OUTER_BOUND ( 'NONE', #7646, .T. ) ;
#63161=ORIENTED_EDGE ( 'NONE', *, *, #11840, .T. ) ;
#63163=CARTESIAN_POINT ( 'NONE',  ( 7.964689158768001320, 3.456780951359999854, -9.320567109458000488 ) ) ;
#63167=CARTESIAN_POINT ( 'NONE',  ( 6.999999691988000095, -2.604139126561000230E-12, 1.310063169058000104E-14 ) ) ;
#63171=CARTESIAN_POINT ( 'NONE',  ( 6.949657512459999964, 12.16386489619000066, 3.090547023080999711 ) ) ;
#63172=AXIS2_PLACEMENT_3D ( 'NONE', #6821, #6124, #38290 ) ;
#63173=VERTEX_POINT ( 'NONE', #8956 ) ;
#63176=CARTESIAN_POINT ( 'NONE',  ( 2.321806799209417793, -3.408904368339104263, -0.9161175952574813763 ) ) ;
#63187=ORIENTED_EDGE ( 'NONE', *, *, #15919, .T. ) ;
#63195=B_SPLINE_CURVE_WITH_KNOTS ( 'NONE', 3,
 ( #12639, #12994, #61227, #38510, #13343, #34318 ),
 .UNSPECIFIED., .F., .F.,
 ( 4, 2, 4 ),
 ( 0.000000000000000000, 0.1860062838997574297, 0.3720125677995148594 ),
 .UNSPECIFIED. ) ;
#63199=ORIENTED_EDGE ( 'NONE', *, *, #43653, .T. ) ;
#63200=ORIENTED_EDGE ( 'NONE', *, *, #65837, .F. ) ;
#63203=CARTESIAN_POINT ( 'NONE',  ( 4.900006121741999010, 2.000000000000000000, 0.000000000000000000 ) ) ;
#63204=CARTESIAN_POINT ( 'NONE',  ( 10.99693586709999948, 2.980605808171000071, -6.418617723582000778 ) ) ;
#63205=DIRECTION ( 'NONE',  ( 1.000000000000000000, 3.552713678845000257E-14, 1.776356839423000267E-14 ) ) ;
#63211=ORIENTED_EDGE ( 'NONE', *, *, #44983, .F. ) ;
#63214=CARTESIAN_POINT ( 'NONE',  ( 9.260906466624998501, 4.901388651757999426, 9.090324495507999814 ) ) ;
#63217=CARTESIAN_POINT ( 'NONE',  ( 9.169760841232999837, 4.728328492779000136, -8.692725459657999920 ) ) ;
#63218=CARTESIAN_POINT ( 'NONE',  ( 10.95123343040000030, 9.911362171613999905, -5.636329857493000084 ) ) ;
#63223=CARTESIAN_POINT ( 'NONE',  ( 10.92101570304880909, 4.925410080013705283, -9.003883028371625130 ) ) ;
#63224=VECTOR ( 'NONE', #37474, 1000.000000000000000 ) ;
#63229=CARTESIAN_POINT ( 'NONE',  ( 8.590779719591999708, 2.836879604150999601, -8.783908972046001296 ) ) ;
#63234=B_SPLINE_CURVE_WITH_KNOTS ( 'NONE', 3,
 ( #42948, #37021, #53093, #4844, #58679, #26877, #41915, #52051, #64257, #63223, #20247, #4496, #25836, #15350, #68817, #20939, #43295, #21956 ),
 .UNSPECIFIED., .F., .F.,
 ( 4, 2, 2, 2, 2, 2, 2, 2, 4 ),
 ( 0.000000000000000000, 0.1250000000000000833, 0.2500000000000001665, 0.3750000000000002220, 0.5000000000000003331, 0.6250000000000004441, 0.7500000000000004441, 0.8750000000000002220, 1.000000000000000000 ),
 .UNSPECIFIED. ) ;
#63237=CIRCLE ( 'NONE', #29798, 13.10000000000000320 ) ;
#63239=CARTESIAN_POINT ( 'NONE',  ( 8.400073341230999802, 2.800103557244999930, 9.079946116129001155 ) ) ;
#63241=CARTESIAN_POINT ( 'NONE',  ( 9.988331016203231272, 2.447533665446552043, 6.696458009942619860 ) ) ;
#63244=EDGE_LOOP ( 'NONE', ( #59260, #39814, #12834, #32401, #52056 ) ) ;
#63245=CARTESIAN_POINT ( 'NONE',  ( 9.848259964010999568, 4.436917881843999822, 6.148031614254000132 ) ) ;
#63251=CARTESIAN_POINT ( 'NONE',  ( 9.214142219592000416, 5.421534627450999899, 6.381126373995999579 ) ) ;
#63265=FACE_OUTER_BOUND ( 'NONE', #20445, .T. ) ;
#63272=LINE ( 'NONE', #68865, #22712 ) ;
#63276=ORIENTED_EDGE ( 'NONE', *, *, #47045, .T. ) ;
#63278=CARTESIAN_POINT ( 'NONE',  ( 9.509901345851000443, 5.077442745148000647, 8.469003100811999474 ) ) ;
#63279=CARTESIAN_POINT ( 'NONE',  ( 10.43284001513000092, 3.279325423736999756, -9.029279369994000604 ) ) ;
#63280=CARTESIAN_POINT ( 'NONE',  ( 8.244330716364007827, 4.955554988691996954, 6.175165069893004954 ) ) ;
#63284=CARTESIAN_POINT ( 'NONE',  ( 9.038697134104578979, 4.943501910544378042, 8.465380656488354916 ) ) ;
#63287=CARTESIAN_POINT ( 'NONE',  ( 7.352704719590999360, 4.773081973066999772, 8.927402469597002010 ) ) ;
#63294=CARTESIAN_POINT ( 'NONE',  ( 9.236022032864006803, 9.967515357128998943, 5.897776175397996035 ) ) ;
#63303=LINE ( 'NONE', #4927, #61666 ) ;
#63308=CARTESIAN_POINT ( 'NONE',  ( 0.07157952889540999952, -0.5148121778627998690, -3.334029978310999898 ) ) ;
#63309=CARTESIAN_POINT ( 'NONE',  ( 9.762727031004574840, 2.920691866409497184, -8.329517998611422058 ) ) ;
#63311=CYLINDRICAL_SURFACE ( 'NONE', #34127, 0.5000000000000002220 ) ;
#63313=CARTESIAN_POINT ( 'NONE',  ( 8.045433776029998540, 2.903894639863001892, -6.425841880607995549 ) ) ;
#63314=CARTESIAN_POINT ( 'NONE',  ( 11.03905471959000018, 3.855072614532999875, -9.179480010827999692 ) ) ;
#63323=CARTESIAN_POINT ( 'NONE',  ( 9.497627230745894877, 3.288461954788812758, -9.126428113227261107 ) ) ;
#63325=FACE_OUTER_BOUND ( 'NONE', #3567, .T. ) ;
#63330=ORIENTED_EDGE ( 'NONE', *, *, #1037, .F. ) ;
#63334=CARTESIAN_POINT ( 'NONE',  ( 9.856851002545999663, 2.832432432432000269, -6.822293592207000934 ) ) ;
#63337=CARTESIAN_POINT ( 'NONE',  ( 8.589811424367198356, 5.008283254081848490, 6.160546554369722649 ) ) ;
#63341=CARTESIAN_POINT ( 'NONE',  ( 8.146781841545999825, 3.121749852590999907, 6.130949854565998614 ) ) ;
#63342=AXIS2_PLACEMENT_3D ( 'NONE', #58571, #52636, #58229 ) ;
#63350=VERTEX_POINT ( 'NONE', #19796 ) ;
#63351=CARTESIAN_POINT ( 'NONE',  ( 8.962479719595000560, 2.546924812613000189, -6.918870225297999887 ) ) ;
#63353=ORIENTED_EDGE ( 'NONE', *, *, #32023, .F. ) ;
#63354=LINE ( 'NONE', #31909, #19492 ) ;
#63357=VERTEX_POINT ( 'NONE', #20136 ) ;
#63359=CARTESIAN_POINT ( 'NONE',  ( 9.044210841233001119, 2.773858540272000184, -8.951250717848999727 ) ) ;
#63360=CARTESIAN_POINT ( 'NONE',  ( 10.20000099824999928, 0.000000000000000000, 0.000000000000000000 ) ) ;
#63363=CARTESIAN_POINT ( 'NONE',  ( 10.98768472639999949, 5.139099012905000485, 4.945212061661000469 ) ) ;
#63367=AXIS2_PLACEMENT_3D ( 'NONE', #49196, #18772, #12836 ) ;
#63368=CARTESIAN_POINT ( 'NONE',  ( 9.635004719593998956, 2.334550724494000029, -7.977056617806000283 ) ) ;
#63372=CARTESIAN_POINT ( 'NONE',  ( 9.843622243630001378, 5.021682716044000294, -8.761466596873999535 ) ) ;
#63373=EDGE_CURVE ( 'NONE', #14790, #12749, #684, .T. ) ;
#63377=CONICAL_SURFACE ( 'NONE', #28936, 2.824973347946000413, 0.7853886971611369061 ) ;
#63383=ORIENTED_EDGE ( 'NONE', *, *, #52838, .F. ) ;
#63385=CARTESIAN_POINT ( 'NONE',  ( 10.93769906950999982, 5.063122007744000008, 4.920829195600999739 ) ) ;
#63390=CARTESIAN_POINT ( 'NONE',  ( 9.983079719591000156, 5.002683760508999988, -8.912673867568997821 ) ) ;
#63393=ORIENTED_EDGE ( 'NONE', *, *, #4016, .F. ) ;
#63395=CIRCLE ( 'NONE', #35524, 1.999999999999999556 ) ;
#63396=CARTESIAN_POINT ( 'NONE',  ( 11.12921181452999875, 5.272412031865999715, -4.816967985768999760 ) ) ;
#63399=CARTESIAN_POINT ( 'NONE',  ( 0.1499942179680000265, 2.678379783547567339, -0.7197945678028350169 ) ) ;
#63403=CARTESIAN_POINT ( 'NONE',  ( 8.345403361566443579, 4.924247179573619349, -6.195500497232360182 ) ) ;
#63412=DIRECTION ( 'NONE',  ( -1.000000000000000000, 0.000000000000000000, 0.000000000000000000 ) ) ;
#63414=CARTESIAN_POINT ( 'NONE',  ( 7.974268290630120326, 2.993798921748313635, -6.483333862739654840 ) ) ;
#63416=DIRECTION ( 'NONE',  ( -1.000000000000000000, 0.000000000000000000, 0.000000000000000000 ) ) ;
#63418=CARTESIAN_POINT ( 'NONE',  ( 0.1499942179680000265, -2.678379783547564674, -0.7197945678028442318 ) ) ;
#63419=VERTEX_POINT ( 'NONE', #68707 ) ;
#63420=ADVANCED_FACE ( 'NONE', ( #10673 ), #57190, .T. ) ;
#63427=CARTESIAN_POINT ( 'NONE',  ( 10.22963300084732552, 4.176697648610399938, -8.850191834421025305 ) ) ;
#63437=CYLINDRICAL_SURFACE ( 'NONE', #27330, 0.5000000000000002220 ) ;
#63439=CARTESIAN_POINT ( 'NONE',  ( 1.300973465874000201, -3.500000000000000000, 0.000000000000000000 ) ) ;
#63440=ORIENTED_EDGE ( 'NONE', *, *, #21019, .T. ) ;
#63447=CARTESIAN_POINT ( 'NONE',  ( 8.228079719590001062, 5.311932732455999506, -8.353077699453999472 ) ) ;
#63452=CARTESIAN_POINT ( 'NONE',  ( 11.09999999999999964, 2.700000000000000178, -6.461133846875999787 ) ) ;
#63454=ORIENTED_EDGE ( 'NONE', *, *, #1654, .T. ) ;
#63456=ORIENTED_EDGE ( 'NONE', *, *, #10275, .F. ) ;
#63467=CARTESIAN_POINT ( 'NONE',  ( 10.33536974457000035, 5.153692264686000613, 8.830864265869999841 ) ) ;
#63469=DIRECTION ( 'NONE',  ( 1.000000000000000000, 0.000000000000000000, 0.000000000000000000 ) ) ;
#63482=CARTESIAN_POINT ( 'NONE',  ( 3.071806799211250549, 3.408904368339104263, 0.9161175952574878156 ) ) ;
#63485=CARTESIAN_POINT ( 'NONE',  ( 9.758140238852000437, 2.901378080241999946, 6.555076849497999625 ) ) ;
#63495=ORIENTED_EDGE ( 'NONE', *, *, #8016, .F. ) ;
#63497=CARTESIAN_POINT ( 'NONE',  ( 9.658629719592001450, 5.496789211521000418, -7.043125396300999874 ) ) ;
#63499=PLANE ( 'NONE',  #4340 ) ;
#63500=B_SPLINE_CURVE_WITH_KNOTS ( 'NONE', 3,
 ( #24277, #56787, #19720, #46640 ),
 .UNSPECIFIED., .F., .F.,
 ( 4, 4 ),
 ( 0.000000000000000000, 1.000000000000000000 ),
 .UNSPECIFIED. ) ;
#63501=EDGE_LOOP ( 'NONE', ( #40485, #33116, #15167, #40343, #36223, #37292 ) ) ;
#63502=AXIS2_PLACEMENT_3D ( 'NONE', #15928, #63469, #19806 ) ;
#63505=CARTESIAN_POINT ( 'NONE',  ( 10.54684221959000112, 3.691673619534999951, -9.157283848447001162 ) ) ;
#63506=ORIENTED_EDGE ( 'NONE', *, *, #57773, .F. ) ;
#63510=CARTESIAN_POINT ( 'NONE',  ( -15.86200481174999943, 2.399999999999999911, -6.571291218949999902 ) ) ;
#63513=CARTESIAN_POINT ( 'NONE',  ( 8.400073341230999802, 2.800103557244999930, 9.079946116129001155 ) ) ;
#63517=EDGE_CURVE ( 'NONE', #25932, #20015, #39819, .T. ) ;
#63519=CARTESIAN_POINT ( 'NONE',  ( 8.502804719591001259, 4.586183217919999500, -9.013777652867000612 ) ) ;
#63533=AXIS2_PLACEMENT_3D ( 'NONE', #40038, #56102, #8211 ) ;
#63539=CARTESIAN_POINT ( 'NONE',  ( 7.101301658771000724, 3.554857159507999853, 8.889479859586000288 ) ) ;
#63540=EDGE_CURVE ( 'NONE', #13916, #35486, #60671, .T. ) ;
#63541=ORIENTED_EDGE ( 'NONE', *, *, #67079, .F. ) ;
#63544=LINE ( 'NONE', #25454, #26793 ) ;
#63547=CARTESIAN_POINT ( 'NONE',  ( 10.91914189278999636, 8.255337631213995664, -7.037376568592996762 ) ) ;
#63548=CARTESIAN_POINT ( 'NONE',  ( 7.921841810112000282, 2.875629839593000003, -6.725486766668000271 ) ) ;
#63559=CARTESIAN_POINT ( 'NONE',  ( 9.922184613163000932, 3.489926301007000298, -9.111807643819000546 ) ) ;
#63563=CARTESIAN_POINT ( 'NONE',  ( 7.805976048735002948, 2.918573024645998881, -6.499545638216004839 ) ) ;
#63564=CARTESIAN_POINT ( 'NONE',  ( 9.972537864286000087, 2.899999999999999911, -6.571291218949999902 ) ) ;
#63569=CARTESIAN_POINT ( 'NONE',  ( 9.843732751558000871, 4.115124343450999866, 9.466620196856998959 ) ) ;
#63571=CARTESIAN_POINT ( 'NONE',  ( 9.576488281553999116, 4.593976206186999534, 5.662041230125000268 ) ) ;
#63573=CARTESIAN_POINT ( 'NONE',  ( 10.16426084122999995, 4.808846957865000604, -8.639578604182998944 ) ) ;
#63578=CARTESIAN_POINT ( 'NONE',  ( 10.62697636434999993, 3.142921793056999924, 8.668445734229999644 ) ) ;
#63581=CARTESIAN_POINT ( 'NONE',  ( 8.639360841228999277, 5.074768364528000397, -8.296267706722000312 ) ) ;
#63584=CARTESIAN_POINT ( 'NONE',  ( 3.396238944115833824, 0.8916813559738958617, -3.415138845704721149 ) ) ;
#63590=CARTESIAN_POINT ( 'NONE',  ( 9.111654719595000174, 4.989193221215000307, -6.287302145481000082 ) ) ;
#63591=DIRECTION ( 'NONE',  ( 0.000000000000000000, 0.8684118361392316743, -0.4958436072526178351 ) ) ;
#63593=ORIENTED_EDGE ( 'NONE', *, *, #23348, .F. ) ;
#63594=CARTESIAN_POINT ( 'NONE',  ( 10.87148757351999961, 5.567567343464999929, 7.772413227960999649 ) ) ;
#63600=CARTESIAN_POINT ( 'NONE',  ( 9.149954719592001240, 4.175915362023999933, 5.699506188181000077 ) ) ;
#63604=DIRECTION ( 'NONE',  ( 0.000000000000000000, -0.8648648648648720183, -0.5020047465136825426 ) ) ;
#63606=CONICAL_SURFACE ( 'NONE', #30148, 13.04999927352999833, 0.7853981075146502233 ) ;
#63609=CARTESIAN_POINT ( 'NONE',  ( 1.070927120944999755, -3.140063525497999830, -0.8725182546194000244 ) ) ;
#63613=CARTESIAN_POINT ( 'NONE',  ( 9.687870098586998324, 5.912263966150999472, 7.772301113561999486 ) ) ;
#63615=ORIENTED_EDGE ( 'NONE', *, *, #8365, .T. ) ;
#63631=CARTESIAN_POINT ( 'NONE',  ( 11.10062015617000064, 3.093053541899000169, -6.153678467293999255 ) ) ;
#63632=CARTESIAN_POINT ( 'NONE',  ( 7.903774407030003779, 5.139635483293002238, 6.776036904885998524 ) ) ;
#63635=CARTESIAN_POINT ( 'NONE',  ( 9.040001050027107965, 4.926961961734873441, 8.481263526778137773 ) ) ;
#63637=CARTESIAN_POINT ( 'NONE',  ( 7.481079719589999399, 2.374037589774999901, 8.293392681990997772 ) ) ;
#63640=CARTESIAN_POINT ( 'NONE',  ( 11.09999999999999964, 5.299316147296000423, -5.124965750789000296 ) ) ;
#63642=CARTESIAN_POINT ( 'NONE',  ( 11.48791672854001433, 9.860991908751987722, 5.543179905927000384 ) ) ;
#63644=CARTESIAN_POINT ( 'NONE',  ( 10.90070920260000165, 9.357678590204999480, 6.160837872949999294 ) ) ;
#63646=CARTESIAN_POINT ( 'NONE',  ( 10.90000000000000036, 0.2999999999999999889, -4.902439024389999567 ) ) ;
#63652=VECTOR ( 'NONE', #511, 999.9999999999998863 ) ;
#63658=CARTESIAN_POINT ( 'NONE',  ( 8.817462135714999150, 5.100000000000000533, 6.571291218949999902 ) ) ;
#63663=CARTESIAN_POINT ( 'NONE',  ( 10.69829221958999987, 2.534027248431999890, -6.667786804432999759 ) ) ;
#63666=CARTESIAN_POINT ( 'NONE',  ( 11.09999233421999953, -1.199999999999999956, -9.776630298829998011 ) ) ;
#63667=CARTESIAN_POINT ( 'NONE',  ( 8.971882233721794719, 5.348858080848509999, 7.441238387768498441 ) ) ;
#63674=B_SPLINE_CURVE_WITH_KNOTS ( 'NONE', 3,
 ( #62969, #15096, #15444, #9845, #25239, #20002, #9494, #62632, #14757 ),
 .UNSPECIFIED., .F., .F.,
 ( 4, 1, 1, 1, 1, 1, 4 ),
 ( 0.1253704142480318307, 0.1591342569109579497, 0.3260226980931646423, 0.4929111392759626398, 0.6597995804581695545, 0.8266880216409677740, 0.8746094594482839435 ),
 .UNSPECIFIED. ) ;
#63681=EDGE_CURVE ( 'NONE', #24788, #64129, #51731, .T. ) ;
#63688=CARTESIAN_POINT ( 'NONE',  ( 8.647284337624714823, 3.603316920592619876, -5.883498474299047487 ) ) ;
#63693=CARTESIAN_POINT ( 'NONE',  ( 9.766851002543001314, 2.832432432432000269, 6.822293592207000934 ) ) ;
#63695=CARTESIAN_POINT ( 'NONE',  ( 4.500000000000000000, 3.200000000000000178, 0.000000000000000000 ) ) ;
#63697=ADVANCED_FACE ( 'NONE', ( #20311 ), #62943, .T. ) ;
#63698=CIRCLE ( 'NONE', #45856, 13.10000000000000142 ) ;
#63700=CARTESIAN_POINT ( 'NONE',  ( 8.307195280408999238, 5.473983809665999622, -8.180077404516000072 ) ) ;
#63709=CARTESIAN_POINT ( 'NONE',  ( 8.696135841231001251, 3.038023536984999939, -5.861661709981000001 ) ) ;
#63716=CARTESIAN_POINT ( 'NONE',  ( 8.731095280410999138, 2.469361196073999842, -7.826019481986000059 ) ) ;
#63718=CARTESIAN_POINT ( 'NONE',  ( 10.16989991304999918, 2.594216849811000092, -6.291257009166999481 ) ) ;
#63719=EDGE_LOOP ( 'NONE', ( #45381, #50209, #38325, #49170 ) ) ;
#63730=DIRECTION ( 'NONE',  ( 0.000000000000000000, 0.9916377111174248249, 0.1290528957048032721 ) ) ;
#63732=CARTESIAN_POINT ( 'NONE',  ( 9.544414158773999901, 2.173570076733999823, -8.023168429484000441 ) ) ;
#63735=EDGE_CURVE ( 'NONE', #61638, #56759, #23240, .T. ) ;
#63736=EDGE_CURVE ( 'NONE', #14947, #60334, #65683, .T. ) ;
#63741=CARTESIAN_POINT ( 'NONE',  ( 7.924878289113897800, 5.349357204871084903, 7.500005630225526687 ) ) ;
#63743=CARTESIAN_POINT ( 'NONE',  ( 0.1499942179679999987, 1.384928887584815138, -2.402872127494067644 ) ) ;
#63747=CARTESIAN_POINT ( 'NONE',  ( 8.339548841713925853, 4.878437372552390627, -6.158507291990058086 ) ) ;
#63753=FACE_OUTER_BOUND ( 'NONE', #58548, .T. ) ;
#63758=ADVANCED_FACE ( 'NONE', ( #60642 ), #3879, .F. ) ;
#63760=CYLINDRICAL_SURFACE ( 'NONE', #27477, 0.5000000000000004441 ) ;
#63764=CARTESIAN_POINT ( 'NONE',  ( 7.000000000000000000, 8.491849194844679261, -4.464079820575392432 ) ) ;
#63770=CARTESIAN_POINT ( 'NONE',  ( 8.523148997455999520, 5.167567567567999731, -6.822293592207000934 ) ) ;
#63771=CARTESIAN_POINT ( 'NONE',  ( 1.800973465875000068, -3.500000000000000000, 0.000000000000000000 ) ) ;
#63773=CARTESIAN_POINT ( 'NONE',  ( 5.000000000000000000, 0.6769230769231000533, 2.665384615385000266 ) ) ;
#63785=CARTESIAN_POINT ( 'NONE',  ( 6.900019030169000089, 12.43894676821000012, 2.828897736577999922 ) ) ;
#63788=B_SPLINE_CURVE_WITH_KNOTS ( 'NONE', 3,
 ( #51181, #67930, #23914, #66557, #13441, #61323, #56072, #8182, #61662, #29531, #50833, #19356, #2929, #24257, #8525, #3277, #19015, #30207 ),
 .UNSPECIFIED., .F., .F.,
 ( 4, 2, 2, 2, 2, 2, 2, 2, 4 ),
 ( 0.000000000000000000, 0.1250000000000000000, 0.2500000000000000000, 0.3750000000000000000, 0.5000000000000000000, 0.6250000000000000000, 0.7500000000000000000, 0.8750000000000000000, 1.000000000000000000 ),
 .UNSPECIFIED. ) ;
#63792=CARTESIAN_POINT ( 'NONE',  ( 7.473345280404999791, 2.591432452475999515, -8.508584064833998539 ) ) ;
#63793=CARTESIAN_POINT ( 'NONE',  ( 9.934999999999998721, 4.640430492595999823, -9.117542781427999898 ) ) ;
#63794=CARTESIAN_POINT ( 'NONE',  ( 7.323364960633568899, 2.795155525963220366, -8.204923913533448854 ) ) ;
#63808=CARTESIAN_POINT ( 'NONE',  ( 9.365090231804463983, 2.650133164351947013, -7.500005474590564880 ) ) ;
#63811=CARTESIAN_POINT ( 'NONE',  ( 3.364061264882832969, -2.483906522064658784, -2.527484337399751091 ) ) ;
#63812=ORIENTED_EDGE ( 'NONE', *, *, #26356, .T. ) ;
#63813=CARTESIAN_POINT ( 'NONE',  ( 9.687870098586998324, 5.912263966150999472, 7.772301113561999486 ) ) ;
#63814=CARTESIAN_POINT ( 'NONE',  ( 10.34266415877000078, 5.750490533313000086, -8.094415907623000450 ) ) ;
#63816=CARTESIAN_POINT ( 'NONE',  ( 8.970860841232001448, 4.131080973160000447, -6.108642999115999395 ) ) ;
#63821=EDGE_CURVE ( 'NONE', #4653, #10847, #31515, .T. ) ;
#63828=CARTESIAN_POINT ( 'NONE',  ( 10.56491664109999995, 4.212242527248999835, 8.933458498617000032 ) ) ;
#63829=CARTESIAN_POINT ( 'NONE',  ( 9.688891943908508608, 2.651205815580220282, 7.263338752445344326 ) ) ;
#63840=CARTESIAN_POINT ( 'NONE',  ( 9.717214158771000143, 3.990126737362999609, -8.809457313313998839 ) ) ;
#63842=CARTESIAN_POINT ( 'NONE',  ( 10.98960529798009489, 6.634415940184054783, 5.386686141248282489 ) ) ;
#63843=ORIENTED_EDGE ( 'NONE', *, *, #39616, .F. ) ;
#63845=ADVANCED_FACE ( 'NONE', ( #36745 ), #37086, .F. ) ;
#63846=CARTESIAN_POINT ( 'NONE',  ( 0.4444555633787999893, -2.390579753276000030, 2.141564200098999837 ) ) ;
#63848=CARTESIAN_POINT ( 'NONE',  ( 10.69016084123000176, 4.391264627567999845, -8.802335896973000118 ) ) ;
#63854=CARTESIAN_POINT ( 'NONE',  ( 7.475045280409000625, 3.276311362504999991, 5.841989464160999290 ) ) ;
#63857=CARTESIAN_POINT ( 'NONE',  ( 7.259679719586999980, 3.516145570366999706, -5.836512876186000121 ) ) ;
#63861=CARTESIAN_POINT ( 'NONE',  ( 3.000973465876999757, 3.500000000000000000, 0.000000000000000000 ) ) ;
#63864=ADVANCED_FACE ( 'NONE', ( #58066 ), #19, .T. ) ;
#63870=CARTESIAN_POINT ( 'NONE',  ( 7.616545958352999968, 8.192027149378999340, 4.617357713344999226 ) ) ;
#63875=CARTESIAN_POINT ( 'NONE',  ( 7.833767219591000419, 2.583668273793999770, 6.684750595573999199 ) ) ;
#63876=VERTEX_POINT ( 'NONE', #41984 ) ;
#63877=CARTESIAN_POINT ( 'NONE',  ( 3.000973465876999757, 3.500000000000000000, 0.000000000000000000 ) ) ;
#63878=B_SPLINE_CURVE_WITH_KNOTS ( 'NONE', 3,
 ( #48585, #12561, #65342, #6964, #16753, #5921, #32852, #11171, #48234, #32507, #54163, #42989, #38434, #27956, #22351, #11508 ),
 .UNSPECIFIED., .F., .F.,
 ( 4, 2, 2, 2, 2, 2, 2, 4 ),
 ( 0.1254192006116268687, 0.2190632745348801147, 0.3127073484581333607, 0.4999954963046393530, 0.5936395702278924880, 0.6872836441511454009, 0.7809277180743985358, 0.8745717919976516708 ),
 .UNSPECIFIED. ) ;
#63884=CARTESIAN_POINT ( 'NONE',  ( 11.00774031427000033, 7.361568041487994485, -6.124472886188995879 ) ) ;
#63897=CARTESIAN_POINT ( 'NONE',  ( 4.900006121741999898, -1.007237960741797389, 1.747572776708516740 ) ) ;
#63898=CARTESIAN_POINT ( 'NONE',  ( 10.36630583688000051, 5.852743870412999705, -7.568014644338999730 ) ) ;
#63899=DIRECTION ( 'NONE',  ( 1.000000000000000000, 0.000000000000000000, 0.000000000000000000 ) ) ;
#63909=EDGE_CURVE ( 'NONE', #57343, #46556, #22345, .T. ) ;
#63910=CARTESIAN_POINT ( 'NONE',  ( 10.09197164456000095, 3.841384681542000301, 5.536408945990000774 ) ) ;
#63911=CARTESIAN_POINT ( 'NONE',  ( 2.050973465875999935, 3.500000000000000000, 0.000000000000000000 ) ) ;
#63917=CARTESIAN_POINT ( 'NONE',  ( 10.87521525736000072, 4.831064930369000088, 6.312796576761000367 ) ) ;
#63920=ORIENTED_EDGE ( 'NONE', *, *, #23066, .T. ) ;
#63921=CARTESIAN_POINT ( 'NONE',  ( 9.368660841232999914, 2.702406276695999754, -6.981052078638000147 ) ) ;
#63927=ORIENTED_EDGE ( 'NONE', *, *, #9861, .F. ) ;
#63931=CARTESIAN_POINT ( 'NONE',  ( 9.881820280408998514, 4.325866256860000369, -9.125812605905000652 ) ) ;
#63934=CARTESIAN_POINT ( 'NONE',  ( 3.400291169224110011, 0.03804497073930836887, 3.257691641818311279 ) ) ;
#63936=CARTESIAN_POINT ( 'NONE',  ( 10.70441484796999987, 3.444517850837000239, 6.009055070331999815 ) ) ;
#63941=VERTEX_POINT ( 'NONE', #47233 ) ;
#63942=CARTESIAN_POINT ( 'NONE',  ( 7.454676658771000497, 2.138190256467000339, 6.814770510101999967 ) ) ;
#63955=CARTESIAN_POINT ( 'NONE',  ( 8.424364158774000799, 3.292387953886000140, -6.294868737226000377 ) ) ;
#63962=FACE_OUTER_BOUND ( 'NONE', #7879, .T. ) ;
#63967=CARTESIAN_POINT ( 'NONE',  ( 10.34224945431000009, 3.348985101650000296, -8.881460768006000706 ) ) ;
#63971=CARTESIAN_POINT ( 'NONE',  ( 9.042739452581361803, 4.892140300096698979, 8.513365777369095611 ) ) ;
#63973=CARTESIAN_POINT ( 'NONE',  ( 8.881823341230997926, 4.977909614887999545, 6.416776202806000029 ) ) ;
#63974=ORIENTED_EDGE ( 'NONE', *, *, #9654, .F. ) ;
#63977=CARTESIAN_POINT ( 'NONE',  ( 10.98768472639999949, 5.139096889661000311, -4.945212061661000469 ) ) ;
#63983=CARTESIAN_POINT ( 'NONE',  ( 8.610944094208999644, 5.100000000000000533, -6.571291218949999902 ) ) ;
#63985=CARTESIAN_POINT ( 'NONE',  ( 8.158337976294000900E-06, 0.000000000000000000, 0.000000000000000000 ) ) ;
#63986=ADVANCED_FACE ( 'NONE', ( #27977 ), #33219, .F. ) ;
#63990=FACE_OUTER_BOUND ( 'NONE', #36915, .T. ) ;
#63996=CARTESIAN_POINT ( 'NONE',  ( 0.3595045405019000051, -1.072119470989999934, 3.198702759649999727 ) ) ;
#64000=CARTESIAN_POINT ( 'NONE',  ( 8.304135841228999837, 3.650414032626000171, 6.083147621602999600 ) ) ;
#64002=CARTESIAN_POINT ( 'NONE',  ( 7.577053541547003945, 3.182130936862002102, -6.424376193309997873 ) ) ;
#64003=CARTESIAN_POINT ( 'NONE',  ( 10.05462971959000029, 3.531217403581000003, -9.119235467071000301 ) ) ;
#64026=CARTESIAN_POINT ( 'NONE',  ( 10.11501430098066656, 5.350017391163124358, -7.499999134156894343 ) ) ;
#64034=CARTESIAN_POINT ( 'NONE',  ( 9.972410841228999345, 4.357364160690000432, -9.282962013144999247 ) ) ;
#64040=VERTEX_POINT ( 'NONE', #28673 ) ;
#64050=CARTESIAN_POINT ( 'NONE',  ( 8.780820280412001466, 2.567871051582000241, -6.869011921437000012 ) ) ;
#64052=CARTESIAN_POINT ( 'NONE',  ( 0.1431889841876702318, -0.3267341222390062194, -3.196183395200867139 ) ) ;
#64053=( LENGTH_UNIT ( ) NAMED_UNIT ( * ) SI_UNIT ( .MILLI., .METRE. ) );
#64061=DIRECTION ( 'NONE',  ( -1.000000000000000000, 0.000000000000000000, 0.000000000000000000 ) ) ;
#64062=EDGE_CURVE ( 'NONE', #15478, #57225, #59866, .T. ) ;
#64064=EDGE_CURVE ( 'NONE', #4640, #10323, #29058, .T. ) ;
#64072=CARTESIAN_POINT ( 'NONE',  ( 8.897989158775001073, 4.990139824845000405, -9.121472988377998803 ) ) ;
#64076=VERTEX_POINT ( 'NONE', #1398 ) ;
#64077=DIRECTION ( 'NONE',  ( 0.000000000000000000, 0.000000000000000000, -1.000000000000000000 ) ) ;
#64080=DIRECTION ( 'NONE',  ( -1.000000000000000000, 0.000000000000000000, 0.000000000000000000 ) ) ;
#64083=EDGE_CURVE ( 'NONE', #40232, #14053, #65711, .T. ) ;
#64090=B_SPLINE_CURVE_WITH_KNOTS ( 'NONE', 3,
 ( #17714, #33795, #28908, #65930, #45659, #39376, #34140, #66966, #23297, #12812, #7907, #61044, #61722, #40400, #44974, #66625, #19072, #2654 ),
 .UNSPECIFIED., .F., .F.,
 ( 4, 2, 2, 2, 2, 2, 2, 2, 4 ),
 ( 0.1254181127249429095, 0.2190640428433491271, 0.3127099729617552892, 0.4063559030801615068, 0.5000018331985677245, 0.5936477633169741086, 0.6872936934353806038, 0.7809396235537870989, 0.8745855536721935941 ),
 .UNSPECIFIED. ) ;
#64091=EDGE_CURVE ( 'NONE', #13916, #38357, #38457, .T. ) ;
#64101=CARTESIAN_POINT ( 'NONE',  ( 10.65896891525000001, 7.495473220363000344, -6.019650519997999716 ) ) ;
#64109=DIRECTION ( 'NONE',  ( 0.7071067811865709984, -0.7011937528853720014, -0.09125415560123631420 ) ) ;
#64111=CARTESIAN_POINT ( 'NONE',  ( 1.790556799208292027, -3.500000000000002220, 0.4581489286484968781 ) ) ;
#64112=ORIENTED_EDGE ( 'NONE', *, *, #38884, .T. ) ;
#64118=CARTESIAN_POINT ( 'NONE',  ( 7.613624210631964040, 5.119274190779043998, -8.282492918286559203 ) ) ;
#64121=AXIS2_PLACEMENT_3D ( 'NONE', #210, #64172, #58250 ) ;
#64124=ORIENTED_EDGE ( 'NONE', *, *, #65257, .T. ) ;
#64127=CARTESIAN_POINT ( 'NONE',  ( 9.170239158775000732, 4.769103072373000352, -8.666849124598000387 ) ) ;
#64129=VERTEX_POINT ( 'NONE', #12240 ) ;
#64131=CARTESIAN_POINT ( 'NONE',  ( 6.867785841228999821, 5.777496342847000754, -7.598381660561000395 ) ) ;
#64142=EDGE_LOOP ( 'NONE', ( #39275, #68700 ) ) ;
#64146=AXIS2_PLACEMENT_3D ( 'NONE', #61061, #65258, #34843 ) ;
#64151=B_SPLINE_CURVE_WITH_KNOTS ( 'NONE', 3,
 ( #19230, #1870, #61884, #17252, #23189, #28445 ),
 .UNSPECIFIED., .F., .F.,
 ( 4, 1, 1, 4 ),
 ( 0.000000000000000000, 0.3333333333333000081, 0.6666666666667000474, 1.000000000000000000 ),
 .UNSPECIFIED. ) ;
#64152=ORIENTED_EDGE ( 'NONE', *, *, #28809, .F. ) ;
#64155=EDGE_CURVE ( 'NONE', #57180, #13267, #59003, .T. ) ;
#64157=CARTESIAN_POINT ( 'NONE',  ( 10.89227882974000039, 3.998355201738000630, 9.261308739708001170 ) ) ;
#64158=CARTESIAN_POINT ( 'NONE',  ( 11.09991415876999987, 2.373387781209999936, -6.776601845694000481 ) ) ;
#64161=CARTESIAN_POINT ( 'NONE',  ( 9.418385841233000377, 3.251172436837000301, -6.320036569851000152 ) ) ;
#64162=CARTESIAN_POINT ( 'NONE',  ( 11.09999999999999964, 2.700688487044999864, -5.124965750789000296 ) ) ;
#64171=CARTESIAN_POINT ( 'NONE',  ( 10.65550720192000078, 4.237674045823999869, 9.105219676299999065 ) ) ;
#64172=DIRECTION ( 'NONE',  ( 1.000000000000000000, 0.000000000000000000, 0.000000000000000000 ) ) ;
#64180=DIRECTION ( 'NONE',  ( 0.000000000000000000, 1.000000000000000000, 0.000000000000000000 ) ) ;
#64190=CARTESIAN_POINT ( 'NONE',  ( 11.22023584123000006, 3.883089684441999978, -8.854806321849000739 ) ) ;
#64196=CARTESIAN_POINT ( 'NONE',  ( 7.346670280409000497, 2.374037589774999901, 8.293392681990997772 ) ) ;
#64199=CARTESIAN_POINT ( 'NONE',  ( 7.508304719586000431, 4.512523768570999572, -9.154878768564000069 ) ) ;
#64216=CIRCLE ( 'NONE', #43020, 0.5000000000000004441 ) ;
#64218=CARTESIAN_POINT ( 'NONE',  ( 8.822982780412001347, 2.678331728353000152, 8.735281589464001684 ) ) ;
#64226=DIRECTION ( 'NONE',  ( 0.000000000000000000, -1.000000000000000000, 0.000000000000000000 ) ) ;
#64227=CARTESIAN_POINT ( 'NONE',  ( 8.960616452296999768, 2.899999999999999911, 6.279946362737000243 ) ) ;
#64236=EDGE_LOOP ( 'NONE', ( #24960, #51819, #18942, #22637, #25339 ) ) ;
#64239=CARTESIAN_POINT ( 'NONE',  ( 4.900006121741999898, -1.599333684796359956, 1.229093439949830557 ) ) ;
#64240=EDGE_CURVE ( 'NONE', #13432, #51187, #58135, .T. ) ;
#64241=CARTESIAN_POINT ( 'NONE',  ( 10.91624242361999997, 5.459834480072999874, -8.642877574935999618 ) ) ;
#64244=DIRECTION ( 'NONE',  ( 0.000000000000000000, 0.000000000000000000, -1.000000000000000000 ) ) ;
#64245=CARTESIAN_POINT ( 'NONE',  ( 7.964620641636996901, 2.867893108869000507, -6.758951315555000505 ) ) ;
#64246=CARTESIAN_POINT ( 'NONE',  ( 10.00637913184999839, 5.119263020957999899, 8.420380450036001108 ) ) ;
#64249=CARTESIAN_POINT ( 'NONE',  ( 11.11845610223999969, 5.767025078915000158, 7.178418469370999588 ) ) ;
#64256=ADVANCED_FACE ( 'NONE', ( #16354 ), #42798, .F. ) ;
#64257=CARTESIAN_POINT ( 'NONE',  ( 10.94856425838729841, 4.366288724067763916, -9.227056792578350652 ) ) ;
#64260=( LENGTH_UNIT ( ) NAMED_UNIT ( * ) SI_UNIT ( .MILLI., .METRE. ) );
#64261=ORIENTED_EDGE ( 'NONE', *, *, #61315, .T. ) ;
#64262=CARTESIAN_POINT ( 'NONE',  ( 11.09999938828999966, 12.24999938819000000, 1.815300846655999940E-09 ) ) ;
#64268=CARTESIAN_POINT ( 'NONE',  ( 6.950045635439000336, -13.87069231928999891, -4.225386915259999654 ) ) ;
#64269=CARTESIAN_POINT ( 'NONE',  ( 8.758795280412000395, 3.977267228909999730, 9.308925224542001331 ) ) ;
#64270=CIRCLE ( 'NONE', #10686, 12.50000000000000178 ) ;
#64271=CARTESIAN_POINT ( 'NONE',  ( 9.202245280414000916, 5.095038542659000136, -6.157541456184000062 ) ) ;
#64275=CARTESIAN_POINT ( 'NONE',  ( 11.12915085989000019, 3.083869275439000024, 8.585995236726001067 ) ) ;
#64281=CARTESIAN_POINT ( 'NONE',  ( 8.957392219593000249, 2.678331728353000152, 8.735281589464001684 ) ) ;
#64286=CARTESIAN_POINT ( 'NONE',  ( 1.213972969267000046, 1.556166911672999920, -2.863499806755999799 ) ) ;
#64294=CARTESIAN_POINT ( 'NONE',  ( 9.807804719590000886, 3.988943694240999704, -8.966360307350999648 ) ) ;
#64300=VERTEX_POINT ( 'NONE', #57626 ) ;
#64306=CARTESIAN_POINT ( 'NONE',  ( 9.820199962102000413, 3.883325513302000154, 6.055618835924000187 ) ) ;
#64307=CARTESIAN_POINT ( 'NONE',  ( 11.05675868087999980, 2.811466576753000268, -4.847348033755999985 ) ) ;
#64313=CARTESIAN_POINT ( 'NONE',  ( 9.475899447075999404, 4.122021000979000149, 9.013569734175000292 ) ) ;
#64315=DIRECTION ( 'NONE',  ( 1.000000000000000000, 0.000000000000000000, 0.000000000000000000 ) ) ;
#64316=CARTESIAN_POINT ( 'NONE',  ( 9.260957905557225089, 2.777225843657625592, 6.918122793223488998 ) ) ;
#64319=CARTESIAN_POINT ( 'NONE',  ( 11.12439302932000018, 6.497997223551999824, 5.557915343071999636 ) ) ;
#64320=CARTESIAN_POINT ( 'NONE',  ( 10.96245900765000059, 7.417179809027999227, 6.111322237281999747 ) ) ;
#64322=DIRECTION ( 'NONE',  ( 1.000000000000000000, 0.000000000000000000, 0.000000000000000000 ) ) ;
#64334=CARTESIAN_POINT ( 'NONE',  ( 0.5323593903514999282, -3.136585174263000209, 0.6804425983637999442 ) ) ;
#64339=CARTESIAN_POINT ( 'NONE',  ( 7.533885841228999958, 4.623631324973000112, 8.651459902566999816 ) ) ;
#64342=CARTESIAN_POINT ( 'NONE',  ( 10.69016084123000176, 4.391264627567999845, -8.802335896973000118 ) ) ;
#64345=DIRECTION ( 'NONE',  ( -1.000000000000000000, 0.000000000000000000, 0.000000000000000000 ) ) ;
#64347=VERTEX_POINT ( 'NONE', #48175 ) ;
#64363=CARTESIAN_POINT ( 'NONE',  ( 8.314979508587148516, 2.649972834346558059, -7.499998738096613771 ) ) ;
#64374=ORIENTED_EDGE ( 'NONE', *, *, #4803, .T. ) ;
#64375=CARTESIAN_POINT ( 'NONE',  ( 7.355268297462892235, 3.356766528212881795, 9.118107836026387858 ) ) ;
#64392=CARTESIAN_POINT ( 'NONE',  ( 10.11453584122999949, 5.322769172805999816, -7.951018786192998178 ) ) ;
#64395=CARTESIAN_POINT ( 'NONE',  ( 9.973493989215999278, 4.344963986309999804, -9.321593970653999861 ) ) ;
#64401=B_SPLINE_CURVE_WITH_KNOTS ( 'NONE', 3,
 ( #44107, #33611, #39195, #54930 ),
 .UNSPECIFIED., .F., .F.,
 ( 4, 4 ),
 ( 0.8745714697001524263, 1.000000000000000000 ),
 .UNSPECIFIED. ) ;
#64405=EDGE_LOOP ( 'NONE', ( #49544, #26133, #7635, #9921, #50615, #52072, #19693, #4805, #25424 ) ) ;
#64412=CARTESIAN_POINT ( 'NONE',  ( 8.798539158775000146, 5.851083642416999631, -7.072167224702999633 ) ) ;
#64418=ADVANCED_FACE ( 'NONE', ( #44673 ), #53893, .T. ) ;
#64420=DIRECTION ( 'NONE',  ( 0.7071059447853028646, -0.7071076175868028502, 3.669598041139013828E-09 ) ) ;
#64421=DIRECTION ( 'NONE',  ( 0.000000000000000000, -1.000000000000000000, 0.000000000000000000 ) ) ;
#64422=DIRECTION ( 'NONE',  ( 0.000000000000000000, -1.000000000000000000, 0.000000000000000000 ) ) ;
#64426=CARTESIAN_POINT ( 'NONE',  ( 8.334999384030673752, 4.800016001909910734, -6.110656516449306075 ) ) ;
#64428=ORIENTED_EDGE ( 'NONE', *, *, #32833, .F. ) ;
#64429=VECTOR ( 'NONE', #16898, 1000.000000000000114 ) ;
#64445=LINE ( 'NONE', #15880, #65534 ) ;
#64447=CARTESIAN_POINT ( 'NONE',  ( 7.000000000000000000, 6.255435840762999966, -3.000000000000000000 ) ) ;
#64449=CARTESIAN_POINT ( 'NONE',  ( 10.90000000000000036, 2.899999999999999911, 6.414037451299000381 ) ) ;
#64450=B_SPLINE_CURVE_WITH_KNOTS ( 'NONE', 3,
 ( #2847, #11008, #24175, #53659, #6789, #61241, #66823, #59932, #32682, #40260 ),
 .UNSPECIFIED., .F., .F.,
 ( 4, 2, 2, 2, 4 ),
 ( 0.1844766778621776404, 0.3883575083966332442, 0.5922383389310887924, 0.7961191694655445072, 1.000000000000000000 ),
 .UNSPECIFIED. ) ;
#64451=ADVANCED_FACE ( 'NONE', ( #51952 ), #15250, .T. ) ;
#64459=EDGE_LOOP ( 'NONE', ( #58149, #45682, #30408, #27346 ) ) ;
#64463=ORIENTED_EDGE ( 'NONE', *, *, #22070, .T. ) ;
#64471=CARTESIAN_POINT ( 'NONE',  ( 9.441296348250521220, 5.329048545047487373, 7.778931234571383690 ) ) ;
#64477=ADVANCED_FACE ( 'NONE', ( #14820 ), #20065, .F. ) ;
#64480=ORIENTED_EDGE ( 'NONE', *, *, #61179, .T. ) ;
#64482=CARTESIAN_POINT ( 'NONE',  ( 5.000000000000000000, 0.000000000000000000, 0.000000000000000000 ) ) ;
#64489=VECTOR ( 'NONE', #56904, 999.9999999999998863 ) ;
#64494=CARTESIAN_POINT ( 'NONE',  ( 9.834151567923001380, 5.173929249342999803, 8.813048229486998508 ) ) ;
#64495=CARTESIAN_POINT ( 'NONE',  ( 10.60770165877000082, 2.392327800351000011, -6.587345916039000215 ) ) ;
#64498=CARTESIAN_POINT ( 'NONE',  ( 3.732263932199000322, -3.201230512442000187, 1.871170248239000022 ) ) ;
#64499=CARTESIAN_POINT ( 'NONE',  ( 11.09999999999999964, 4.000000000000000000, 7.500000000000000000 ) ) ;
#64502=ORIENTED_EDGE ( 'NONE', *, *, #34469, .T. ) ;
#64508=B_SPLINE_CURVE_WITH_KNOTS ( 'NONE', 3,
 ( #24170, #2500, #19265, #23482, #50746, #55301, #39565, #8096, #66819, #29786 ),
 .UNSPECIFIED., .F., .F.,
 ( 4, 2, 2, 2, 4 ),
 ( 0.4999999999999994449, 0.6249999999999996669, 0.7499999999999997780, 0.8750000000000000000, 1.000000000000000000 ),
 .UNSPECIFIED. ) ;
#64521=ORIENTED_EDGE ( 'NONE', *, *, #6692, .F. ) ;
#64523=CARTESIAN_POINT ( 'NONE',  ( 8.672989158774999652, 4.728328492779000136, -8.692725459657999920 ) ) ;
#64524=CARTESIAN_POINT ( 'NONE',  ( 9.266851002542999538, 2.832432432432000269, 6.822293592207000934 ) ) ;
#64526=VECTOR ( 'NONE', #35089, 1000.000000000000114 ) ;
#64527=CARTESIAN_POINT ( 'NONE',  ( 0.7490331185628000821, -2.413104819777999843, -2.586865767356999690 ) ) ;
#64529=CARTESIAN_POINT ( 'NONE',  ( 2.218610394918000051, -2.772870583375000031, 2.537629777733000136 ) ) ;
#64533=AXIS2_PLACEMENT_3D ( 'NONE', #12986, #2146, #23465 ) ;
#64537=CARTESIAN_POINT ( 'NONE',  ( 9.208107780409999776, 5.057081813675999626, 8.967637988488998957 ) ) ;
#64538=ORIENTED_EDGE ( 'NONE', *, *, #54147, .T. ) ;
#64541=EDGE_CURVE ( 'NONE', #866, #19742, #42423, .T. ) ;
#64542=CARTESIAN_POINT ( 'NONE',  ( 8.245320280407000268, 2.435784185744999775, -7.548665584409000040 ) ) ;
#64547=ORIENTED_EDGE ( 'NONE', *, *, #55055, .T. ) ;
#64548=CARTESIAN_POINT ( 'NONE',  ( 2.948890132543457998, 2.798833948393634863, -2.150913519912196925 ) ) ;
#64561=CARTESIAN_POINT ( 'NONE',  ( 8.668204719592999652, 3.979464555644999901, 9.134076336209998814 ) ) ;
#64585=CARTESIAN_POINT ( 'NONE',  ( 9.693589158772999426, 4.047146749018000200, -5.600703114891000034 ) ) ;
#64586=CARTESIAN_POINT ( 'NONE',  ( 10.20918109782000016, 3.334760637131999772, -5.769467581755999497 ) ) ;
#64592=ORIENTED_EDGE ( 'NONE', *, *, #68078, .F. ) ;
#64593=CARTESIAN_POINT ( 'NONE',  ( 1.877754220768333537, -2.003492624900453212, -2.889646723249190696 ) ) ;
#64594=CARTESIAN_POINT ( 'NONE',  ( 9.414312736919001168, 3.941041961981000430, 5.878350450964999752 ) ) ;
#64595=CARTESIAN_POINT ( 'NONE',  ( 2.186390132542666898, -0.4581489286485234680, 3.499999999999998668 ) ) ;
#64598=B_SPLINE_CURVE_WITH_KNOTS ( 'NONE', 3,
 ( #69182, #33170, #11148, #58696, #10801, #38057, #32482, #21294, #60083, #43314, #53796, #5893, #53460, #5554, #22320, #48558, #49238, #33517, #1347, #16727, #22665, #44008, #17429, #5214, #663, #59381, #38757, #32822, #54138, #26551, #63934, #7283, #13235, #55178, #40467 ),
 .UNSPECIFIED., .F., .F.,
 ( 4, 1, 1, 1, 1, 1, 1, 1, 1, 1, 1, 1, 1, 1, 1, 1, 1, 1, 1, 1, 1, 1, 1, 1, 1, 1, 1, 1, 1, 1, 1, 1, 4 ),
 ( 0.000000000000000000, 0.01250316081579585549, 0.04500295842620007786, 0.07750275603660429502, 0.1100025536470085330, 0.1425023512574696283, 0.1750021488678738524, 0.2075019464782780765, 0.2400017440886822728, 0.2725015416990865802, 0.3050013393094908043, 0.3375011369198949729, 0.3700009345302991970, 0.4025007321407034766, 0.4350005297511077007, 0.4675003273615118693, 0.5000001249719160379, 0.5324999225823202620, 0.5649997201927245971, 0.5974995178031287102, 0.6299993154135330453, 0.6624991130239372694, 0.6949989106343413825, 0.7274987082447457176, 0.7599985058551499417, 0.7924983034655541658, 0.8249981010759582789, 0.8574978986863625030, 0.8899976962967667271, 0.9224974939071709512, 0.9549972915175752863, 0.9874970891279795104, 1.000000000000000000 ),
 .UNSPECIFIED. ) ;
#64601=CARTESIAN_POINT ( 'NONE',  ( 10.26001294666571795, 5.278409861158100291, 8.694118350725130284 ) ) ;
#64602=ADVANCED_FACE ( 'NONE', ( #3968 ), #46643, .T. ) ;
#64603=ADVANCED_FACE ( 'NONE', ( #9914 ), #52217, .F. ) ;
#64606=B_SPLINE_CURVE_WITH_KNOTS ( 'NONE', 3,
 ( #15098, #42366, #63667, #21369, #15784, #37114, #48636, #26970, #32900, #22743 ),
 .UNSPECIFIED., .F., .F.,
 ( 4, 2, 2, 2, 4 ),
 ( 0.7044197654457721169, 0.7413672947650503664, 0.7783148240843286159, 0.8522098827228861140, 1.000000000000000000 ),
 .UNSPECIFIED. ) ;
#64607=CARTESIAN_POINT ( 'NONE',  ( 2.250973465874000379, -3.500000000000000000, 0.000000000000000000 ) ) ;
#64612=CARTESIAN_POINT ( 'NONE',  ( 10.76874784332534141, 4.963431926995326648, 4.838413582109893696 ) ) ;
#64616=CARTESIAN_POINT ( 'NONE',  ( 8.154704719592000828, 4.255646040929000229, 9.114085578076998928 ) ) ;
#64617=CARTESIAN_POINT ( 'NONE',  ( 9.798945280410000791, 5.639765292528999829, -8.059103558718000215 ) ) ;
#64619=CARTESIAN_POINT ( 'NONE',  ( 10.83325145537689593, 2.985356913319267669, 4.869878758720406431 ) ) ;
#64621=CARTESIAN_POINT ( 'NONE',  ( 9.778460659405999067, 5.743717947473999885, 7.748300625457000379 ) ) ;
#64630=ADVANCED_FACE ( 'NONE', ( #29470 ), #66845, .T. ) ;
#64634=LINE ( 'NONE', #53808, #61605 ) ;
#64644=CARTESIAN_POINT ( 'NONE',  ( 9.310554719594000161, 3.934138271021000222, -9.063586117809000697 ) ) ;
#64648=CARTESIAN_POINT ( 'NONE',  ( 7.949316606270907748, 4.924545613133609834, -6.408127913758977279 ) ) ;
#64658=CARTESIAN_POINT ( 'NONE',  ( 11.04798050650000008, 2.753316326401999969, -5.092742990910999801 ) ) ;
#64659=CARTESIAN_POINT ( 'NONE',  ( 7.758693699415004197, 5.085317049932003286, 6.543835681441004581 ) ) ;
#64660=CARTESIAN_POINT ( 'NONE',  ( 5.000000000000000000, -1.199999999999999956, -9.776630298829998011 ) ) ;
#64665=CARTESIAN_POINT ( 'NONE',  ( 8.277732780410000046, 4.874567052833000069, 6.119507471270999588 ) ) ;
#64670=CARTESIAN_POINT ( 'NONE',  ( 7.921841810112000282, 2.875629839593000003, -6.725486766668000271 ) ) ;
#64674=CARTESIAN_POINT ( 'NONE',  ( 10.97914836376999936, 9.415954400956000114, 6.236115164281000212 ) ) ;
#64680=CARTESIAN_POINT ( 'NONE',  ( 10.12671450658999994, 3.117528978489000124, 8.613535509676999880 ) ) ;
#64686=CARTESIAN_POINT ( 'NONE',  ( 9.176357780411999343, 2.935741164366000522, 6.259844213126999790 ) ) ;
#64692=CARTESIAN_POINT ( 'NONE',  ( 10.72802334123000101, 3.751278653658999929, -8.836901076820000256 ) ) ;
#64693=PLANE ( 'NONE',  #37192 ) ;
#64696=DIRECTION ( 'NONE',  ( 1.000000000000000000, 0.000000000000000000, 0.000000000000000000 ) ) ;
#64703=PLANE ( 'NONE',  #9646 ) ;
#64704=DIRECTION ( 'NONE',  ( 0.7071067811865475727, 0.7071067811865475727, 0.000000000000000000 ) ) ;
#64708=CARTESIAN_POINT ( 'NONE',  ( 0.000000000000000000, 0.000000000000000000, 0.000000000000000000 ) ) ;
#64717=CARTESIAN_POINT ( 'NONE',  ( 3.500000000000000000, 3.499738125128000199, -0.04281419768536000314 ) ) ;
#64718=DIRECTION ( 'NONE',  ( 0.000000000000000000, 0.000000000000000000, 1.000000000000000000 ) ) ;
#64722=CARTESIAN_POINT ( 'NONE',  ( 7.412220152880141022, 2.451433362863415510, 8.294844223128800209 ) ) ;
#64724=EDGE_LOOP ( 'NONE', ( #22239, #59356, #419, #51264, #32177, #27802, #35500, #25498 ) ) ;
#64730=EDGE_CURVE ( 'NONE', #523, #58875, #49711, .T. ) ;
#64739=ORIENTED_EDGE ( 'NONE', *, *, #51300, .T. ) ;
#64753=VERTEX_POINT ( 'NONE', #61265 ) ;
#64754=CARTESIAN_POINT ( 'NONE',  ( 6.945228317543000074, 4.037115771921000018, -6.023232697733999608 ) ) ;
#64756=DIRECTION ( 'NONE',  ( -1.000000000000000000, 0.000000000000000000, 0.000000000000000000 ) ) ;
#64758=CARTESIAN_POINT ( 'NONE',  ( 9.187479719595000205, 2.391443348526999912, -6.856688371964000162 ) ) ;
#64764=CARTESIAN_POINT ( 'NONE',  ( 8.210775250489261268, 3.646521065535271333, -8.815119237327296631 ) ) ;
#64765=FACE_OUTER_BOUND ( 'NONE', #9376, .T. ) ;
#64778=VECTOR ( 'NONE', #37166, 1000.000000000000114 ) ;
#64791=CARTESIAN_POINT ( 'NONE',  ( 6.999999999999999112, 8.351195738565051485, -4.351195741810073514 ) ) ;
#64813=CARTESIAN_POINT ( 'NONE',  ( 8.672989158774999652, 4.728328492779000136, -8.692725459657999920 ) ) ;
#64817=CARTESIAN_POINT ( 'NONE',  ( 8.110910841226001367, 2.101036793381999779, -7.559080181511999896 ) ) ;
#64820=CARTESIAN_POINT ( 'NONE',  ( 9.454578519446510398, 5.254263437105202605, 7.998700540161328476 ) ) ;
#64821=EDGE_LOOP ( 'NONE', ( #21590, #3116, #22401 ) ) ;
#64822=CARTESIAN_POINT ( 'NONE',  ( 0.000000000000000000, 0.000000000000000000, 0.000000000000000000 ) ) ;
#64826=PLANE ( 'NONE',  #44302 ) ;
#64840=CARTESIAN_POINT ( 'NONE',  ( 9.888314158772001150, 5.105193280231000053, -8.895607399415000671 ) ) ;
#64849=CARTESIAN_POINT ( 'NONE',  ( 9.854942824136999846, 2.800308224477999985, 9.013816726157999781 ) ) ;
#64851=EDGE_CURVE ( 'NONE', #68916, #5127, #13937, .T. ) ;
#64853=ADVANCED_FACE ( 'NONE', ( #28395 ), #13010, .F. ) ;
#64857=CARTESIAN_POINT ( 'NONE',  ( 27.64127793187000037, 5.599999999999999645, -6.571291218949999902 ) ) ;
#64858=CARTESIAN_POINT ( 'NONE',  ( 8.739649184022093564, 2.648220570447237243, 7.263719241076208810 ) ) ;
#64862=CARTESIAN_POINT ( 'NONE',  ( 8.649445371194000032, 5.100000000000000533, -6.459601070175000181 ) ) ;
#64868=CARTESIAN_POINT ( 'NONE',  ( 9.170239158775000732, 4.769103072373000352, -8.666849124598000387 ) ) ;
#64872=FACE_OUTER_BOUND ( 'NONE', #33447, .T. ) ;
#64874=CARTESIAN_POINT ( 'NONE',  ( 0.4694343787449999916, 2.854424451075999958, -2.356853325602000115 ) ) ;
#64876=CARTESIAN_POINT ( 'NONE',  ( 2.933839636531999862, 1.438508091966000046, -3.472617419920999815 ) ) ;
#64883=CARTESIAN_POINT ( 'NONE',  ( 9.272295280408998863, 3.705846972803000128, 9.096435887808000942 ) ) ;
#64886=CARTESIAN_POINT ( 'NONE',  ( 7.607754719585000380, 2.591432452475999515, -8.508584064833998539 ) ) ;
#64893=VERTEX_POINT ( 'NONE', #45168 ) ;
#64894=CARTESIAN_POINT ( 'NONE',  ( 11.10000000000000320, 2.288692731476340114, -7.672306050762143670 ) ) ;
#64896=CONICAL_SURFACE ( 'NONE', #31433, 12.44999944941000081, 0.7853981146832407223 ) ;
#64906=DIRECTION ( 'NONE',  ( 1.000000000000000000, 0.000000000000000000, 0.000000000000000000 ) ) ;
#64910=CARTESIAN_POINT ( 'NONE',  ( 11.12341687003999979, 6.064977932649999737, -5.276126571066000359 ) ) ;
#64911=ORIENTED_EDGE ( 'NONE', *, *, #32770, .F. ) ;
#64914=CARTESIAN_POINT ( 'NONE',  ( 7.739722165042043578, 4.561671897555351407, -5.729814629414840432 ) ) ;
#64922=ORIENTED_EDGE ( 'NONE', *, *, #20430, .F. ) ;
#64924=CARTESIAN_POINT ( 'NONE',  ( 9.047164158776000775, 2.156584729807999867, -7.959751745006000689 ) ) ;
#64925=CARTESIAN_POINT ( 'NONE',  ( 9.933148997456999751, 5.167567567567999731, 6.822293592207000934 ) ) ;
#64927=DIRECTION ( 'NONE',  ( -0.7071067811865159314, -0.5062022020404108869, 0.4937198908789108831 ) ) ;
#64930=VECTOR ( 'NONE', #31503, 1000.000000000000227 ) ;
#64932=CARTESIAN_POINT ( 'NONE',  ( 1.969891126640333390, 1.842658540278710566, -2.994770506591986070 ) ) ;
#64934=CARTESIAN_POINT ( 'NONE',  ( 9.256664404737000140, 4.025830366070999311, 9.295863330698999505 ) ) ;
#64935=EDGE_CURVE ( 'NONE', #23807, #33299, #60721, .T. ) ;
#64936=CARTESIAN_POINT ( 'NONE',  ( 2.196806799209333416, -0.9161175952574931447, 3.408904368339101598 ) ) ;
#64940=CARTESIAN_POINT ( 'NONE',  ( 10.22737811154219223, 5.662262400723353295, 8.092495838525170626 ) ) ;
#64943=CARTESIAN_POINT ( 'NONE',  ( 5.000000000000000000, -11.35000000000000142, 0.000000000000000000 ) ) ;
#64946=CARTESIAN_POINT ( 'NONE',  ( 9.769471092180999960, 5.100000000000000533, -6.152188490330000370 ) ) ;
#64950=CARTESIAN_POINT ( 'NONE',  ( 10.73994861681368285, 4.937004252026683915, 4.824365178933474496 ) ) ;
#64956=CARTESIAN_POINT ( 'NONE',  ( 8.977760841230999489, 2.019067547072999957, 7.390982789861999969 ) ) ;
#64957=CARTESIAN_POINT ( 'NONE',  ( 8.514954719592999766, 3.207599814920999659, -6.150466394809999571 ) ) ;
#64961=CARTESIAN_POINT ( 'NONE',  ( 9.260906466624998501, 4.901388651757999426, 9.090324495507999814 ) ) ;
#64965=CARTESIAN_POINT ( 'NONE',  ( 7.761763193589995780, 2.840593260277998411, 6.815714094171000603 ) ) ;
#64973=ORIENTED_EDGE ( 'NONE', *, *, #48179, .T. ) ;
#64975=DIRECTION ( 'NONE',  ( 0.000000000000000000, 0.000000000000000000, -1.000000000000000000 ) ) ;
#64977=CARTESIAN_POINT ( 'NONE',  ( 8.332048273611004419, 2.867478057767001154, 6.314276212112998721 ) ) ;
#64980=CARTESIAN_POINT ( 'NONE',  ( 8.971339158776000744, 4.082930418187999955, -6.104944817728999773 ) ) ;
#64984=DIRECTION ( 'NONE',  ( -1.000000000000000000, 0.000000000000000000, 0.000000000000000000 ) ) ;
#64986=ORIENTED_EDGE ( 'NONE', *, *, #2792, .F. ) ;
#65002=CARTESIAN_POINT ( 'NONE',  ( 7.711426658771000753, 5.797099724369999763, 8.340484548805999765 ) ) ;
#65005=DIRECTION ( 'NONE',  ( 1.000000000000000000, 0.000000000000000000, 2.714292073215000052E-14 ) ) ;
#65008=CARTESIAN_POINT ( 'NONE',  ( 11.12487850024999858, 5.426340361321000394, 5.164841153873000579 ) ) ;
#65009=B_SPLINE_CURVE_WITH_KNOTS ( 'NONE', 3,
 ( #34648, #45129, #66093, #13324, #18211, #60858, #8065, #50717, #34297, #55620 ),
 .UNSPECIFIED., .F., .F.,
 ( 4, 2, 2, 2, 4 ),
 ( 0.000000000000000000, 0.1250000000000003053, 0.2500000000000006106, 0.3750000000000009437, 0.5000000000000011102 ),
 .UNSPECIFIED. ) ;
#65010=CARTESIAN_POINT ( 'NONE',  ( 11.01763844555000027, 7.435008031470999867, 6.253913913716999673 ) ) ;
#65021=CIRCLE ( 'NONE', #54964, 12.39999890530000037 ) ;
#65025=CARTESIAN_POINT ( 'NONE',  ( 9.368920280410000245, 5.618384167307999277, 7.727742442702000503 ) ) ;
#65026=CARTESIAN_POINT ( 'NONE',  ( 9.939321360490000146, 2.638097915594000309, 6.328629954376999933 ) ) ;
#65028=ORIENTED_EDGE ( 'NONE', *, *, #24999, .F. ) ;
#65031=CARTESIAN_POINT ( 'NONE',  ( 11.04968150330033438, 2.750318496699665438, -6.534572094925334085 ) ) ;
#65037=ORIENTED_EDGE ( 'NONE', *, *, #32992, .F. ) ;
#65038=VECTOR ( 'NONE', #50043, 1000.000000000000000 ) ;
#65039=CARTESIAN_POINT ( 'NONE',  ( 2.116066937563999772, -3.284887521161000024, -0.9717780471415999877 ) ) ;
#65048=DIRECTION ( 'NONE',  ( 1.000000000000000000, 0.000000000000000000, 0.000000000000000000 ) ) ;
#65049=CARTESIAN_POINT ( 'NONE',  ( 9.856851002545999663, 2.832432432432000269, -6.822293592207000934 ) ) ;
#65050=CARTESIAN_POINT ( 'NONE',  ( 10.89999960551999969, -1.382741157691000033, 11.26545764026000107 ) ) ;
#65051=CARTESIAN_POINT ( 'NONE',  ( 1.080473797070000019, 3.196468001211000054, -1.639036658905000055 ) ) ;
#65054=CARTESIAN_POINT ( 'NONE',  ( 11.12915085989000019, 3.083869275439000024, 8.585995236726001067 ) ) ;
#65062=FACE_OUTER_BOUND ( 'NONE', #9613, .T. ) ;
#65072=CARTESIAN_POINT ( 'NONE',  ( 8.424688440789140031, 5.350083765069828523, 7.500019236172019710 ) ) ;
#65076=CARTESIAN_POINT ( 'NONE',  ( 3.250973465878000290, -3.500000000000000000, 0.000000000000000000 ) ) ;
#65077=CARTESIAN_POINT ( 'NONE',  ( 11.09999999999999964, 10.03015638309000046, -5.726993439934999763 ) ) ;
#65078=DIRECTION ( 'NONE',  ( 1.000000000000000000, 0.000000000000000000, 0.000000000000000000 ) ) ;
#65082=CARTESIAN_POINT ( 'NONE',  ( 10.01508584123000034, 4.845406482350000488, -6.387189183984999907 ) ) ;
#65084=VECTOR ( 'NONE', #28743, 1000.000000000000000 ) ;
#65090=VECTOR ( 'NONE', #65005, 1000.000000000000000 ) ;
#65091=CARTESIAN_POINT ( 'NONE',  ( 7.971709343838234041, 4.577294333992332653, -6.273541878819468565 ) ) ;
#65095=CARTESIAN_POINT ( 'NONE',  ( 10.06577346837133291, 5.100000000000000533, 6.304440313804915874 ) ) ;
#65098=CARTESIAN_POINT ( 'NONE',  ( 10.96132811691999898, 2.899462099209999977, 4.932355079819999766 ) ) ;
#65100=CARTESIAN_POINT ( 'NONE',  ( 10.71093936573047145, 4.907409303783653698, -4.810214324746542758 ) ) ;
#65104=CARTESIAN_POINT ( 'NONE',  ( 8.988579719593998263, 4.902869380824999901, -8.978557145469999057 ) ) ;
#65114=B_SPLINE_CURVE_WITH_KNOTS ( 'NONE', 3,
 ( #7132, #1542, #60620, #55727 ),
 .UNSPECIFIED., .F., .F.,
 ( 4, 4 ),
 ( 0.7545333173052201081, 1.000000000000000000 ),
 .UNSPECIFIED. ) ;
#65120=CARTESIAN_POINT ( 'NONE',  ( 10.90000000000000036, 2.778483479159999714, -6.925197956411000000 ) ) ;
#65124=EDGE_CURVE ( 'NONE', #55522, #23367, #26088, .T. ) ;
#65134=LINE ( 'NONE', #49412, #59989 ) ;
#65142=CARTESIAN_POINT ( 'NONE',  ( 10.96985954691664844, 5.113501917432773602, 4.936516852154429813 ) ) ;
#65144=CARTESIAN_POINT ( 'NONE',  ( 0.9988901325417289812, 2.798833948393634419, -2.150913519912196925 ) ) ;
#65151=CARTESIAN_POINT ( 'NONE',  ( 10.62120626703515214, 3.646797508062010529, 8.848526273074872606 ) ) ;
#65156=ORIENTED_EDGE ( 'NONE', *, *, #40205, .F. ) ;
#65159=CARTESIAN_POINT ( 'NONE',  ( 9.708354719591000048, 5.481267232667000222, -8.005061172455999241 ) ) ;
#65160=ADVANCED_FACE ( 'NONE', ( #22025 ), #885, .F. ) ;
#65164=CARTESIAN_POINT ( 'NONE',  ( 7.862285841224999849, 5.899700469177000528, -7.473738753146999869 ) ) ;
#65169=DIRECTION ( 'NONE',  ( 0.000000000000000000, -1.000000000000000000, 0.000000000000000000 ) ) ;
#65170=VECTOR ( 'NONE', #56104, 1000.000000000000000 ) ;
#65174=AXIS2_PLACEMENT_3D ( 'NONE', #25391, #25742, #4403 ) ;
#65183=DIRECTION ( 'NONE',  ( 1.000000000000000000, 0.000000000000000000, 0.000000000000000000 ) ) ;
#65188=CARTESIAN_POINT ( 'NONE',  ( 10.63743278041000018, 3.721476136598000028, -8.997092462634000753 ) ) ;
#65198=ORIENTED_EDGE ( 'NONE', *, *, #21019, .F. ) ;
#65199=CARTESIAN_POINT ( 'NONE',  ( 10.02201554968999986, 3.298015135926000152, 5.700522662207000657 ) ) ;
#65202=B_SPLINE_CURVE_WITH_KNOTS ( 'NONE', 3,
 ( #20103, #20444, #151, #26733, #47367, #21469, #37548, #58531, #63427, #20790, #69024, #10986, #41771, #5397, #36183, #31982, #14860, #42120 ),
 .UNSPECIFIED., .F., .F.,
 ( 4, 2, 2, 2, 2, 2, 2, 2, 4 ),
 ( 0.1254150264828375605, 0.2190616449219018325, 0.3127082633609661322, 0.4063548818000304319, 0.5000015002390947316, 0.5936481186781590313, 0.6872947371172232200, 0.7809413555562875198, 0.8745879739953518195 ),
 .UNSPECIFIED. ) ;
#65222=CARTESIAN_POINT ( 'NONE',  ( 8.307195280408999238, 5.473983809665999622, -8.180077404516000072 ) ) ;
#65226=B_SPLINE_CURVE_WITH_KNOTS ( 'NONE', 3,
 ( #41739, #52226, #10606, #4324 ),
 .UNSPECIFIED., .F., .F.,
 ( 4, 4 ),
 ( 0.000000000000000000, 1.000000000000000000 ),
 .UNSPECIFIED. ) ;
#65227=CARTESIAN_POINT ( 'NONE',  ( 0.5433723959866999520, 0.6801881511091000254, 3.471639432493999866 ) ) ;
#65229=CARTESIAN_POINT ( 'NONE',  ( 9.401555021597628681, 2.569600868085949674, 8.509762776563993825 ) ) ;
#65230=CARTESIAN_POINT ( 'NONE',  ( 2.547610702941999872, 2.269953836787999890, -2.784090233961999949 ) ) ;
#65233=FACE_OUTER_BOUND ( 'NONE', #47273, .T. ) ;
#65236=CARTESIAN_POINT ( 'NONE',  ( 7.191892219589999691, 3.501518846194999757, 9.055971388486000251 ) ) ;
#65239=CARTESIAN_POINT ( 'NONE',  ( 7.101645280409999650, 4.411055010497999973, -9.010057343561001630 ) ) ;
#65241=CARTESIAN_POINT ( 'NONE',  ( 9.576488281553999116, 4.593976206186999534, 5.662041230125000268 ) ) ;
#65254=FACE_OUTER_BOUND ( 'NONE', #63083, .T. ) ;
#65257=EDGE_CURVE ( 'NONE', #10305, #39016, #48906, .T. ) ;
#65258=DIRECTION ( 'NONE',  ( 1.000000000000000000, 0.000000000000000000, 0.000000000000000000 ) ) ;
#65260=CARTESIAN_POINT ( 'NONE',  ( 8.385051658773999606, 4.977909614887999545, 6.416776202806000029 ) ) ;
#65266=VERTEX_POINT ( 'NONE', #1402 ) ;
#65269=CARTESIAN_POINT ( 'NONE',  ( 7.590547165042061728, 2.142854238949568835, -7.493582139438092149 ) ) ;
#65270=CARTESIAN_POINT ( 'NONE',  ( 5.000030787343000327, 1.834918991542629385, 1.057581170753186806 ) ) ;
#65271=FACE_OUTER_BOUND ( 'NONE', #54145, .T. ) ;
#65275=ORIENTED_EDGE ( 'NONE', *, *, #6773, .T. ) ;
#65282=CARTESIAN_POINT ( 'NONE',  ( 2.545075687104000117, -2.780561538855000236, 1.920602712081999952 ) ) ;
#65289=CARTESIAN_POINT ( 'NONE',  ( 1.900788447236333445, -1.095349359437870485, -3.341294758621923044 ) ) ;
#65290=CARTESIAN_POINT ( 'NONE',  ( 10.49785886974000171, 3.776281431161999880, 5.717632172928999168 ) ) ;
#65296=CARTESIAN_POINT ( 'NONE',  ( 7.100000000000139977, 3.928301696086603734, -8.885577256977402527 ) ) ;
#65311=CARTESIAN_POINT ( 'NONE',  ( 7.320267219589999819, 2.466388272391000225, 6.935562100014999842 ) ) ;
#65312=CARTESIAN_POINT ( 'NONE',  ( 8.605545280412000508, 3.122811675949999977, -6.006064052396999919 ) ) ;
#65315=CARTESIAN_POINT ( 'NONE',  ( 11.00588826681000043, 3.012760565655999923, 5.961496895743000124 ) ) ;
#65319=CARTESIAN_POINT ( 'NONE',  ( 7.545207810761997536, 3.529659010889000026, 6.570477302111996210 ) ) ;
#65333=CARTESIAN_POINT ( 'NONE',  ( 7.581295643773000137, 2.929975047062999050, 6.543750339501001712 ) ) ;
#65335=ORIENTED_EDGE ( 'NONE', *, *, #62988, .T. ) ;
#65336=CARTESIAN_POINT ( 'NONE',  ( 9.120514158775000269, 5.306366356490000769, -7.996450761531000317 ) ) ;
#65341=B_SPLINE_CURVE_WITH_KNOTS ( 'NONE', 3,
 ( #9003, #19846, #29672, #18824 ),
 .UNSPECIFIED., .F., .F.,
 ( 4, 4 ),
 ( 0.000000000000000000, 0.1253320266324779719 ),
 .UNSPECIFIED. ) ;
#65342=CARTESIAN_POINT ( 'NONE',  ( 9.294016886149316647, 2.684778767696973212, -7.853313980369418523 ) ) ;
#65343=CARTESIAN_POINT ( 'NONE',  ( 10.90000053908999966, 9.856474340180000127, -5.627824942316999923 ) ) ;
#65344=VERTEX_POINT ( 'NONE', #3124 ) ;
#65352=CARTESIAN_POINT ( 'NONE',  ( 11.05576032679999976, 2.800783223368999764, -4.875271127325000009 ) ) ;
#65359=CARTESIAN_POINT ( 'NONE',  ( 7.454676658771000497, 2.138190256467000339, 6.814770510101999967 ) ) ;
#65363=CARTESIAN_POINT ( 'NONE',  ( 4.500000000000000000, 3.200000000000000178, 0.000000000000000000 ) ) ;
#65371=VERTEX_POINT ( 'NONE', #56269 ) ;
#65379=VECTOR ( 'NONE', #35401, 1000.000000000000000 ) ;
#65380=CARTESIAN_POINT ( 'NONE',  ( 9.331135841230999262, 4.141907758973999876, 6.047574021139999978 ) ) ;
#65381=CARTESIAN_POINT ( 'NONE',  ( 9.657553581808000942, 5.333455947841000189, 6.049916795084000043 ) ) ;
#65384=FACE_OUTER_BOUND ( 'NONE', #22125, .T. ) ;
#65387=CARTESIAN_POINT ( 'NONE',  ( 8.166615904750996080, 4.665939084510003276, 6.165875187757999143 ) ) ;
#65391=ORIENTED_EDGE ( 'NONE', *, *, #34745, .T. ) ;
#65394=CARTESIAN_POINT ( 'NONE',  ( 2.025476376744999918, -3.125150066150999884, -0.9245224406458000255 ) ) ;
#65396=CIRCLE ( 'NONE', #8471, 1.500000000000000000 ) ;
#65401=CARTESIAN_POINT ( 'NONE',  ( 11.05568736508000072, 2.800099964430999844, 4.877315660663000152 ) ) ;
#65405=CARTESIAN_POINT ( 'NONE',  ( 7.562916666663876519, 5.079550237237543620, -6.670361928033864629 ) ) ;
#65410=CARTESIAN_POINT ( 'NONE',  ( 1.980140132539667253, 3.408904368339106927, -0.9161175952574746040 ) ) ;
#65412=CARTESIAN_POINT ( 'NONE',  ( 9.736878146978000359, 2.742182981761000171, 6.839230404018000087 ) ) ;
#65414=B_SPLINE_CURVE_WITH_KNOTS ( 'NONE', 3,
 ( #44957, #18382, #60336, #34809 ),
 .UNSPECIFIED., .F., .F.,
 ( 4, 4 ),
 ( 0.000000000000000000, 1.000000000000000000 ),
 .UNSPECIFIED. ) ;
#65415=CARTESIAN_POINT ( 'NONE',  ( 27.64127793187000037, 2.399999999999999911, 6.571291218949999902 ) ) ;
#65421=ADVANCED_FACE ( 'NONE', ( #45780 ), #9386, .F. ) ;
#65423=CARTESIAN_POINT ( 'NONE',  ( 8.397785841227999981, 5.616457598545999907, -8.245813000738998255 ) ) ;
#65432=CARTESIAN_POINT ( 'NONE',  ( 9.905792474809000936, 2.698958900805999761, 8.979236532123000103 ) ) ;
#65442=CARTESIAN_POINT ( 'NONE',  ( 0.7431103717477000048, 2.848815883361000001, -1.248255999701999963 ) ) ;
#65456=CARTESIAN_POINT ( 'NONE',  ( 9.457462135716001583, 5.100000000000000533, -6.571291218949999902 ) ) ;
#65459=CARTESIAN_POINT ( 'NONE',  ( 8.491329719591000469, 4.851303550474000303, -9.008742670124000540 ) ) ;
#65487=CARTESIAN_POINT ( 'NONE',  ( 8.765417767663000959, 5.029951493281999753, -6.097931603992000404 ) ) ;
#65500=ADVANCED_FACE ( 'NONE', ( #5866 ), #58884, .F. ) ;
#65503=CARTESIAN_POINT ( 'NONE',  ( 7.000000000000000000, 10.13680670596995625, 4.410575858471027288 ) ) ;
#65509=EDGE_LOOP ( 'NONE', ( #15589, #32713, #40740, #17957, #5336, #29088 ) ) ;
#65520=CARTESIAN_POINT ( 'NONE',  ( 9.892489158770999325, 5.099602161831000124, -9.049221499261999924 ) ) ;
#65521=ORIENTED_EDGE ( 'NONE', *, *, #11044, .F. ) ;
#65522=AXIS2_PLACEMENT_3D ( 'NONE', #30146, #2866, #13377 ) ;
#65523=CARTESIAN_POINT ( 'NONE',  ( 11.01002959534999981, 3.180718072098000171, -6.283812549199000230 ) ) ;
#65528=EDGE_CURVE ( 'NONE', #7896, #4640, #52239, .T. ) ;
#65529=VECTOR ( 'NONE', #42055, 1000.000000000000000 ) ;
#65530=CARTESIAN_POINT ( 'NONE',  ( 10.99143984058726353, 6.551946267843069549, -5.305482051232298879 ) ) ;
#65534=VECTOR ( 'NONE', #64109, 1000.000000000000114 ) ;
#65538=CARTESIAN_POINT ( 'NONE',  ( 10.74599736040000053, 5.242718773683000322, 8.978699897073999736 ) ) ;
#65539=CARTESIAN_POINT ( 'NONE',  ( 10.14522028041000112, 3.576529456695000331, -8.962721799438000403 ) ) ;
#65540=DIRECTION ( 'NONE',  ( -1.000000000000000000, 0.000000000000000000, 0.000000000000000000 ) ) ;
#65548=VERTEX_POINT ( 'NONE', #54458 ) ;
#65549=EDGE_LOOP ( 'NONE', ( #24316, #55059, #17758, #56050, #7998, #24223, #63812, #16235, #68333 ) ) ;
#65550=VECTOR ( 'NONE', #59770, 1000.000000000000000 ) ;
#65551=CARTESIAN_POINT ( 'NONE',  ( 9.635004719593998956, 2.334550724494000029, -7.977056617806000283 ) ) ;
#65555=DIRECTION ( 'NONE',  ( 1.000000000000000000, 0.000000000000000000, 0.000000000000000000 ) ) ;
#65562=CARTESIAN_POINT ( 'NONE',  ( 6.999999691988000095, 1.243449787579999883E-13, -1.714942017578999994E-13 ) ) ;
#65567=CARTESIAN_POINT ( 'NONE',  ( 4.149992563291998948, 1.747525841223984910, 1.007210908820209916 ) ) ;
#65570=CARTESIAN_POINT ( 'NONE',  ( 9.615109647822677630, 5.349900357012234764, -7.499993490198826329 ) ) ;
#65571=CARTESIAN_POINT ( 'NONE',  ( 9.351420280414000530, 4.953415418491999844, -8.946479654552000227 ) ) ;
#65576=CIRCLE ( 'NONE', #14238, 2.000000000000000888 ) ;
#65577=CARTESIAN_POINT ( 'NONE',  ( 0.4527818351675000352, 0.6486458134353999538, 3.310649237188999727 ) ) ;
#65579=CARTESIAN_POINT ( 'NONE',  ( 2.590519314319999822, 0.2902467568208999538, -3.413293928950000389 ) ) ;
#65584=CARTESIAN_POINT ( 'NONE',  ( 7.127704719590999716, 4.698356649019999942, 8.789431186081998248 ) ) ;
#65587=CARTESIAN_POINT ( 'NONE',  ( 8.037560841226000008, 5.122039080790999677, -6.666882531104000087 ) ) ;
#65603=CARTESIAN_POINT ( 'NONE',  ( 7.689964158769000413, 4.459320617394000763, -8.819879155908999735 ) ) ;
#65604=LINE ( 'NONE', #1294, #54298 ) ;
#65615=CARTESIAN_POINT ( 'NONE',  ( 5.000030787343001215, -0.2748844998327719669, 2.099962892531005654 ) ) ;
#65620=VERTEX_POINT ( 'NONE', #46384 ) ;
#65621=( BOUNDED_SURFACE ( )  B_SPLINE_SURFACE ( 3, 3, ( 
 ( #16734, #17435, #64965, #1701, #2389, #33523, #54842, #22671, #38411, #65667, #17079 ),
 ( #49942, #54144, #23713, #54493, #59735, #33176, #2053, #66009, #27584, #55537, #33869 ),
 ( #38764, #7634, #45048, #6594, #60089, #55184, #38063, #49244, #59388, #44015, #23020 ),
 ( #11488, #32828, #18132, #65319, #12195, #49593, #51988, #39801, #30346, #40820, #61125 ) ),
 .UNSPECIFIED., .F., .F., .T. ) 
 B_SPLINE_SURFACE_WITH_KNOTS ( ( 4, 4 ),
 ( 4, 1, 1, 1, 1, 1, 1, 1, 4 ),
 ( 0.000000000000000000, 1.000000000000000000 ),
 ( 0.8312902889582000077, 0.8338388411866000105, 0.8555869174461000481, 0.8794646334507000285, 0.9056938526918999477, 0.9344431701381999966, 0.9658387281735000274, 1.000000000000000000, 1.004668145018999814 ),
 .UNSPECIFIED. ) 
 GEOMETRIC_REPRESENTATION_ITEM ( )  RATIONAL_B_SPLINE_SURFACE ( (
 ( 1.221026506593000160, 1.221026506593000160, 1.221026506593000160, 1.221026506593000160, 1.221026506593000160, 1.221026506593000160, 1.221026506593000160, 1.221026506593000160, 1.221026506593000160, 1.221026506593000160, 1.221026506593000160),
 ( 0.9263244978021999421, 0.9263244978021999421, 0.9263244978021999421, 0.9263244978021999421, 0.9263244978021999421, 0.9263244978021999421, 0.9263244978021999421, 0.9263244978021999421, 0.9263244978021999421, 0.9263244978021999421, 0.9263244978021999421),
 ( 0.9263244978021999421, 0.9263244978021999421, 0.9263244978021999421, 0.9263244978021999421, 0.9263244978021999421, 0.9263244978021999421, 0.9263244978021999421, 0.9263244978021999421, 0.9263244978021999421, 0.9263244978021999421, 0.9263244978021999421),
 ( 1.221026506593000160, 1.221026506593000160, 1.221026506593000160, 1.221026506593000160, 1.221026506593000160, 1.221026506593000160, 1.221026506593000160, 1.221026506593000160, 1.221026506593000160, 1.221026506593000160, 1.221026506593000160) ) ) 
 REPRESENTATION_ITEM ( '' )  SURFACE ( )  );
#65624=CARTESIAN_POINT ( 'NONE',  ( 0.1499942179679999987, 2.750000000000000000, 0.000000000000000000 ) ) ;
#65625=CARTESIAN_POINT ( 'NONE',  ( 8.848264158775000610, 5.751585344281000545, -8.235867044345999588 ) ) ;
#65626=CARTESIAN_POINT ( 'NONE',  ( 3.006162285354999852, -1.552497165750999830, 3.001664479667999874 ) ) ;
#65629=DIRECTION ( 'NONE',  ( 0.000000000000000000, -0.3258275053806940491, 0.9454292341245821296 ) ) ;
#65635=CARTESIAN_POINT ( 'NONE',  ( 10.00138108374000012, 3.855364958793999985, 5.709478909302000638 ) ) ;
#65638=CARTESIAN_POINT ( 'NONE',  ( 9.115731781212220497, 3.733300398746750570, 8.827344556479088666 ) ) ;
#65641=CARTESIAN_POINT ( 'NONE',  ( 7.100000000000208367, 2.697694540754497883, -7.975585739598743729 ) ) ;
#65647=CARTESIAN_POINT ( 'NONE',  ( 8.114681124177748117, 5.046545375811008149, -6.488671702751082293 ) ) ;
#65658=CARTESIAN_POINT ( 'NONE',  ( 8.566232780412001091, 5.212261578733999201, 6.157186134061999994 ) ) ;
#65659=CARTESIAN_POINT ( 'NONE',  ( 8.307195280408999238, 5.473983809665999622, -8.180077404516000072 ) ) ;
#65661=CARTESIAN_POINT ( 'NONE',  ( 11.09991415876999987, 2.373387781209999936, -6.776601845694000481 ) ) ;
#65663=CARTESIAN_POINT ( 'NONE',  ( 10.80168826891999956, 3.998196217194999846, 9.431555066626000183 ) ) ;
#65667=CARTESIAN_POINT ( 'NONE',  ( 8.493443684196000376, 2.902502839086001263, 6.607649189245996091 ) ) ;
#65675=DIRECTION ( 'NONE',  ( 0.000000000000000000, -0.8648648648648720183, 0.5020047465136825426 ) ) ;
#65677=EDGE_LOOP ( 'NONE', ( #61988, #46930, #44315, #52190 ) ) ;
#65683=B_SPLINE_CURVE_WITH_KNOTS ( 'NONE', 3,
 ( #9818, #67854, #35712, #34436 ),
 .UNSPECIFIED., .F., .F.,
 ( 4, 4 ),
 ( 0.000000000000000000, 1.000000000000000000 ),
 .UNSPECIFIED. ) ;
#65684=CARTESIAN_POINT ( 'NONE',  ( 8.307195280408999238, 5.473983809665999622, -8.180077404516000072 ) ) ;
#65690=CARTESIAN_POINT ( 'NONE',  ( 7.953777748866911246, 4.974397447652631143, -6.453194790817486926 ) ) ;
#65700=CARTESIAN_POINT ( 'NONE',  ( 10.56271176071999918, 2.509373760909999973, -8.602415192333999983 ) ) ;
#65705=ADVANCED_FACE ( 'NONE', ( #41479 ), #3761, .T. ) ;
#65706=CARTESIAN_POINT ( 'NONE',  ( 6.999998782146999332, -11.95749337870000062, 3.642574926947999892 ) ) ;
#65708=CARTESIAN_POINT ( 'NONE',  ( 8.160739158772001289, 5.944584532500000407, 7.106843289410999631 ) ) ;
#65711=LINE ( 'NONE', #43711, #65090 ) ;
#65712=CARTESIAN_POINT ( 'NONE',  ( 9.848259964010999568, 4.436917881843999822, 6.148031614254000132 ) ) ;
#65716=CARTESIAN_POINT ( 'NONE',  ( 10.85685100254000091, 2.832432432432000269, -6.822293592207000934 ) ) ;
#65717=CARTESIAN_POINT ( 'NONE',  ( 9.504903297738000134, 3.934733353759999552, 5.704831249548000471 ) ) ;
#65720=ORIENTED_EDGE ( 'NONE', *, *, #58395, .T. ) ;
#65728=CARTESIAN_POINT ( 'NONE',  ( 9.566490007895001924, 4.108964550738000376, 8.851615252874999840 ) ) ;
#65729=CARTESIAN_POINT ( 'NONE',  ( 9.967852198058999136, 2.034774058634999605, 7.636878205663998997 ) ) ;
#65732=CARTESIAN_POINT ( 'NONE',  ( 8.351014158771000950, 5.616457598545999907, -8.245813000738998255 ) ) ;
#65741=ORIENTED_EDGE ( 'NONE', *, *, #15421, .T. ) ;
#65742=CARTESIAN_POINT ( 'NONE',  ( 2.068384988122999868, -3.260690222378000325, 1.050103212221999982 ) ) ;
#65746=CARTESIAN_POINT ( 'NONE',  ( 10.47094409420000005, 5.100000000000000533, 6.571291218949999902 ) ) ;
#65748=DIRECTION ( 'NONE',  ( 1.000000000000000000, 0.000000000000000000, 0.000000000000000000 ) ) ;
#65756=CARTESIAN_POINT ( 'NONE',  ( 10.65293113562639959, 5.100000000000000533, -6.444141223575878819 ) ) ;
#65758=ORIENTED_EDGE ( 'NONE', *, *, #40787, .F. ) ;
#65766=CARTESIAN_POINT ( 'NONE',  ( 9.631052653747600445, 5.349725748959462734, -7.768783048622874610 ) ) ;
#65767=CARTESIAN_POINT ( 'NONE',  ( 9.470944094206000585, 5.100000000000000533, 6.571291218949999902 ) ) ;
#65769=CARTESIAN_POINT ( 'NONE',  ( 7.371899607694904155, 3.032515528092295298, 8.944945008364053152 ) ) ;
#65772=CARTESIAN_POINT ( 'NONE',  ( 7.760748336203000086, 3.157321061061999945, 6.445092363529999702 ) ) ;
#65777=CARTESIAN_POINT ( 'NONE',  ( 10.15403136780999915, 5.267988602993999514, 5.992335067371000079 ) ) ;
#65781=CIRCLE ( 'NONE', #51269, 13.10000000000000142 ) ;
#65784=CARTESIAN_POINT ( 'NONE',  ( 3.999971066382000284, -2.149963194831999935, 0.000000000000000000 ) ) ;
#65796=ORIENTED_EDGE ( 'NONE', *, *, #17136, .T. ) ;
#65797=CARTESIAN_POINT ( 'NONE',  ( 10.29353630808639863, 2.899999999999999911, 6.665341197380421079 ) ) ;
#65800=CARTESIAN_POINT ( 'NONE',  ( 7.003728317543000514, 5.017953588770000195, -6.429833855306000601 ) ) ;
#65806=CARTESIAN_POINT ( 'NONE',  ( 9.725595280412999699, 2.495531372253999791, -7.930944806125000746 ) ) ;
#65807=CYLINDRICAL_SURFACE ( 'NONE', #7920, 1.350000000000000533 ) ;
#65809=CARTESIAN_POINT ( 'NONE',  ( 8.169101745083519717, 4.353498524260636771, -8.815135294168911173 ) ) ;
#65814=CARTESIAN_POINT ( 'NONE',  ( 1.136390132542124398, -0.4581489286485235790, 3.499999999999998224 ) ) ;
#65816=ADVANCED_FACE ( 'NONE', ( #32712 ), #12072, .F. ) ;
#65821=CARTESIAN_POINT ( 'NONE',  ( 10.91620964606000044, 2.818413279081999789, -6.814156272943999504 ) ) ;
#65837=EDGE_CURVE ( 'NONE', #2005, #56175, #35807, .T. ) ;
#65838=CARTESIAN_POINT ( 'NONE',  ( 6.999999999999999112, 10.24473655391737204, -4.324905599572709036 ) ) ;
#65846=CARTESIAN_POINT ( 'NONE',  ( 10.90000016885999834, 9.856474585920999232, -5.627825103726000755 ) ) ;
#65858=CARTESIAN_POINT ( 'NONE',  ( 8.434805295391889501, 5.349284795551519700, 7.676787393164572038 ) ) ;
#65860=CARTESIAN_POINT ( 'NONE',  ( 8.506095280410999493, 2.305580295895999665, -7.860904109308999743 ) ) ;
#65870=CARTESIAN_POINT ( 'NONE',  ( 9.741003491525001223, 3.588532719919999892, -8.800216240366001585 ) ) ;
#65875=EDGE_CURVE ( 'NONE', #19742, #12021, #54724, .T. ) ;
#65881=ORIENTED_EDGE ( 'NONE', *, *, #62743, .T. ) ;
#65883=CARTESIAN_POINT ( 'NONE',  ( 10.78888278041000071, 2.675726696512000125, -6.748227692827999391 ) ) ;
#65892=CARTESIAN_POINT ( 'NONE',  ( 8.947714158774999760, 3.854507394315999758, -9.394302886912999639 ) ) ;
#65896=DIRECTION ( 'NONE',  ( -1.000000000000000000, 0.000000000000000000, 3.552713678967001067E-14 ) ) ;
#65898=EDGE_CURVE ( 'NONE', #36822, #46708, #59798, .T. ) ;
#65908=CARTESIAN_POINT ( 'NONE',  ( 7.883148997456999929, 5.167567567567999731, 6.822293592207000934 ) ) ;
#65911=EDGE_LOOP ( 'NONE', ( #23651, #54450, #17977, #9815, #55630, #51517, #23613, #5441, #1627, #39355 ) ) ;
#65914=CARTESIAN_POINT ( 'NONE',  ( 9.509454719593000149, 3.116293075258000478, -6.208411413796000033 ) ) ;
#65917=FACE_OUTER_BOUND ( 'NONE', #58900, .T. ) ;
#65919=CARTESIAN_POINT ( 'NONE',  ( 8.191498566858999908, 3.399962487441000381, 6.146646668338000552 ) ) ;
#65920=CARTESIAN_POINT ( 'NONE',  ( 2.833702399587000098, -3.260318005001999975, 1.508036922365999954 ) ) ;
#65925=CARTESIAN_POINT ( 'NONE',  ( 7.101301658771000724, 3.554857159507999853, 8.889479859586000288 ) ) ;
#65926=ORIENTED_EDGE ( 'NONE', *, *, #64062, .F. ) ;
#65928=CARTESIAN_POINT ( 'NONE',  ( 10.94699683900224230, 9.189629059784236276, 6.317109415722915067 ) ) ;
#65929=CARTESIAN_POINT ( 'NONE',  ( 8.883148997460001084, 5.167567567567999731, 6.822293592207000934 ) ) ;
#65930=CARTESIAN_POINT ( 'NONE',  ( 10.77332351902737528, 2.820285017511521719, -8.179908095962574066 ) ) ;
#65937=CARTESIAN_POINT ( 'NONE',  ( -15.86200481174999943, 0.8000000000000000444, -3.149999999999999911 ) ) ;
#65939=ORIENTED_EDGE ( 'NONE', *, *, #62889, .T. ) ;
#65942=CARTESIAN_POINT ( 'NONE',  ( 4.500000000000000000, -3.200000000000000178, 0.000000000000000000 ) ) ;
#65943=CARTESIAN_POINT ( 'NONE',  ( 9.933536308084500277, 2.899999999999999911, -6.665341197412895546 ) ) ;
#65950=CARTESIAN_POINT ( 'NONE',  ( 10.97360312464731713, 5.212835794440835002, 6.753664309372819474 ) ) ;
#65953=FACE_OUTER_BOUND ( 'NONE', #33006, .T. ) ;
#65954=CARTESIAN_POINT ( 'NONE',  ( 0.1499942179679999987, -2.750000000000000000, 0.000000000000000000 ) ) ;
#65957=CARTESIAN_POINT ( 'NONE',  ( 5.000030787343000327, -2.045306479342562156, 0.5496608443529843457 ) ) ;
#65958=CARTESIAN_POINT ( 'NONE',  ( 11.09999999999999964, 2.274006712557999688, -7.281956340829000673 ) ) ;
#65965=DIRECTION ( 'NONE',  ( 1.000000000000000000, 0.000000000000000000, 0.000000000000000000 ) ) ;
#65966=CARTESIAN_POINT ( 'NONE',  ( 9.743314158772999889, 5.149303692842000402, -5.987168472229000393 ) ) ;
#65967=CARTESIAN_POINT ( 'NONE',  ( 2.586992650581000142, -3.369180291263000004, 0.2624141663141000280 ) ) ;
#65973=ORIENTED_EDGE ( 'NONE', *, *, #39227, .F. ) ;
#65975=AXIS2_PLACEMENT_3D ( 'NONE', #8908, #24650, #29914 ) ;
#65977=CARTESIAN_POINT ( 'NONE',  ( 10.13049857835000012, 3.092060693447000297, 8.629378633793999498 ) ) ;
#65980=CARTESIAN_POINT ( 'NONE',  ( 9.319055905798999007, 2.899999999999999911, -6.571291218949999902 ) ) ;
#65982=ADVANCED_FACE ( 'NONE', ( #46820 ), #36395, .T. ) ;
#65984=CARTESIAN_POINT ( 'NONE',  ( 7.100000000000113332, 4.265775746597376461, -8.859935407261559703 ) ) ;
#65988=CARTESIAN_POINT ( 'NONE',  ( 0.8143050634219124451, -2.465875601137460293, -2.515512106780213308 ) ) ;
#65989=CARTESIAN_POINT ( 'NONE',  ( 11.37168584123000059, 2.803494217761000495, -6.967881733280000489 ) ) ;
#65992=B_SPLINE_CURVE_WITH_KNOTS ( 'NONE', 3,
 ( #39041, #12121, #44298, #11761 ),
 .UNSPECIFIED., .F., .F.,
 ( 4, 4 ),
 ( 0.6941764652077998532, 1.000000000000000000 ),
 .UNSPECIFIED. ) ;
#65996=EDGE_LOOP ( 'NONE', ( #44241, #1894, #9848, #38976, #17623, #40667, #67149 ) ) ;
#65998=CARTESIAN_POINT ( 'NONE',  ( 8.385051658773999606, 4.977909614887999545, 6.416776202806000029 ) ) ;
#66000=CARTESIAN_POINT ( 'NONE',  ( 9.193385841233000733, 2.981992329588000423, -5.895876591910999664 ) ) ;
#66003=CARTESIAN_POINT ( 'NONE',  ( 10.11548915876999999, 2.489190114737999782, -6.434635778494999236 ) ) ;
#66005=CARTESIAN_POINT ( 'NONE',  ( 11.00366064676999933, 2.264078662261999941, 7.798351372501000078 ) ) ;
#66009=CARTESIAN_POINT ( 'NONE',  ( 8.160036350658002036, 2.891230335795000883, 6.361714733157999291 ) ) ;
#66010=ORIENTED_EDGE ( 'NONE', *, *, #63821, .F. ) ;
#66012=CARTESIAN_POINT ( 'NONE',  ( 1.303056799208125005, -2.798833948393629978, -2.150913519912204031 ) ) ;
#66019=B_SPLINE_CURVE_WITH_KNOTS ( 'NONE', 3,
 ( #37416, #52114, #58737, #31161, #63971, #68881, #10844, #31491, #63635, #4906, #58060, #63284, #32186, #62938, #21335, #15062, #4219, #30801, #42333, #31838, #53500, #57702, #26595, #53154, #68530, #52462 ),
 .UNSPECIFIED., .F., .F.,
 ( 4, 2, 2, 2, 2, 2, 2, 2, 2, 2, 2, 2, 4 ),
 ( 0.000000000000000000, 0.1761049413614339532, 0.2201311767017935517, 0.2421442943719733232, 0.2476475737895179607, 0.2531508532070625428, 0.2641574120421518179, 0.3522098827228736795, 0.4402623534035955410, 0.4842885887439561943, 0.5063017064141377421, 0.5283148240843194010, 0.7044197654457721169 ),
 .UNSPECIFIED. ) ;
#66021=ORIENTED_EDGE ( 'NONE', *, *, #40584, .T. ) ;
#66025=CARTESIAN_POINT ( 'NONE',  ( 8.605545280412000508, 3.122811675949999977, -6.006064052396999919 ) ) ;
#66031=( BOUNDED_SURFACE ( )  B_SPLINE_SURFACE ( 3, 3, ( 
 ( #34249, #42575, #4464, #25804, #62852, #9366, #15319, #57266, #63884, #20904 ),
 ( #15996, #25459, #62515, #14634, #56938, #9034, #10066, #46791, #31400, #63547 ),
 ( #47829, #30375, #19875, #9716, #57967, #21247, #68097, #51683, #41205, #41884 ),
 ( #3781, #25119, #14970, #69139, #46451, #67750, #52716, #15660, #36991, #4814 ) ),
 .UNSPECIFIED., .F., .F., .T. ) 
 B_SPLINE_SURFACE_WITH_KNOTS ( ( 4, 4 ),
 ( 4, 1, 1, 1, 1, 1, 1, 4 ),
 ( 0.000000000000000000, 1.000000000000000000 ),
 ( 0.6764685980817000122, 0.6779455865321999397, 0.6880926466457000235, 0.6995436293012999851, 0.7123096649787999946, 0.7264343954043999130, 0.7420586980075000172, 0.7441198533032000739 ),
 .UNSPECIFIED. ) 
 GEOMETRIC_REPRESENTATION_ITEM ( )  RATIONAL_B_SPLINE_SURFACE ( (
 ( 1.325324334266000159, 1.325324334266000159, 1.325324334266000159, 1.325324334266000159, 1.325324334266000159, 1.325324334266000159, 1.325324334266000159, 1.325324334266000159, 1.325324334266000159, 1.325324334266000159),
 ( 0.8915585552447999884, 0.8915585552447999884, 0.8915585552447999884, 0.8915585552447999884, 0.8915585552447999884, 0.8915585552447999884, 0.8915585552447999884, 0.8915585552447999884, 0.8915585552447999884, 0.8915585552447999884),
 ( 0.8915585552447999884, 0.8915585552447999884, 0.8915585552447999884, 0.8915585552447999884, 0.8915585552447999884, 0.8915585552447999884, 0.8915585552447999884, 0.8915585552447999884, 0.8915585552447999884, 0.8915585552447999884),
 ( 1.325324334266000159, 1.325324334266000159, 1.325324334266000159, 1.325324334266000159, 1.325324334266000159, 1.325324334266000159, 1.325324334266000159, 1.325324334266000159, 1.325324334266000159, 1.325324334266000159) ) ) 
 REPRESENTATION_ITEM ( '' )  SURFACE ( )  );
#66034=VERTEX_POINT ( 'NONE', #55332 ) ;
#66037=ORIENTED_EDGE ( 'NONE', *, *, #62974, .T. ) ;
#66044=CARTESIAN_POINT ( 'NONE',  ( 5.500000000000000000, -11.95749337870000062, -3.642574926947999892 ) ) ;
#66053=CARTESIAN_POINT ( 'NONE',  ( 7.326301658771000369, 3.394842219570000097, 9.388954446285000088 ) ) ;
#66057=CARTESIAN_POINT ( 'NONE',  ( 8.142152878612547440, 3.293758513149187994, 8.705677052449509290 ) ) ;
#66058=CARTESIAN_POINT ( 'NONE',  ( 10.33022126302999943, 2.650190549566000087, -7.694579890082000162 ) ) ;
#66061=CARTESIAN_POINT ( 'NONE',  ( 11.01654498872999888, 5.423831355693000233, 4.991935587166999255 ) ) ;
#66062=CARTESIAN_POINT ( 'NONE',  ( 9.939321360490000146, 2.638097915594000309, 6.328629954376999933 ) ) ;
#66065=ORIENTED_EDGE ( 'NONE', *, *, #44843, .T. ) ;
#66068=CARTESIAN_POINT ( 'NONE',  ( 9.736878146978000359, 2.742182981761000171, 6.839230404018000087 ) ) ;
#66072=CARTESIAN_POINT ( 'NONE',  ( 8.213545280409999094, 3.608525622520999843, 5.913376237674000002 ) ) ;
#66073=CARTESIAN_POINT ( 'NONE',  ( 11.25041981190000051, 5.730782764036999488, 8.122675980938000251 ) ) ;
#66075=VERTEX_POINT ( 'NONE', #52401 ) ;
#66076=CARTESIAN_POINT ( 'NONE',  ( 9.983079719591000156, 5.002683760508999988, -8.912673867568997821 ) ) ;
#66086=CARTESIAN_POINT ( 'NONE',  ( 0.9240182015432000240, 1.804890371571000074, 2.911542930280999641 ) ) ;
#66088=EDGE_CURVE ( 'NONE', #24517, #54370, #68964, .T. ) ;
#66092=ADVANCED_FACE ( 'NONE', ( #61268 ), #32698, .F. ) ;
#66093=CARTESIAN_POINT ( 'NONE',  ( 4.900006121741999898, -1.947945353336633323, -0.5234957687185524122 ) ) ;
#66094=CARTESIAN_POINT ( 'NONE',  ( 8.477766462057999775, 2.899999999999999911, -6.558719934578999933 ) ) ;
#66097=ORIENTED_EDGE ( 'NONE', *, *, #15560, .T. ) ;
#66098=CARTESIAN_POINT ( 'NONE',  ( 6.666501733306198219, 5.101307144762445844, -8.327526203928272253 ) ) ;
#66099=CARTESIAN_POINT ( 'NONE',  ( 10.96087378980999993, 5.155384868709999679, 5.099797507357000548 ) ) ;
#66103=CARTESIAN_POINT ( 'NONE',  ( 0.5559723532207999641, 2.401393137604999950, -2.383704365015999915 ) ) ;
#66104=ORIENTED_EDGE ( 'NONE', *, *, #45887, .F. ) ;
#66105=CARTESIAN_POINT ( 'NONE',  ( 10.78170625604383659, 3.320082702567634048, -8.679590637732799152 ) ) ;
#66117=CARTESIAN_POINT ( 'NONE',  ( 7.891027728344822023, 2.717852728070912605, 8.706984646977891984 ) ) ;
#66118=ORIENTED_EDGE ( 'NONE', *, *, #63681, .T. ) ;
#66121=ORIENTED_EDGE ( 'NONE', *, *, #66836, .F. ) ;
#66127=CARTESIAN_POINT ( 'NONE',  ( 10.60518955639999916, 5.343965917319999370, -7.731522121091999544 ) ) ;
#66132=CARTESIAN_POINT ( 'NONE',  ( 11.03977792509980915, 5.161925716702778111, -8.467638888446076706 ) ) ;
#66137=DIRECTION ( 'NONE',  ( 1.000000000000000000, 0.000000000000000000, 0.000000000000000000 ) ) ;
#66147=CARTESIAN_POINT ( 'NONE',  ( 9.970944094204998720, 5.100000000000000533, 6.571291218949999902 ) ) ;
#66150=CARTESIAN_POINT ( 'NONE',  ( 6.769728317542999640, 2.788803157567000035, -8.345558963038001821 ) ) ;
#66154=CARTESIAN_POINT ( 'NONE',  ( 8.480233239714511484, 3.061143994416841263, 6.132506423769173765 ) ) ;
#66156=CARTESIAN_POINT ( 'NONE',  ( 10.07367028041000090, 4.905765359186999852, -8.776126235875999271 ) ) ;
#66158=CARTESIAN_POINT ( 'NONE',  ( 10.94936583238000161, 8.462332231760997914, -6.519047867360999504 ) ) ;
#66184=CARTESIAN_POINT ( 'NONE',  ( 10.84999882987999875, 12.50000000000000000, 0.000000000000000000 ) ) ;
#66187=DIRECTION ( 'NONE',  ( 0.000000000000000000, -1.000000000000000000, 0.000000000000000000 ) ) ;
#66189=DIRECTION ( 'NONE',  ( 0.7071068156326932863, 0.000000000000000000, -0.7071067467404001938 ) ) ;
#66190=VERTEX_POINT ( 'NONE', #41063 ) ;
#66196=CARTESIAN_POINT ( 'NONE',  ( 7.000000000000000000, 9.903195496255079888, 4.550777181346948197 ) ) ;
#66198=ORIENTED_EDGE ( 'NONE', *, *, #63909, .T. ) ;
#66199=DIRECTION ( 'NONE',  ( -1.000000000000000000, 0.000000000000000000, 0.000000000000000000 ) ) ;
#66202=DIRECTION ( 'NONE',  ( 0.8660254037844288266, 0.000000000000000000, -0.5000000000000169864 ) ) ;
#66203=CARTESIAN_POINT ( 'NONE',  ( 2.748890132544458353, -2.798833948393641080, 2.150913519912190708 ) ) ;
#66204=CARTESIAN_POINT ( 'NONE',  ( 9.939260841229000221, 5.099602161831000124, -9.049221499261999924 ) ) ;
#66214=DIRECTION ( 'NONE',  ( -1.000000000000000000, 0.000000000000000000, 0.000000000000000000 ) ) ;
#66216=B_SPLINE_CURVE_WITH_KNOTS ( 'NONE', 3,
 ( #7722, #21456, #50373, #49325 ),
 .UNSPECIFIED., .F., .F.,
 ( 4, 4 ),
 ( 0.000000000000000000, 1.000000000000000000 ),
 .UNSPECIFIED. ) ;
#66217=CARTESIAN_POINT ( 'NONE',  ( 10.36950244779999863, 2.719131864236000062, -7.031786688683999920 ) ) ;
#66219=VERTEX_POINT ( 'NONE', #8903 ) ;
#66228=VERTEX_POINT ( 'NONE', #29213 ) ;
#66231=CARTESIAN_POINT ( 'NONE',  ( 10.35752971959000135, 5.367812128871999988, -6.514736131541999598 ) ) ;
#66232=ADVANCED_FACE ( 'NONE', ( #51887 ), #35819, .T. ) ;
#66236=CARTESIAN_POINT ( 'NONE',  ( 9.051550650638001017, 2.899999999999999911, 6.227445478845999638 ) ) ;
#66237=EDGE_CURVE ( 'NONE', #44976, #29684, #27237, .T. ) ;
#66241=VERTEX_POINT ( 'NONE', #62042 ) ;
#66242=ORIENTED_EDGE ( 'NONE', *, *, #57603, .T. ) ;
#66243=CARTESIAN_POINT ( 'NONE',  ( 9.585279719593998493, 2.928319778732999978, -8.861178115809998701 ) ) ;
#66246=LINE ( 'NONE', #28517, #59590 ) ;
#66251=VECTOR ( 'NONE', #62064, 1000.000000000000114 ) ;
#66254=VECTOR ( 'NONE', #51871, 1000.000000000000000 ) ;
#66256=CARTESIAN_POINT ( 'NONE',  ( 11.09999999999999964, 5.299999999999999822, 6.469505845987999493 ) ) ;
#66261=CARTESIAN_POINT ( 'NONE',  ( 7.956354808247001031, 3.389562910887999880, -6.282406754076000688 ) ) ;
#66262=CARTESIAN_POINT ( 'NONE',  ( 9.053070280414001303, 2.391443348526999912, -6.856688371964000162 ) ) ;
#66263=CARTESIAN_POINT ( 'NONE',  ( 8.573148997459998810, 5.167567567567999731, -6.822293592207000934 ) ) ;
#66267=CARTESIAN_POINT ( 'NONE',  ( 9.456592480104376364, 2.253870038478822391, 7.362952920305176008 ) ) ;
#66268=CARTESIAN_POINT ( 'NONE',  ( 3.533037658052000207, 1.664759391734999872, -3.022254788923000035 ) ) ;
#66274=EDGE_LOOP ( 'NONE', ( #31991, #58, #13550, #64112 ) ) ;
#66276=CARTESIAN_POINT ( 'NONE',  ( 7.888385841225999506, 2.869384229876999814, -6.678559560168999987 ) ) ;
#66280=ORIENTED_EDGE ( 'NONE', *, *, #25394, .T. ) ;
#66289=CARTESIAN_POINT ( 'NONE',  ( 10.15000066238999921, -1.714184350020999865E-13, 8.688602249551999193E-14 ) ) ;
#66292=FACE_OUTER_BOUND ( 'NONE', #19355, .T. ) ;
#66294=CARTESIAN_POINT ( 'NONE',  ( 9.472537864290000442, 2.899999999999999911, -6.571291218949999902 ) ) ;
#66299=CONICAL_SURFACE ( 'NONE', #29497, 12.49999584805000019, 0.7853981146832407223 ) ;
#66307=DIRECTION ( 'NONE',  ( 1.000000000000000000, 0.000000000000000000, 0.000000000000000000 ) ) ;
#66314=CARTESIAN_POINT ( 'NONE',  ( 9.775320280412000074, 2.527713920559999661, -6.969421869128999525 ) ) ;
#66316=CARTESIAN_POINT ( 'NONE',  ( 2.964245321877999828, 0.1669473377653999946, 3.375257869341000028 ) ) ;
#66317=EDGE_CURVE ( 'NONE', #23033, #34088, #35543, .T. ) ;
#66324=CARTESIAN_POINT ( 'NONE',  ( 10.09696969267000100, 5.253376380222999131, 8.530663119653999260 ) ) ;
#66327=CARTESIAN_POINT ( 'NONE',  ( 9.217201318830829493, 2.656563516783068124, 7.632949642608349627 ) ) ;
#66328=AXIS2_PLACEMENT_3D ( 'NONE', #18971, #8822, #62304 ) ;
#66334=CARTESIAN_POINT ( 'NONE',  ( 8.100037824936533681, 5.084629185201427148, -6.579660631752214606 ) ) ;
#66335=CARTESIAN_POINT ( 'NONE',  ( 10.75102028041000146, 2.478469530773999896, -7.438303846328000013 ) ) ;
#66336=ORIENTED_EDGE ( 'NONE', *, *, #36928, .T. ) ;
#66346=CARTESIAN_POINT ( 'NONE',  ( 0.5294218405026995811, 3.414111695701551152, -0.9298589507122824172 ) ) ;
#66347=CARTESIAN_POINT ( 'NONE',  ( 10.56983915876999980, 2.152856944368999770, -7.425100664021000441 ) ) ;
#66350=EDGE_CURVE ( 'NONE', #30029, #52567, #30920, .T. ) ;
#66351=CARTESIAN_POINT ( 'NONE',  ( 11.11504246380000005, 3.456610836627000083, 5.970339330302000036 ) ) ;
#66367=ORIENTED_EDGE ( 'NONE', *, *, #6736, .T. ) ;
#66371=CARTESIAN_POINT ( 'NONE',  ( 8.323770280408998801, 5.332332124071999857, -8.487089944253000340 ) ) ;
#66373=CARTESIAN_POINT ( 'NONE',  ( -15.86200481174999943, 5.599999999999999645, 6.571291218949999902 ) ) ;
#66380=AXIS2_PLACEMENT_3D ( 'NONE', #45480, #33955, #18909 ) ;
#66382=ORIENTED_EDGE ( 'NONE', *, *, #24482, .F. ) ;
#66397=CARTESIAN_POINT ( 'NONE',  ( 8.866801658774001282, 2.550580605805000012, 8.854682662413999594 ) ) ;
#66400=CARTESIAN_POINT ( 'NONE',  ( 10.98768472639999949, 5.139096889661000311, -4.945212061661000469 ) ) ;
#66402=CARTESIAN_POINT ( 'NONE',  ( 10.13381533919000077, 5.176445833090999926, -8.189798585019000043 ) ) ;
#66403=B_SPLINE_CURVE_WITH_KNOTS ( 'NONE', 3,
 ( #31480, #52803, #10831, #32175, #32855, #17465, #6967, #1380, #33895, #342 ),
 .UNSPECIFIED., .F., .F.,
 ( 4, 2, 2, 2, 4 ),
 ( 0.1253320266324779719, 0.3126457153657128396, 0.4999594040989477906, 0.6872730928321826305, 0.8745867815654175814 ),
 .UNSPECIFIED. ) ;
#66408=CARTESIAN_POINT ( 'NONE',  ( 9.877261637240000169, 2.207988120125000009, 7.624813826992999921 ) ) ;
#66414=CARTESIAN_POINT ( 'NONE',  ( 10.70441484796999987, 3.444517850837000239, 6.009055070331999815 ) ) ;
#66418=CARTESIAN_POINT ( 'NONE',  ( 8.930989158774000458, 2.019067547072999957, 7.390982789861999969 ) ) ;
#66420=DIRECTION ( 'NONE',  ( -1.000000000000000000, 2.664535259100999844E-14, -3.552713678802000396E-14 ) ) ;
#66423=CARTESIAN_POINT ( 'NONE',  ( 8.798539158775000146, 5.851083642416999631, -7.072167224702999633 ) ) ;
#66431=CARTESIAN_POINT ( 'NONE',  ( 0.9669268129214999563, 3.284885639805000146, 1.453889781857000019 ) ) ;
#66436=EDGE_CURVE ( 'NONE', #6658, #20386, #56462, .T. ) ;
#66443=ORIENTED_EDGE ( 'NONE', *, *, #28518, .F. ) ;
#66444=ADVANCED_FACE ( 'NONE', ( #12347 ), #49060, .T. ) ;
#66445=CARTESIAN_POINT ( 'NONE',  ( 8.020982780409999791, 3.245534453799999941, 8.949623695221001540 ) ) ;
#66449=CARTESIAN_POINT ( 'NONE',  ( 1.938748887005000032, -2.269833785962000139, -2.784166953248000009 ) ) ;
#66451=CARTESIAN_POINT ( 'NONE',  ( 10.75046352948212380, 3.823292445202991274, -8.850187295431105383 ) ) ;
#66453=CARTESIAN_POINT ( 'NONE',  ( 10.55813337864000090, 2.466561068647000532, 6.633529813744000414 ) ) ;
#66456=CARTESIAN_POINT ( 'NONE',  ( 7.921841810112000282, 2.875629839593000003, -6.725486766668000271 ) ) ;
#66461=CARTESIAN_POINT ( 'NONE',  ( 8.077529320371693800, 4.037993861317246136, 5.758221802075652818 ) ) ;
#66471=CARTESIAN_POINT ( 'NONE',  ( 10.90634530628000043, 3.089682683751000081, -6.534327427410000055 ) ) ;
#66477=AXIS2_PLACEMENT_3D ( 'NONE', #16953, #65540, #19030 ) ;
#66479=ORIENTED_EDGE ( 'NONE', *, *, #15779, .F. ) ;
#66480=FACE_OUTER_BOUND ( 'NONE', #49346, .T. ) ;
#66481=CARTESIAN_POINT ( 'NONE',  ( 10.90000668870999867, -1.199999999999999956, -11.27663029882999801 ) ) ;
#66482=EDGE_CURVE ( 'NONE', #44634, #28703, #68820, .T. ) ;
#66492=VERTEX_POINT ( 'NONE', #49399 ) ;
#66493=DIRECTION ( 'NONE',  ( 0.8480635683783692702, 0.3746919961710865610, -0.3746919961710865610 ) ) ;
#66496=CARTESIAN_POINT ( 'NONE',  ( 8.510694764413049285, 3.299154217465439132, 5.962358501161194368 ) ) ;
#66500=CARTESIAN_POINT ( 'NONE',  ( 11.12554667867999925, 8.127034475866000918, -6.768926555484000573 ) ) ;
#66501=CARTESIAN_POINT ( 'NONE',  ( 0.4745747022587999409, -0.8195100712853999880, -3.441407140921999730 ) ) ;
#66507=CARTESIAN_POINT ( 'NONE',  ( 11.08729332543999924, 2.258658230726000138, -7.034579402814999938 ) ) ;
#66509=CARTESIAN_POINT ( 'NONE',  ( 10.96226112747999970, 2.399999999999999911, -6.571291218949999902 ) ) ;
#66523=EDGE_CURVE ( 'NONE', #64300, #43460, #8788, .T. ) ;
#66527=CARTESIAN_POINT ( 'NONE',  ( 7.000000000000000888, 10.16543706753050635, -4.390894937880035265 ) ) ;
#66535=LINE ( 'NONE', #65846, #64526 ) ;
#66539=EDGE_CURVE ( 'NONE', #38520, #23293, #2956, .T. ) ;
#66541=CARTESIAN_POINT ( 'NONE',  ( 9.509454719593000149, 3.116293075258000478, -6.208411413796000033 ) ) ;
#66547=ORIENTED_EDGE ( 'NONE', *, *, #34016, .T. ) ;
#66551=CARTESIAN_POINT ( 'NONE',  ( 9.351420280414000530, 4.953415418491999844, -8.946479654552000227 ) ) ;
#66557=CARTESIAN_POINT ( 'NONE',  ( 7.663649704783383143, 5.119381272888222867, -8.282547693636418629 ) ) ;
#66559=CARTESIAN_POINT ( 'NONE',  ( 9.743314158772999889, 5.149303692842000402, -5.987168472229000393 ) ) ;
#66561=CARTESIAN_POINT ( 'NONE',  ( 10.40878363256000050, 3.093886843363999883, -6.480781753756000185 ) ) ;
#66562=DIRECTION ( 'NONE',  ( 1.000000000000000000, 0.000000000000000000, 0.000000000000000000 ) ) ;
#66571=CARTESIAN_POINT ( 'NONE',  ( 27.64127793187000037, 2.399999999999999911, 6.571291218949999902 ) ) ;
#66575=CARTESIAN_POINT ( 'NONE',  ( 10.31966721959000033, 4.764593388688000530, -5.997651217580999727 ) ) ;
#66583=CARTESIAN_POINT ( 'NONE',  ( 7.871384581343000342, 5.129340811002999878, 6.740051537885999977 ) ) ;
#66586=CARTESIAN_POINT ( 'NONE',  ( 8.590779719591999708, 2.836879604150999601, -8.783908972046001296 ) ) ;
#66592=B_SPLINE_CURVE_WITH_KNOTS ( 'NONE', 3,
 ( #60221, #59523, #28413, #17922, #44154, #22113, #39240, #43458, #34004, #43799, #49727, #16867, #33657, #28766 ),
 .UNSPECIFIED., .F., .F.,
 ( 4, 2, 2, 2, 2, 2, 4 ),
 ( 0.000000000000000000, 0.1250000000000019984, 0.1875000000000012768, 0.2187499999999998335, 0.2499999999999983902, 0.4999999999999975575, 1.000000000000000000 ),
 .UNSPECIFIED. ) ;
#66600=CARTESIAN_POINT ( 'NONE',  ( 11.10000000000000142, 5.582294820874221131, 7.480015404794160716 ) ) ;
#66603=ORIENTED_EDGE ( 'NONE', *, *, #65875, .F. ) ;
#66604=LINE ( 'NONE', #18722, #9547 ) ;
#66606=CARTESIAN_POINT ( 'NONE',  ( 8.605545280412000508, 3.122811675949999977, -6.006064052396999919 ) ) ;
#66608=B_SPLINE_CURVE_WITH_KNOTS ( 'NONE', 3,
 ( #6888, #28224, #49539, #65270, #1651, #27886, #22969, #44319, #49198, #65615, #60382, #33822, #55137, #7240, #44664, #65957, #59001, #21929 ),
 .UNSPECIFIED., .F., .F.,
 ( 4, 2, 2, 2, 2, 2, 2, 2, 4 ),
 ( 0.000000000000000000, 0.1250000000000000555, 0.2500000000000001110, 0.3750000000000001665, 0.5000000000000001110, 0.6250000000000001110, 0.7500000000000001110, 0.8750000000000000000, 1.000000000000000000 ),
 .UNSPECIFIED. ) ;
#66612=CARTESIAN_POINT ( 'NONE',  ( 9.429073750851015845, 2.311705066330824732, 7.962955877358613321 ) ) ;
#66613=CARTESIAN_POINT ( 'NONE',  ( 2.971974909847999946, -3.378548644117000066, -0.5658866386176000240 ) ) ;
#66620=VERTEX_POINT ( 'NONE', #60935 ) ;
#66622=CARTESIAN_POINT ( 'NONE',  ( 7.788935841227000445, 2.863733890340999899, -8.313606627241000524 ) ) ;
#66625=CARTESIAN_POINT ( 'NONE',  ( 10.58580560302224782, 5.314991280552380459, -7.853445763305330729 ) ) ;
#66632=EDGE_CURVE ( 'NONE', #5657, #57674, #17426, .T. ) ;
#66640=DIRECTION ( 'NONE',  ( -1.000000000000000000, 0.000000000000000000, 0.000000000000000000 ) ) ;
#66648=AXIS2_PLACEMENT_3D ( 'NONE', #18817, #60425, #56212 ) ;
#66652=CARTESIAN_POINT ( 'NONE',  ( 0.2066231058121046349, -2.618168328974044765E-06, -3.206444164765644977 ) ) ;
#66653=CARTESIAN_POINT ( 'NONE',  ( 3.500000000000000444, 0.8984343939224210818, 3.199201382548016337 ) ) ;
#66663=CARTESIAN_POINT ( 'NONE',  ( 10.21398584123000042, 3.990126737362999609, -8.809457313313998839 ) ) ;
#66664=CARTESIAN_POINT ( 'NONE',  ( 2.999405651491000135, -3.212481615617999609, 0.1285223249498000098 ) ) ;
#66670=CARTESIAN_POINT ( 'NONE',  ( 9.820199962102000413, 3.883325513302000154, 6.055618835924000187 ) ) ;
#66673=CARTESIAN_POINT ( 'NONE',  ( 10.74609776273999984, 4.263105564403999459, 9.276980853981999786 ) ) ;
#66674=CARTESIAN_POINT ( 'NONE',  ( 11.04166666666769103, 2.793604566010535528, 8.411630010704181259 ) ) ;
#66677=CARTESIAN_POINT ( 'NONE',  ( 10.95905699168409697, 2.826108491929388844, -6.684704321099483870 ) ) ;
#66681=CARTESIAN_POINT ( 'NONE',  ( 8.127093974303878809, 4.981402631029236083, -6.380819531419545498 ) ) ;
#66683=VERTEX_POINT ( 'NONE', #24210 ) ;
#66687=EDGE_CURVE ( 'NONE', #51766, #13783, #13732, .T. ) ;
#66690=CARTESIAN_POINT ( 'NONE',  ( 10.47530200610849604, 5.350262918594154371, 7.499984559551275964 ) ) ;
#66691=ORIENTED_EDGE ( 'NONE', *, *, #9463, .F. ) ;
#66692=CARTESIAN_POINT ( 'NONE',  ( 7.935739158771999868, 5.430400319332999715, 7.210801214872999410 ) ) ;
#66693=CARTESIAN_POINT ( 'NONE',  ( 8.506095280410999493, 2.305580295895999665, -7.860904109308999743 ) ) ;
#66694=CARTESIAN_POINT ( 'NONE',  ( 0.7768612129559736568, -3.384277603090292352, 1.036914961361027343 ) ) ;
#66695=CARTESIAN_POINT ( 'NONE',  ( 11.17788388625999829, 2.412139249855000056, -7.075601348558000048 ) ) ;
#66705=CARTESIAN_POINT ( 'NONE',  ( 1.250973465874999802, -3.500000000000000000, 0.000000000000000000 ) ) ;
#66720=CARTESIAN_POINT ( 'NONE',  ( 9.939260841229000221, 5.099602161831000124, -9.049221499261999924 ) ) ;
#66722=CARTESIAN_POINT ( 'NONE',  ( 8.330224159023998709, 2.898680183691999979, -6.607597200868999820 ) ) ;
#66727=DIRECTION ( 'NONE',  ( 1.000000000000000000, 0.000000000000000000, 0.000000000000000000 ) ) ;
#66728=VECTOR ( 'NONE', #15462, 1000.000000000000000 ) ;
#66737=CARTESIAN_POINT ( 'NONE',  ( 9.907648723390195755, 5.170927832464149887, -8.821309888205709271 ) ) ;
#66746=ORIENTED_EDGE ( 'NONE', *, *, #63821, .T. ) ;
#66755=EDGE_CURVE ( 'NONE', #12694, #20104, #10533, .T. ) ;
#66756=CARTESIAN_POINT ( 'NONE',  ( 9.215291255903000689, 4.861981595026999337, 8.938817176893000038 ) ) ;
#66761=CARTESIAN_POINT ( 'NONE',  ( 9.351497027444999333, 4.821940693094999730, 8.950154065657999425 ) ) ;
#66767=CARTESIAN_POINT ( 'NONE',  ( 9.342517219591000455, 5.057081813675999626, 8.967637988488998957 ) ) ;
#66768=CARTESIAN_POINT ( 'NONE',  ( 9.261662452849000360, 2.944259351255000379, 6.507396354981000108 ) ) ;
#66771=CARTESIAN_POINT ( 'NONE',  ( 9.643864158774000828, 2.927176851028000293, -5.932007155957999878 ) ) ;
#66773=EDGE_CURVE ( 'NONE', #15877, #11716, #9847, .T. ) ;
#66782=CARTESIAN_POINT ( 'NONE',  ( 2.206657498381999982, -3.444624976169999631, -1.019033653642999804 ) ) ;
#66787=CARTESIAN_POINT ( 'NONE',  ( 9.996463691909600158, 5.100000000000000533, -6.665341197398679363 ) ) ;
#66788=VECTOR ( 'NONE', #57048, 1000.000000000000000 ) ;
#66794=CARTESIAN_POINT ( 'NONE',  ( 8.085170280410000743, 2.431401017850999935, 7.958393275880999873 ) ) ;
#66799=CARTESIAN_POINT ( 'NONE',  ( 0.6465629140399999919, 2.290033430544000215, -2.273164938691999648 ) ) ;
#66804=CARTESIAN_POINT ( 'NONE',  ( 9.778460659405999067, 5.743717947473999885, 7.748300625457000379 ) ) ;
#66807=CARTESIAN_POINT ( 'NONE',  ( 5.000000000000000000, 0.000000000000000000, 0.000000000000000000 ) ) ;
#66810=CARTESIAN_POINT ( 'NONE',  ( 10.56498513754044311, 5.349957030113837497, -7.500000808964303545 ) ) ;
#66811=CARTESIAN_POINT ( 'NONE',  ( 9.565773468336619345, 5.100000000000000533, 6.304440313901286785 ) ) ;
#66812=CARTESIAN_POINT ( 'NONE',  ( 8.017695689388432356, 2.842496704177993827, 6.173521863453695246 ) ) ;
#66813=ORIENTED_EDGE ( 'NONE', *, *, #53493, .T. ) ;
#66815=DIRECTION ( 'NONE',  ( 0.000000000000000000, -1.000000000000000000, 0.000000000000000000 ) ) ;
#66819=CARTESIAN_POINT ( 'NONE',  ( 4.149992563291998948, 1.999946284944287722, -0.2617923565147984299 ) ) ;
#66820=CARTESIAN_POINT ( 'NONE',  ( 6.999999691988000095, -12.89129024452999950, -1.677687644161999891 ) ) ;
#66821=CARTESIAN_POINT ( 'NONE',  ( 11.09999999999999964, 4.000000000000000000, 7.500000000000000000 ) ) ;
#66822=CARTESIAN_POINT ( 'NONE',  ( 10.36950244779999863, 2.719131864236000062, -7.031786688683999920 ) ) ;
#66823=CARTESIAN_POINT ( 'NONE',  ( 8.691485517493021007, 3.974336348583935141, -8.874742188917888797 ) ) ;
#66829=ORIENTED_EDGE ( 'NONE', *, *, #49027, .T. ) ;
#66831=CARTESIAN_POINT ( 'NONE',  ( 5.966666563206250551, -12.43894743589586405, -2.828924746354209763 ) ) ;
#66832=CARTESIAN_POINT ( 'NONE',  ( 6.308784017580002512, 8.386574891157003719, 3.907856452066002184 ) ) ;
#66834=EDGE_CURVE ( 'NONE', #14790, #30735, #481, .T. ) ;
#66836=EDGE_CURVE ( 'NONE', #45160, #56759, #39617, .T. ) ;
#66841=ORIENTED_EDGE ( 'NONE', *, *, #18109, .F. ) ;
#66845=CYLINDRICAL_SURFACE ( 'NONE', #29455, 0.5000000000000002220 ) ;
#66847=CARTESIAN_POINT ( 'NONE',  ( 8.844321844545273592, 2.684787752319955256, -7.853330290198121233 ) ) ;
#66849=CARTESIAN_POINT ( 'NONE',  ( 7.966460921982568166, 5.180256874905277975, 8.180071673469157645 ) ) ;
#66853=FACE_OUTER_BOUND ( 'NONE', #1003, .T. ) ;
#66858=VECTOR ( 'NONE', #65965, 1000.000000000000000 ) ;
#66867=CARTESIAN_POINT ( 'NONE',  ( 6.949993407501000142, 13.87069231928999891, 4.225386915259999654 ) ) ;
#66871=CARTESIAN_POINT ( 'NONE',  ( 8.654006363156080184, 3.802134689404237378, 5.879617511049012535 ) ) ;
#66872=EDGE_CURVE ( 'NONE', #21901, #16690, #58796, .T. ) ;
#66875=CARTESIAN_POINT ( 'NONE',  ( 5.399998984437000438, 12.98068687585000092, 1.765643277144999912 ) ) ;
#66883=CARTESIAN_POINT ( 'NONE',  ( 8.392998836384890637, 2.713269406560838259, -7.026678396099404367 ) ) ;
#66885=CARTESIAN_POINT ( 'NONE',  ( 2.978056799211333594, 2.150913519912206695, -2.798833948393626869 ) ) ;
#66886=CARTESIAN_POINT ( 'NONE',  ( 9.468589158772999781, 4.034680274230000308, -6.102912434217000026 ) ) ;
#66888=ORIENTED_EDGE ( 'NONE', *, *, #66237, .F. ) ;
#66889=CARTESIAN_POINT ( 'NONE',  ( 4.000000000000000000, -0.5625597044909159683, 2.094005558844440174 ) ) ;
#66894=CARTESIAN_POINT ( 'NONE',  ( 8.614404719593999005, 5.030502105212999453, -6.322203460290999999 ) ) ;
#66899=CARTESIAN_POINT ( 'NONE',  ( 5.399998535875000449, 6.217248937900999058E-14, 3.708144902247999495E-14 ) ) ;
#66900=ORIENTED_EDGE ( 'NONE', *, *, #35927, .F. ) ;
#66901=DIRECTION ( 'NONE',  ( -1.000000000000000000, 0.000000000000000000, 0.000000000000000000 ) ) ;
#66905=CARTESIAN_POINT ( 'NONE',  ( 10.49937419337999955, 2.985313722448000195, -6.358656051156999389 ) ) ;
#66910=EDGE_CURVE ( 'NONE', #61746, #15326, #64606, .T. ) ;
#66911=ADVANCED_FACE ( 'NONE', ( #37795 ), #11222, .F. ) ;
#66926=ORIENTED_EDGE ( 'NONE', *, *, #27025, .F. ) ;
#66928=CARTESIAN_POINT ( 'NONE',  ( 9.427245280414000561, 4.989193221215000307, -6.287302145481000082 ) ) ;
#66948=B_SPLINE_CURVE_WITH_KNOTS ( 'NONE', 3,
 ( #17015, #23311, #55124, #43951 ),
 .UNSPECIFIED., .F., .F.,
 ( 4, 4 ),
 ( 0.8746471354527770581, 1.000000000000000000 ),
 .UNSPECIFIED. ) ;
#66953=ADVANCED_FACE ( 'NONE', ( #391 ), #14048, .T. ) ;
#66954=CARTESIAN_POINT ( 'NONE',  ( 0.3408104211468100941, -2.670907248151955571, 2.053682415916353587 ) ) ;
#66955=CARTESIAN_POINT ( 'NONE',  ( 9.884776718858692135, 2.675334876101736814, -7.165831161227206536 ) ) ;
#66956=ORIENTED_EDGE ( 'NONE', *, *, #6207, .F. ) ;
#66961=CARTESIAN_POINT ( 'NONE',  ( 7.935739158771999868, 5.430400319332999715, 7.210801214872999410 ) ) ;
#66963=ORIENTED_EDGE ( 'NONE', *, *, #24475, .F. ) ;
#66965=CARTESIAN_POINT ( 'NONE',  ( 7.241960841228999968, 3.508889101792000087, -8.808374944720000599 ) ) ;
#66966=CARTESIAN_POINT ( 'NONE',  ( 10.71081754702572120, 3.646708176540620183, -8.814774986206115770 ) ) ;
#66967=CARTESIAN_POINT ( 'NONE',  ( 1.542640132540499254, 3.058252359239899132, 1.762666431298154146 ) ) ;
#66976=CARTESIAN_POINT ( 'NONE',  ( 10.95792420851827664, 8.961205178941138882, -6.431113706263509755 ) ) ;
#66977=CARTESIAN_POINT ( 'NONE',  ( 7.605092582665629486, 3.121316641526586277, 8.549894104503566794 ) ) ;
#66981=ORIENTED_EDGE ( 'NONE', *, *, #56121, .F. ) ;
#66985=CARTESIAN_POINT ( 'NONE',  ( 11.00503223350061610, 5.210128592361205513, 6.635071905858886510 ) ) ;
#66988=ORIENTED_EDGE ( 'NONE', *, *, #64935, .T. ) ;
#66991=CARTESIAN_POINT ( 'NONE',  ( 7.143022165044063065, 2.536141393688100987, -6.357131192860917324 ) ) ;
#67000=B_SPLINE_CURVE_WITH_KNOTS ( 'NONE', 3,
 ( #32261, #36199, #57175, #66977, #9271, #68004, #57513, #67315, #46700, #25023 ),
 .UNSPECIFIED., .F., .F.,
 ( 4, 2, 2, 2, 4 ),
 ( 0.000000000000000000, 0.2500000000000000000, 0.5000000000000000000, 0.7500000000000000000, 1.000000000000000000 ),
 .UNSPECIFIED. ) ;
#67002=CARTESIAN_POINT ( 'NONE',  ( 10.37026939687000038, 5.571553923009999743, 7.748385725654999945 ) ) ;
#67004=CARTESIAN_POINT ( 'NONE',  ( 0.1499942179680000265, -2.678379783547566895, 0.7197945678028326855 ) ) ;
#67005=CARTESIAN_POINT ( 'NONE',  ( 9.965360841230999966, 4.034680274230000308, -6.102912434217000026 ) ) ;
#67006=CARTESIAN_POINT ( 'NONE',  ( 3.061592516560999844, 3.309521440799999770, 1.672333154171000036 ) ) ;
#67012=CARTESIAN_POINT ( 'NONE',  ( 10.99933470386000067, 5.081013421858999735, 8.239043921879998678 ) ) ;
#67014=EDGE_CURVE ( 'NONE', #53328, #68916, #12268, .T. ) ;
#67016=CARTESIAN_POINT ( 'NONE',  ( 9.504903297738000134, 3.934733353759999552, 5.704831249548000471 ) ) ;
#67021=B_SPLINE_CURVE_WITH_KNOTS ( 'NONE', 3,
 ( #66705, #23024, #7637, #49945, #66012, #17794, #50293, #12891, #50635, #18135, #24407, #29322, #2736, #39457, #34220, #2392, #23716, #13588 ),
 .UNSPECIFIED., .F., .F.,
 ( 4, 2, 2, 2, 2, 2, 2, 2, 4 ),
 ( 0.000000000000000000, 0.1250000000000000278, 0.2500000000000000555, 0.3749999999999999445, 0.4999999999999999445, 0.6249999999999998890, 0.7499999999999998890, 0.8750000000000000000, 1.000000000000000000 ),
 .UNSPECIFIED. ) ;
#67024=CARTESIAN_POINT ( 'NONE',  ( 8.112357311251360059, 5.053573198694982338, -6.503562400629845364 ) ) ;
#67029=CARTESIAN_POINT ( 'NONE',  ( 2.500973465876000112, 3.500000000000000000, 0.000000000000000000 ) ) ;
#67031=ORIENTED_EDGE ( 'NONE', *, *, #58006, .F. ) ;
#67032=CARTESIAN_POINT ( 'NONE',  ( 7.037114158771000660, 4.623631324973000112, 8.651459902566999816 ) ) ;
#67035=CARTESIAN_POINT ( 'NONE',  ( 0.8009734658753000502, -3.500000000000000000, 0.000000000000000000 ) ) ;
#67036=CARTESIAN_POINT ( 'NONE',  ( 10.34266415877000078, 5.750490533313000086, -8.094415907623000450 ) ) ;
#67038=CARTESIAN_POINT ( 'NONE',  ( 1.498890132540667164, 2.798833948393634419, -2.150913519912196925 ) ) ;
#67054=CARTESIAN_POINT ( 'NONE',  ( 0.5120809256593666925, 3.099336848560416247, -1.647554626188311167 ) ) ;
#67059=CARTESIAN_POINT ( 'NONE',  ( 9.152520280414000453, 4.102804347295999854, -5.770625657082999460 ) ) ;
#67061=CARTESIAN_POINT ( 'NONE',  ( 8.228368194308000483, 4.806758213781000322, 6.177034601037000527 ) ) ;
#67065=ORIENTED_EDGE ( 'NONE', *, *, #18232, .T. ) ;
#67073=CARTESIAN_POINT ( 'NONE',  ( 9.209122513651813335, 5.100000000000000533, 6.320295141290149132 ) ) ;
#67079=EDGE_CURVE ( 'NONE', #47667, #14966, #64270, .T. ) ;
#67083=ORIENTED_EDGE ( 'NONE', *, *, #3647, .T. ) ;
#67089=CARTESIAN_POINT ( 'NONE',  ( 8.688561307509338860, 5.076530052485727751, 6.260338817618603002 ) ) ;
#67092=CARTESIAN_POINT ( 'NONE',  ( 9.104014120666999332, 5.045862207587999748, 8.527865280865999154 ) ) ;
#67096=EDGE_LOOP ( 'NONE', ( #26897, #17778 ) ) ;
#67099=CARTESIAN_POINT ( 'NONE',  ( 9.757669403192000601, 4.489270656625000022, 5.986034819543999852 ) ) ;
#67105=CARTESIAN_POINT ( 'NONE',  ( 8.122954719591000128, 3.566637212418000136, 5.743604853744000316 ) ) ;
#67106=CARTESIAN_POINT ( 'NONE',  ( 9.972850246170999355, 5.044468801812000081, 6.258104779495000436 ) ) ;
#67117=CARTESIAN_POINT ( 'NONE',  ( 1.677382716469999924, -1.296472565164999979, 3.528106597684999901 ) ) ;
#67125=LINE ( 'NONE', #55274, #43336 ) ;
#67128=CARTESIAN_POINT ( 'NONE',  ( 7.481079719589999399, 2.374037589774999901, 8.293392681990997772 ) ) ;
#67132=CARTESIAN_POINT ( 'NONE',  ( 1.075700459007000065, -0.3467249428283000201, -3.408020022541999872 ) ) ;
#67134=PLANE ( 'NONE',  #23242 ) ;
#67137=CARTESIAN_POINT ( 'NONE',  ( 9.534905769125000319, 3.030948166328000237, 8.761984216465000586 ) ) ;
#67145=CARTESIAN_POINT ( 'NONE',  ( 8.550530719455091244, 3.458520770602964589, 5.843532653519790898 ) ) ;
#67149=ORIENTED_EDGE ( 'NONE', *, *, #8276, .F. ) ;
#67153=DIRECTION ( 'NONE',  ( -1.000000000000000000, 0.000000000000000000, 0.000000000000000000 ) ) ;
#67155=CARTESIAN_POINT ( 'NONE',  ( 9.753142190738998352, 4.104977339646000090, 9.293283246364000050 ) ) ;
#67156=DIRECTION ( 'NONE',  ( 0.9999999999999997780, -1.366939932386999783E-09, -2.239632587909999191E-08 ) ) ;
#67157=CARTESIAN_POINT ( 'NONE',  ( 7.550000000000000711, 4.000000000000000000, 8.849999999999999645 ) ) ;
#67162=EDGE_CURVE ( 'NONE', #10085, #51086, #13007, .T. ) ;
#67177=CARTESIAN_POINT ( 'NONE',  ( 10.98768472639999949, 2.860903110339000133, 4.945212061661000469 ) ) ;
#67178=CARTESIAN_POINT ( 'NONE',  ( 6.999999691988000095, -1.865174681369999698E-13, 1.040631529540999901E-13 ) ) ;
#67180=CARTESIAN_POINT ( 'NONE',  ( 8.469851049286248212, 3.034069930634795575, 6.168783214997897169 ) ) ;
#67184=CARTESIAN_POINT ( 'NONE',  ( 10.31905590579000176, 2.899999999999999911, -6.571291218949999902 ) ) ;
#67186=CARTESIAN_POINT ( 'NONE',  ( 11.03681693200000069, 2.776621198269999979, 5.023845135586999966 ) ) ;
#67190=CARTESIAN_POINT ( 'NONE',  ( 6.899999691988000450, -12.20988339176000004, -3.111064831550000243 ) ) ;
#67205=CARTESIAN_POINT ( 'NONE',  ( 7.100000000000000533, 4.000000000000000000, 7.500000000000000000 ) ) ;
#67206=EDGE_LOOP ( 'NONE', ( #36819, #52946, #9214, #36781 ) ) ;
#67212=CARTESIAN_POINT ( 'NONE',  ( 2.667640132542667963, -1.762666431298160141, 3.058252359239895579 ) ) ;
#67220=CARTESIAN_POINT ( 'NONE',  ( -0.000000000000000000, -1.781870588985605464, -2.319407620233724820 ) ) ;
#67225=CARTESIAN_POINT ( 'NONE',  ( 8.971339158776000744, 4.082930418187999955, -6.104944817728999773 ) ) ;
#67228=CARTESIAN_POINT ( 'NONE',  ( 4.000000000000000000, 2.149963194831999935, 0.1424560705006994998 ) ) ;
#67233=CARTESIAN_POINT ( 'NONE',  ( 8.555820280412000045, 2.414630869937000046, -6.801495146585999407 ) ) ;
#67234=DIRECTION ( 'NONE',  ( 0.000000000000000000, -1.000000000000000000, 0.000000000000000000 ) ) ;
#67239=CARTESIAN_POINT ( 'NONE',  ( 3.452384183491000069, 1.140396268832999827, -3.309002319436000317 ) ) ;
#67241=CARTESIAN_POINT ( 'NONE',  ( 8.929995280412999392, 5.030502105212999453, -6.322203460290999999 ) ) ;
#67245=CARTESIAN_POINT ( 'NONE',  ( 10.00074698269999907, 2.373893144840999891, -7.962435130300000274 ) ) ;
#67252=DIRECTION ( 'NONE',  ( 0.000000000000000000, 0.8648648648648717963, 0.5020047465136829867 ) ) ;
#67254=ORIENTED_EDGE ( 'NONE', *, *, #722, .F. ) ;
#67255=CARTESIAN_POINT ( 'NONE',  ( 8.616995677562000466, 4.876077402042000131, 5.996974966532000018 ) ) ;
#67256=CARTESIAN_POINT ( 'NONE',  ( 10.46298584122999920, 3.993164721578000176, -6.140176455708999725 ) ) ;
#67266=CARTESIAN_POINT ( 'NONE',  ( 9.228345280414000484, 2.481540185810000132, -7.878707153279001396 ) ) ;
#67274=CARTESIAN_POINT ( 'NONE',  ( 8.785641572568696489, 4.855572132619596637, 9.057504313711934429 ) ) ;
#67276=EDGE_LOOP ( 'NONE', ( #17844, #59070, #1544, #61111, #57194 ) ) ;
#67281=CARTESIAN_POINT ( 'NONE',  ( 7.953506848056347778, 4.927760041869837515, 6.408859279631051287 ) ) ;
#67289=CARTESIAN_POINT ( 'NONE',  ( 9.216851002545999094, 2.832432432432000269, 6.822293592207000934 ) ) ;
#67290=CARTESIAN_POINT ( 'NONE',  ( 3.448794404255000057, -3.398741721523000248, 0.4282444512000999626 ) ) ;
#67301=EDGE_CURVE ( 'NONE', #54836, #58875, #22971, .T. ) ;
#67305=CARTESIAN_POINT ( 'NONE',  ( 1.730140132539749853, -3.408904368339107815, 0.9161175952574674985 ) ) ;
#67315=CARTESIAN_POINT ( 'NONE',  ( 7.688669563556804754, 2.651071518674656513, 7.261053863064154790 ) ) ;
#67316=CARTESIAN_POINT ( 'NONE',  ( 7.830279719588000731, 3.552539078410000162, -8.999639305067001160 ) ) ;
#67318=DIRECTION ( 'NONE',  ( 0.000000000000000000, 0.000000000000000000, 1.000000000000000000 ) ) ;
#67319=ORIENTED_EDGE ( 'NONE', *, *, #1092, .T. ) ;
#67326=VERTEX_POINT ( 'NONE', #33824 ) ;
#67331=CARTESIAN_POINT ( 'NONE',  ( 3.105140132544083276, 0.9161175952574701631, 3.408904368339106927 ) ) ;
#67336=EDGE_LOOP ( 'NONE', ( #59665, #1776 ) ) ;
#67337=CARTESIAN_POINT ( 'NONE',  ( 9.701978494675000064, 3.399139198672999740, 6.026757051093999173 ) ) ;
#67339=CARTESIAN_POINT ( 'NONE',  ( 9.874770280412001000, 4.038835765825999680, -5.935509327774999733 ) ) ;
#67340=CARTESIAN_POINT ( 'NONE',  ( 3.515922480947999862, 1.817153928780999905, 3.042350142939999724 ) ) ;
#67349=CARTESIAN_POINT ( 'NONE',  ( 9.034110134264999203, 4.695345051283999815, 8.660667941667000491 ) ) ;
#67351=CARTESIAN_POINT ( 'NONE',  ( 11.09999999999999964, 2.899999999999999911, 4.467422426380999845 ) ) ;
#67352=CARTESIAN_POINT ( 'NONE',  ( 9.124700695083998170, 4.778663323155000420, 8.799742559280000265 ) ) ;
#67360=CARTESIAN_POINT ( 'NONE',  ( 0.4511054431563896183, 3.350439766384084361, -0.9395068199138416620 ) ) ;
#67363=AXIS2_PLACEMENT_3D ( 'NONE', #35533, #42151, #9280 ) ;
#67364=CARTESIAN_POINT ( 'NONE',  ( 4.000000000000000888, 1.719428477288966750, -1.321180510578594758 ) ) ;
#67369=CARTESIAN_POINT ( 'NONE',  ( 8.668204719592999652, 3.979464555644999901, 9.134076336209998814 ) ) ;
#67372=CARTESIAN_POINT ( 'NONE',  ( 10.35752971959000135, 5.367812128871999988, -6.514736131541999598 ) ) ;
#67380=ORIENTED_EDGE ( 'NONE', *, *, #618, .F. ) ;
#67384=DIRECTION ( 'NONE',  ( 0.000000000000000000, -1.000000000000000000, 0.000000000000000000 ) ) ;
#67394=EDGE_LOOP ( 'NONE', ( #23741, #16669, #35933, #53797, #64261, #36304, #10817, #54371 ) ) ;
#67396=CARTESIAN_POINT ( 'NONE',  ( 8.447510841229000533, 4.933589693325000525, -9.154576215408999573 ) ) ;
#67401=CARTESIAN_POINT ( 'NONE',  ( 7.539232780409000689, 4.696238830159999544, 5.830273622963999536 ) ) ;
#67403=ORIENTED_EDGE ( 'NONE', *, *, #29901, .T. ) ;
#67404=CARTESIAN_POINT ( 'NONE',  ( 9.277969429786152133, 2.899999999999999911, -6.446868419509604209 ) ) ;
#67407=VERTEX_POINT ( 'NONE', #67562 ) ;
#67418=FACE_OUTER_BOUND ( 'NONE', #21399, .T. ) ;
#67425=CARTESIAN_POINT ( 'NONE',  ( 10.46009300862000124, 2.565654508827999614, -6.975684004278000394 ) ) ;
#67429=CARTESIAN_POINT ( 'NONE',  ( 10.62197831623999988, 5.779783227492000464, 7.256572995198999898 ) ) ;
#67435=CARTESIAN_POINT ( 'NONE',  ( 10.76010575649000067, 4.535386075958999896, 6.001721352166000223 ) ) ;
#67438=B_SPLINE_CURVE_WITH_KNOTS ( 'NONE', 3,
 ( #16380, #59721, #68828, #54479 ),
 .UNSPECIFIED., .F., .F.,
 ( 4, 4 ),
 ( 0.000000000000000000, 1.000000000000000000 ),
 .UNSPECIFIED. ) ;
#67441=AXIS2_PLACEMENT_3D ( 'NONE', #2578, #28473, #18666 ) ;
#67442=CARTESIAN_POINT ( 'NONE',  ( 8.032364158772001161, 3.524748802314000340, 5.573833469815000718 ) ) ;
#67443=CARTESIAN_POINT ( 'NONE',  ( 10.77962664842000073, 2.397507474987000009, 7.755423212350999407 ) ) ;
#67447=CARTESIAN_POINT ( 'NONE',  ( 8.640504719592000171, 2.305580295895999665, -7.860904109308999743 ) ) ;
#67448=CARTESIAN_POINT ( 'NONE',  ( 11.09999999999999964, 4.000000000000000000, 7.500000000000000000 ) ) ;
#67451=CARTESIAN_POINT ( 'NONE',  ( 3.365110627350583083, -0.4777639219876382293, -3.497143207087723304 ) ) ;
#67455=CARTESIAN_POINT ( 'NONE',  ( 2.201884160320000117, -2.304706330186000240, 2.969293668968000066 ) ) ;
#67457=CARTESIAN_POINT ( 'NONE',  ( 9.170239158775000732, 4.769103072373000352, -8.666849124598000387 ) ) ;
#67459=CARTESIAN_POINT ( 'NONE',  ( 10.83253786428999987, 2.899999999999999911, 6.571291218949999902 ) ) ;
#67466=CARTESIAN_POINT ( 'NONE',  ( 9.368920280410000245, 5.618384167307999277, 7.727742442702000503 ) ) ;
#67467=ADVANCED_FACE ( 'NONE', ( #57419 ), #28619, .F. ) ;
#67474=AXIS2_PLACEMENT_3D ( 'NONE', #34110, #23265, #39007 ) ;
#67476=CARTESIAN_POINT ( 'NONE',  ( 0.9803365601255999984, -3.300563260077000294, -0.9171157435373999967 ) ) ;
#67477=EDGE_LOOP ( 'NONE', ( #50194, #9338, #3679, #1407 ) ) ;
#67478=CARTESIAN_POINT ( 'NONE',  ( 1.047957204161283018, -3.182233228816532922, -0.8842357997067202824 ) ) ;
#67481=CARTESIAN_POINT ( 'NONE',  ( 9.945533384955998812, 2.906048475816000121, 8.880389653997999844 ) ) ;
#67488=CARTESIAN_POINT ( 'NONE',  ( 8.173029125821519969, 5.656335574181040826, 6.888602418924802961 ) ) ;
#67491=B_SPLINE_CURVE_WITH_KNOTS ( 'NONE', 3,
 ( #6362, #58480, #15828, #26328, #43089, #48680, #1131, #10582, #32272, #26680 ),
 .UNSPECIFIED., .F., .F.,
 ( 4, 2, 2, 2, 4 ),
 ( 0.1254224513349476711, 0.3127176035874427718, 0.5000127558399378724, 0.6873079080924326956, 0.8746030603449276297 ),
 .UNSPECIFIED. ) ;
#67500=CARTESIAN_POINT ( 'NONE',  ( 11.15982925107999968, 5.578232410510000072, 8.067793621926998782 ) ) ;
#67502=CARTESIAN_POINT ( 'NONE',  ( 10.93146722582000052, 2.472885155055999817, -7.514158739122999364 ) ) ;
#67508=CARTESIAN_POINT ( 'NONE',  ( 8.047385841228999581, 4.468366666325000125, 8.882140983065999862 ) ) ;
#67510=AXIS2_PLACEMENT_3D ( 'NONE', #17462, #21656, #48932 ) ;
#67512=CARTESIAN_POINT ( 'NONE',  ( 10.65729680854845540, 3.174840887412555546, -4.784047223682147632 ) ) ;
#67526=CARTESIAN_POINT ( 'NONE',  ( 8.688131671361706054, 4.829518895119560895, -8.579743915872116489 ) ) ;
#67528=CARTESIAN_POINT ( 'NONE',  ( 0.1455175461370999956, 3.330914467393999878, 1.191613524625000142 ) ) ;
#67534=CARTESIAN_POINT ( 'NONE',  ( 10.49411415877000131, 2.866942652264999669, -8.960728730887002058 ) ) ;
#67546=DIRECTION ( 'NONE',  ( 0.000000000000000000, 1.000000000000000000, 0.000000000000000000 ) ) ;
#67547=DIRECTION ( 'NONE',  ( 0.000000000000000000, 1.000000000000000000, 0.000000000000000000 ) ) ;
#67555=CARTESIAN_POINT ( 'NONE',  ( 7.000000000000000000, 10.80467225524999897, 3.475853594956999970 ) ) ;
#67562=CARTESIAN_POINT ( 'NONE',  ( 2.435247277619000172, 2.372532593102000043, -2.573147701680999599 ) ) ;
#67563=DIRECTION ( 'NONE',  ( 1.000000000000000000, 0.000000000000000000, 0.000000000000000000 ) ) ;
#67575=CARTESIAN_POINT ( 'NONE',  ( 8.397785841227999981, 5.616457598545999907, -8.245813000738998255 ) ) ;
#67576=CARTESIAN_POINT ( 'NONE',  ( 2.262975856965000254, 2.754481206214999922, -1.355138954038999977 ) ) ;
#67577=CARTESIAN_POINT ( 'NONE',  ( 10.10733666362725991, 2.230327070931253264, -7.110663345345299646 ) ) ;
#67582=DIRECTION ( 'NONE',  ( -0.000000000000000000, 0.9454292341245821296, 0.3258275053806940491 ) ) ;
#67584=CARTESIAN_POINT ( 'NONE',  ( 8.889129719593999113, 5.687930027805999877, -7.109876198051000351 ) ) ;
#67585=VERTEX_POINT ( 'NONE', #59484 ) ;
#67586=CARTESIAN_POINT ( 'NONE',  ( 11.19121071698999970, 3.005389011699000079, -6.023544385387999966 ) ) ;
#67596=CARTESIAN_POINT ( 'NONE',  ( 10.19794834123000093, 4.262170647947000290, -8.834315641189999013 ) ) ;
#67601=CARTESIAN_POINT ( 'NONE',  ( 7.851231298947399573, 5.072114957085871012, 6.622200184418144175 ) ) ;
#67604=VERTEX_POINT ( 'NONE', #10560 ) ;
#67606=CARTESIAN_POINT ( 'NONE',  ( 9.377520280414000098, 4.092867382745001059, -5.937785237406000505 ) ) ;
#67607=CARTESIAN_POINT ( 'NONE',  ( 9.293683662962452630, 4.685540010276588063, 9.106439227925379853 ) ) ;
#67610=CARTESIAN_POINT ( 'NONE',  ( 7.800894426331000275, 3.218815461055000160, 6.398977422524000147 ) ) ;
#67617=CARTESIAN_POINT ( 'NONE',  ( 10.08422653160753413, 2.899999999999999911, 6.304440313740826696 ) ) ;
#67619=CARTESIAN_POINT ( 'NONE',  ( 9.319055905798999007, 2.899999999999999911, -6.571291218949999902 ) ) ;
#67621=DIRECTION ( 'NONE',  ( -2.340984983634000236E-09, 1.000000000000000000, 1.141937478005999895E-09 ) ) ;
#67622=CARTESIAN_POINT ( 'NONE',  ( 4.966698988835610784, 2.066632171653634664, -9.814801839911485045E-10 ) ) ;
#67625=EDGE_CURVE ( 'NONE', #58126, #10880, #68691, .T. ) ;
#67626=ADVANCED_FACE ( 'NONE', ( #21731 ), #58118, .F. ) ;
#67629=VECTOR ( 'NONE', #41326, 1000.000000000000000 ) ;
#67631=CARTESIAN_POINT ( 'NONE',  ( 11.10000057264999995, 0.4999994248636999705, 9.776630284457000997 ) ) ;
#67633=CARTESIAN_POINT ( 'NONE',  ( 9.906851002540999929, 2.832432432432000269, -6.822293592207000934 ) ) ;
#67638=CARTESIAN_POINT ( 'NONE',  ( 8.834364158772999076, 4.141907758973999876, 6.047574021139999978 ) ) ;
#67653=ORIENTED_EDGE ( 'NONE', *, *, #3138, .F. ) ;
#67655=CARTESIAN_POINT ( 'NONE',  ( 9.050000000000000711, 0.000000000000000000, -4.000000000000000000 ) ) ;
#67656=CARTESIAN_POINT ( 'NONE',  ( 7.929729719587999881, 2.435784185744999775, -7.548665584409000040 ) ) ;
#67660=CARTESIAN_POINT ( 'NONE',  ( 2.146806799206917304, -0.9161175952574931447, 3.408904368339100710 ) ) ;
#67665=CARTESIAN_POINT ( 'NONE',  ( 9.152446624286001864, 2.899999999999999911, -6.169193161299999950 ) ) ;
#67669=DIRECTION ( 'NONE',  ( 0.000000000000000000, 1.000000000000000000, 0.000000000000000000 ) ) ;
#67671=CARTESIAN_POINT ( 'NONE',  ( 10.93769853197999886, 5.063116524846000388, -4.920828787216999345 ) ) ;
#67676=VERTEX_POINT ( 'NONE', #5652 ) ;
#67677=CARTESIAN_POINT ( 'NONE',  ( 10.29378723213999969, 3.483632952461999999, 6.176337842045999338 ) ) ;
#67681=CARTESIAN_POINT ( 'NONE',  ( 8.880270280412998929, 4.146787477634999775, -5.941926545671999627 ) ) ;
#67682=CARTESIAN_POINT ( 'NONE',  ( 2.726256808742000270, -3.050987738140999994, 2.107392784704999578 ) ) ;
#67689=EDGE_CURVE ( 'NONE', #28055, #10085, #47973, .T. ) ;
#67691=CARTESIAN_POINT ( 'NONE',  ( 3.290556799210374805, -3.500000000000002220, 0.4581489286484968781 ) ) ;
#67694=CARTESIAN_POINT ( 'NONE',  ( 10.65050915380999896, 5.200037120669999346, 5.937706951697999891 ) ) ;
#67703=ORIENTED_EDGE ( 'NONE', *, *, #57773, .T. ) ;
#67708=VERTEX_POINT ( 'NONE', #53894 ) ;
#67713=CARTESIAN_POINT ( 'NONE',  ( 11.20537028040999949, 2.688545137295000220, -8.273930556758998023 ) ) ;
#67718=CARTESIAN_POINT ( 'NONE',  ( 11.09999999999999964, 5.350000000000000533, 7.500000000000000000 ) ) ;
#67719=AXIS2_PLACEMENT_3D ( 'NONE', #68321, #63073, #57846 ) ;
#67720=CARTESIAN_POINT ( 'NONE',  ( 9.884624721933931824, 2.899999999999999911, 6.445686799102332110 ) ) ;
#67723=B_SPLINE_CURVE_WITH_KNOTS ( 'NONE', 3,
 ( #48086, #1226, #54355, #536, #16609, #43183, #15917, #6113, #59604, #190, #42839, #37934 ),
 .UNSPECIFIED., .F., .F.,
 ( 4, 2, 2, 2, 2, 4 ),
 ( 0.000000000000000000, 0.2500000000000000000, 0.5000000000000000000, 0.7500000000000000000, 0.8750000000000000000, 1.000000000000000000 ),
 .UNSPECIFIED. ) ;
#67741=CARTESIAN_POINT ( 'NONE',  ( 8.849385841230999361, 3.975069902178000270, 9.483774112875002160 ) ) ;
#67750=CARTESIAN_POINT ( 'NONE',  ( 9.600562361968000502, 10.31800062403999441, -4.698177885259996245 ) ) ;
#67764=CARTESIAN_POINT ( 'NONE',  ( 10.78637067803999905, 5.666041748529999644, -7.787005432561999285 ) ) ;
#67766=( GEOMETRIC_REPRESENTATION_CONTEXT ( 3 ) GLOBAL_UNCERTAINTY_ASSIGNED_CONTEXT ( ( #53457 ) ) GLOBAL_UNIT_ASSIGNED_CONTEXT ( ( #64053, #38182, #15831 ) ) REPRESENTATION_CONTEXT ( 'NONE', 'WORKASPACE' ) );
#67769=EDGE_CURVE ( 'NONE', #56890, #58925, #8646, .T. ) ;
#67770=CARTESIAN_POINT ( 'NONE',  ( 10.65550720192000078, 4.237674045823999869, 9.105219676299999065 ) ) ;
#67772=VECTOR ( 'NONE', #33842, 1000.000000000000000 ) ;
#67775=EDGE_CURVE ( 'NONE', #61078, #57180, #19858, .T. ) ;
#67779=CARTESIAN_POINT ( 'NONE',  ( 10.59303303094000093, 2.436236667456999960, 7.793464546548000804 ) ) ;
#67781=CARTESIAN_POINT ( 'NONE',  ( 9.865910841232000905, 2.685250982074999904, -7.026194612421999608 ) ) ;
#67783=CARTESIAN_POINT ( 'NONE',  ( 11.01659413146999889, 7.354810577943000638, -6.171169745271000373 ) ) ;
#67787=CARTESIAN_POINT ( 'NONE',  ( 8.738426658774001154, 5.414918126383000185, 8.890678916765999418 ) ) ;
#67788=CARTESIAN_POINT ( 'NONE',  ( 10.28314886242000092, 2.387776420306999992, 7.684265965147999644 ) ) ;
#67792=CARTESIAN_POINT ( 'NONE',  ( 9.924495280410999598, 4.946705552514000459, -6.253848946732999181 ) ) ;
#67799=ORIENTED_EDGE ( 'NONE', *, *, #65528, .T. ) ;
#67800=CARTESIAN_POINT ( 'NONE',  ( 2.254339447823000331, -2.269833785962000139, -2.784166953248000009 ) ) ;
#67802=CARTESIAN_POINT ( 'NONE',  ( 10.00464026716699806, 2.641193587372907103, 6.397822249176915221 ) ) ;
#67803=DIRECTION ( 'NONE',  ( 1.000000000000000000, 0.000000000000000000, 0.000000000000000000 ) ) ;
#67810=ORIENTED_EDGE ( 'NONE', *, *, #36707, .T. ) ;
#67811=CARTESIAN_POINT ( 'NONE',  ( 9.304732780410999382, 5.284130523641000110, 6.489275570566000795 ) ) ;
#67817=CARTESIAN_POINT ( 'NONE',  ( 1.790929700619999787, 1.756325177964999984, 2.941112093452000309 ) ) ;
#67818=ORIENTED_EDGE ( 'NONE', *, *, #24618, .F. ) ;
#67822=CARTESIAN_POINT ( 'NONE',  ( 10.81579666500999970, 5.374569445151000657, 6.698728322222000209 ) ) ;
#67832=CARTESIAN_POINT ( 'NONE',  ( 8.356851002541000994, 2.832432432432000269, -6.822293592207000934 ) ) ;
#67833=VECTOR ( 'NONE', #49246, 1000.000000000000000 ) ;
#67842=CARTESIAN_POINT ( 'NONE',  ( 10.77962664842000073, 2.397507474987000009, 7.755423212350999407 ) ) ;
#67843=CARTESIAN_POINT ( 'NONE',  ( 9.831594052344000190, 3.539229510464000139, -8.956011942092999334 ) ) ;
#67854=CARTESIAN_POINT ( 'NONE',  ( 8.996463691919831973, 5.100000000000000533, -6.665341197420957542 ) ) ;
#67855=CARTESIAN_POINT ( 'NONE',  ( 8.688612068284333745, 2.650857310365788422, 7.263856826349759821 ) ) ;
#67859=ORIENTED_EDGE ( 'NONE', *, *, #36784, .T. ) ;
#67861=AXIS2_PLACEMENT_3D ( 'NONE', #50062, #22439, #17555 ) ;
#67864=ADVANCED_FACE ( 'NONE', ( #52004 ), #4040, .T. ) ;
#67871=VECTOR ( 'NONE', #27320, 1000.000000000000000 ) ;
#67872=CARTESIAN_POINT ( 'NONE',  ( 8.729782384210551527, 4.176498446805472220, -8.849932004427472521 ) ) ;
#67879=CARTESIAN_POINT ( 'NONE',  ( 10.62947109217999930, 5.100000000000000533, 6.152188490330000370 ) ) ;
#67883=CARTESIAN_POINT ( 'NONE',  ( 10.99999648468999958, -1.199999999999999956, -9.776630298829998011 ) ) ;
#67886=ORIENTED_EDGE ( 'NONE', *, *, #68106, .F. ) ;
#67887=AXIS2_PLACEMENT_3D ( 'NONE', #30265, #31294, #20446 ) ;
#67889=CARTESIAN_POINT ( 'NONE',  ( 9.546517828664185856, 2.481203689726812822, -8.418993938519275133 ) ) ;
#67904=CARTESIAN_POINT ( 'NONE',  ( 2.730140132542667963, -3.408904368339107815, 0.9161175952574674985 ) ) ;
#67910=CARTESIAN_POINT ( 'NONE',  ( 8.906851002547000462, 2.832432432432000269, -6.822293592207000934 ) ) ;
#67915=CARTESIAN_POINT ( 'NONE',  ( 8.772439158776000667, 3.098073081301000009, -8.567513114264999174 ) ) ;
#67929=ORIENTED_EDGE ( 'NONE', *, *, #1799, .F. ) ;
#67930=CARTESIAN_POINT ( 'NONE',  ( 7.627164364716389144, 5.349908229800731441, -7.706112628381206697 ) ) ;
#67931=CARTESIAN_POINT ( 'NONE',  ( 8.988579719593998263, 4.902869380824999901, -8.978557145469999057 ) ) ;
#67933=AXIS2_PLACEMENT_3D ( 'NONE', #32262, #21745, #59155 ) ;
#67934=CARTESIAN_POINT ( 'NONE',  ( 10.60199294549000193, 2.164976235211999889, -7.764525279724000306 ) ) ;
#67936=ORIENTED_EDGE ( 'NONE', *, *, #48446, .T. ) ;
#67946=DIRECTION ( 'NONE',  ( 1.000000000000000000, 0.000000000000000000, 0.000000000000000000 ) ) ;
#67947=CARTESIAN_POINT ( 'NONE',  ( 11.37168584123000059, 2.803494217761000495, -6.967881733280000489 ) ) ;
#67956=CARTESIAN_POINT ( 'NONE',  ( 9.169760841232999837, 4.728328492779000136, -8.692725459657999920 ) ) ;
#67957=CARTESIAN_POINT ( 'NONE',  ( 10.99999999997000089, 4.000000000000000000, -8.949999999967999997 ) ) ;
#67958=CARTESIAN_POINT ( 'NONE',  ( 2.716661701819526709, -2.750000000000000000, -3.881553357679799511E-10 ) ) ;
#67960=CARTESIAN_POINT ( 'NONE',  ( 7.875706921239332914, 4.438897210574712204, 6.198347075216069868 ) ) ;
#67966=ORIENTED_EDGE ( 'NONE', *, *, #24474, .T. ) ;
#67972=VECTOR ( 'NONE', #61451, 1000.000000000000000 ) ;
#67977=CARTESIAN_POINT ( 'NONE',  ( 7.967646874132946699, 2.971274813974494222, -6.517255511639618248 ) ) ;
#67979=CARTESIAN_POINT ( 'NONE',  ( 0.1426929024220463249, 0.4105104488565842202, -3.142673126269484030 ) ) ;
#67980=CARTESIAN_POINT ( 'NONE',  ( 3.491703015634000096, -2.440397167367000186, 2.160034081118999971 ) ) ;
#67981=ORIENTED_EDGE ( 'NONE', *, *, #53978, .F. ) ;
#67986=CARTESIAN_POINT ( 'NONE',  ( 3.500000000000000888, 0.002369752946726449983, 3.285293661413511312 ) ) ;
#67991=CARTESIAN_POINT ( 'NONE',  ( 0.5734567831477479505, 2.175120696137909260, 2.781256206680508658 ) ) ;
#67992=CARTESIAN_POINT ( 'NONE',  ( 10.93769906950999982, 5.063122007744000008, 4.920829195600999739 ) ) ;
#67993=CARTESIAN_POINT ( 'NONE',  ( 1.678056799206624872, -2.150913519912214245, 2.798833948393621984 ) ) ;
#68004=CARTESIAN_POINT ( 'NONE',  ( 7.646881073111088334, 2.711253299328941768, 7.970042138743662186 ) ) ;
#68005=CARTESIAN_POINT ( 'NONE',  ( 7.043539158770000697, 5.150153908582999485, -6.706147112165000479 ) ) ;
#68009=CARTESIAN_POINT ( 'NONE',  ( 2.000973465872999846, 3.500000000000000000, 0.000000000000000000 ) ) ;
#68012=ORIENTED_EDGE ( 'NONE', *, *, #63736, .T. ) ;
#68016=CARTESIAN_POINT ( 'NONE',  ( 10.94990783606475837, 2.251524537340385379, 7.510583322451364729 ) ) ;
#68019=CARTESIAN_POINT ( 'NONE',  ( 3.115556799210791539, 0.4581489286485002088, 3.500000000000001776 ) ) ;
#68029=CARTESIAN_POINT ( 'NONE',  ( 9.646287586158999616, 2.591467678478000192, 6.760055064032999717 ) ) ;
#68031=CARTESIAN_POINT ( 'NONE',  ( 27.64127793187000037, 2.399999999999999911, 6.571291218949999902 ) ) ;
#68033=CARTESIAN_POINT ( 'NONE',  ( 2.384164467059000092, 2.877138355028999506, -2.068711953730999920 ) ) ;
#68035=CARTESIAN_POINT ( 'NONE',  ( 10.98768472569999943, 6.720753179915999631, -5.471698458723999181 ) ) ;
#68039=LINE ( 'NONE', #20155, #4134 ) ;
#68043=CARTESIAN_POINT ( 'NONE',  ( 11.27110638630999873, 5.469603964121000139, 8.504707115835000053 ) ) ;
#68055=CARTESIAN_POINT ( 'NONE',  ( 4.000000000000000000, 1.878475312369307426, -1.082895748632574984 ) ) ;
#68057=ORIENTED_EDGE ( 'NONE', *, *, #44809, .T. ) ;
#68060=CARTESIAN_POINT ( 'NONE',  ( 10.28180471959000108, 3.991526675591000384, -5.814300410279999554 ) ) ;
#68061=EDGE_LOOP ( 'NONE', ( #8847, #58804, #54168, #45238 ) ) ;
#68063=LINE ( 'NONE', #57233, #49886 ) ;
#68066=DIRECTION ( 'NONE',  ( 0.9999999999999987788, -4.835300858369983927E-08, -1.472962857897996183E-08 ) ) ;
#68069=CARTESIAN_POINT ( 'NONE',  ( 4.000000000000000000, 0.000000000000000000, 0.000000000000000000 ) ) ;
#68073=CARTESIAN_POINT ( 'NONE',  ( 2.792640132542833165, -3.058252359239901796, -1.762666431298149039 ) ) ;
#68076=CARTESIAN_POINT ( 'NONE',  ( 9.496463691920835615, 5.100000000000000533, -6.665341197420965536 ) ) ;
#68077=VERTEX_POINT ( 'NONE', #61398 ) ;
#68078=EDGE_CURVE ( 'NONE', #53328, #7557, #57934, .T. ) ;
#68086=CARTESIAN_POINT ( 'NONE',  ( 8.271698341229999585, 5.629399530851999955, 8.631829656822000985 ) ) ;
#68089=CARTESIAN_POINT ( 'NONE',  ( 3.500000000000000000, -2.946081722130999836, 0.9972449351501998516 ) ) ;
#68091=LINE ( 'NONE', #35947, #37957 ) ;
#68092=ORIENTED_EDGE ( 'NONE', *, *, #43046, .F. ) ;
#68097=CARTESIAN_POINT ( 'NONE',  ( 10.06162737365999682, 9.774413574170004892, -6.274226718126997504 ) ) ;
#68098=CARTESIAN_POINT ( 'NONE',  ( 2.446201642328499570, 2.726743374470192993, -2.246552915429936181 ) ) ;
#68102=CARTESIAN_POINT ( 'NONE',  ( 10.49316089255587414, 4.959455279339148426, 8.606798394218628800 ) ) ;
#68104=LINE ( 'NONE', #30053, #53430 ) ;
#68106=EDGE_CURVE ( 'NONE', #1011, #24471, #44585, .T. ) ;
#68112=CARTESIAN_POINT ( 'NONE',  ( 9.976690600124999975, 4.172224310749999887, -6.147156451669999910 ) ) ;
#68116=CARTESIAN_POINT ( 'NONE',  ( 9.571961069101000419, 4.084683332033999470, 8.946609345378000455 ) ) ;
#68121=CARTESIAN_POINT ( 'NONE',  ( 8.618968789468430813, 5.058209485103853709, -8.358329603623534609 ) ) ;
#68122=CARTESIAN_POINT ( 'NONE',  ( 9.353724647487000610, 2.823567847429000022, 9.032053040610000139 ) ) ;
#68126=CYLINDRICAL_SURFACE ( 'NONE', #53222, 1.350000000000000533 ) ;
#68131=CARTESIAN_POINT ( 'NONE',  ( 10.97534709859457003, 5.193992591246429313, -6.717726803886520770 ) ) ;
#68133=ORIENTED_EDGE ( 'NONE', *, *, #59561, .T. ) ;
#68134=CARTESIAN_POINT ( 'NONE',  ( 9.187479719595000205, 2.391443348526999912, -6.856688371964000162 ) ) ;
#68135=CARTESIAN_POINT ( 'NONE',  ( -0.000000000000000000, -0.3800960799355100894, 2.900041633271500441 ) ) ;
#68136=CARTESIAN_POINT ( 'NONE',  ( 5.500000000000000000, -13.87069231928999891, -4.225386915259999654 ) ) ;
#68142=CARTESIAN_POINT ( 'NONE',  ( 2.063611650058999825, -0.2184777168079999887, 3.585542759708000293 ) ) ;
#68143=CARTESIAN_POINT ( 'NONE',  ( 7.308885841229000313, 4.847807297114000491, 9.065373753110998578 ) ) ;
#68145=CARTESIAN_POINT ( 'NONE',  ( 9.120514158775000269, 5.306366356490000769, -7.996450761531000317 ) ) ;
#68153=ORIENTED_EDGE ( 'NONE', *, *, #61702, .T. ) ;
#68159=CARTESIAN_POINT ( 'NONE',  ( 1.833838311998000181, 2.957881470139000157, 1.368292308076999975 ) ) ;
#68161=LINE ( 'NONE', #36361, #12061 ) ;
#68163=CARTESIAN_POINT ( 'NONE',  ( 10.52638970730999901, 2.451081172664000274, 6.282749363171999946 ) ) ;
#68164=CARTESIAN_POINT ( 'NONE',  ( 10.74599736040000053, 5.242718773683000322, 8.978699897073999736 ) ) ;
#68166=EDGE_CURVE ( 'NONE', #58906, #32433, #14478, .T. ) ;
#68169=EDGE_CURVE ( 'NONE', #38774, #9042, #10247, .T. ) ;
#68173=CARTESIAN_POINT ( 'NONE',  ( 11.09999999999999964, 2.700688487044999864, -5.124965750789000296 ) ) ;
#68183=CARTESIAN_POINT ( 'NONE',  ( 10.28314886242000092, 2.387776420306999992, 7.684265965147999644 ) ) ;
#68184=CARTESIAN_POINT ( 'NONE',  ( 10.18512471524999974, 5.526143977810000329, -7.556025088797999167 ) ) ;
#68190=LINE ( 'NONE', #25557, #38911 ) ;
#68191=ORIENTED_EDGE ( 'NONE', *, *, #44372, .T. ) ;
#68195=CARTESIAN_POINT ( 'NONE',  ( 7.156203327080998378, 10.79836147658999757, 3.492272478327004492 ) ) ;
#68207=CARTESIAN_POINT ( 'NONE',  ( 8.719369705998316178, 4.353260231620209808, -8.814526689006324744 ) ) ;
#68213=AXIS2_PLACEMENT_3D ( 'NONE', #40637, #56386, #3573 ) ;
#68216=CARTESIAN_POINT ( 'NONE',  ( 9.926176658771000305, 4.356412802752999802, -9.313960415320000408 ) ) ;
#68225=CARTESIAN_POINT ( 'NONE',  ( 9.644299024500105233, 2.624632560452479169, -6.377853817079278897 ) ) ;
#68232=CARTESIAN_POINT ( 'NONE',  ( 8.156123186758179600, 2.990802688239547535, 6.388664891360845033 ) ) ;
#68233=EDGE_LOOP ( 'NONE', ( #16979, #25690, #61423, #63495 ) ) ;
#68236=LINE ( 'NONE', #2898, #35451 ) ;
#68246=ADVANCED_FACE ( 'NONE', ( #170 ), #23010, .F. ) ;
#68250=CARTESIAN_POINT ( 'NONE',  ( 11.09999999999999964, 7.281355457699000056, 6.286510842043999681 ) ) ;
#68253=CARTESIAN_POINT ( 'NONE',  ( 9.152520280414000453, 4.102804347295999854, -5.770625657082999460 ) ) ;
#68258=ORIENTED_EDGE ( 'NONE', *, *, #6207, .T. ) ;
#68260=CARTESIAN_POINT ( 'NONE',  ( 8.414360841228999632, 5.461114003844000031, -8.582501063019000398 ) ) ;
#68268=CARTESIAN_POINT ( 'NONE',  ( 9.278070280414000948, 2.546924812613000189, -6.918870225297999887 ) ) ;
#68271=CARTESIAN_POINT ( 'NONE',  ( 9.831594052344000190, 3.539229510464000139, -8.956011942092999334 ) ) ;
#68283=CARTESIAN_POINT ( 'NONE',  ( 7.325000000000000178, 4.000000000000000000, 9.239711431703000244 ) ) ;
#68288=CIRCLE ( 'NONE', #33683, 2.750000000000000000 ) ;
#68291=ORIENTED_EDGE ( 'NONE', *, *, #37341, .F. ) ;
#68292=CARTESIAN_POINT ( 'NONE',  ( 10.12339528040999959, 3.988943694240999704, -8.966360307350999648 ) ) ;
#68295=CARTESIAN_POINT ( 'NONE',  ( 8.470944094208999076, 5.100000000000000533, 6.571291218949999902 ) ) ;
#68304=CARTESIAN_POINT ( 'NONE',  ( 0.1499942179679999987, 2.750000000000000000, 0.000000000000000000 ) ) ;
#68310=CARTESIAN_POINT ( 'NONE',  ( 9.044210841233001119, 2.773858540272000184, -8.951250717848999727 ) ) ;
#68313=VECTOR ( 'NONE', #29609, 1000.000000000000000 ) ;
#68317=CARTESIAN_POINT ( 'NONE',  ( 9.865041550948095761, 2.650034642413356512, -7.500002425457249267 ) ) ;
#68321=CARTESIAN_POINT ( 'NONE',  ( 11.09999999999999964, 5.599999999999999645, -6.571291218949999902 ) ) ;
#68323=CARTESIAN_POINT ( 'NONE',  ( 1.603056799207541738, 2.798833948393625981, 2.150913519912208471 ) ) ;
#68326=EDGE_CURVE ( 'NONE', #59469, #51368, #39792, .T. ) ;
#68327=PRODUCT_CONTEXT ( 'NONE', #50760, 'mechanical' ) ;
#68329=CARTESIAN_POINT ( 'NONE',  ( 10.98611853005698968, 8.045559802946883110, 6.520188272055316148 ) ) ;
#68331=CARTESIAN_POINT ( 'NONE',  ( 10.72510394928502286, 2.650147065043140238, 7.500007457243191844 ) ) ;
#68333=ORIENTED_EDGE ( 'NONE', *, *, #66317, .T. ) ;
#68336=CARTESIAN_POINT ( 'NONE',  ( 9.525000000000000355, 4.417172942406000224, 8.783926296998000538 ) ) ;
#68343=CARTESIAN_POINT ( 'NONE',  ( 7.192714158770000310, 4.413443707129999893, -8.834960942136000028 ) ) ;
#68349=DIRECTION ( 'NONE',  ( 1.000000000000000000, 0.000000000000000000, 0.000000000000000000 ) ) ;
#68350=ORIENTED_EDGE ( 'NONE', *, *, #57375, .F. ) ;
#68356=CARTESIAN_POINT ( 'NONE',  ( 10.93388704970945824, 2.287708072853963159, 7.858003405079239556 ) ) ;
#68359=CARTESIAN_POINT ( 'NONE',  ( 10.16052890781999984, 2.899999999999999911, -6.152188490330000370 ) ) ;
#68362=B_SPLINE_CURVE_WITH_KNOTS ( 'NONE', 3,
 ( #1270, #38676, #27496, #49504, #59997 ),
 .UNSPECIFIED., .F., .F.,
 ( 4, 1, 4 ),
 ( 0.000000000000000000, 0.5000000000000000000, 1.000000000000000000 ),
 .UNSPECIFIED. ) ;
#68367=ORIENTED_EDGE ( 'NONE', *, *, #4218, .F. ) ;
#68368=CARTESIAN_POINT ( 'NONE',  ( 9.632179190069999564, 5.638172764974000550, 6.476627236431999890 ) ) ;
#68370=CARTESIAN_POINT ( 'NONE',  ( 9.567560841232999991, 5.349936549139000519, -7.138437102151999447 ) ) ;
#68371=CARTESIAN_POINT ( 'NONE',  ( 3.390171590515999700, 3.025066006789999928, -1.845780140648000112 ) ) ;
#68373=CYLINDRICAL_SURFACE ( 'NONE', #65174, 0.4999999999999998335 ) ;
#68378=CARTESIAN_POINT ( 'NONE',  ( 10.57907406728876865, 2.241676822008003889, -7.748197378945968161 ) ) ;
#68381=CARTESIAN_POINT ( 'NONE',  ( 10.50285691784999997, 5.158890929072000198, 8.369954994793999958 ) ) ;
#68396=CARTESIAN_POINT ( 'NONE',  ( 0.07426626274182999976, -1.906427021235999941, -2.406055758466000061 ) ) ;
#68398=CARTESIAN_POINT ( 'NONE',  ( 10.43325471958999984, 5.596203146559000530, -8.042024377770999877 ) ) ;
#68401=CARTESIAN_POINT ( 'NONE',  ( 8.620740978634000129, 4.599999999999999645, 5.898823289756999877 ) ) ;
#68404=CARTESIAN_POINT ( 'NONE',  ( 7.308885841229000313, 4.847807297114000491, 9.065373753110998578 ) ) ;
#68409=CARTESIAN_POINT ( 'NONE',  ( 8.213314158768998396, 4.511685119297999869, -5.670317910541000650 ) ) ;
#68416=VERTEX_POINT ( 'NONE', #2924 ) ;
#68417=CARTESIAN_POINT ( 'NONE',  ( 9.523148997461001741, 5.167567567567999731, -6.822293592207000934 ) ) ;
#68419=VERTEX_POINT ( 'NONE', #13771 ) ;
#68428=CARTESIAN_POINT ( 'NONE',  ( 9.362885841227999606, 3.677414437776999723, 9.250745771096999803 ) ) ;
#68445=EDGE_LOOP ( 'NONE', ( #42152, #51921, #67653, #52395 ) ) ;
#68449=CARTESIAN_POINT ( 'NONE',  ( 10.58996475420000039, 2.876740601533999797, -6.236530348556999392 ) ) ;
#68453=CARTESIAN_POINT ( 'NONE',  ( 9.228133567168001150, 2.875367362387999837, 8.669940206484001877 ) ) ;
#68460=CARTESIAN_POINT ( 'NONE',  ( 11.05935155529000014, 2.480238120735000162, 6.610075178640000715 ) ) ;
#68464=CARTESIAN_POINT ( 'NONE',  ( 11.12454631916000025, 7.322342417344000154, -6.385060111035000041 ) ) ;
#68469=CARTESIAN_POINT ( 'NONE',  ( 8.288068612932629975, 3.223876500227366382, -8.634712533562288073 ) ) ;
#68470=CARTESIAN_POINT ( 'NONE',  ( 10.31667774810000004, 3.819530253758000260, 6.062195927068000145 ) ) ;
#68472=ORIENTED_EDGE ( 'NONE', *, *, #14055, .F. ) ;
#68473=CARTESIAN_POINT ( 'NONE',  ( 8.731095280410999138, 2.469361196073999842, -7.826019481986000059 ) ) ;
#68481=B_SPLINE_CURVE_WITH_KNOTS ( 'NONE', 3,
 ( #34673, #44480, #29086, #65772, #49701, #7051 ),
 .UNSPECIFIED., .F., .F.,
 ( 4, 1, 1, 4 ),
 ( 0.000000000000000000, 0.3333333333333000081, 0.6666666666667000474, 1.000000000000000000 ),
 .UNSPECIFIED. ) ;
#68483=CARTESIAN_POINT ( 'NONE',  ( 8.207510841230000409, 5.944584532500000407, 7.106843289410999631 ) ) ;
#68485=CARTESIAN_POINT ( 'NONE',  ( 9.418864158773999407, 3.210851187372000037, -6.346613542714999667 ) ) ;
#68489=CARTESIAN_POINT ( 'NONE',  ( 9.736878146978000359, 2.742182981761000171, 6.839230404018000087 ) ) ;
#68495=CARTESIAN_POINT ( 'NONE',  ( 7.711426658771000753, 5.797099724369999763, 8.340484548805999765 ) ) ;
#68501=CARTESIAN_POINT ( 'NONE',  ( 1.404700767030999886, 0.7969358895047999880, 3.160091737778000009 ) ) ;
#68503=CARTESIAN_POINT ( 'NONE',  ( 1.238685001925042384, 2.938954507330893140, -1.506992772821682314 ) ) ;
#68504=EDGE_CURVE ( 'NONE', #39994, #37746, #52538, .T. ) ;
#68506=CARTESIAN_POINT ( 'NONE',  ( 9.719613305057999142, 5.967773797872000685, 7.406643507784999692 ) ) ;
#68507=CARTESIAN_POINT ( 'NONE',  ( 9.353724647487000610, 2.823567847429000022, 9.032053040610000139 ) ) ;
#68510=CARTESIAN_POINT ( 'NONE',  ( 10.98768472569999943, 6.720753179915999631, -5.471698458723999181 ) ) ;
#68513=DIRECTION ( 'NONE',  ( 0.000000000000000000, -1.000000000000000000, 0.000000000000000000 ) ) ;
#68515=AXIS2_PLACEMENT_3D ( 'NONE', #657, #21970, #26890 ) ;
#68519=DIRECTION ( 'NONE',  ( 0.000000000000000000, 0.000000000000000000, -1.000000000000000000 ) ) ;
#68522=CARTESIAN_POINT ( 'NONE',  ( 8.216851002544000693, 2.832432432432000269, 6.822293592207000934 ) ) ;
#68525=CARTESIAN_POINT ( 'NONE',  ( 11.18051582549000145, 5.340073783367000892, 8.416152717850000187 ) ) ;
#68526=CARTESIAN_POINT ( 'NONE',  ( 9.922184613163000932, 3.489926301007000298, -9.111807643819000546 ) ) ;
#68530=CARTESIAN_POINT ( 'NONE',  ( 8.983360123997224278, 5.350320840654694265, 7.640098978919741768 ) ) ;
#68533=ORIENTED_EDGE ( 'NONE', *, *, #31344, .T. ) ;
#68535=CARTESIAN_POINT ( 'NONE',  ( 7.474999999999996980, 4.000000000000000000, 8.979903810567666511 ) ) ;
#68537=CARTESIAN_POINT ( 'NONE',  ( 8.674830025576062198, 2.649890579813255709, 7.499988935010339475 ) ) ;
#68539=CARTESIAN_POINT ( 'NONE',  ( 11.32763480027999137, 9.448540156737001539, 6.821721532523001841 ) ) ;
#68545=VERTEX_POINT ( 'NONE', #4635 ) ;
#68553=EDGE_CURVE ( 'NONE', #10113, #27484, #19411, .T. ) ;
#68554=CARTESIAN_POINT ( 'NONE',  ( 9.112942518363999156, 5.100000000000000533, 6.192000867487999827 ) ) ;
#68555=CARTESIAN_POINT ( 'NONE',  ( 9.731470621293439649, 3.294701422184862949, -8.705110408592389604 ) ) ;
#68558=EDGE_CURVE ( 'NONE', #68596, #51514, #36486, .T. ) ;
#68560=CARTESIAN_POINT ( 'NONE',  ( 8.283628111110997949, 2.878995628920999916, -6.357604486408997779 ) ) ;
#68561=CARTESIAN_POINT ( 'NONE',  ( 10.01676721958999927, 4.324998751150999965, -9.154078823942999321 ) ) ;
#68567=VECTOR ( 'NONE', #22222, 1000.000000000000000 ) ;
#68586=CARTESIAN_POINT ( 'NONE',  ( 7.764631182151003230, 2.924915923740001311, 6.482382710726004582 ) ) ;
#68593=B_SPLINE_CURVE_WITH_KNOTS ( 'NONE', 3,
 ( #68751, #15284, #53032, #5478 ),
 .UNSPECIFIED., .F., .F.,
 ( 4, 4 ),
 ( 0.000000000000000000, 1.000000000000000000 ),
 .UNSPECIFIED. ) ;
#68596=VERTEX_POINT ( 'NONE', #58132 ) ;
#68597=CARTESIAN_POINT ( 'NONE',  ( 9.600045280412000892, 3.021734963141999852, -6.070209284876999511 ) ) ;
#68600=B_SPLINE_CURVE_WITH_KNOTS ( 'NONE', 3,
 ( #37108, #16799, #65031, #56540 ),
 .UNSPECIFIED., .F., .F.,
 ( 4, 4 ),
 ( 0.000000000000000000, 1.000000000000000000 ),
 .UNSPECIFIED. ) ;
#68606=CARTESIAN_POINT ( 'NONE',  ( 9.591185841232000797, 2.173570076733999823, -8.023168429484000441 ) ) ;
#68610=DIRECTION ( 'NONE',  ( 1.000000000000000000, 0.000000000000000000, 0.000000000000000000 ) ) ;
#68612=CARTESIAN_POINT ( 'NONE',  ( 11.09999999999999964, 5.553261372860998968, 5.124965741905999295 ) ) ;
#68613=VERTEX_POINT ( 'NONE', #20382 ) ;
#68615=CARTESIAN_POINT ( 'NONE',  ( 8.351014158771000950, 5.616457598545999907, -8.245813000738998255 ) ) ;
#68618=CARTESIAN_POINT ( 'NONE',  ( 9.882903428397000312, 4.314559027837000293, -9.161039561412001930 ) ) ;
#68635=EDGE_CURVE ( 'NONE', #34076, #26471, #25231, .T. ) ;
#68638=CARTESIAN_POINT ( 'NONE',  ( 11.13509627103000099, 5.337904119774999678, -5.086083210688999934 ) ) ;
#68643=CARTESIAN_POINT ( 'NONE',  ( 0.1499942179679999710, 2.199046806507071405, -1.689975037551097348 ) ) ;
#68649=ORIENTED_EDGE ( 'NONE', *, *, #54535, .T. ) ;
#68650=B_SPLINE_CURVE_WITH_KNOTS ( 'NONE', 3,
 ( #49788, #65858, #60623, #2245, #28828, #39998, #8174, #29523, #50825, #20037, #40669, #52192, #36114, #4291 ),
 .UNSPECIFIED., .F., .F.,
 ( 4, 2, 2, 2, 2, 2, 4 ),
 ( 0.1255288371561983085, 0.2191765140581366789, 0.3128241909600750770, 0.4064718678620133918, 0.5001195447639518177, 0.6874148985678291135, 0.8747102523717062983 ),
 .UNSPECIFIED. ) ;
#68651=CARTESIAN_POINT ( 'NONE',  ( 1.000973465875999890, 3.500000000000000000, 0.000000000000000000 ) ) ;
#68665=CARTESIAN_POINT ( 'NONE',  ( 6.899999691988000450, -11.00717859340000082, 1.432487142323000118 ) ) ;
#68666=DIRECTION ( 'NONE',  ( 0.000000000000000000, -1.000000000000000000, 0.000000000000000000 ) ) ;
#68672=CARTESIAN_POINT ( 'NONE',  ( 1.728056799208041561, -2.150913519912213800, 2.798833948393621540 ) ) ;
#68677=CARTESIAN_POINT ( 'NONE',  ( 10.98395291507793381, 8.151105813983006598, 6.540856040902778723 ) ) ;
#68686=CIRCLE ( 'NONE', #11743, 2.000000000000001332 ) ;
#68690=CARTESIAN_POINT ( 'NONE',  ( 0.000000000000000000, 0.3800960799355100894, -2.900041633271500441 ) ) ;
#68691=B_SPLINE_CURVE_WITH_KNOTS ( 'NONE', 3,
 ( #63693, #15808, #43424, #16832 ),
 .UNSPECIFIED., .F., .F.,
 ( 4, 4 ),
 ( 0.000000000000000000, 1.000000000000000000 ),
 .UNSPECIFIED. ) ;
#68692=CARTESIAN_POINT ( 'NONE',  ( 6.703179719589999586, 5.447281585506000390, -7.886005609586001164 ) ) ;
#68695=CARTESIAN_POINT ( 'NONE',  ( 9.487498405967778936, 4.950355006253724710, 8.458582407359203970 ) ) ;
#68700=ORIENTED_EDGE ( 'NONE', *, *, #14872, .F. ) ;
#68707=CARTESIAN_POINT ( 'NONE',  ( 6.899999691988000450, 13.10000000000000142, -1.604287306883032847E-15 ) ) ;
#68713=CARTESIAN_POINT ( 'NONE',  ( 9.722769750889000306, 5.493785011855999656, 6.566826815556000341 ) ) ;
#68714=CARTESIAN_POINT ( 'NONE',  ( 9.926176658771000305, 4.356412802752999802, -9.313960415320000408 ) ) ;
#68715=CIRCLE ( 'NONE', #29677, 0.4999999999999998335 ) ;
#68716=FACE_OUTER_BOUND ( 'NONE', #4457, .T. ) ;
#68718=CARTESIAN_POINT ( 'NONE',  ( 10.16052890781999984, 2.899999999999999911, -6.152188490330000370 ) ) ;
#68722=ORIENTED_EDGE ( 'NONE', *, *, #4247, .F. ) ;
#68726=CARTESIAN_POINT ( 'NONE',  ( 3.165556799210874406, 0.4581489286485003198, 3.500000000000000444 ) ) ;
#68727=ADVANCED_FACE ( 'NONE', ( #777 ), #45509, .F. ) ;
#68730=CARTESIAN_POINT ( 'NONE',  ( 9.696080515601000371, 2.554416243104999928, 7.600685069647000525 ) ) ;
#68733=AXIS2_PLACEMENT_3D ( 'NONE', #57143, #7888, #9241 ) ;
#68742=CARTESIAN_POINT ( 'NONE',  ( 9.791229719590001324, 4.294368353031000396, -8.968663198664000191 ) ) ;
#68747=CARTESIAN_POINT ( 'NONE',  ( 0.2882532571067000227, 2.601420761213999899, -2.147952162500999851 ) ) ;
#68749=CARTESIAN_POINT ( 'NONE',  ( 10.25880778041000063, 2.491777456852000139, -7.289938575364999451 ) ) ;
#68751=CARTESIAN_POINT ( 'NONE',  ( 8.832537864289999874, 2.899999999999999911, 6.571291218949999902 ) ) ;
#68752=DIRECTION ( 'NONE',  ( 1.000000000000000000, 0.000000000000000000, 4.050801148937999854E-14 ) ) ;
#68755=CARTESIAN_POINT ( 'NONE',  ( 7.950760841228999176, 2.095715612964000218, 8.056490963156001328 ) ) ;
#68758=CARTESIAN_POINT ( 'NONE',  ( 7.367989158767000113, 5.517512745430000365, -8.643112676966000052 ) ) ;
#68767=AXIS2_PLACEMENT_3D ( 'NONE', #32640, #28437, #54651 ) ;
#68771=CARTESIAN_POINT ( 'NONE',  ( 2.540556799210292205, 3.500000000000000888, -0.4581489286485045387 ) ) ;
#68778=CARTESIAN_POINT ( 'NONE',  ( 9.181704719590001673, 3.734279507827999556, 8.942126004519000304 ) ) ;
#68779=EDGE_LOOP ( 'NONE', ( #11477, #3283, #55612, #17186 ) ) ;
#68780=CARTESIAN_POINT ( 'NONE',  ( 7.773264469372000107, 2.859518616742000141, 6.768376720750000075 ) ) ;
#68781=AXIS2_PLACEMENT_3D ( 'NONE', #36936, #31689, #53010 ) ;
#68798=CARTESIAN_POINT ( 'NONE',  ( 4.900006121741999010, 1.599333684796362398, 1.229093439949826561 ) ) ;
#68799=CARTESIAN_POINT ( 'NONE',  ( 10.18512471524999974, 5.526143977810000329, -7.556025088797999167 ) ) ;
#68802=CARTESIAN_POINT ( 'NONE',  ( 8.493376396436000064, 2.902501347630999984, -6.607668289109998483 ) ) ;
#68803=CARTESIAN_POINT ( 'NONE',  ( 9.882259685352000389, 4.932708901218999742, 6.390989635557000170 ) ) ;
#68805=CARTESIAN_POINT ( 'NONE',  ( 8.897208772779700681, 5.334183864695357435, -8.671862932165968374 ) ) ;
#68809=ADVANCED_FACE ( 'NONE', ( #18594 ), #15920, .F. ) ;
#68811=CARTESIAN_POINT ( 'NONE',  ( 9.743561007103998861, 5.287400066955999733, 8.939966147452000911 ) ) ;
#68813=CARTESIAN_POINT ( 'NONE',  ( 8.871410841230998656, 2.721111233225000259, -6.936528696292000085 ) ) ;
#68817=CARTESIAN_POINT ( 'NONE',  ( 10.82459575937373586, 5.732063870690240925, -7.156463326781315359 ) ) ;
#68819=CARTESIAN_POINT ( 'NONE',  ( 9.383148997457999130, 5.167567567567999731, 6.822293592207000934 ) ) ;
#68820=B_SPLINE_CURVE_WITH_KNOTS ( 'NONE', 3,
 ( #53950, #49750, #6745, #32982 ),
 .UNSPECIFIED., .F., .F.,
 ( 4, 4 ),
 ( 0.000000000000000000, 1.000000000000000000 ),
 .UNSPECIFIED. ) ;
#68824=CARTESIAN_POINT ( 'NONE',  ( 0.000000000000000000, -2.533699434757234137, 1.460905701136922197 ) ) ;
#68828=CARTESIAN_POINT ( 'NONE',  ( 11.09999999999999964, 5.299999998610999796, -5.148506132424000015 ) ) ;
#68831=VECTOR ( 'NONE', #46070, 1000.000000000000000 ) ;
#68834=CARTESIAN_POINT ( 'NONE',  ( 8.592635841230999105, 3.856772556595000179, 5.521246073317000125 ) ) ;
#68836=CARTESIAN_POINT ( 'NONE',  ( 9.269689158774999882, 3.135494838036999798, -8.598037907310999373 ) ) ;
#68839=EDGE_LOOP ( 'NONE', ( #25657, #2348, #55528, #940 ) ) ;
#68840=CARTESIAN_POINT ( 'NONE',  ( 9.442087588264000075, 4.742492734433000123, 8.809983635807000724 ) ) ;
#68846=CARTESIAN_POINT ( 'NONE',  ( 8.674239158774001979, 5.983047240001000411, 7.440798119034999658 ) ) ;
#68848=CARTESIAN_POINT ( 'NONE',  ( 10.37902717885803483, 2.650237472150223095, -7.263327126957213054 ) ) ;
#68851=CARTESIAN_POINT ( 'NONE',  ( 1.023245171504000073, -3.085119672805999524, 1.050391531144999835 ) ) ;
#68855=CARTESIAN_POINT ( 'NONE',  ( 9.298033738970000073, 4.087077023028999001, 9.429414864145000408 ) ) ;
#68857=ORIENTED_EDGE ( 'NONE', *, *, #47267, .T. ) ;
#68865=CARTESIAN_POINT ( 'NONE',  ( 10.90000037895999796, 0.2999996193951000034, 9.776630289319001577 ) ) ;
#68870=ORIENTED_EDGE ( 'NONE', *, *, #14134, .F. ) ;
#68876=CARTESIAN_POINT ( 'NONE',  ( 10.22440590001000160, 5.317411003666999925, -8.272452263128000638 ) ) ;
#68877=CARTESIAN_POINT ( 'NONE',  ( 8.166615904750996080, 4.665939084510003276, 6.165875187757999143 ) ) ;
#68881=CARTESIAN_POINT ( 'NONE',  ( 9.041114868689660966, 4.912818212989734867, 8.494533580134559614 ) ) ;
#68883=CARTESIAN_POINT ( 'NONE',  ( 8.149357780409999918, 2.583668273793999770, 6.684750595573999199 ) ) ;
#68884=EDGE_LOOP ( 'NONE', ( #9187, #66547, #5398, #6792 ) ) ;
#68885=CARTESIAN_POINT ( 'NONE',  ( 11.10000000000000320, 2.503699319922003674, -6.700110939026191481 ) ) ;
#68886=DIRECTION ( 'NONE',  ( 1.000000000000000000, 0.000000000000000000, 0.000000000000000000 ) ) ;
#68887=CARTESIAN_POINT ( 'NONE',  ( 8.561977803070984550, 2.916400247641351751, -6.350095013862320670 ) ) ;
#68889=DIRECTION ( 'NONE',  ( 0.000000000000000000, 0.000000000000000000, 1.000000000000000000 ) ) ;
#68891=CARTESIAN_POINT ( 'NONE',  ( 10.93665077113000095, 8.761693334770001229, 6.467187816040000037 ) ) ;
#68900=DIRECTION ( 'NONE',  ( 1.000000000000000000, 0.000000000000000000, 0.000000000000000000 ) ) ;
#68905=CARTESIAN_POINT ( 'NONE',  ( 0.4006366850170999805, -2.512770725774000180, 2.251027108384000108 ) ) ;
#68908=DIRECTION ( 'NONE',  ( 1.000000000000000000, 0.000000000000000000, 0.000000000000000000 ) ) ;
#68911=CARTESIAN_POINT ( 'NONE',  ( 10.11548915876999999, 2.489190114737999782, -6.434635778494999236 ) ) ;
#68913=LINE ( 'NONE', #51806, #67629 ) ;
#68916=VERTEX_POINT ( 'NONE', #15747 ) ;
#68921=DIRECTION ( 'NONE',  ( 0.000000000000000000, -1.000000000000000000, 0.000000000000000000 ) ) ;
#68925=FACE_OUTER_BOUND ( 'NONE', #51692, .T. ) ;
#68929=CARTESIAN_POINT ( 'NONE',  ( 8.155024894413680059, 3.133330062225388346, 6.255279687528450872 ) ) ;
#68934=FACE_OUTER_BOUND ( 'NONE', #67206, .T. ) ;
#68939=CARTESIAN_POINT ( 'NONE',  ( 7.778861800931997195, 3.520498707107000858, 6.411393241748998051 ) ) ;
#68950=CARTESIAN_POINT ( 'NONE',  ( 8.406645280410000254, 3.807713920470999991, -9.221758713517999695 ) ) ;
#68952=EDGE_LOOP ( 'NONE', ( #52379, #22030, #6399, #40073, #39790 ) ) ;
#68955=EDGE_LOOP ( 'NONE', ( #30648, #29606, #17088, #63920 ) ) ;
#68957=CARTESIAN_POINT ( 'NONE',  ( 8.845310841232000953, 5.851083642416999631, -7.072167224702999633 ) ) ;
#68958=EDGE_CURVE ( 'NONE', #64347, #45997, #219, .T. ) ;
#68964=B_SPLINE_CURVE_WITH_KNOTS ( 'NONE', 3,
 ( #19905, #23858, #34364, #14999 ),
 .UNSPECIFIED., .F., .F.,
 ( 4, 4 ),
 ( 0.000000000000000000, 1.000000000000000000 ),
 .UNSPECIFIED. ) ;
#68965=CARTESIAN_POINT ( 'NONE',  ( 11.09999999999999964, 6.593648131501000265, 5.598803515845999890 ) ) ;
#68966=ORIENTED_EDGE ( 'NONE', *, *, #62917, .F. ) ;
#68968=CARTESIAN_POINT ( 'NONE',  ( 8.880270280412998929, 4.146787477634999775, -5.941926545671999627 ) ) ;
#68978=CARTESIAN_POINT ( 'NONE',  ( 8.576923877145999242, 3.399999999999999911, 5.924121105096999962 ) ) ;
#68984=CARTESIAN_POINT ( 'NONE',  ( -15.86200481174999943, 11.00717859340000082, 1.432487142323000118 ) ) ;
#68986=CARTESIAN_POINT ( 'NONE',  ( 9.146614158775999925, 2.981992329588000423, -5.895876591910999664 ) ) ;
#68993=CARTESIAN_POINT ( 'NONE',  ( 10.99999999997000089, 4.000000000000000000, -7.500000000000000000 ) ) ;
#68994=CARTESIAN_POINT ( 'NONE',  ( 1.155140132541250031, 0.9161175952574702741, 3.408904368339106927 ) ) ;
#68995=FACE_OUTER_BOUND ( 'NONE', #22296, .T. ) ;
#69008=LINE ( 'NONE', #5381, #48638 ) ;
#69011=CARTESIAN_POINT ( 'NONE',  ( 11.09999999999999964, 4.000000000000000000, -7.500000000000000000 ) ) ;
#69014=CARTESIAN_POINT ( 'NONE',  ( 6.999999999999999112, 8.814407058729466726, -4.633674960078741023 ) ) ;
#69017=VERTEX_POINT ( 'NONE', #6451 ) ;
#69024=CARTESIAN_POINT ( 'NONE',  ( 10.26088874562948128, 3.646602187524448535, -8.814783671671067466 ) ) ;
#69031=CARTESIAN_POINT ( 'NONE',  ( 7.589309517775307157, 5.301171624786114478, -7.912166694486026053 ) ) ;
#69032=AXIS2_PLACEMENT_3D ( 'NONE', #19266, #67153, #2501 ) ;
#69034=VERTEX_POINT ( 'NONE', #6799 ) ;
#69038=CARTESIAN_POINT ( 'NONE',  ( 7.000000000000000000, 0.3230303992915000144, -3.000000000000000000 ) ) ;
#69049=CARTESIAN_POINT ( 'NONE',  ( 7.219277519215202332, 4.353512721038384825, -8.815217796131234351 ) ) ;
#69052=EDGE_CURVE ( 'NONE', #26809, #8503, #43175, .T. ) ;
#69058=ORIENTED_EDGE ( 'NONE', *, *, #18274, .T. ) ;
#69062=CARTESIAN_POINT ( 'NONE',  ( 7.801679552337999368, 4.516824445382995989, -6.385720355065998000 ) ) ;
#69068=CARTESIAN_POINT ( 'NONE',  ( 9.260906466624998501, 4.901388651757999426, 9.090324495507999814 ) ) ;
#69069=CARTESIAN_POINT ( 'NONE',  ( 10.79701415876999882, 5.792870175253000298, -7.049262931951000510 ) ) ;
#69075=CARTESIAN_POINT ( 'NONE',  ( 6.949999692073999924, 11.00717859340000082, -1.432487142323000118 ) ) ;
#69087=ADVANCED_FACE ( 'NONE', ( #876 ), #64826, .T. ) ;
#69096=CARTESIAN_POINT ( 'NONE',  ( 9.319414158774000256, 2.656512020013999997, -7.884832994446999699 ) ) ;
#69101=CARTESIAN_POINT ( 'NONE',  ( 0.2799269853179000012, 3.021985743044000028, 1.081096232840000004 ) ) ;
#69103=CARTESIAN_POINT ( 'NONE',  ( 2.981521585972999766, 3.146372654723999851, -2.056384300341000060 ) ) ;
#69112=CARTESIAN_POINT ( 'NONE',  ( 7.856379719586000121, 5.390931070480998955, -6.467229401624000396 ) ) ;
#69115=EDGE_LOOP ( 'NONE', ( #32367, #59228, #50491, #64592 ) ) ;
#69123=DIRECTION ( 'NONE',  ( 1.000000000000000000, 0.000000000000000000, 0.000000000000000000 ) ) ;
#69124=CARTESIAN_POINT ( 'NONE',  ( 6.999999691988000095, 12.49999909016000110, -4.772673758002000880E-10 ) ) ;
#69130=VERTEX_POINT ( 'NONE', #55048 ) ;
#69131=CARTESIAN_POINT ( 'NONE',  ( 7.550614158771000284, 4.468366666325000125, 8.882140983065999862 ) ) ;
#69133=ORIENTED_EDGE ( 'NONE', *, *, #60188, .T. ) ;
#69136=CARTESIAN_POINT ( 'NONE',  ( 11.12376201898999994, 6.339186361347000087, -5.425853403269999653 ) ) ;
#69139=CARTESIAN_POINT ( 'NONE',  ( 7.848356335646994530, 10.67649265946998938, -3.847892590697003623 ) ) ;
#69141=DIRECTION ( 'NONE',  ( -0.7071060865237062121, 0.7071074758487063683, 8.141784862113073118E-10 ) ) ;
#69152=CARTESIAN_POINT ( 'NONE',  ( 4.900006121741998122, 1.747572776708516740, 1.007237960741796057 ) ) ;
#69153=CARTESIAN_POINT ( 'NONE',  ( 10.71983649979000042, 3.571741329336999726, -5.696148467328000287 ) ) ;
#69154=DIRECTION ( 'NONE',  ( 0.000000000000000000, -1.000000000000000000, 0.000000000000000000 ) ) ;
#69158=ORIENTED_EDGE ( 'NONE', *, *, #62743, .F. ) ;
#69167=CARTESIAN_POINT ( 'NONE',  ( 9.634020792350998619, 3.042978295541999945, 8.588098960242001922 ) ) ;
#69170=ORIENTED_EDGE ( 'NONE', *, *, #741, .T. ) ;
#69173=DIRECTION ( 'NONE',  ( 0.000000000000000000, 0.9565994702956990281, 0.2914059941558995726 ) ) ;
#69174=CARTESIAN_POINT ( 'NONE',  ( 3.448119472057917800, 2.777709467148614664, -2.177750925185379050 ) ) ;
#69179=CARTESIAN_POINT ( 'NONE',  ( 8.785198341231000185, 5.414918126383000185, 8.890678916765999418 ) ) ;
#69180=CARTESIAN_POINT ( 'NONE',  ( 8.266329719591000824, 4.769017407621999993, -8.862909124839001507 ) ) ;
#69181=CARTESIAN_POINT ( 'NONE',  ( 4.900006121741999010, -2.000000000000000000, 0.000000000000000000 ) ) ;
#69182=CARTESIAN_POINT ( 'NONE',  ( 2.210247277619000084, 2.108360286353999413, -2.286637680308000409 ) ) ;
#69184=CARTESIAN_POINT ( 'NONE',  ( 11.07345995138000028, 3.998673170817999889, 8.920816085870999501 ) ) ;
#69190=CARTESIAN_POINT ( 'NONE',  ( 8.802614158774000330, 3.975069902178000270, 9.483774112875002160 ) ) ;
ENDSEC;
END-ISO-10303-21;
